ISO-10303-21;
HEADER;
/* Generated by software containing ST-Developer
 * from STEP Tools, Inc. (www.steptools.com) 
 */

FILE_DESCRIPTION(
/* description */ (''),
/* implementation_level */ '2;1');

FILE_NAME(
/* name */ 'Screw_03.step',
/* time_stamp */ '2026-10-05T00:14:20-07:00',
/* author */ (''),
/* organization */ (''),
/* preprocessor_version */ 'ST-DEVELOPER v20.2',
/* originating_system */ 'Autodesk Translation Framework v15.15.0.0',
/* authorisation */ '');

FILE_SCHEMA (('AUTOMOTIVE_DESIGN { 1 0 10303 214 3 1 1 }'));
ENDSEC;

DATA;
#10=MECHANICAL_DESIGN_GEOMETRIC_PRESENTATION_REPRESENTATION('',(#3378),#75336);
#47=(
BOUNDED_SURFACE()
B_SPLINE_SURFACE(1,2,((#73432,#73433,#73434,#73435,#73436,#73437,#73438,
#73439,#73440,#73441,#73442,#73443,#73444,#73445,#73446,#73447,#73448,#73449,
#73450,#73451,#73452,#73453,#73454,#73455,#73456,#73457,#73458,#73459,#73460,
#73461,#73462,#73463,#73464,#73465,#73466,#73467,#73468,#73469,#73470,#73471,
#73472,#73473,#73474,#73475,#73476,#73477,#73478,#73479,#73480,#73481,#73482,
#73483,#73484,#73485,#73486,#73487,#73488,#73489,#73490,#73491,#73492,#73493,
#73494,#73495,#73496,#73497,#73498,#73499,#73500,#73501,#73502,#73503,#73504,
#73505,#73506,#73507,#73508,#73509,#73510,#73511,#73512,#73513,#73514,#73515,
#73516,#73517,#73518,#73519,#73520,#73521,#73522,#73523,#73524,#73525,#73526,
#73527,#73528,#73529,#73530,#73531,#73532,#73533,#73534,#73535,#73536,#73537,
#73538,#73539,#73540,#73541,#73542,#73543,#73544,#73545,#73546,#73547,#73548,
#73549,#73550,#73551,#73552,#73553,#73554,#73555,#73556,#73557,#73558,#73559,
#73560,#73561,#73562,#73563,#73564,#73565,#73566,#73567,#73568,#73569,#73570,
#73571,#73572,#73573,#73574,#73575,#73576,#73577,#73578,#73579,#73580,#73581,
#73582,#73583,#73584,#73585,#73586,#73587,#73588,#73589,#73590,#73591,#73592,
#73593,#73594,#73595,#73596,#73597,#73598,#73599,#73600,#73601,#73602,#73603,
#73604,#73605,#73606,#73607,#73608,#73609,#73610,#73611,#73612,#73613,#73614,
#73615,#73616,#73617,#73618,#73619,#73620,#73621,#73622,#73623,#73624,#73625,
#73626,#73627,#73628,#73629,#73630,#73631,#73632,#73633,#73634,#73635,#73636,
#73637,#73638,#73639,#73640,#73641,#73642,#73643,#73644,#73645,#73646,#73647,
#73648,#73649,#73650,#73651,#73652,#73653,#73654,#73655,#73656,#73657,#73658,
#73659,#73660,#73661,#73662,#73663,#73664,#73665,#73666,#73667,#73668,#73669,
#73670,#73671,#73672,#73673,#73674,#73675,#73676,#73677,#73678,#73679,#73680,
#73681,#73682,#73683,#73684,#73685,#73686,#73687,#73688,#73689,#73690,#73691,
#73692,#73693,#73694,#73695,#73696,#73697,#73698,#73699,#73700,#73701,#73702,
#73703,#73704,#73705,#73706,#73707,#73708,#73709,#73710,#73711,#73712,#73713,
#73714,#73715,#73716,#73717,#73718,#73719,#73720,#73721,#73722,#73723,#73724,
#73725,#73726,#73727,#73728,#73729,#73730,#73731,#73732,#73733,#73734,#73735,
#73736,#73737,#73738,#73739,#73740,#73741,#73742,#73743,#73744,#73745,#73746,
#73747,#73748,#73749,#73750,#73751,#73752,#73753,#73754,#73755,#73756,#73757,
#73758,#73759,#73760,#73761,#73762,#73763,#73764,#73765,#73766,#73767,#73768,
#73769,#73770,#73771,#73772,#73773,#73774,#73775,#73776,#73777,#73778,#73779,
#73780,#73781,#73782,#73783,#73784,#73785,#73786,#73787,#73788,#73789,#73790,
#73791,#73792,#73793,#73794,#73795,#73796,#73797,#73798,#73799,#73800,#73801,
#73802,#73803,#73804),(#73805,#73806,#73807,#73808,#73809,#73810,#73811,
#73812,#73813,#73814,#73815,#73816,#73817,#73818,#73819,#73820,#73821,#73822,
#73823,#73824,#73825,#73826,#73827,#73828,#73829,#73830,#73831,#73832,#73833,
#73834,#73835,#73836,#73837,#73838,#73839,#73840,#73841,#73842,#73843,#73844,
#73845,#73846,#73847,#73848,#73849,#73850,#73851,#73852,#73853,#73854,#73855,
#73856,#73857,#73858,#73859,#73860,#73861,#73862,#73863,#73864,#73865,#73866,
#73867,#73868,#73869,#73870,#73871,#73872,#73873,#73874,#73875,#73876,#73877,
#73878,#73879,#73880,#73881,#73882,#73883,#73884,#73885,#73886,#73887,#73888,
#73889,#73890,#73891,#73892,#73893,#73894,#73895,#73896,#73897,#73898,#73899,
#73900,#73901,#73902,#73903,#73904,#73905,#73906,#73907,#73908,#73909,#73910,
#73911,#73912,#73913,#73914,#73915,#73916,#73917,#73918,#73919,#73920,#73921,
#73922,#73923,#73924,#73925,#73926,#73927,#73928,#73929,#73930,#73931,#73932,
#73933,#73934,#73935,#73936,#73937,#73938,#73939,#73940,#73941,#73942,#73943,
#73944,#73945,#73946,#73947,#73948,#73949,#73950,#73951,#73952,#73953,#73954,
#73955,#73956,#73957,#73958,#73959,#73960,#73961,#73962,#73963,#73964,#73965,
#73966,#73967,#73968,#73969,#73970,#73971,#73972,#73973,#73974,#73975,#73976,
#73977,#73978,#73979,#73980,#73981,#73982,#73983,#73984,#73985,#73986,#73987,
#73988,#73989,#73990,#73991,#73992,#73993,#73994,#73995,#73996,#73997,#73998,
#73999,#74000,#74001,#74002,#74003,#74004,#74005,#74006,#74007,#74008,#74009,
#74010,#74011,#74012,#74013,#74014,#74015,#74016,#74017,#74018,#74019,#74020,
#74021,#74022,#74023,#74024,#74025,#74026,#74027,#74028,#74029,#74030,#74031,
#74032,#74033,#74034,#74035,#74036,#74037,#74038,#74039,#74040,#74041,#74042,
#74043,#74044,#74045,#74046,#74047,#74048,#74049,#74050,#74051,#74052,#74053,
#74054,#74055,#74056,#74057,#74058,#74059,#74060,#74061,#74062,#74063,#74064,
#74065,#74066,#74067,#74068,#74069,#74070,#74071,#74072,#74073,#74074,#74075,
#74076,#74077,#74078,#74079,#74080,#74081,#74082,#74083,#74084,#74085,#74086,
#74087,#74088,#74089,#74090,#74091,#74092,#74093,#74094,#74095,#74096,#74097,
#74098,#74099,#74100,#74101,#74102,#74103,#74104,#74105,#74106,#74107,#74108,
#74109,#74110,#74111,#74112,#74113,#74114,#74115,#74116,#74117,#74118,#74119,
#74120,#74121,#74122,#74123,#74124,#74125,#74126,#74127,#74128,#74129,#74130,
#74131,#74132,#74133,#74134,#74135,#74136,#74137,#74138,#74139,#74140,#74141,
#74142,#74143,#74144,#74145,#74146,#74147,#74148,#74149,#74150,#74151,#74152,
#74153,#74154,#74155,#74156,#74157,#74158,#74159,#74160,#74161,#74162,#74163,
#74164,#74165,#74166,#74167,#74168,#74169,#74170,#74171,#74172,#74173,#74174,
#74175,#74176,#74177)),.UNSPECIFIED.,.F.,.F.,.F.)
B_SPLINE_SURFACE_WITH_KNOTS((2,2),(3,2,2,2,2,2,2,2,2,2,2,2,2,2,2,2,2,2,
2,2,2,2,2,2,2,2,2,2,2,2,2,2,2,2,2,2,2,2,2,2,2,2,2,2,2,2,2,2,2,2,2,2,2,2,
2,2,2,2,2,2,2,2,2,2,2,2,2,2,2,2,2,2,2,2,2,2,2,2,2,2,2,2,2,2,2,2,2,2,2,2,
2,2,2,2,2,2,2,2,2,2,2,2,2,2,2,2,2,2,2,2,2,2,2,2,2,2,2,2,2,2,2,2,2,2,2,2,
2,2,2,2,2,2,2,2,2,2,2,2,2,2,2,2,2,2,2,2,2,2,2,2,2,2,2,2,2,2,2,2,2,2,2,2,
2,2,2,2,2,2,2,2,2,2,2,2,2,2,2,2,2,2,2,2,2,2,2,2,3),(-2.30253870309941E-5,
1.),(0.,0.00537634408602151,0.010752688172043,0.0161290322580645,0.021505376344086,
0.0268817204301075,0.032258064516129,0.0376344086021505,0.043010752688172,
0.0483870967741935,0.0537634408602151,0.0591397849462366,0.0645161290322581,
0.0698924731182796,0.0752688172043011,0.0806451612903226,0.0860215053763441,
0.0913978494623656,0.0967741935483871,0.102150537634409,0.10752688172043,
0.112903225806452,0.118279569892473,0.123655913978495,0.129032258064516,
0.134408602150538,0.139784946236559,0.145161290322581,0.150537634408602,
0.155913978494624,0.161290322580645,0.166666666666667,0.172043010752688,
0.17741935483871,0.182795698924731,0.188172043010753,0.193548387096774,
0.198924731182796,0.204301075268817,0.209677419354839,0.21505376344086,
0.220430107526882,0.225806451612903,0.231182795698925,0.236559139784946,
0.241935483870968,0.247311827956989,0.252688172043011,0.258064516129032,
0.263440860215054,0.268817204301075,0.274193548387097,0.279569892473118,
0.28494623655914,0.290322580645161,0.295698924731183,0.301075268817204,
0.306451612903226,0.311827956989247,0.317204301075269,0.32258064516129,
0.327956989247312,0.333333333333333,0.338709677419355,0.344086021505376,
0.349462365591398,0.354838709677419,0.360215053763441,0.365591397849462,
0.370967741935484,0.376344086021505,0.381720430107527,0.387096774193548,
0.39247311827957,0.397849462365591,0.403225806451613,0.408602150537634,
0.413978494623656,0.419354838709677,0.424731182795699,0.43010752688172,
0.435483870967742,0.440860215053763,0.446236559139785,0.451612903225806,
0.456989247311828,0.462365591397849,0.467741935483871,0.473118279569892,
0.478494623655914,0.483870967741935,0.489247311827957,0.494623655913978,
0.5,0.505376344086022,0.510752688172043,0.516129032258065,0.521505376344086,
0.526881720430108,0.532258064516129,0.537634408602151,0.543010752688172,
0.548387096774194,0.553763440860215,0.559139784946237,0.564516129032258,
0.56989247311828,0.575268817204301,0.580645161290323,0.586021505376344,
0.591397849462366,0.596774193548387,0.602150537634409,0.60752688172043,
0.612903225806452,0.618279569892473,0.623655913978495,0.629032258064516,
0.634408602150538,0.639784946236559,0.645161290322581,0.650537634408602,
0.655913978494624,0.661290322580645,0.666666666666667,0.672043010752688,
0.67741935483871,0.682795698924731,0.688172043010753,0.693548387096774,
0.698924731182796,0.704301075268817,0.709677419354839,0.71505376344086,
0.720430107526882,0.725806451612903,0.731182795698925,0.736559139784946,
0.741935483870968,0.747311827956989,0.752688172043011,0.758064516129032,
0.763440860215054,0.768817204301075,0.774193548387097,0.779569892473118,
0.78494623655914,0.790322580645161,0.795698924731183,0.801075268817204,
0.806451612903226,0.811827956989247,0.817204301075269,0.82258064516129,
0.827956989247312,0.833333333333333,0.838709677419355,0.844086021505376,
0.849462365591398,0.854838709677419,0.860215053763441,0.865591397849462,
0.870967741935484,0.876344086021505,0.881720430107527,0.887096774193548,
0.89247311827957,0.897849462365591,0.903225806451613,0.908602150537634,
0.913978494623656,0.919354838709677,0.924731182795699,0.93010752688172,
0.935483870967742,0.940860215053763,0.946236559139785,0.951612903225806,
0.956989247311828,0.962365591397849,0.967741935483871,0.973118279569892,
0.978494623655914,0.983870967741935,0.989247311827957,0.994623655913978,
1.),.UNSPECIFIED.)
GEOMETRIC_REPRESENTATION_ITEM()
RATIONAL_B_SPLINE_SURFACE(((1.,0.866025403784439,1.,0.866025403784439,1.,
0.866025403784439,1.,0.866025403784439,1.,0.866025403784439,1.,0.866025403784439,
1.,0.866025403784439,1.,0.866025403784439,1.,0.866025403784439,1.,0.866025403784439,
1.,0.866025403784439,1.,0.866025403784439,1.,0.866025403784439,1.,0.866025403784439,
1.,0.866025403784439,1.,0.866025403784439,1.,0.866025403784439,1.,0.866025403784439,
1.,0.866025403784439,1.,0.866025403784439,1.,0.866025403784439,1.,0.866025403784439,
1.,0.866025403784439,1.,0.866025403784439,1.,0.866025403784439,1.,0.866025403784439,
1.,0.866025403784439,1.,0.866025403784439,1.,0.866025403784439,1.,0.866025403784439,
1.,0.866025403784439,1.,0.866025403784439,1.,0.866025403784439,1.,0.866025403784439,
1.,0.866025403784439,1.,0.866025403784439,1.,0.866025403784439,1.,0.866025403784439,
1.,0.866025403784439,1.,0.866025403784439,1.,0.866025403784439,1.,0.866025403784439,
1.,0.866025403784439,1.,0.866025403784439,1.,0.866025403784439,1.,0.866025403784439,
1.,0.866025403784439,1.,0.866025403784439,1.,0.866025403784439,1.,0.866025403784439,
1.,0.866025403784439,1.,0.866025403784439,1.,0.866025403784439,1.,0.866025403784439,
1.,0.866025403784439,1.,0.866025403784439,1.,0.866025403784439,1.,0.866025403784439,
1.,0.866025403784439,1.,0.866025403784439,1.,0.866025403784439,1.,0.866025403784439,
1.,0.866025403784439,1.,0.866025403784439,1.,0.866025403784439,1.,0.866025403784439,
1.,0.866025403784439,1.,0.866025403784439,1.,0.866025403784439,1.,0.866025403784439,
1.,0.866025403784439,1.,0.866025403784439,1.,0.866025403784439,1.,0.866025403784439,
1.,0.866025403784439,1.,0.866025403784439,1.,0.866025403784439,1.,0.866025403784439,
1.,0.866025403784439,1.,0.866025403784439,1.,0.866025403784439,1.,0.866025403784439,
1.,0.866025403784439,1.,0.866025403784439,1.,0.866025403784439,1.,0.866025403784439,
1.,0.866025403784439,1.,0.866025403784439,1.,0.866025403784439,1.,0.866025403784439,
1.,0.866025403784439,1.,0.866025403784439,1.,0.866025403784439,1.,0.866025403784439,
1.,0.866025403784439,1.,0.866025403784439,1.,0.866025403784439,1.,0.866025403784439,
1.,0.866025403784439,1.,0.866025403784439,1.,0.866025403784439,1.,0.866025403784439,
1.,0.866025403784439,1.,0.866025403784439,1.,0.866025403784439,1.,0.866025403784439,
1.,0.866025403784439,1.,0.866025403784439,1.,0.866025403784439,1.,0.866025403784439,
1.,0.866025403784439,1.,0.866025403784439,1.,0.866025403784439,1.,0.866025403784439,
1.,0.866025403784439,1.,0.866025403784439,1.,0.866025403784439,1.,0.866025403784439,
1.,0.866025403784439,1.,0.866025403784439,1.,0.866025403784439,1.,0.866025403784439,
1.,0.866025403784439,1.,0.866025403784439,1.,0.866025403784439,1.,0.866025403784439,
1.,0.866025403784439,1.,0.866025403784439,1.,0.866025403784439,1.,0.866025403784439,
1.,0.866025403784439,1.,0.866025403784439,1.,0.866025403784439,1.,0.866025403784439,
1.,0.866025403784439,1.,0.866025403784439,1.,0.866025403784439,1.,0.866025403784439,
1.,0.866025403784439,1.,0.866025403784439,1.,0.866025403784439,1.,0.866025403784439,
1.,0.866025403784439,1.,0.866025403784439,1.,0.866025403784439,1.,0.866025403784439,
1.,0.866025403784439,1.,0.866025403784439,1.,0.866025403784439,1.,0.866025403784439,
1.,0.866025403784439,1.,0.866025403784439,1.,0.866025403784439,1.,0.866025403784439,
1.,0.866025403784439,1.,0.866025403784439,1.,0.866025403784439,1.,0.866025403784439,
1.,0.866025403784439,1.,0.866025403784439,1.,0.866025403784439,1.,0.866025403784439,
1.,0.866025403784439,1.,0.866025403784439,1.,0.866025403784439,1.,0.866025403784439,
1.,0.866025403784439,1.,0.866025403784439,1.,0.866025403784439,1.,0.866025403784439,
1.,0.866025403784439,1.,0.866025403784439,1.,0.866025403784439,1.,0.866025403784439,
1.,0.866025403784439,1.,0.866025403784439,1.,0.866025403784439,1.,0.866025403784439,
1.,0.866025403784439,1.,0.866025403784439,1.,0.866025403784439,1.,0.866025403784439,
1.,0.866025403784439,1.,0.866025403784439,1.,0.866025403784439,1.,0.866025403784439,
1.),(1.,0.866025403784439,1.,0.866025403784439,1.,0.866025403784439,1.,
0.866025403784439,1.,0.866025403784439,1.,0.866025403784439,1.,0.866025403784439,
1.,0.866025403784439,1.,0.866025403784439,1.,0.866025403784439,1.,0.866025403784439,
1.,0.866025403784439,1.,0.866025403784439,1.,0.866025403784439,1.,0.866025403784439,
1.,0.866025403784439,1.,0.866025403784439,1.,0.866025403784439,1.,0.866025403784439,
1.,0.866025403784439,1.,0.866025403784439,1.,0.866025403784439,1.,0.866025403784439,
1.,0.866025403784439,1.,0.866025403784439,1.,0.866025403784439,1.,0.866025403784439,
1.,0.866025403784439,1.,0.866025403784439,1.,0.866025403784439,1.,0.866025403784439,
1.,0.866025403784439,1.,0.866025403784439,1.,0.866025403784439,1.,0.866025403784439,
1.,0.866025403784439,1.,0.866025403784439,1.,0.866025403784439,1.,0.866025403784439,
1.,0.866025403784439,1.,0.866025403784439,1.,0.866025403784439,1.,0.866025403784439,
1.,0.866025403784439,1.,0.866025403784439,1.,0.866025403784439,1.,0.866025403784439,
1.,0.866025403784439,1.,0.866025403784439,1.,0.866025403784439,1.,0.866025403784439,
1.,0.866025403784439,1.,0.866025403784439,1.,0.866025403784439,1.,0.866025403784439,
1.,0.866025403784439,1.,0.866025403784439,1.,0.866025403784439,1.,0.866025403784439,
1.,0.866025403784439,1.,0.866025403784439,1.,0.866025403784439,1.,0.866025403784439,
1.,0.866025403784439,1.,0.866025403784439,1.,0.866025403784439,1.,0.866025403784439,
1.,0.866025403784439,1.,0.866025403784439,1.,0.866025403784439,1.,0.866025403784439,
1.,0.866025403784439,1.,0.866025403784439,1.,0.866025403784439,1.,0.866025403784439,
1.,0.866025403784439,1.,0.866025403784439,1.,0.866025403784439,1.,0.866025403784439,
1.,0.866025403784439,1.,0.866025403784439,1.,0.866025403784439,1.,0.866025403784439,
1.,0.866025403784439,1.,0.866025403784439,1.,0.866025403784439,1.,0.866025403784439,
1.,0.866025403784439,1.,0.866025403784439,1.,0.866025403784439,1.,0.866025403784439,
1.,0.866025403784439,1.,0.866025403784439,1.,0.866025403784439,1.,0.866025403784439,
1.,0.866025403784439,1.,0.866025403784439,1.,0.866025403784439,1.,0.866025403784439,
1.,0.866025403784439,1.,0.866025403784439,1.,0.866025403784439,1.,0.866025403784439,
1.,0.866025403784439,1.,0.866025403784439,1.,0.866025403784439,1.,0.866025403784439,
1.,0.866025403784439,1.,0.866025403784439,1.,0.866025403784439,1.,0.866025403784439,
1.,0.866025403784439,1.,0.866025403784439,1.,0.866025403784439,1.,0.866025403784439,
1.,0.866025403784439,1.,0.866025403784439,1.,0.866025403784439,1.,0.866025403784439,
1.,0.866025403784439,1.,0.866025403784439,1.,0.866025403784439,1.,0.866025403784439,
1.,0.866025403784439,1.,0.866025403784439,1.,0.866025403784439,1.,0.866025403784439,
1.,0.866025403784439,1.,0.866025403784439,1.,0.866025403784439,1.,0.866025403784439,
1.,0.866025403784439,1.,0.866025403784439,1.,0.866025403784439,1.,0.866025403784439,
1.,0.866025403784439,1.,0.866025403784439,1.,0.866025403784439,1.,0.866025403784439,
1.,0.866025403784439,1.,0.866025403784439,1.,0.866025403784439,1.,0.866025403784439,
1.,0.866025403784439,1.,0.866025403784439,1.,0.866025403784439,1.,0.866025403784439,
1.,0.866025403784439,1.,0.866025403784439,1.,0.866025403784439,1.,0.866025403784439,
1.,0.866025403784439,1.,0.866025403784439,1.,0.866025403784439,1.,0.866025403784439,
1.,0.866025403784439,1.,0.866025403784439,1.,0.866025403784439,1.,0.866025403784439,
1.,0.866025403784439,1.,0.866025403784439,1.,0.866025403784439,1.,0.866025403784439,
1.,0.866025403784439,1.,0.866025403784439,1.,0.866025403784439,1.,0.866025403784439,
1.,0.866025403784439,1.,0.866025403784439,1.,0.866025403784439,1.,0.866025403784439,
1.,0.866025403784439,1.,0.866025403784439,1.,0.866025403784439,1.,0.866025403784439,
1.,0.866025403784439,1.,0.866025403784439,1.,0.866025403784439,1.,0.866025403784439,
1.,0.866025403784439,1.,0.866025403784439,1.,0.866025403784439,1.,0.866025403784439,
1.,0.866025403784439,1.,0.866025403784439,1.,0.866025403784439,1.)))
REPRESENTATION_ITEM('')
SURFACE()
);
#48=(
BOUNDED_SURFACE()
B_SPLINE_SURFACE(1,2,((#74206,#74207,#74208,#74209,#74210,#74211,#74212,
#74213,#74214,#74215,#74216,#74217,#74218,#74219,#74220,#74221,#74222,#74223,
#74224,#74225,#74226,#74227,#74228,#74229,#74230,#74231,#74232,#74233,#74234,
#74235,#74236,#74237,#74238,#74239,#74240,#74241,#74242,#74243,#74244,#74245,
#74246,#74247,#74248,#74249,#74250,#74251,#74252,#74253,#74254,#74255,#74256,
#74257,#74258,#74259,#74260,#74261,#74262,#74263,#74264,#74265,#74266,#74267,
#74268,#74269,#74270,#74271,#74272,#74273,#74274,#74275,#74276,#74277,#74278,
#74279,#74280,#74281,#74282,#74283,#74284,#74285,#74286,#74287,#74288,#74289,
#74290,#74291,#74292,#74293,#74294,#74295,#74296,#74297,#74298,#74299,#74300,
#74301,#74302,#74303,#74304,#74305,#74306,#74307,#74308,#74309,#74310,#74311,
#74312,#74313,#74314,#74315,#74316,#74317,#74318,#74319,#74320,#74321,#74322,
#74323,#74324,#74325,#74326,#74327,#74328,#74329,#74330,#74331,#74332,#74333,
#74334,#74335,#74336,#74337,#74338,#74339,#74340,#74341,#74342,#74343,#74344,
#74345,#74346,#74347,#74348,#74349,#74350,#74351,#74352,#74353,#74354,#74355,
#74356,#74357,#74358,#74359,#74360,#74361,#74362,#74363,#74364,#74365,#74366,
#74367,#74368,#74369,#74370,#74371,#74372,#74373,#74374,#74375,#74376,#74377,
#74378,#74379,#74380,#74381,#74382,#74383,#74384,#74385,#74386,#74387,#74388,
#74389,#74390,#74391,#74392,#74393,#74394,#74395,#74396,#74397,#74398,#74399,
#74400,#74401,#74402,#74403,#74404,#74405,#74406,#74407,#74408,#74409,#74410,
#74411,#74412,#74413,#74414,#74415,#74416,#74417,#74418,#74419,#74420,#74421,
#74422,#74423,#74424,#74425,#74426,#74427,#74428,#74429,#74430,#74431,#74432,
#74433,#74434,#74435,#74436,#74437,#74438,#74439,#74440,#74441,#74442,#74443,
#74444,#74445,#74446,#74447,#74448,#74449,#74450,#74451,#74452,#74453,#74454,
#74455,#74456,#74457,#74458,#74459,#74460,#74461,#74462,#74463,#74464,#74465,
#74466,#74467,#74468,#74469,#74470,#74471,#74472,#74473,#74474,#74475,#74476,
#74477,#74478,#74479,#74480,#74481,#74482,#74483,#74484,#74485,#74486,#74487,
#74488,#74489,#74490,#74491,#74492,#74493,#74494,#74495,#74496,#74497,#74498,
#74499,#74500,#74501,#74502,#74503,#74504,#74505,#74506,#74507,#74508,#74509,
#74510,#74511,#74512,#74513,#74514,#74515,#74516,#74517,#74518,#74519,#74520,
#74521,#74522,#74523,#74524,#74525,#74526,#74527,#74528,#74529,#74530,#74531,
#74532,#74533,#74534,#74535,#74536,#74537,#74538,#74539,#74540,#74541,#74542,
#74543,#74544,#74545,#74546,#74547,#74548,#74549,#74550,#74551,#74552,#74553,
#74554,#74555,#74556,#74557,#74558,#74559,#74560,#74561,#74562,#74563,#74564,
#74565,#74566,#74567,#74568,#74569,#74570,#74571,#74572,#74573,#74574,#74575,
#74576,#74577,#74578),(#74579,#74580,#74581,#74582,#74583,#74584,#74585,
#74586,#74587,#74588,#74589,#74590,#74591,#74592,#74593,#74594,#74595,#74596,
#74597,#74598,#74599,#74600,#74601,#74602,#74603,#74604,#74605,#74606,#74607,
#74608,#74609,#74610,#74611,#74612,#74613,#74614,#74615,#74616,#74617,#74618,
#74619,#74620,#74621,#74622,#74623,#74624,#74625,#74626,#74627,#74628,#74629,
#74630,#74631,#74632,#74633,#74634,#74635,#74636,#74637,#74638,#74639,#74640,
#74641,#74642,#74643,#74644,#74645,#74646,#74647,#74648,#74649,#74650,#74651,
#74652,#74653,#74654,#74655,#74656,#74657,#74658,#74659,#74660,#74661,#74662,
#74663,#74664,#74665,#74666,#74667,#74668,#74669,#74670,#74671,#74672,#74673,
#74674,#74675,#74676,#74677,#74678,#74679,#74680,#74681,#74682,#74683,#74684,
#74685,#74686,#74687,#74688,#74689,#74690,#74691,#74692,#74693,#74694,#74695,
#74696,#74697,#74698,#74699,#74700,#74701,#74702,#74703,#74704,#74705,#74706,
#74707,#74708,#74709,#74710,#74711,#74712,#74713,#74714,#74715,#74716,#74717,
#74718,#74719,#74720,#74721,#74722,#74723,#74724,#74725,#74726,#74727,#74728,
#74729,#74730,#74731,#74732,#74733,#74734,#74735,#74736,#74737,#74738,#74739,
#74740,#74741,#74742,#74743,#74744,#74745,#74746,#74747,#74748,#74749,#74750,
#74751,#74752,#74753,#74754,#74755,#74756,#74757,#74758,#74759,#74760,#74761,
#74762,#74763,#74764,#74765,#74766,#74767,#74768,#74769,#74770,#74771,#74772,
#74773,#74774,#74775,#74776,#74777,#74778,#74779,#74780,#74781,#74782,#74783,
#74784,#74785,#74786,#74787,#74788,#74789,#74790,#74791,#74792,#74793,#74794,
#74795,#74796,#74797,#74798,#74799,#74800,#74801,#74802,#74803,#74804,#74805,
#74806,#74807,#74808,#74809,#74810,#74811,#74812,#74813,#74814,#74815,#74816,
#74817,#74818,#74819,#74820,#74821,#74822,#74823,#74824,#74825,#74826,#74827,
#74828,#74829,#74830,#74831,#74832,#74833,#74834,#74835,#74836,#74837,#74838,
#74839,#74840,#74841,#74842,#74843,#74844,#74845,#74846,#74847,#74848,#74849,
#74850,#74851,#74852,#74853,#74854,#74855,#74856,#74857,#74858,#74859,#74860,
#74861,#74862,#74863,#74864,#74865,#74866,#74867,#74868,#74869,#74870,#74871,
#74872,#74873,#74874,#74875,#74876,#74877,#74878,#74879,#74880,#74881,#74882,
#74883,#74884,#74885,#74886,#74887,#74888,#74889,#74890,#74891,#74892,#74893,
#74894,#74895,#74896,#74897,#74898,#74899,#74900,#74901,#74902,#74903,#74904,
#74905,#74906,#74907,#74908,#74909,#74910,#74911,#74912,#74913,#74914,#74915,
#74916,#74917,#74918,#74919,#74920,#74921,#74922,#74923,#74924,#74925,#74926,
#74927,#74928,#74929,#74930,#74931,#74932,#74933,#74934,#74935,#74936,#74937,
#74938,#74939,#74940,#74941,#74942,#74943,#74944,#74945,#74946,#74947,#74948,
#74949,#74950,#74951)),.UNSPECIFIED.,.F.,.F.,.F.)
B_SPLINE_SURFACE_WITH_KNOTS((2,2),(3,2,2,2,2,2,2,2,2,2,2,2,2,2,2,2,2,2,
2,2,2,2,2,2,2,2,2,2,2,2,2,2,2,2,2,2,2,2,2,2,2,2,2,2,2,2,2,2,2,2,2,2,2,2,
2,2,2,2,2,2,2,2,2,2,2,2,2,2,2,2,2,2,2,2,2,2,2,2,2,2,2,2,2,2,2,2,2,2,2,2,
2,2,2,2,2,2,2,2,2,2,2,2,2,2,2,2,2,2,2,2,2,2,2,2,2,2,2,2,2,2,2,2,2,2,2,2,
2,2,2,2,2,2,2,2,2,2,2,2,2,2,2,2,2,2,2,2,2,2,2,2,2,2,2,2,2,2,2,2,2,2,2,2,
2,2,2,2,2,2,2,2,2,2,2,2,2,2,2,2,2,2,2,2,2,2,2,2,3),(0.,1.00001535537392),
(0.,0.00537634408602151,0.010752688172043,0.0161290322580645,0.021505376344086,
0.0268817204301075,0.032258064516129,0.0376344086021505,0.043010752688172,
0.0483870967741935,0.0537634408602151,0.0591397849462366,0.0645161290322581,
0.0698924731182796,0.0752688172043011,0.0806451612903226,0.0860215053763441,
0.0913978494623656,0.0967741935483871,0.102150537634409,0.10752688172043,
0.112903225806452,0.118279569892473,0.123655913978495,0.129032258064516,
0.134408602150538,0.139784946236559,0.145161290322581,0.150537634408602,
0.155913978494624,0.161290322580645,0.166666666666667,0.172043010752688,
0.17741935483871,0.182795698924731,0.188172043010753,0.193548387096774,
0.198924731182796,0.204301075268817,0.209677419354839,0.21505376344086,
0.220430107526882,0.225806451612903,0.231182795698925,0.236559139784946,
0.241935483870968,0.247311827956989,0.252688172043011,0.258064516129032,
0.263440860215054,0.268817204301075,0.274193548387097,0.279569892473118,
0.28494623655914,0.290322580645161,0.295698924731183,0.301075268817204,
0.306451612903226,0.311827956989247,0.317204301075269,0.32258064516129,
0.327956989247312,0.333333333333333,0.338709677419355,0.344086021505376,
0.349462365591398,0.354838709677419,0.360215053763441,0.365591397849462,
0.370967741935484,0.376344086021505,0.381720430107527,0.387096774193548,
0.39247311827957,0.397849462365591,0.403225806451613,0.408602150537634,
0.413978494623656,0.419354838709677,0.424731182795699,0.43010752688172,
0.435483870967742,0.440860215053763,0.446236559139785,0.451612903225806,
0.456989247311828,0.462365591397849,0.467741935483871,0.473118279569892,
0.478494623655914,0.483870967741935,0.489247311827957,0.494623655913978,
0.5,0.505376344086022,0.510752688172043,0.516129032258065,0.521505376344086,
0.526881720430108,0.532258064516129,0.537634408602151,0.543010752688172,
0.548387096774194,0.553763440860215,0.559139784946237,0.564516129032258,
0.56989247311828,0.575268817204301,0.580645161290323,0.586021505376344,
0.591397849462366,0.596774193548387,0.602150537634409,0.60752688172043,
0.612903225806452,0.618279569892473,0.623655913978495,0.629032258064516,
0.634408602150538,0.639784946236559,0.645161290322581,0.650537634408602,
0.655913978494624,0.661290322580645,0.666666666666667,0.672043010752688,
0.67741935483871,0.682795698924731,0.688172043010753,0.693548387096774,
0.698924731182796,0.704301075268817,0.709677419354839,0.71505376344086,
0.720430107526882,0.725806451612903,0.731182795698925,0.736559139784946,
0.741935483870968,0.747311827956989,0.752688172043011,0.758064516129032,
0.763440860215054,0.768817204301075,0.774193548387097,0.779569892473118,
0.78494623655914,0.790322580645161,0.795698924731183,0.801075268817204,
0.806451612903226,0.811827956989247,0.817204301075269,0.82258064516129,
0.827956989247312,0.833333333333333,0.838709677419355,0.844086021505376,
0.849462365591398,0.854838709677419,0.860215053763441,0.865591397849462,
0.870967741935484,0.876344086021505,0.881720430107527,0.887096774193548,
0.89247311827957,0.897849462365591,0.903225806451613,0.908602150537634,
0.913978494623656,0.919354838709677,0.924731182795699,0.93010752688172,
0.935483870967742,0.940860215053763,0.946236559139785,0.951612903225806,
0.956989247311828,0.962365591397849,0.967741935483871,0.973118279569892,
0.978494623655914,0.983870967741935,0.989247311827957,0.994623655913978,
1.),.UNSPECIFIED.)
GEOMETRIC_REPRESENTATION_ITEM()
RATIONAL_B_SPLINE_SURFACE(((1.,0.866025403784439,1.,0.866025403784439,1.,
0.866025403784439,1.,0.866025403784439,1.,0.866025403784439,1.,0.866025403784439,
1.,0.866025403784439,1.,0.866025403784439,1.,0.866025403784439,1.,0.866025403784439,
1.,0.866025403784439,1.,0.866025403784439,1.,0.866025403784439,1.,0.866025403784439,
1.,0.866025403784439,1.,0.866025403784439,1.,0.866025403784439,1.,0.866025403784439,
1.,0.866025403784439,1.,0.866025403784439,1.,0.866025403784439,1.,0.866025403784439,
1.,0.866025403784439,1.,0.866025403784439,1.,0.866025403784439,1.,0.866025403784439,
1.,0.866025403784439,1.,0.866025403784439,1.,0.866025403784439,1.,0.866025403784439,
1.,0.866025403784439,1.,0.866025403784439,1.,0.866025403784439,1.,0.866025403784439,
1.,0.866025403784439,1.,0.866025403784439,1.,0.866025403784439,1.,0.866025403784439,
1.,0.866025403784439,1.,0.866025403784439,1.,0.866025403784439,1.,0.866025403784439,
1.,0.866025403784439,1.,0.866025403784439,1.,0.866025403784439,1.,0.866025403784439,
1.,0.866025403784439,1.,0.866025403784439,1.,0.866025403784439,1.,0.866025403784439,
1.,0.866025403784439,1.,0.866025403784439,1.,0.866025403784439,1.,0.866025403784439,
1.,0.866025403784439,1.,0.866025403784439,1.,0.866025403784439,1.,0.866025403784439,
1.,0.866025403784439,1.,0.866025403784439,1.,0.866025403784439,1.,0.866025403784439,
1.,0.866025403784439,1.,0.866025403784439,1.,0.866025403784439,1.,0.866025403784439,
1.,0.866025403784439,1.,0.866025403784439,1.,0.866025403784439,1.,0.866025403784439,
1.,0.866025403784439,1.,0.866025403784439,1.,0.866025403784439,1.,0.866025403784439,
1.,0.866025403784439,1.,0.866025403784439,1.,0.866025403784439,1.,0.866025403784439,
1.,0.866025403784439,1.,0.866025403784439,1.,0.866025403784439,1.,0.866025403784439,
1.,0.866025403784439,1.,0.866025403784439,1.,0.866025403784439,1.,0.866025403784439,
1.,0.866025403784439,1.,0.866025403784439,1.,0.866025403784439,1.,0.866025403784439,
1.,0.866025403784439,1.,0.866025403784439,1.,0.866025403784439,1.,0.866025403784439,
1.,0.866025403784439,1.,0.866025403784439,1.,0.866025403784439,1.,0.866025403784439,
1.,0.866025403784439,1.,0.866025403784439,1.,0.866025403784439,1.,0.866025403784439,
1.,0.866025403784439,1.,0.866025403784439,1.,0.866025403784439,1.,0.866025403784439,
1.,0.866025403784439,1.,0.866025403784439,1.,0.866025403784439,1.,0.866025403784439,
1.,0.866025403784439,1.,0.866025403784439,1.,0.866025403784439,1.,0.866025403784439,
1.,0.866025403784439,1.,0.866025403784439,1.,0.866025403784439,1.,0.866025403784439,
1.,0.866025403784439,1.,0.866025403784439,1.,0.866025403784439,1.,0.866025403784439,
1.,0.866025403784439,1.,0.866025403784439,1.,0.866025403784439,1.,0.866025403784439,
1.,0.866025403784439,1.,0.866025403784439,1.,0.866025403784439,1.,0.866025403784439,
1.,0.866025403784439,1.,0.866025403784439,1.,0.866025403784439,1.,0.866025403784439,
1.,0.866025403784439,1.,0.866025403784439,1.,0.866025403784439,1.,0.866025403784439,
1.,0.866025403784439,1.,0.866025403784439,1.,0.866025403784439,1.,0.866025403784439,
1.,0.866025403784439,1.,0.866025403784439,1.,0.866025403784439,1.,0.866025403784439,
1.,0.866025403784439,1.,0.866025403784439,1.,0.866025403784439,1.,0.866025403784439,
1.,0.866025403784439,1.,0.866025403784439,1.,0.866025403784439,1.,0.866025403784439,
1.,0.866025403784439,1.,0.866025403784439,1.,0.866025403784439,1.,0.866025403784439,
1.,0.866025403784439,1.,0.866025403784439,1.,0.866025403784439,1.,0.866025403784439,
1.,0.866025403784439,1.,0.866025403784439,1.,0.866025403784439,1.,0.866025403784439,
1.,0.866025403784439,1.,0.866025403784439,1.,0.866025403784439,1.,0.866025403784439,
1.,0.866025403784439,1.,0.866025403784439,1.,0.866025403784439,1.,0.866025403784439,
1.,0.866025403784439,1.,0.866025403784439,1.,0.866025403784439,1.,0.866025403784439,
1.,0.866025403784439,1.,0.866025403784439,1.,0.866025403784439,1.,0.866025403784439,
1.,0.866025403784439,1.,0.866025403784439,1.,0.866025403784439,1.,0.866025403784439,
1.),(1.,0.866025403784439,1.,0.866025403784439,1.,0.866025403784439,1.,
0.866025403784439,1.,0.866025403784439,1.,0.866025403784439,1.,0.866025403784439,
1.,0.866025403784439,1.,0.866025403784439,1.,0.866025403784439,1.,0.866025403784439,
1.,0.866025403784439,1.,0.866025403784439,1.,0.866025403784439,1.,0.866025403784439,
1.,0.866025403784439,1.,0.866025403784439,1.,0.866025403784439,1.,0.866025403784439,
1.,0.866025403784439,1.,0.866025403784439,1.,0.866025403784439,1.,0.866025403784439,
1.,0.866025403784439,1.,0.866025403784439,1.,0.866025403784439,1.,0.866025403784439,
1.,0.866025403784439,1.,0.866025403784439,1.,0.866025403784439,1.,0.866025403784439,
1.,0.866025403784439,1.,0.866025403784439,1.,0.866025403784439,1.,0.866025403784439,
1.,0.866025403784439,1.,0.866025403784439,1.,0.866025403784439,1.,0.866025403784439,
1.,0.866025403784439,1.,0.866025403784439,1.,0.866025403784439,1.,0.866025403784439,
1.,0.866025403784439,1.,0.866025403784439,1.,0.866025403784439,1.,0.866025403784439,
1.,0.866025403784439,1.,0.866025403784439,1.,0.866025403784439,1.,0.866025403784439,
1.,0.866025403784439,1.,0.866025403784439,1.,0.866025403784439,1.,0.866025403784439,
1.,0.866025403784439,1.,0.866025403784439,1.,0.866025403784439,1.,0.866025403784439,
1.,0.866025403784439,1.,0.866025403784439,1.,0.866025403784439,1.,0.866025403784439,
1.,0.866025403784439,1.,0.866025403784439,1.,0.866025403784439,1.,0.866025403784439,
1.,0.866025403784439,1.,0.866025403784439,1.,0.866025403784439,1.,0.866025403784439,
1.,0.866025403784439,1.,0.866025403784439,1.,0.866025403784439,1.,0.866025403784439,
1.,0.866025403784439,1.,0.866025403784439,1.,0.866025403784439,1.,0.866025403784439,
1.,0.866025403784439,1.,0.866025403784439,1.,0.866025403784439,1.,0.866025403784439,
1.,0.866025403784439,1.,0.866025403784439,1.,0.866025403784439,1.,0.866025403784439,
1.,0.866025403784439,1.,0.866025403784439,1.,0.866025403784439,1.,0.866025403784439,
1.,0.866025403784439,1.,0.866025403784439,1.,0.866025403784439,1.,0.866025403784439,
1.,0.866025403784439,1.,0.866025403784439,1.,0.866025403784439,1.,0.866025403784439,
1.,0.866025403784439,1.,0.866025403784439,1.,0.866025403784439,1.,0.866025403784439,
1.,0.866025403784439,1.,0.866025403784439,1.,0.866025403784439,1.,0.866025403784439,
1.,0.866025403784439,1.,0.866025403784439,1.,0.866025403784439,1.,0.866025403784439,
1.,0.866025403784439,1.,0.866025403784439,1.,0.866025403784439,1.,0.866025403784439,
1.,0.866025403784439,1.,0.866025403784439,1.,0.866025403784439,1.,0.866025403784439,
1.,0.866025403784439,1.,0.866025403784439,1.,0.866025403784439,1.,0.866025403784439,
1.,0.866025403784439,1.,0.866025403784439,1.,0.866025403784439,1.,0.866025403784439,
1.,0.866025403784439,1.,0.866025403784439,1.,0.866025403784439,1.,0.866025403784439,
1.,0.866025403784439,1.,0.866025403784439,1.,0.866025403784439,1.,0.866025403784439,
1.,0.866025403784439,1.,0.866025403784439,1.,0.866025403784439,1.,0.866025403784439,
1.,0.866025403784439,1.,0.866025403784439,1.,0.866025403784439,1.,0.866025403784439,
1.,0.866025403784439,1.,0.866025403784439,1.,0.866025403784439,1.,0.866025403784439,
1.,0.866025403784439,1.,0.866025403784439,1.,0.866025403784439,1.,0.866025403784439,
1.,0.866025403784439,1.,0.866025403784439,1.,0.866025403784439,1.,0.866025403784439,
1.,0.866025403784439,1.,0.866025403784439,1.,0.866025403784439,1.,0.866025403784439,
1.,0.866025403784439,1.,0.866025403784439,1.,0.866025403784439,1.,0.866025403784439,
1.,0.866025403784439,1.,0.866025403784439,1.,0.866025403784439,1.,0.866025403784439,
1.,0.866025403784439,1.,0.866025403784439,1.,0.866025403784439,1.,0.866025403784439,
1.,0.866025403784439,1.,0.866025403784439,1.,0.866025403784439,1.,0.866025403784439,
1.,0.866025403784439,1.,0.866025403784439,1.,0.866025403784439,1.,0.866025403784439,
1.,0.866025403784439,1.,0.866025403784439,1.,0.866025403784439,1.,0.866025403784439,
1.,0.866025403784439,1.,0.866025403784439,1.,0.866025403784439,1.)))
REPRESENTATION_ITEM('')
SURFACE()
);
#377=TOROIDAL_SURFACE('',#35074,2.58058373926377,0.0468749999999982);
#378=TOROIDAL_SURFACE('',#35370,2.721875,0.0468749999999996);
#379=TOROIDAL_SURFACE('',#35375,2.60625,0.0687500000000002);
#380=TOROIDAL_SURFACE('',#35378,1.65,0.15);
#381=TOROIDAL_SURFACE('',#35381,2.703125,0.0468750000000018);
#382=TOROIDAL_SURFACE('',#35385,2.703125,0.0468750000000018);
#383=TOROIDAL_SURFACE('',#35389,2.703125,0.0468750000000018);
#384=TOROIDAL_SURFACE('',#35393,2.703125,0.0468750000000018);
#385=TOROIDAL_SURFACE('',#35397,2.703125,0.0468750000000018);
#386=TOROIDAL_SURFACE('',#35401,2.703125,0.0468750000000018);
#387=TOROIDAL_SURFACE('',#35405,2.703125,0.0468750000000018);
#388=TOROIDAL_SURFACE('',#35409,2.703125,0.0468750000000018);
#389=TOROIDAL_SURFACE('',#35413,2.703125,0.0468750000000018);
#390=TOROIDAL_SURFACE('',#35417,2.703125,0.0468750000000018);
#391=TOROIDAL_SURFACE('',#35421,2.703125,0.0468750000000018);
#392=TOROIDAL_SURFACE('',#35425,2.703125,0.0468750000000018);
#393=TOROIDAL_SURFACE('',#35429,2.703125,0.0468750000000018);
#394=TOROIDAL_SURFACE('',#35433,2.703125,0.0468750000000018);
#395=TOROIDAL_SURFACE('',#35437,2.703125,0.0468750000000018);
#396=TOROIDAL_SURFACE('',#35441,2.703125,0.0468750000000018);
#397=TOROIDAL_SURFACE('',#35445,2.703125,0.0468750000000018);
#398=TOROIDAL_SURFACE('',#35449,2.703125,0.0468750000000018);
#399=TOROIDAL_SURFACE('',#35453,2.703125,0.0468750000000018);
#400=TOROIDAL_SURFACE('',#35457,2.703125,0.0468750000000018);
#401=TOROIDAL_SURFACE('',#35461,2.703125,0.0468750000000018);
#402=TOROIDAL_SURFACE('',#35465,2.703125,0.0468750000000018);
#403=TOROIDAL_SURFACE('',#35469,2.703125,0.0468750000000018);
#404=TOROIDAL_SURFACE('',#35473,2.703125,0.0468750000000018);
#405=TOROIDAL_SURFACE('',#35477,2.703125,0.0468750000000018);
#406=TOROIDAL_SURFACE('',#35481,2.703125,0.0468750000000018);
#407=TOROIDAL_SURFACE('',#35485,2.703125,0.0468750000000018);
#408=TOROIDAL_SURFACE('',#35489,2.703125,0.0468750000000018);
#409=TOROIDAL_SURFACE('',#35493,2.703125,0.0468750000000018);
#410=TOROIDAL_SURFACE('',#35497,2.703125,0.0468750000000018);
#411=TOROIDAL_SURFACE('',#35501,2.703125,0.0468750000000018);
#412=TOROIDAL_SURFACE('',#35505,2.703125,0.0468750000000018);
#413=TOROIDAL_SURFACE('',#35509,2.703125,0.0468750000000018);
#414=TOROIDAL_SURFACE('',#35513,2.703125,0.0468750000000018);
#415=TOROIDAL_SURFACE('',#35517,2.703125,0.0468750000000018);
#416=TOROIDAL_SURFACE('',#35521,2.703125,0.0468750000000018);
#417=TOROIDAL_SURFACE('',#35525,2.703125,0.0468750000000018);
#418=TOROIDAL_SURFACE('',#35529,2.703125,0.0468750000000018);
#419=TOROIDAL_SURFACE('',#35533,2.703125,0.0468750000000018);
#420=TOROIDAL_SURFACE('',#35537,2.703125,0.0468750000000018);
#421=TOROIDAL_SURFACE('',#35541,2.703125,0.0468750000000018);
#422=TOROIDAL_SURFACE('',#35545,2.703125,0.0468750000000018);
#423=TOROIDAL_SURFACE('',#35549,2.703125,0.0468750000000018);
#424=TOROIDAL_SURFACE('',#35553,2.703125,0.0468750000000018);
#425=TOROIDAL_SURFACE('',#35557,2.703125,0.0468750000000018);
#426=TOROIDAL_SURFACE('',#35561,2.703125,0.0468750000000018);
#427=TOROIDAL_SURFACE('',#35565,2.703125,0.0468750000000018);
#428=TOROIDAL_SURFACE('',#35569,2.703125,0.0468750000000018);
#429=TOROIDAL_SURFACE('',#35573,2.703125,0.0468750000000018);
#430=TOROIDAL_SURFACE('',#35577,2.703125,0.0468750000000018);
#431=TOROIDAL_SURFACE('',#35581,2.703125,0.0468750000000018);
#432=TOROIDAL_SURFACE('',#35585,2.703125,0.0468750000000018);
#433=TOROIDAL_SURFACE('',#35589,2.703125,0.0468750000000018);
#434=TOROIDAL_SURFACE('',#35593,2.703125,0.0468750000000018);
#435=TOROIDAL_SURFACE('',#35597,2.703125,0.0468750000000018);
#436=TOROIDAL_SURFACE('',#35601,2.703125,0.0468750000000018);
#437=TOROIDAL_SURFACE('',#35605,2.703125,0.0468750000000018);
#438=TOROIDAL_SURFACE('',#35609,2.703125,0.0468750000000018);
#439=TOROIDAL_SURFACE('',#35613,2.703125,0.0468750000000018);
#440=TOROIDAL_SURFACE('',#35617,2.703125,0.0468750000000018);
#441=TOROIDAL_SURFACE('',#35621,2.703125,0.0468750000000018);
#442=TOROIDAL_SURFACE('',#35625,2.703125,0.0468750000000018);
#443=TOROIDAL_SURFACE('',#35629,2.703125,0.0468750000000018);
#444=TOROIDAL_SURFACE('',#35633,2.703125,0.0468750000000018);
#445=TOROIDAL_SURFACE('',#35637,2.703125,0.0468750000000018);
#446=TOROIDAL_SURFACE('',#35641,2.703125,0.0468750000000018);
#447=TOROIDAL_SURFACE('',#35645,2.703125,0.0468750000000018);
#448=TOROIDAL_SURFACE('',#35649,2.703125,0.0468750000000018);
#449=TOROIDAL_SURFACE('',#35653,2.703125,0.0468750000000018);
#450=TOROIDAL_SURFACE('',#35657,2.703125,0.0468750000000018);
#451=TOROIDAL_SURFACE('',#35661,2.703125,0.0468750000000018);
#452=TOROIDAL_SURFACE('',#35665,2.703125,0.0468750000000018);
#453=TOROIDAL_SURFACE('',#35669,2.703125,0.0468750000000018);
#454=TOROIDAL_SURFACE('',#35673,2.703125,0.0468750000000018);
#455=TOROIDAL_SURFACE('',#35677,2.703125,0.0468750000000018);
#456=TOROIDAL_SURFACE('',#35681,2.703125,0.0468750000000018);
#457=TOROIDAL_SURFACE('',#35685,2.703125,0.0468750000000018);
#458=TOROIDAL_SURFACE('',#35689,2.703125,0.0468750000000018);
#459=TOROIDAL_SURFACE('',#35693,2.703125,0.0468750000000018);
#460=TOROIDAL_SURFACE('',#35855,2.703125,0.046874999999999);
#461=TOROIDAL_SURFACE('',#35858,2.703125,0.046874999999999);
#462=TOROIDAL_SURFACE('',#35861,2.703125,0.046874999999999);
#463=TOROIDAL_SURFACE('',#35864,2.703125,0.046874999999999);
#464=TOROIDAL_SURFACE('',#35867,2.703125,0.046874999999999);
#465=TOROIDAL_SURFACE('',#35870,2.703125,0.046874999999999);
#466=TOROIDAL_SURFACE('',#35873,2.703125,0.046874999999999);
#467=TOROIDAL_SURFACE('',#35876,2.703125,0.046874999999999);
#468=TOROIDAL_SURFACE('',#35879,2.703125,0.046874999999999);
#469=TOROIDAL_SURFACE('',#35882,2.703125,0.046874999999999);
#470=TOROIDAL_SURFACE('',#35885,2.703125,0.046874999999999);
#471=TOROIDAL_SURFACE('',#35888,2.703125,0.046874999999999);
#472=TOROIDAL_SURFACE('',#35891,2.703125,0.046874999999999);
#473=TOROIDAL_SURFACE('',#35894,2.703125,0.046874999999999);
#474=TOROIDAL_SURFACE('',#35897,2.703125,0.046874999999999);
#475=TOROIDAL_SURFACE('',#35900,2.703125,0.046874999999999);
#476=TOROIDAL_SURFACE('',#35903,2.703125,0.046874999999999);
#477=TOROIDAL_SURFACE('',#35906,2.703125,0.046874999999999);
#478=TOROIDAL_SURFACE('',#35909,2.703125,0.046874999999999);
#479=TOROIDAL_SURFACE('',#35912,2.703125,0.046874999999999);
#480=TOROIDAL_SURFACE('',#35915,2.703125,0.046874999999999);
#481=TOROIDAL_SURFACE('',#35918,2.703125,0.046874999999999);
#482=TOROIDAL_SURFACE('',#35921,2.703125,0.046874999999999);
#483=TOROIDAL_SURFACE('',#35924,2.703125,0.046874999999999);
#484=TOROIDAL_SURFACE('',#35927,2.703125,0.046874999999999);
#485=TOROIDAL_SURFACE('',#35930,2.703125,0.046874999999999);
#486=TOROIDAL_SURFACE('',#35933,2.703125,0.046874999999999);
#487=TOROIDAL_SURFACE('',#35936,2.703125,0.046874999999999);
#488=TOROIDAL_SURFACE('',#35939,2.703125,0.046874999999999);
#489=TOROIDAL_SURFACE('',#35942,2.703125,0.046874999999999);
#490=TOROIDAL_SURFACE('',#35945,2.703125,0.046874999999999);
#491=TOROIDAL_SURFACE('',#35948,2.703125,0.046874999999999);
#492=TOROIDAL_SURFACE('',#35951,2.703125,0.046874999999999);
#493=TOROIDAL_SURFACE('',#35954,2.703125,0.046874999999999);
#494=TOROIDAL_SURFACE('',#35957,2.703125,0.046874999999999);
#495=TOROIDAL_SURFACE('',#35960,2.703125,0.046874999999999);
#496=TOROIDAL_SURFACE('',#35963,2.703125,0.046874999999999);
#497=TOROIDAL_SURFACE('',#35966,2.703125,0.046874999999999);
#498=TOROIDAL_SURFACE('',#35969,2.703125,0.046874999999999);
#499=TOROIDAL_SURFACE('',#35972,2.703125,0.046874999999999);
#500=TOROIDAL_SURFACE('',#35975,2.703125,0.046874999999999);
#501=TOROIDAL_SURFACE('',#35978,2.703125,0.046874999999999);
#502=TOROIDAL_SURFACE('',#35981,2.703125,0.046874999999999);
#503=TOROIDAL_SURFACE('',#35984,2.703125,0.046874999999999);
#504=TOROIDAL_SURFACE('',#35987,2.703125,0.046874999999999);
#505=TOROIDAL_SURFACE('',#35990,2.703125,0.046874999999999);
#506=TOROIDAL_SURFACE('',#35993,2.703125,0.046874999999999);
#507=TOROIDAL_SURFACE('',#35996,2.703125,0.046874999999999);
#508=TOROIDAL_SURFACE('',#35999,2.703125,0.046874999999999);
#509=TOROIDAL_SURFACE('',#36002,2.703125,0.046874999999999);
#510=TOROIDAL_SURFACE('',#36005,2.703125,0.046874999999999);
#511=TOROIDAL_SURFACE('',#36008,2.703125,0.046874999999999);
#512=TOROIDAL_SURFACE('',#36011,2.703125,0.046874999999999);
#513=TOROIDAL_SURFACE('',#36014,2.703125,0.046874999999999);
#514=TOROIDAL_SURFACE('',#36017,2.703125,0.046874999999999);
#515=TOROIDAL_SURFACE('',#36020,2.703125,0.046874999999999);
#516=TOROIDAL_SURFACE('',#36023,2.703125,0.046874999999999);
#517=TOROIDAL_SURFACE('',#36026,2.703125,0.046874999999999);
#518=TOROIDAL_SURFACE('',#36029,2.703125,0.046874999999999);
#519=TOROIDAL_SURFACE('',#36032,2.703125,0.046874999999999);
#520=TOROIDAL_SURFACE('',#36035,2.703125,0.046874999999999);
#521=TOROIDAL_SURFACE('',#36038,2.703125,0.046874999999999);
#522=TOROIDAL_SURFACE('',#36041,2.703125,0.046874999999999);
#523=TOROIDAL_SURFACE('',#36044,2.703125,0.046874999999999);
#524=TOROIDAL_SURFACE('',#36047,2.703125,0.046874999999999);
#525=TOROIDAL_SURFACE('',#36050,2.703125,0.046874999999999);
#526=TOROIDAL_SURFACE('',#36053,2.703125,0.046874999999999);
#527=TOROIDAL_SURFACE('',#36056,2.703125,0.046874999999999);
#528=TOROIDAL_SURFACE('',#36059,2.703125,0.046874999999999);
#529=TOROIDAL_SURFACE('',#36062,2.703125,0.046874999999999);
#530=TOROIDAL_SURFACE('',#36065,2.703125,0.046874999999999);
#531=TOROIDAL_SURFACE('',#36068,2.703125,0.046874999999999);
#532=TOROIDAL_SURFACE('',#36071,2.703125,0.046874999999999);
#533=TOROIDAL_SURFACE('',#36074,2.703125,0.046874999999999);
#534=TOROIDAL_SURFACE('',#36077,2.703125,0.046874999999999);
#535=TOROIDAL_SURFACE('',#36080,2.703125,0.046874999999999);
#536=TOROIDAL_SURFACE('',#36083,2.703125,0.046874999999999);
#537=TOROIDAL_SURFACE('',#36086,2.703125,0.046874999999999);
#538=TOROIDAL_SURFACE('',#36089,2.703125,0.046874999999999);
#539=TOROIDAL_SURFACE('',#36094,2.703125,0.0468750000000018);
#540=TOROIDAL_SURFACE('',#36100,2.703125,0.046874999999999);
#1195=(
BOUNDED_CURVE()
B_SPLINE_CURVE(2,(#70283,#70284,#70285),.UNSPECIFIED.,.F.,.F.)
B_SPLINE_CURVE_WITH_KNOTS((3,3),(-0.375752880509706,-0.25773139970398),
 .UNSPECIFIED.)
CURVE()
GEOMETRIC_REPRESENTATION_ITEM()
RATIONAL_B_SPLINE_CURVE((1.41147367097488,1.52065153937885,1.52065153937885))
REPRESENTATION_ITEM('')
);
#1196=(
BOUNDED_CURVE()
B_SPLINE_CURVE(2,(#70287,#70288,#70289),.UNSPECIFIED.,.F.,.F.)
B_SPLINE_CURVE_WITH_KNOTS((3,3),(-0.375752880509709,-0.139709918898254),
 .UNSPECIFIED.)
CURVE()
GEOMETRIC_REPRESENTATION_ITEM()
RATIONAL_B_SPLINE_CURVE((1.41147367097488,1.62982940778282,1.41147367097488))
REPRESENTATION_ITEM('')
);
#1197=(
BOUNDED_CURVE()
B_SPLINE_CURVE(2,(#70291,#70292,#70293),.UNSPECIFIED.,.F.,.F.)
B_SPLINE_CURVE_WITH_KNOTS((3,3),(-0.375752880509709,-0.139709918898254),
 .UNSPECIFIED.)
CURVE()
GEOMETRIC_REPRESENTATION_ITEM()
RATIONAL_B_SPLINE_CURVE((1.41147367097488,1.62982940778282,1.41147367097488))
REPRESENTATION_ITEM('')
);
#1198=(
BOUNDED_CURVE()
B_SPLINE_CURVE(2,(#70295,#70296,#70297),.UNSPECIFIED.,.F.,.F.)
B_SPLINE_CURVE_WITH_KNOTS((3,3),(-0.375752880509708,-0.139709918898254),
 .UNSPECIFIED.)
CURVE()
GEOMETRIC_REPRESENTATION_ITEM()
RATIONAL_B_SPLINE_CURVE((1.41147367097487,1.62982940778281,1.41147367097487))
REPRESENTATION_ITEM('')
);
#1199=(
BOUNDED_CURVE()
B_SPLINE_CURVE(2,(#70299,#70300,#70301),.UNSPECIFIED.,.F.,.F.)
B_SPLINE_CURVE_WITH_KNOTS((3,3),(-0.375752880509709,-0.139709918898253),
 .UNSPECIFIED.)
CURVE()
GEOMETRIC_REPRESENTATION_ITEM()
RATIONAL_B_SPLINE_CURVE((1.41147367097488,1.62982940778282,1.41147367097488))
REPRESENTATION_ITEM('')
);
#1200=(
BOUNDED_CURVE()
B_SPLINE_CURVE(2,(#70303,#70304,#70305),.UNSPECIFIED.,.F.,.F.)
B_SPLINE_CURVE_WITH_KNOTS((3,3),(-0.375752880509709,-0.139709918898254),
 .UNSPECIFIED.)
CURVE()
GEOMETRIC_REPRESENTATION_ITEM()
RATIONAL_B_SPLINE_CURVE((1.41147367097488,1.62982940778282,1.41147367097488))
REPRESENTATION_ITEM('')
);
#1201=(
BOUNDED_CURVE()
B_SPLINE_CURVE(2,(#70306,#70307,#70308),.UNSPECIFIED.,.F.,.F.)
B_SPLINE_CURVE_WITH_KNOTS((3,3),(-0.25773139970398,-0.139709918898256),
 .UNSPECIFIED.)
CURVE()
GEOMETRIC_REPRESENTATION_ITEM()
RATIONAL_B_SPLINE_CURVE((1.52065153937885,1.52065153937885,1.41147367097488))
REPRESENTATION_ITEM('')
);
#1202=(
BOUNDED_CURVE()
B_SPLINE_CURVE(2,(#70330,#70331,#70332),.UNSPECIFIED.,.F.,.F.)
B_SPLINE_CURVE_WITH_KNOTS((3,3),(0.367644516946548,0.373830527582523),
 .UNSPECIFIED.)
CURVE()
GEOMETRIC_REPRESENTATION_ITEM()
RATIONAL_B_SPLINE_CURVE((1.13426390111316,1.13389822901309,1.13348223894575))
REPRESENTATION_ITEM('')
);
#1203=(
BOUNDED_CURVE()
B_SPLINE_CURVE(2,(#70336,#70337,#70338),.UNSPECIFIED.,.F.,.F.)
B_SPLINE_CURVE_WITH_KNOTS((3,3),(0.271548216895916,0.277734227531904),
 .UNSPECIFIED.)
CURVE()
GEOMETRIC_REPRESENTATION_ITEM()
RATIONAL_B_SPLINE_CURVE((1.13348223894615,1.1338982290135,1.13426390111357))
REPRESENTATION_ITEM('')
);
#1204=(
BOUNDED_CURVE()
B_SPLINE_CURVE(2,(#70342,#70343,#70344),.UNSPECIFIED.,.F.,.F.)
B_SPLINE_CURVE_WITH_KNOTS((3,3),(0.36764451694656,0.373830527582529),
 .UNSPECIFIED.)
CURVE()
GEOMETRIC_REPRESENTATION_ITEM()
RATIONAL_B_SPLINE_CURVE((1.13426390111306,1.13389822901299,1.13348223894565))
REPRESENTATION_ITEM('')
);
#1205=(
BOUNDED_CURVE()
B_SPLINE_CURVE(2,(#70348,#70349,#70350),.UNSPECIFIED.,.F.,.F.)
B_SPLINE_CURVE_WITH_KNOTS((3,3),(0.271548216895914,0.277734227531901),
 .UNSPECIFIED.)
CURVE()
GEOMETRIC_REPRESENTATION_ITEM()
RATIONAL_B_SPLINE_CURVE((1.13348223894612,1.13389822901347,1.13426390111354))
REPRESENTATION_ITEM('')
);
#1206=(
BOUNDED_CURVE()
B_SPLINE_CURVE(2,(#70354,#70355,#70356),.UNSPECIFIED.,.F.,.F.)
B_SPLINE_CURVE_WITH_KNOTS((3,3),(0.367644516946562,0.373830527582532),
 .UNSPECIFIED.)
CURVE()
GEOMETRIC_REPRESENTATION_ITEM()
RATIONAL_B_SPLINE_CURVE((1.13426390111304,1.13389822901297,1.13348223894563))
REPRESENTATION_ITEM('')
);
#1207=(
BOUNDED_CURVE()
B_SPLINE_CURVE(2,(#70360,#70361,#70362),.UNSPECIFIED.,.F.,.F.)
B_SPLINE_CURVE_WITH_KNOTS((3,3),(0.27154821689591,0.277734227531895),
 .UNSPECIFIED.)
CURVE()
GEOMETRIC_REPRESENTATION_ITEM()
RATIONAL_B_SPLINE_CURVE((1.13348223894613,1.13389822901348,1.13426390111355))
REPRESENTATION_ITEM('')
);
#1208=(
BOUNDED_CURVE()
B_SPLINE_CURVE(2,(#70366,#70367,#70368),.UNSPECIFIED.,.F.,.F.)
B_SPLINE_CURVE_WITH_KNOTS((3,3),(0.367644516946554,0.373830527582529),
 .UNSPECIFIED.)
CURVE()
GEOMETRIC_REPRESENTATION_ITEM()
RATIONAL_B_SPLINE_CURVE((1.13426390111305,1.13389822901299,1.13348223894564))
REPRESENTATION_ITEM('')
);
#1209=(
BOUNDED_CURVE()
B_SPLINE_CURVE(2,(#70372,#70373,#70374),.UNSPECIFIED.,.F.,.F.)
B_SPLINE_CURVE_WITH_KNOTS((3,3),(0.271548216895907,0.277734227531893),
 .UNSPECIFIED.)
CURVE()
GEOMETRIC_REPRESENTATION_ITEM()
RATIONAL_B_SPLINE_CURVE((1.13348223894611,1.13389822901346,1.13426390111353))
REPRESENTATION_ITEM('')
);
#1210=(
BOUNDED_CURVE()
B_SPLINE_CURVE(2,(#70378,#70379,#70380),.UNSPECIFIED.,.F.,.F.)
B_SPLINE_CURVE_WITH_KNOTS((3,3),(0.367644516946562,0.373830527582532),
 .UNSPECIFIED.)
CURVE()
GEOMETRIC_REPRESENTATION_ITEM()
RATIONAL_B_SPLINE_CURVE((1.13426390111302,1.13389822901296,1.13348223894561))
REPRESENTATION_ITEM('')
);
#1211=(
BOUNDED_CURVE()
B_SPLINE_CURVE(2,(#70384,#70385,#70386),.UNSPECIFIED.,.F.,.F.)
B_SPLINE_CURVE_WITH_KNOTS((3,3),(0.271548216895914,0.277734227531899),
 .UNSPECIFIED.)
CURVE()
GEOMETRIC_REPRESENTATION_ITEM()
RATIONAL_B_SPLINE_CURVE((1.13348223894609,1.13389822901344,1.13426390111351))
REPRESENTATION_ITEM('')
);
#1212=(
BOUNDED_CURVE()
B_SPLINE_CURVE(2,(#70390,#70391,#70392),.UNSPECIFIED.,.F.,.F.)
B_SPLINE_CURVE_WITH_KNOTS((3,3),(0.36764451694656,0.373830527582535),
 .UNSPECIFIED.)
CURVE()
GEOMETRIC_REPRESENTATION_ITEM()
RATIONAL_B_SPLINE_CURVE((1.13426390111302,1.13389822901295,1.1334822389456))
REPRESENTATION_ITEM('')
);
#1213=(
BOUNDED_CURVE()
B_SPLINE_CURVE(2,(#70396,#70397,#70398),.UNSPECIFIED.,.F.,.F.)
B_SPLINE_CURVE_WITH_KNOTS((3,3),(0.271548216895908,0.277734227531894),
 .UNSPECIFIED.)
CURVE()
GEOMETRIC_REPRESENTATION_ITEM()
RATIONAL_B_SPLINE_CURVE((1.1334822389461,1.13389822901345,1.13426390111352))
REPRESENTATION_ITEM('')
);
#1214=(
BOUNDED_CURVE()
B_SPLINE_CURVE(2,(#70402,#70403,#70404),.UNSPECIFIED.,.F.,.F.)
B_SPLINE_CURVE_WITH_KNOTS((3,3),(0.367644516946558,0.373830527582536),
 .UNSPECIFIED.)
CURVE()
GEOMETRIC_REPRESENTATION_ITEM()
RATIONAL_B_SPLINE_CURVE((1.13426390111302,1.13389822901295,1.13348223894561))
REPRESENTATION_ITEM('')
);
#1215=(
BOUNDED_CURVE()
B_SPLINE_CURVE(2,(#70408,#70409,#70410),.UNSPECIFIED.,.F.,.F.)
B_SPLINE_CURVE_WITH_KNOTS((3,3),(0.271548216895914,0.277734227531899),
 .UNSPECIFIED.)
CURVE()
GEOMETRIC_REPRESENTATION_ITEM()
RATIONAL_B_SPLINE_CURVE((1.13348223894613,1.13389822901348,1.13426390111355))
REPRESENTATION_ITEM('')
);
#1216=(
BOUNDED_CURVE()
B_SPLINE_CURVE(2,(#70414,#70415,#70416),.UNSPECIFIED.,.F.,.F.)
B_SPLINE_CURVE_WITH_KNOTS((3,3),(0.367644516946564,0.373830527582534),
 .UNSPECIFIED.)
CURVE()
GEOMETRIC_REPRESENTATION_ITEM()
RATIONAL_B_SPLINE_CURVE((1.13426390111303,1.13389822901296,1.13348223894561))
REPRESENTATION_ITEM('')
);
#1217=(
BOUNDED_CURVE()
B_SPLINE_CURVE(2,(#70420,#70421,#70422),.UNSPECIFIED.,.F.,.F.)
B_SPLINE_CURVE_WITH_KNOTS((3,3),(0.271548216895916,0.277734227531901),
 .UNSPECIFIED.)
CURVE()
GEOMETRIC_REPRESENTATION_ITEM()
RATIONAL_B_SPLINE_CURVE((1.13348223894614,1.13389822901349,1.13426390111357))
REPRESENTATION_ITEM('')
);
#1218=(
BOUNDED_CURVE()
B_SPLINE_CURVE(2,(#70426,#70427,#70428),.UNSPECIFIED.,.F.,.F.)
B_SPLINE_CURVE_WITH_KNOTS((3,3),(0.367644516946554,0.373830527582527),
 .UNSPECIFIED.)
CURVE()
GEOMETRIC_REPRESENTATION_ITEM()
RATIONAL_B_SPLINE_CURVE((1.13426390111312,1.13389822901305,1.13348223894571))
REPRESENTATION_ITEM('')
);
#1219=(
BOUNDED_CURVE()
B_SPLINE_CURVE(2,(#70432,#70433,#70434),.UNSPECIFIED.,.F.,.F.)
B_SPLINE_CURVE_WITH_KNOTS((3,3),(0.271548216895913,0.2777342275319),
 .UNSPECIFIED.)
CURVE()
GEOMETRIC_REPRESENTATION_ITEM()
RATIONAL_B_SPLINE_CURVE((1.13348223894615,1.1338982290135,1.13426390111358))
REPRESENTATION_ITEM('')
);
#1220=(
BOUNDED_CURVE()
B_SPLINE_CURVE(2,(#70438,#70439,#70440),.UNSPECIFIED.,.F.,.F.)
B_SPLINE_CURVE_WITH_KNOTS((3,3),(0.367644516946564,0.373830527582538),
 .UNSPECIFIED.)
CURVE()
GEOMETRIC_REPRESENTATION_ITEM()
RATIONAL_B_SPLINE_CURVE((1.134263901113,1.13389822901293,1.13348223894559))
REPRESENTATION_ITEM('')
);
#1221=(
BOUNDED_CURVE()
B_SPLINE_CURVE(2,(#70444,#70445,#70446),.UNSPECIFIED.,.F.,.F.)
B_SPLINE_CURVE_WITH_KNOTS((3,3),(0.271548216895908,0.277734227531895),
 .UNSPECIFIED.)
CURVE()
GEOMETRIC_REPRESENTATION_ITEM()
RATIONAL_B_SPLINE_CURVE((1.13348223894615,1.1338982290135,1.13426390111358))
REPRESENTATION_ITEM('')
);
#1222=(
BOUNDED_CURVE()
B_SPLINE_CURVE(2,(#70450,#70451,#70452),.UNSPECIFIED.,.F.,.F.)
B_SPLINE_CURVE_WITH_KNOTS((3,3),(0.367644516946561,0.373830527582532),
 .UNSPECIFIED.)
CURVE()
GEOMETRIC_REPRESENTATION_ITEM()
RATIONAL_B_SPLINE_CURVE((1.13426390111309,1.13389822901302,1.13348223894568))
REPRESENTATION_ITEM('')
);
#1223=(
BOUNDED_CURVE()
B_SPLINE_CURVE(2,(#70456,#70457,#70458),.UNSPECIFIED.,.F.,.F.)
B_SPLINE_CURVE_WITH_KNOTS((3,3),(0.271548216895921,0.277734227531907),
 .UNSPECIFIED.)
CURVE()
GEOMETRIC_REPRESENTATION_ITEM()
RATIONAL_B_SPLINE_CURVE((1.13348223894616,1.13389822901351,1.13426390111358))
REPRESENTATION_ITEM('')
);
#1224=(
BOUNDED_CURVE()
B_SPLINE_CURVE(2,(#70462,#70463,#70464),.UNSPECIFIED.,.F.,.F.)
B_SPLINE_CURVE_WITH_KNOTS((3,3),(0.367644516946558,0.373830527582535),
 .UNSPECIFIED.)
CURVE()
GEOMETRIC_REPRESENTATION_ITEM()
RATIONAL_B_SPLINE_CURVE((1.13426390111305,1.13389822901298,1.13348223894564))
REPRESENTATION_ITEM('')
);
#1225=(
BOUNDED_CURVE()
B_SPLINE_CURVE(2,(#70468,#70469,#70470),.UNSPECIFIED.,.F.,.F.)
B_SPLINE_CURVE_WITH_KNOTS((3,3),(0.271548216895908,0.27773422753189),
 .UNSPECIFIED.)
CURVE()
GEOMETRIC_REPRESENTATION_ITEM()
RATIONAL_B_SPLINE_CURVE((1.13348223894616,1.13389822901351,1.13426390111359))
REPRESENTATION_ITEM('')
);
#1226=(
BOUNDED_CURVE()
B_SPLINE_CURVE(2,(#70474,#70475,#70476),.UNSPECIFIED.,.F.,.F.)
B_SPLINE_CURVE_WITH_KNOTS((3,3),(0.367644516946548,0.373830527582523),
 .UNSPECIFIED.)
CURVE()
GEOMETRIC_REPRESENTATION_ITEM()
RATIONAL_B_SPLINE_CURVE((1.13426390111314,1.13389822901308,1.13348223894573))
REPRESENTATION_ITEM('')
);
#1227=(
BOUNDED_CURVE()
B_SPLINE_CURVE(2,(#70480,#70481,#70482),.UNSPECIFIED.,.F.,.F.)
B_SPLINE_CURVE_WITH_KNOTS((3,3),(0.271548216895905,0.277734227531892),
 .UNSPECIFIED.)
CURVE()
GEOMETRIC_REPRESENTATION_ITEM()
RATIONAL_B_SPLINE_CURVE((1.13348223894608,1.13389822901343,1.1342639011135))
REPRESENTATION_ITEM('')
);
#1228=(
BOUNDED_CURVE()
B_SPLINE_CURVE(2,(#70486,#70487,#70488),.UNSPECIFIED.,.F.,.F.)
B_SPLINE_CURVE_WITH_KNOTS((3,3),(0.36764451694655,0.373830527582528),
 .UNSPECIFIED.)
CURVE()
GEOMETRIC_REPRESENTATION_ITEM()
RATIONAL_B_SPLINE_CURVE((1.1342639011131,1.13389822901304,1.13348223894569))
REPRESENTATION_ITEM('')
);
#1229=(
BOUNDED_CURVE()
B_SPLINE_CURVE(2,(#70492,#70493,#70494),.UNSPECIFIED.,.F.,.F.)
B_SPLINE_CURVE_WITH_KNOTS((3,3),(0.27154821689591,0.277734227531895),
 .UNSPECIFIED.)
CURVE()
GEOMETRIC_REPRESENTATION_ITEM()
RATIONAL_B_SPLINE_CURVE((1.13348223894612,1.13389822901347,1.13426390111354))
REPRESENTATION_ITEM('')
);
#1230=(
BOUNDED_CURVE()
B_SPLINE_CURVE(2,(#70498,#70499,#70500),.UNSPECIFIED.,.F.,.F.)
B_SPLINE_CURVE_WITH_KNOTS((3,3),(0.367644516946551,0.373830527582525),
 .UNSPECIFIED.)
CURVE()
GEOMETRIC_REPRESENTATION_ITEM()
RATIONAL_B_SPLINE_CURVE((1.13426390111313,1.13389822901307,1.13348223894572))
REPRESENTATION_ITEM('')
);
#1231=(
BOUNDED_CURVE()
B_SPLINE_CURVE(2,(#70504,#70505,#70506),.UNSPECIFIED.,.F.,.F.)
B_SPLINE_CURVE_WITH_KNOTS((3,3),(0.271548216895914,0.277734227531894),
 .UNSPECIFIED.)
CURVE()
GEOMETRIC_REPRESENTATION_ITEM()
RATIONAL_B_SPLINE_CURVE((1.13348223894619,1.13389822901354,1.13426390111361))
REPRESENTATION_ITEM('')
);
#1232=(
BOUNDED_CURVE()
B_SPLINE_CURVE(2,(#70510,#70511,#70512),.UNSPECIFIED.,.F.,.F.)
B_SPLINE_CURVE_WITH_KNOTS((3,3),(0.367644516946565,0.373830527582531),
 .UNSPECIFIED.)
CURVE()
GEOMETRIC_REPRESENTATION_ITEM()
RATIONAL_B_SPLINE_CURVE((1.134263901113,1.13389822901293,1.13348223894559))
REPRESENTATION_ITEM('')
);
#1233=(
BOUNDED_CURVE()
B_SPLINE_CURVE(2,(#70516,#70517,#70518),.UNSPECIFIED.,.F.,.F.)
B_SPLINE_CURVE_WITH_KNOTS((3,3),(0.271548216895912,0.277734227531896),
 .UNSPECIFIED.)
CURVE()
GEOMETRIC_REPRESENTATION_ITEM()
RATIONAL_B_SPLINE_CURVE((1.13348223894612,1.13389822901347,1.13426390111354))
REPRESENTATION_ITEM('')
);
#1234=(
BOUNDED_CURVE()
B_SPLINE_CURVE(2,(#70522,#70523,#70524),.UNSPECIFIED.,.F.,.F.)
B_SPLINE_CURVE_WITH_KNOTS((3,3),(0.367644516946563,0.373830527582537),
 .UNSPECIFIED.)
CURVE()
GEOMETRIC_REPRESENTATION_ITEM()
RATIONAL_B_SPLINE_CURVE((1.13426390111305,1.13389822901298,1.13348223894564))
REPRESENTATION_ITEM('')
);
#1235=(
BOUNDED_CURVE()
B_SPLINE_CURVE(2,(#70528,#70529,#70530),.UNSPECIFIED.,.F.,.F.)
B_SPLINE_CURVE_WITH_KNOTS((3,3),(0.271548216895909,0.277734227531891),
 .UNSPECIFIED.)
CURVE()
GEOMETRIC_REPRESENTATION_ITEM()
RATIONAL_B_SPLINE_CURVE((1.13348223894604,1.13389822901339,1.13426390111346))
REPRESENTATION_ITEM('')
);
#1236=(
BOUNDED_CURVE()
B_SPLINE_CURVE(2,(#70534,#70535,#70536),.UNSPECIFIED.,.F.,.F.)
B_SPLINE_CURVE_WITH_KNOTS((3,3),(0.367644516946552,0.373830527582532),
 .UNSPECIFIED.)
CURVE()
GEOMETRIC_REPRESENTATION_ITEM()
RATIONAL_B_SPLINE_CURVE((1.13426390111305,1.13389822901299,1.13348223894564))
REPRESENTATION_ITEM('')
);
#1237=(
BOUNDED_CURVE()
B_SPLINE_CURVE(2,(#70540,#70541,#70542),.UNSPECIFIED.,.F.,.F.)
B_SPLINE_CURVE_WITH_KNOTS((3,3),(0.271548216895916,0.277734227531902),
 .UNSPECIFIED.)
CURVE()
GEOMETRIC_REPRESENTATION_ITEM()
RATIONAL_B_SPLINE_CURVE((1.13348223894616,1.13389822901351,1.13426390111359))
REPRESENTATION_ITEM('')
);
#1238=(
BOUNDED_CURVE()
B_SPLINE_CURVE(2,(#70546,#70547,#70548),.UNSPECIFIED.,.F.,.F.)
B_SPLINE_CURVE_WITH_KNOTS((3,3),(0.367644516946562,0.373830527582535),
 .UNSPECIFIED.)
CURVE()
GEOMETRIC_REPRESENTATION_ITEM()
RATIONAL_B_SPLINE_CURVE((1.13426390111309,1.13389822901302,1.13348223894568))
REPRESENTATION_ITEM('')
);
#1239=(
BOUNDED_CURVE()
B_SPLINE_CURVE(2,(#70552,#70553,#70554),.UNSPECIFIED.,.F.,.F.)
B_SPLINE_CURVE_WITH_KNOTS((3,3),(0.271548216895913,0.277734227531904),
 .UNSPECIFIED.)
CURVE()
GEOMETRIC_REPRESENTATION_ITEM()
RATIONAL_B_SPLINE_CURVE((1.13348223894619,1.13389822901354,1.13426390111362))
REPRESENTATION_ITEM('')
);
#1240=(
BOUNDED_CURVE()
B_SPLINE_CURVE(2,(#70558,#70559,#70560),.UNSPECIFIED.,.F.,.F.)
B_SPLINE_CURVE_WITH_KNOTS((3,3),(0.36764451694655,0.373830527582524),
 .UNSPECIFIED.)
CURVE()
GEOMETRIC_REPRESENTATION_ITEM()
RATIONAL_B_SPLINE_CURVE((1.13426390111312,1.13389822901305,1.13348223894571))
REPRESENTATION_ITEM('')
);
#1241=(
BOUNDED_CURVE()
B_SPLINE_CURVE(2,(#70564,#70565,#70566),.UNSPECIFIED.,.F.,.F.)
B_SPLINE_CURVE_WITH_KNOTS((3,3),(0.271548216895921,0.277734227531899),
 .UNSPECIFIED.)
CURVE()
GEOMETRIC_REPRESENTATION_ITEM()
RATIONAL_B_SPLINE_CURVE((1.13348223894619,1.13389822901354,1.13426390111361))
REPRESENTATION_ITEM('')
);
#1242=(
BOUNDED_CURVE()
B_SPLINE_CURVE(2,(#70570,#70571,#70572),.UNSPECIFIED.,.F.,.F.)
B_SPLINE_CURVE_WITH_KNOTS((3,3),(0.367644516946559,0.373830527582526),
 .UNSPECIFIED.)
CURVE()
GEOMETRIC_REPRESENTATION_ITEM()
RATIONAL_B_SPLINE_CURVE((1.1342639011131,1.13389822901303,1.13348223894569))
REPRESENTATION_ITEM('')
);
#1243=(
BOUNDED_CURVE()
B_SPLINE_CURVE(2,(#70576,#70577,#70578),.UNSPECIFIED.,.F.,.F.)
B_SPLINE_CURVE_WITH_KNOTS((3,3),(0.271548216895914,0.2777342275319),
 .UNSPECIFIED.)
CURVE()
GEOMETRIC_REPRESENTATION_ITEM()
RATIONAL_B_SPLINE_CURVE((1.13348223894616,1.13389822901351,1.13426390111358))
REPRESENTATION_ITEM('')
);
#1244=(
BOUNDED_CURVE()
B_SPLINE_CURVE(2,(#70582,#70583,#70584),.UNSPECIFIED.,.F.,.F.)
B_SPLINE_CURVE_WITH_KNOTS((3,3),(0.367644516946557,0.373830527582536),
 .UNSPECIFIED.)
CURVE()
GEOMETRIC_REPRESENTATION_ITEM()
RATIONAL_B_SPLINE_CURVE((1.13426390111309,1.13389822901303,1.13348223894568))
REPRESENTATION_ITEM('')
);
#1245=(
BOUNDED_CURVE()
B_SPLINE_CURVE(2,(#70588,#70589,#70590),.UNSPECIFIED.,.F.,.F.)
B_SPLINE_CURVE_WITH_KNOTS((3,3),(0.271548216895912,0.277734227531897),
 .UNSPECIFIED.)
CURVE()
GEOMETRIC_REPRESENTATION_ITEM()
RATIONAL_B_SPLINE_CURVE((1.13348223894616,1.13389822901351,1.13426390111358))
REPRESENTATION_ITEM('')
);
#1246=(
BOUNDED_CURVE()
B_SPLINE_CURVE(2,(#70594,#70595,#70596),.UNSPECIFIED.,.F.,.F.)
B_SPLINE_CURVE_WITH_KNOTS((3,3),(0.367644516946558,0.373830527582532),
 .UNSPECIFIED.)
CURVE()
GEOMETRIC_REPRESENTATION_ITEM()
RATIONAL_B_SPLINE_CURVE((1.13426390111307,1.13389822901301,1.13348223894566))
REPRESENTATION_ITEM('')
);
#1247=(
BOUNDED_CURVE()
B_SPLINE_CURVE(2,(#70600,#70601,#70602),.UNSPECIFIED.,.F.,.F.)
B_SPLINE_CURVE_WITH_KNOTS((3,3),(0.271548216895914,0.277734227531905),
 .UNSPECIFIED.)
CURVE()
GEOMETRIC_REPRESENTATION_ITEM()
RATIONAL_B_SPLINE_CURVE((1.13348223894616,1.13389822901351,1.13426390111358))
REPRESENTATION_ITEM('')
);
#1248=(
BOUNDED_CURVE()
B_SPLINE_CURVE(2,(#70606,#70607,#70608),.UNSPECIFIED.,.F.,.F.)
B_SPLINE_CURVE_WITH_KNOTS((3,3),(0.367644516946569,0.373830527582539),
 .UNSPECIFIED.)
CURVE()
GEOMETRIC_REPRESENTATION_ITEM()
RATIONAL_B_SPLINE_CURVE((1.13426390111301,1.13389822901295,1.1334822389456))
REPRESENTATION_ITEM('')
);
#1249=(
BOUNDED_CURVE()
B_SPLINE_CURVE(2,(#70612,#70613,#70614),.UNSPECIFIED.,.F.,.F.)
B_SPLINE_CURVE_WITH_KNOTS((3,3),(0.271548216895913,0.2777342275319),
 .UNSPECIFIED.)
CURVE()
GEOMETRIC_REPRESENTATION_ITEM()
RATIONAL_B_SPLINE_CURVE((1.13348223894614,1.13389822901349,1.13426390111356))
REPRESENTATION_ITEM('')
);
#1250=(
BOUNDED_CURVE()
B_SPLINE_CURVE(2,(#70618,#70619,#70620),.UNSPECIFIED.,.F.,.F.)
B_SPLINE_CURVE_WITH_KNOTS((3,3),(0.367644516946566,0.373830527582539),
 .UNSPECIFIED.)
CURVE()
GEOMETRIC_REPRESENTATION_ITEM()
RATIONAL_B_SPLINE_CURVE((1.13426390111297,1.1338982290129,1.13348223894556))
REPRESENTATION_ITEM('')
);
#1251=(
BOUNDED_CURVE()
B_SPLINE_CURVE(2,(#70624,#70625,#70626),.UNSPECIFIED.,.F.,.F.)
B_SPLINE_CURVE_WITH_KNOTS((3,3),(0.271548216895926,0.277734227531904),
 .UNSPECIFIED.)
CURVE()
GEOMETRIC_REPRESENTATION_ITEM()
RATIONAL_B_SPLINE_CURVE((1.13348223894627,1.13389822901362,1.1342639011137))
REPRESENTATION_ITEM('')
);
#1252=(
BOUNDED_CURVE()
B_SPLINE_CURVE(2,(#70630,#70631,#70632),.UNSPECIFIED.,.F.,.F.)
B_SPLINE_CURVE_WITH_KNOTS((3,3),(0.367644516946557,0.373830527582532),
 .UNSPECIFIED.)
CURVE()
GEOMETRIC_REPRESENTATION_ITEM()
RATIONAL_B_SPLINE_CURVE((1.13426390111306,1.13389822901299,1.13348223894565))
REPRESENTATION_ITEM('')
);
#1253=(
BOUNDED_CURVE()
B_SPLINE_CURVE(2,(#70636,#70637,#70638),.UNSPECIFIED.,.F.,.F.)
B_SPLINE_CURVE_WITH_KNOTS((3,3),(0.271548216895913,0.277734227531899),
 .UNSPECIFIED.)
CURVE()
GEOMETRIC_REPRESENTATION_ITEM()
RATIONAL_B_SPLINE_CURVE((1.13348223894618,1.13389822901353,1.13426390111361))
REPRESENTATION_ITEM('')
);
#1254=(
BOUNDED_CURVE()
B_SPLINE_CURVE(2,(#70642,#70643,#70644),.UNSPECIFIED.,.F.,.F.)
B_SPLINE_CURVE_WITH_KNOTS((3,3),(0.367644516946561,0.373830527582535),
 .UNSPECIFIED.)
CURVE()
GEOMETRIC_REPRESENTATION_ITEM()
RATIONAL_B_SPLINE_CURVE((1.13426390111305,1.13389822901298,1.13348223894564))
REPRESENTATION_ITEM('')
);
#1255=(
BOUNDED_CURVE()
B_SPLINE_CURVE(2,(#70648,#70649,#70650),.UNSPECIFIED.,.F.,.F.)
B_SPLINE_CURVE_WITH_KNOTS((3,3),(0.271548216895915,0.277734227531905),
 .UNSPECIFIED.)
CURVE()
GEOMETRIC_REPRESENTATION_ITEM()
RATIONAL_B_SPLINE_CURVE((1.13348223894613,1.13389822901348,1.13426390111356))
REPRESENTATION_ITEM('')
);
#1256=(
BOUNDED_CURVE()
B_SPLINE_CURVE(2,(#70654,#70655,#70656),.UNSPECIFIED.,.F.,.F.)
B_SPLINE_CURVE_WITH_KNOTS((3,3),(0.367644516946559,0.373830527582528),
 .UNSPECIFIED.)
CURVE()
GEOMETRIC_REPRESENTATION_ITEM()
RATIONAL_B_SPLINE_CURVE((1.13426390111303,1.13389822901297,1.13348223894562))
REPRESENTATION_ITEM('')
);
#1257=(
BOUNDED_CURVE()
B_SPLINE_CURVE(2,(#70660,#70661,#70662),.UNSPECIFIED.,.F.,.F.)
B_SPLINE_CURVE_WITH_KNOTS((3,3),(0.271548216895913,0.277734227531899),
 .UNSPECIFIED.)
CURVE()
GEOMETRIC_REPRESENTATION_ITEM()
RATIONAL_B_SPLINE_CURVE((1.13348223894613,1.13389822901348,1.13426390111356))
REPRESENTATION_ITEM('')
);
#1258=(
BOUNDED_CURVE()
B_SPLINE_CURVE(2,(#70666,#70667,#70668),.UNSPECIFIED.,.F.,.F.)
B_SPLINE_CURVE_WITH_KNOTS((3,3),(0.367644516946557,0.373830527582533),
 .UNSPECIFIED.)
CURVE()
GEOMETRIC_REPRESENTATION_ITEM()
RATIONAL_B_SPLINE_CURVE((1.13426390111302,1.13389822901296,1.13348223894561))
REPRESENTATION_ITEM('')
);
#1259=(
BOUNDED_CURVE()
B_SPLINE_CURVE(2,(#70672,#70673,#70674),.UNSPECIFIED.,.F.,.F.)
B_SPLINE_CURVE_WITH_KNOTS((3,3),(0.271548216895926,0.277734227531906),
 .UNSPECIFIED.)
CURVE()
GEOMETRIC_REPRESENTATION_ITEM()
RATIONAL_B_SPLINE_CURVE((1.13348223894624,1.13389822901359,1.13426390111366))
REPRESENTATION_ITEM('')
);
#1260=(
BOUNDED_CURVE()
B_SPLINE_CURVE(2,(#70678,#70679,#70680),.UNSPECIFIED.,.F.,.F.)
B_SPLINE_CURVE_WITH_KNOTS((3,3),(0.367644516946561,0.373830527582536),
 .UNSPECIFIED.)
CURVE()
GEOMETRIC_REPRESENTATION_ITEM()
RATIONAL_B_SPLINE_CURVE((1.13426390111306,1.13389822901299,1.13348223894564))
REPRESENTATION_ITEM('')
);
#1261=(
BOUNDED_CURVE()
B_SPLINE_CURVE(2,(#70684,#70685,#70686),.UNSPECIFIED.,.F.,.F.)
B_SPLINE_CURVE_WITH_KNOTS((3,3),(0.271548216895911,0.277734227531901),
 .UNSPECIFIED.)
CURVE()
GEOMETRIC_REPRESENTATION_ITEM()
RATIONAL_B_SPLINE_CURVE((1.13348223894609,1.13389822901344,1.13426390111352))
REPRESENTATION_ITEM('')
);
#1262=(
BOUNDED_CURVE()
B_SPLINE_CURVE(2,(#70690,#70691,#70692),.UNSPECIFIED.,.F.,.F.)
B_SPLINE_CURVE_WITH_KNOTS((3,3),(0.367644516946558,0.373830527582533),
 .UNSPECIFIED.)
CURVE()
GEOMETRIC_REPRESENTATION_ITEM()
RATIONAL_B_SPLINE_CURVE((1.1342639011131,1.13389822901303,1.13348223894569))
REPRESENTATION_ITEM('')
);
#1263=(
BOUNDED_CURVE()
B_SPLINE_CURVE(2,(#70696,#70697,#70698),.UNSPECIFIED.,.F.,.F.)
B_SPLINE_CURVE_WITH_KNOTS((3,3),(0.271548216895922,0.277734227531909),
 .UNSPECIFIED.)
CURVE()
GEOMETRIC_REPRESENTATION_ITEM()
RATIONAL_B_SPLINE_CURVE((1.13348223894623,1.13389822901358,1.13426390111366))
REPRESENTATION_ITEM('')
);
#1264=(
BOUNDED_CURVE()
B_SPLINE_CURVE(2,(#70702,#70703,#70704),.UNSPECIFIED.,.F.,.F.)
B_SPLINE_CURVE_WITH_KNOTS((3,3),(0.367644516946562,0.373830527582538),
 .UNSPECIFIED.)
CURVE()
GEOMETRIC_REPRESENTATION_ITEM()
RATIONAL_B_SPLINE_CURVE((1.13426390111305,1.13389822901298,1.13348223894563))
REPRESENTATION_ITEM('')
);
#1265=(
BOUNDED_CURVE()
B_SPLINE_CURVE(2,(#70708,#70709,#70710),.UNSPECIFIED.,.F.,.F.)
B_SPLINE_CURVE_WITH_KNOTS((3,3),(0.271548216895906,0.277734227531898),
 .UNSPECIFIED.)
CURVE()
GEOMETRIC_REPRESENTATION_ITEM()
RATIONAL_B_SPLINE_CURVE((1.13348223894604,1.13389822901339,1.13426390111346))
REPRESENTATION_ITEM('')
);
#1266=(
BOUNDED_CURVE()
B_SPLINE_CURVE(2,(#70714,#70715,#70716),.UNSPECIFIED.,.F.,.F.)
B_SPLINE_CURVE_WITH_KNOTS((3,3),(0.367644516946563,0.373830527582537),
 .UNSPECIFIED.)
CURVE()
GEOMETRIC_REPRESENTATION_ITEM()
RATIONAL_B_SPLINE_CURVE((1.134263901113,1.13389822901294,1.13348223894559))
REPRESENTATION_ITEM('')
);
#1267=(
BOUNDED_CURVE()
B_SPLINE_CURVE(2,(#70720,#70721,#70722),.UNSPECIFIED.,.F.,.F.)
B_SPLINE_CURVE_WITH_KNOTS((3,3),(0.271548216895914,0.277734227531897),
 .UNSPECIFIED.)
CURVE()
GEOMETRIC_REPRESENTATION_ITEM()
RATIONAL_B_SPLINE_CURVE((1.13348223894613,1.13389822901348,1.13426390111355))
REPRESENTATION_ITEM('')
);
#1268=(
BOUNDED_CURVE()
B_SPLINE_CURVE(2,(#70726,#70727,#70728),.UNSPECIFIED.,.F.,.F.)
B_SPLINE_CURVE_WITH_KNOTS((3,3),(0.367644516946558,0.373830527582532),
 .UNSPECIFIED.)
CURVE()
GEOMETRIC_REPRESENTATION_ITEM()
RATIONAL_B_SPLINE_CURVE((1.13426390111307,1.133898229013,1.13348223894566))
REPRESENTATION_ITEM('')
);
#1269=(
BOUNDED_CURVE()
B_SPLINE_CURVE(2,(#70732,#70733,#70734),.UNSPECIFIED.,.F.,.F.)
B_SPLINE_CURVE_WITH_KNOTS((3,3),(0.271548216895917,0.277734227531901),
 .UNSPECIFIED.)
CURVE()
GEOMETRIC_REPRESENTATION_ITEM()
RATIONAL_B_SPLINE_CURVE((1.13348223894616,1.1338982290135,1.13426390111358))
REPRESENTATION_ITEM('')
);
#1270=(
BOUNDED_CURVE()
B_SPLINE_CURVE(2,(#70738,#70739,#70740),.UNSPECIFIED.,.F.,.F.)
B_SPLINE_CURVE_WITH_KNOTS((3,3),(0.367644516946556,0.37383052758253),
 .UNSPECIFIED.)
CURVE()
GEOMETRIC_REPRESENTATION_ITEM()
RATIONAL_B_SPLINE_CURVE((1.13426390111304,1.13389822901297,1.13348223894563))
REPRESENTATION_ITEM('')
);
#1271=(
BOUNDED_CURVE()
B_SPLINE_CURVE(2,(#70744,#70745,#70746),.UNSPECIFIED.,.F.,.F.)
B_SPLINE_CURVE_WITH_KNOTS((3,3),(0.271548216895911,0.277734227531893),
 .UNSPECIFIED.)
CURVE()
GEOMETRIC_REPRESENTATION_ITEM()
RATIONAL_B_SPLINE_CURVE((1.13348223894607,1.13389822901342,1.13426390111349))
REPRESENTATION_ITEM('')
);
#1272=(
BOUNDED_CURVE()
B_SPLINE_CURVE(2,(#70750,#70751,#70752),.UNSPECIFIED.,.F.,.F.)
B_SPLINE_CURVE_WITH_KNOTS((3,3),(0.367644516946565,0.373830527582539),
 .UNSPECIFIED.)
CURVE()
GEOMETRIC_REPRESENTATION_ITEM()
RATIONAL_B_SPLINE_CURVE((1.13426390111301,1.13389822901295,1.1334822389456))
REPRESENTATION_ITEM('')
);
#1273=(
BOUNDED_CURVE()
B_SPLINE_CURVE(2,(#70756,#70757,#70758),.UNSPECIFIED.,.F.,.F.)
B_SPLINE_CURVE_WITH_KNOTS((3,3),(0.271548216895916,0.277734227531897),
 .UNSPECIFIED.)
CURVE()
GEOMETRIC_REPRESENTATION_ITEM()
RATIONAL_B_SPLINE_CURVE((1.13348223894613,1.13389822901348,1.13426390111355))
REPRESENTATION_ITEM('')
);
#1274=(
BOUNDED_CURVE()
B_SPLINE_CURVE(2,(#70762,#70763,#70764),.UNSPECIFIED.,.F.,.F.)
B_SPLINE_CURVE_WITH_KNOTS((3,3),(0.36764451694656,0.373830527582534),
 .UNSPECIFIED.)
CURVE()
GEOMETRIC_REPRESENTATION_ITEM()
RATIONAL_B_SPLINE_CURVE((1.13426390111306,1.13389822901299,1.13348223894564))
REPRESENTATION_ITEM('')
);
#1275=(
BOUNDED_CURVE()
B_SPLINE_CURVE(2,(#70768,#70769,#70770),.UNSPECIFIED.,.F.,.F.)
B_SPLINE_CURVE_WITH_KNOTS((3,3),(0.271548216895918,0.277734227531904),
 .UNSPECIFIED.)
CURVE()
GEOMETRIC_REPRESENTATION_ITEM()
RATIONAL_B_SPLINE_CURVE((1.13348223894613,1.13389822901348,1.13426390111355))
REPRESENTATION_ITEM('')
);
#1276=(
BOUNDED_CURVE()
B_SPLINE_CURVE(2,(#70774,#70775,#70776),.UNSPECIFIED.,.F.,.F.)
B_SPLINE_CURVE_WITH_KNOTS((3,3),(0.367644516946555,0.373830527582533),
 .UNSPECIFIED.)
CURVE()
GEOMETRIC_REPRESENTATION_ITEM()
RATIONAL_B_SPLINE_CURVE((1.13426390111305,1.13389822901298,1.13348223894564))
REPRESENTATION_ITEM('')
);
#1277=(
BOUNDED_CURVE()
B_SPLINE_CURVE(2,(#70780,#70781,#70782),.UNSPECIFIED.,.F.,.F.)
B_SPLINE_CURVE_WITH_KNOTS((3,3),(0.271548216895928,0.277734227531916),
 .UNSPECIFIED.)
CURVE()
GEOMETRIC_REPRESENTATION_ITEM()
RATIONAL_B_SPLINE_CURVE((1.13348223894621,1.13389822901356,1.13426390111363))
REPRESENTATION_ITEM('')
);
#1278=(
BOUNDED_CURVE()
B_SPLINE_CURVE(2,(#70786,#70787,#70788),.UNSPECIFIED.,.F.,.F.)
B_SPLINE_CURVE_WITH_KNOTS((3,3),(0.367644516946548,0.373830527582523),
 .UNSPECIFIED.)
CURVE()
GEOMETRIC_REPRESENTATION_ITEM()
RATIONAL_B_SPLINE_CURVE((1.13426390111312,1.13389822901305,1.13348223894571))
REPRESENTATION_ITEM('')
);
#1279=(
BOUNDED_CURVE()
B_SPLINE_CURVE(2,(#70792,#70793,#70794),.UNSPECIFIED.,.F.,.F.)
B_SPLINE_CURVE_WITH_KNOTS((3,3),(0.271548216895918,0.277734227531905),
 .UNSPECIFIED.)
CURVE()
GEOMETRIC_REPRESENTATION_ITEM()
RATIONAL_B_SPLINE_CURVE((1.13348223894611,1.13389822901346,1.13426390111354))
REPRESENTATION_ITEM('')
);
#1280=(
BOUNDED_CURVE()
B_SPLINE_CURVE(2,(#70798,#70799,#70800),.UNSPECIFIED.,.F.,.F.)
B_SPLINE_CURVE_WITH_KNOTS((3,3),(0.367644516946559,0.373830527582532),
 .UNSPECIFIED.)
CURVE()
GEOMETRIC_REPRESENTATION_ITEM()
RATIONAL_B_SPLINE_CURVE((1.13426390111305,1.13389822901298,1.13348223894564))
REPRESENTATION_ITEM('')
);
#1281=(
BOUNDED_CURVE()
B_SPLINE_CURVE(2,(#70804,#70805,#70806),.UNSPECIFIED.,.F.,.F.)
B_SPLINE_CURVE_WITH_KNOTS((3,3),(0.271548216895915,0.277734227531901),
 .UNSPECIFIED.)
CURVE()
GEOMETRIC_REPRESENTATION_ITEM()
RATIONAL_B_SPLINE_CURVE((1.13348223894615,1.1338982290135,1.13426390111357))
REPRESENTATION_ITEM('')
);
#1282=(
BOUNDED_CURVE()
B_SPLINE_CURVE(2,(#70810,#70811,#70812),.UNSPECIFIED.,.F.,.F.)
B_SPLINE_CURVE_WITH_KNOTS((3,3),(0.367644516946548,0.373830527582526),
 .UNSPECIFIED.)
CURVE()
GEOMETRIC_REPRESENTATION_ITEM()
RATIONAL_B_SPLINE_CURVE((1.13426390111308,1.13389822901302,1.13348223894567))
REPRESENTATION_ITEM('')
);
#1283=(
BOUNDED_CURVE()
B_SPLINE_CURVE(2,(#70816,#70817,#70818),.UNSPECIFIED.,.F.,.F.)
B_SPLINE_CURVE_WITH_KNOTS((3,3),(0.271548216895917,0.277734227531902),
 .UNSPECIFIED.)
CURVE()
GEOMETRIC_REPRESENTATION_ITEM()
RATIONAL_B_SPLINE_CURVE((1.13348223894615,1.1338982290135,1.13426390111358))
REPRESENTATION_ITEM('')
);
#1284=(
BOUNDED_CURVE()
B_SPLINE_CURVE(2,(#70822,#70823,#70824),.UNSPECIFIED.,.F.,.F.)
B_SPLINE_CURVE_WITH_KNOTS((3,3),(0.367644516946561,0.373830527582534),
 .UNSPECIFIED.)
CURVE()
GEOMETRIC_REPRESENTATION_ITEM()
RATIONAL_B_SPLINE_CURVE((1.13426390111303,1.13389822901296,1.13348223894562))
REPRESENTATION_ITEM('')
);
#1285=(
BOUNDED_CURVE()
B_SPLINE_CURVE(2,(#70828,#70829,#70830),.UNSPECIFIED.,.F.,.F.)
B_SPLINE_CURVE_WITH_KNOTS((3,3),(0.271548216895922,0.277734227531908),
 .UNSPECIFIED.)
CURVE()
GEOMETRIC_REPRESENTATION_ITEM()
RATIONAL_B_SPLINE_CURVE((1.13348223894617,1.13389822901352,1.1342639011136))
REPRESENTATION_ITEM('')
);
#1286=(
BOUNDED_CURVE()
B_SPLINE_CURVE(2,(#70834,#70835,#70836),.UNSPECIFIED.,.F.,.F.)
B_SPLINE_CURVE_WITH_KNOTS((3,3),(0.367644516946555,0.373830527582532),
 .UNSPECIFIED.)
CURVE()
GEOMETRIC_REPRESENTATION_ITEM()
RATIONAL_B_SPLINE_CURVE((1.13426390111307,1.133898229013,1.13348223894566))
REPRESENTATION_ITEM('')
);
#1287=(
BOUNDED_CURVE()
B_SPLINE_CURVE(2,(#70840,#70841,#70842),.UNSPECIFIED.,.F.,.F.)
B_SPLINE_CURVE_WITH_KNOTS((3,3),(0.27154821689592,0.277734227531907),
 .UNSPECIFIED.)
CURVE()
GEOMETRIC_REPRESENTATION_ITEM()
RATIONAL_B_SPLINE_CURVE((1.13348223894614,1.13389822901349,1.13426390111356))
REPRESENTATION_ITEM('')
);
#1288=(
BOUNDED_CURVE()
B_SPLINE_CURVE(2,(#70846,#70847,#70848),.UNSPECIFIED.,.F.,.F.)
B_SPLINE_CURVE_WITH_KNOTS((3,3),(0.367644516946564,0.373830527582538),
 .UNSPECIFIED.)
CURVE()
GEOMETRIC_REPRESENTATION_ITEM()
RATIONAL_B_SPLINE_CURVE((1.13426390111299,1.13389822901292,1.13348223894557))
REPRESENTATION_ITEM('')
);
#1289=(
BOUNDED_CURVE()
B_SPLINE_CURVE(2,(#70852,#70853,#70854),.UNSPECIFIED.,.F.,.F.)
B_SPLINE_CURVE_WITH_KNOTS((3,3),(0.271548216895926,0.277734227531912),
 .UNSPECIFIED.)
CURVE()
GEOMETRIC_REPRESENTATION_ITEM()
RATIONAL_B_SPLINE_CURVE((1.13348223894617,1.13389822901352,1.13426390111359))
REPRESENTATION_ITEM('')
);
#1290=(
BOUNDED_CURVE()
B_SPLINE_CURVE(2,(#70858,#70859,#70860),.UNSPECIFIED.,.F.,.F.)
B_SPLINE_CURVE_WITH_KNOTS((3,3),(0.367644516946548,0.373830527582525),
 .UNSPECIFIED.)
CURVE()
GEOMETRIC_REPRESENTATION_ITEM()
RATIONAL_B_SPLINE_CURVE((1.13426390111308,1.13389822901301,1.13348223894567))
REPRESENTATION_ITEM('')
);
#1291=(
BOUNDED_CURVE()
B_SPLINE_CURVE(2,(#70864,#70865,#70866),.UNSPECIFIED.,.F.,.F.)
B_SPLINE_CURVE_WITH_KNOTS((3,3),(0.271548216895921,0.277734227531907),
 .UNSPECIFIED.)
CURVE()
GEOMETRIC_REPRESENTATION_ITEM()
RATIONAL_B_SPLINE_CURVE((1.13348223894617,1.13389822901352,1.13426390111359))
REPRESENTATION_ITEM('')
);
#1292=(
BOUNDED_CURVE()
B_SPLINE_CURVE(2,(#70870,#70871,#70872),.UNSPECIFIED.,.F.,.F.)
B_SPLINE_CURVE_WITH_KNOTS((3,3),(0.367644516946557,0.373830527582527),
 .UNSPECIFIED.)
CURVE()
GEOMETRIC_REPRESENTATION_ITEM()
RATIONAL_B_SPLINE_CURVE((1.1342639011131,1.13389822901303,1.13348223894569))
REPRESENTATION_ITEM('')
);
#1293=(
BOUNDED_CURVE()
B_SPLINE_CURVE(2,(#70875,#70876,#70877),.UNSPECIFIED.,.F.,.F.)
B_SPLINE_CURVE_WITH_KNOTS((3,3),(0.271548216895922,0.277734227531908),
 .UNSPECIFIED.)
CURVE()
GEOMETRIC_REPRESENTATION_ITEM()
RATIONAL_B_SPLINE_CURVE((1.13348223894615,1.1338982290135,1.13426390111358))
REPRESENTATION_ITEM('')
);
#1294=(
BOUNDED_CURVE()
B_SPLINE_CURVE(2,(#70879,#70880,#70881),.UNSPECIFIED.,.F.,.F.)
B_SPLINE_CURVE_WITH_KNOTS((3,3),(0.367644516946556,0.373830527582529),
 .UNSPECIFIED.)
CURVE()
GEOMETRIC_REPRESENTATION_ITEM()
RATIONAL_B_SPLINE_CURVE((1.13426390111308,1.13389822901301,1.13348223894567))
REPRESENTATION_ITEM('')
);
#1295=(
BOUNDED_CURVE()
B_SPLINE_CURVE(2,(#70884,#70885,#70886),.UNSPECIFIED.,.F.,.F.)
B_SPLINE_CURVE_WITH_KNOTS((3,3),(0.271548216895921,0.277734227531909),
 .UNSPECIFIED.)
CURVE()
GEOMETRIC_REPRESENTATION_ITEM()
RATIONAL_B_SPLINE_CURVE((1.13348223894619,1.13389822901354,1.13426390111361))
REPRESENTATION_ITEM('')
);
#1296=(
BOUNDED_CURVE()
B_SPLINE_CURVE(2,(#70888,#70889,#70890),.UNSPECIFIED.,.F.,.F.)
B_SPLINE_CURVE_WITH_KNOTS((3,3),(0.36764451694656,0.37383052758253),
 .UNSPECIFIED.)
CURVE()
GEOMETRIC_REPRESENTATION_ITEM()
RATIONAL_B_SPLINE_CURVE((1.13426390111303,1.13389822901296,1.13348223894562))
REPRESENTATION_ITEM('')
);
#1297=(
BOUNDED_CURVE()
B_SPLINE_CURVE(2,(#70893,#70894,#70895),.UNSPECIFIED.,.F.,.F.)
B_SPLINE_CURVE_WITH_KNOTS((3,3),(0.271548216895921,0.277734227531907),
 .UNSPECIFIED.)
CURVE()
GEOMETRIC_REPRESENTATION_ITEM()
RATIONAL_B_SPLINE_CURVE((1.13348223894618,1.13389822901353,1.1342639011136))
REPRESENTATION_ITEM('')
);
#1298=(
BOUNDED_CURVE()
B_SPLINE_CURVE(2,(#70897,#70898,#70899),.UNSPECIFIED.,.F.,.F.)
B_SPLINE_CURVE_WITH_KNOTS((3,3),(0.367644516946553,0.373830527582534),
 .UNSPECIFIED.)
CURVE()
GEOMETRIC_REPRESENTATION_ITEM()
RATIONAL_B_SPLINE_CURVE((1.13426390111306,1.13389822901299,1.13348223894565))
REPRESENTATION_ITEM('')
);
#1299=(
BOUNDED_CURVE()
B_SPLINE_CURVE(2,(#70902,#70903,#70904),.UNSPECIFIED.,.F.,.F.)
B_SPLINE_CURVE_WITH_KNOTS((3,3),(0.271548216895916,0.277734227531903),
 .UNSPECIFIED.)
CURVE()
GEOMETRIC_REPRESENTATION_ITEM()
RATIONAL_B_SPLINE_CURVE((1.13348223894615,1.1338982290135,1.13426390111357))
REPRESENTATION_ITEM('')
);
#1300=(
BOUNDED_CURVE()
B_SPLINE_CURVE(2,(#70906,#70907,#70908),.UNSPECIFIED.,.F.,.F.)
B_SPLINE_CURVE_WITH_KNOTS((3,3),(0.367644516946558,0.373830527582532),
 .UNSPECIFIED.)
CURVE()
GEOMETRIC_REPRESENTATION_ITEM()
RATIONAL_B_SPLINE_CURVE((1.13426390111307,1.13389822901301,1.13348223894566))
REPRESENTATION_ITEM('')
);
#1301=(
BOUNDED_CURVE()
B_SPLINE_CURVE(2,(#70911,#70912,#70913),.UNSPECIFIED.,.F.,.F.)
B_SPLINE_CURVE_WITH_KNOTS((3,3),(0.271548216895911,0.277734227531895),
 .UNSPECIFIED.)
CURVE()
GEOMETRIC_REPRESENTATION_ITEM()
RATIONAL_B_SPLINE_CURVE((1.13348223894606,1.13389822901341,1.13426390111348))
REPRESENTATION_ITEM('')
);
#1302=(
BOUNDED_CURVE()
B_SPLINE_CURVE(2,(#70915,#70916,#70917),.UNSPECIFIED.,.F.,.F.)
B_SPLINE_CURVE_WITH_KNOTS((3,3),(0.367644516946553,0.373830527582531),
 .UNSPECIFIED.)
CURVE()
GEOMETRIC_REPRESENTATION_ITEM()
RATIONAL_B_SPLINE_CURVE((1.13426390111307,1.133898229013,1.13348223894566))
REPRESENTATION_ITEM('')
);
#1303=(
BOUNDED_CURVE()
B_SPLINE_CURVE(2,(#70920,#70921,#70922),.UNSPECIFIED.,.F.,.F.)
B_SPLINE_CURVE_WITH_KNOTS((3,3),(0.271548216895918,0.277734227531903),
 .UNSPECIFIED.)
CURVE()
GEOMETRIC_REPRESENTATION_ITEM()
RATIONAL_B_SPLINE_CURVE((1.13348223894611,1.13389822901346,1.13426390111353))
REPRESENTATION_ITEM('')
);
#1304=(
BOUNDED_CURVE()
B_SPLINE_CURVE(2,(#70924,#70925,#70926),.UNSPECIFIED.,.F.,.F.)
B_SPLINE_CURVE_WITH_KNOTS((3,3),(0.367644516946551,0.373830527582526),
 .UNSPECIFIED.)
CURVE()
GEOMETRIC_REPRESENTATION_ITEM()
RATIONAL_B_SPLINE_CURVE((1.1342639011131,1.13389822901304,1.13348223894569))
REPRESENTATION_ITEM('')
);
#1305=(
BOUNDED_CURVE()
B_SPLINE_CURVE(2,(#70929,#70930,#70931),.UNSPECIFIED.,.F.,.F.)
B_SPLINE_CURVE_WITH_KNOTS((3,3),(0.271548216895922,0.277734227531909),
 .UNSPECIFIED.)
CURVE()
GEOMETRIC_REPRESENTATION_ITEM()
RATIONAL_B_SPLINE_CURVE((1.13348223894615,1.1338982290135,1.13426390111357))
REPRESENTATION_ITEM('')
);
#1306=(
BOUNDED_CURVE()
B_SPLINE_CURVE(2,(#70933,#70934,#70935),.UNSPECIFIED.,.F.,.F.)
B_SPLINE_CURVE_WITH_KNOTS((3,3),(0.36764451694656,0.373830527582534),
 .UNSPECIFIED.)
CURVE()
GEOMETRIC_REPRESENTATION_ITEM()
RATIONAL_B_SPLINE_CURVE((1.13426390111304,1.13389822901297,1.13348223894563))
REPRESENTATION_ITEM('')
);
#1307=(
BOUNDED_CURVE()
B_SPLINE_CURVE(2,(#70938,#70939,#70940),.UNSPECIFIED.,.F.,.F.)
B_SPLINE_CURVE_WITH_KNOTS((3,3),(0.271548216895917,0.277734227531904),
 .UNSPECIFIED.)
CURVE()
GEOMETRIC_REPRESENTATION_ITEM()
RATIONAL_B_SPLINE_CURVE((1.13348223894616,1.13389822901351,1.13426390111359))
REPRESENTATION_ITEM('')
);
#1308=(
BOUNDED_CURVE()
B_SPLINE_CURVE(2,(#70942,#70943,#70944),.UNSPECIFIED.,.F.,.F.)
B_SPLINE_CURVE_WITH_KNOTS((3,3),(0.367644516946562,0.373830527582537),
 .UNSPECIFIED.)
CURVE()
GEOMETRIC_REPRESENTATION_ITEM()
RATIONAL_B_SPLINE_CURVE((1.13426390111298,1.13389822901291,1.13348223894556))
REPRESENTATION_ITEM('')
);
#1309=(
BOUNDED_CURVE()
B_SPLINE_CURVE(2,(#70947,#70948,#70949),.UNSPECIFIED.,.F.,.F.)
B_SPLINE_CURVE_WITH_KNOTS((3,3),(0.271548216895925,0.277734227531911),
 .UNSPECIFIED.)
CURVE()
GEOMETRIC_REPRESENTATION_ITEM()
RATIONAL_B_SPLINE_CURVE((1.13348223894616,1.13389822901351,1.13426390111359))
REPRESENTATION_ITEM('')
);
#1310=(
BOUNDED_CURVE()
B_SPLINE_CURVE(2,(#70951,#70952,#70953),.UNSPECIFIED.,.F.,.F.)
B_SPLINE_CURVE_WITH_KNOTS((3,3),(0.367644516946555,0.373830527582529),
 .UNSPECIFIED.)
CURVE()
GEOMETRIC_REPRESENTATION_ITEM()
RATIONAL_B_SPLINE_CURVE((1.13426390111312,1.13389822901305,1.13348223894571))
REPRESENTATION_ITEM('')
);
#1311=(
BOUNDED_CURVE()
B_SPLINE_CURVE(2,(#70956,#70957,#70958),.UNSPECIFIED.,.F.,.F.)
B_SPLINE_CURVE_WITH_KNOTS((3,3),(0.271548216895925,0.277734227531912),
 .UNSPECIFIED.)
CURVE()
GEOMETRIC_REPRESENTATION_ITEM()
RATIONAL_B_SPLINE_CURVE((1.13348223894618,1.13389822901353,1.1342639011136))
REPRESENTATION_ITEM('')
);
#1312=(
BOUNDED_CURVE()
B_SPLINE_CURVE(2,(#70960,#70961,#70962),.UNSPECIFIED.,.F.,.F.)
B_SPLINE_CURVE_WITH_KNOTS((3,3),(0.367644516946557,0.373830527582532),
 .UNSPECIFIED.)
CURVE()
GEOMETRIC_REPRESENTATION_ITEM()
RATIONAL_B_SPLINE_CURVE((1.13426390111306,1.13389822901299,1.13348223894564))
REPRESENTATION_ITEM('')
);
#1313=(
BOUNDED_CURVE()
B_SPLINE_CURVE(2,(#70965,#70966,#70967),.UNSPECIFIED.,.F.,.F.)
B_SPLINE_CURVE_WITH_KNOTS((3,3),(0.271548216895908,0.277734227531892),
 .UNSPECIFIED.)
CURVE()
GEOMETRIC_REPRESENTATION_ITEM()
RATIONAL_B_SPLINE_CURVE((1.13348223894609,1.13389822901344,1.13426390111352))
REPRESENTATION_ITEM('')
);
#1314=(
BOUNDED_CURVE()
B_SPLINE_CURVE(2,(#70969,#70970,#70971),.UNSPECIFIED.,.F.,.F.)
B_SPLINE_CURVE_WITH_KNOTS((3,3),(0.367644516946557,0.373830527582522),
 .UNSPECIFIED.)
CURVE()
GEOMETRIC_REPRESENTATION_ITEM()
RATIONAL_B_SPLINE_CURVE((1.13426390111309,1.13389822901302,1.13348223894568))
REPRESENTATION_ITEM('')
);
#1315=(
BOUNDED_CURVE()
B_SPLINE_CURVE(2,(#70974,#70975,#70976),.UNSPECIFIED.,.F.,.F.)
B_SPLINE_CURVE_WITH_KNOTS((3,3),(0.271548216895913,0.277734227531902),
 .UNSPECIFIED.)
CURVE()
GEOMETRIC_REPRESENTATION_ITEM()
RATIONAL_B_SPLINE_CURVE((1.1334822389461,1.13389822901345,1.13426390111352))
REPRESENTATION_ITEM('')
);
#1316=(
BOUNDED_CURVE()
B_SPLINE_CURVE(2,(#70978,#70979,#70980),.UNSPECIFIED.,.F.,.F.)
B_SPLINE_CURVE_WITH_KNOTS((3,3),(0.367644516946559,0.373830527582539),
 .UNSPECIFIED.)
CURVE()
GEOMETRIC_REPRESENTATION_ITEM()
RATIONAL_B_SPLINE_CURVE((1.13426390111296,1.13389822901289,1.13348223894555))
REPRESENTATION_ITEM('')
);
#1317=(
BOUNDED_CURVE()
B_SPLINE_CURVE(2,(#70983,#70984,#70985),.UNSPECIFIED.,.F.,.F.)
B_SPLINE_CURVE_WITH_KNOTS((3,3),(0.271548216895926,0.277734227531913),
 .UNSPECIFIED.)
CURVE()
GEOMETRIC_REPRESENTATION_ITEM()
RATIONAL_B_SPLINE_CURVE((1.13348223894622,1.13389822901357,1.13426390111365))
REPRESENTATION_ITEM('')
);
#1318=(
BOUNDED_CURVE()
B_SPLINE_CURVE(2,(#70987,#70988,#70989),.UNSPECIFIED.,.F.,.F.)
B_SPLINE_CURVE_WITH_KNOTS((3,3),(0.36764451694656,0.373830527582534),
 .UNSPECIFIED.)
CURVE()
GEOMETRIC_REPRESENTATION_ITEM()
RATIONAL_B_SPLINE_CURVE((1.13426390111298,1.13389822901291,1.13348223894557))
REPRESENTATION_ITEM('')
);
#1319=(
BOUNDED_CURVE()
B_SPLINE_CURVE(2,(#70992,#70993,#70994),.UNSPECIFIED.,.F.,.F.)
B_SPLINE_CURVE_WITH_KNOTS((3,3),(0.271548216895926,0.277734227531909),
 .UNSPECIFIED.)
CURVE()
GEOMETRIC_REPRESENTATION_ITEM()
RATIONAL_B_SPLINE_CURVE((1.13348223894617,1.13389822901352,1.13426390111359))
REPRESENTATION_ITEM('')
);
#1320=(
BOUNDED_CURVE()
B_SPLINE_CURVE(2,(#70996,#70997,#70998),.UNSPECIFIED.,.F.,.F.)
B_SPLINE_CURVE_WITH_KNOTS((3,3),(0.367644516946566,0.373830527582539),
 .UNSPECIFIED.)
CURVE()
GEOMETRIC_REPRESENTATION_ITEM()
RATIONAL_B_SPLINE_CURVE((1.13426390111296,1.13389822901289,1.13348223894555))
REPRESENTATION_ITEM('')
);
#1321=(
BOUNDED_CURVE()
B_SPLINE_CURVE(2,(#71001,#71002,#71003),.UNSPECIFIED.,.F.,.F.)
B_SPLINE_CURVE_WITH_KNOTS((3,3),(0.271548216895918,0.277734227531904),
 .UNSPECIFIED.)
CURVE()
GEOMETRIC_REPRESENTATION_ITEM()
RATIONAL_B_SPLINE_CURVE((1.13348223894611,1.13389822901346,1.13426390111353))
REPRESENTATION_ITEM('')
);
#1322=(
BOUNDED_CURVE()
B_SPLINE_CURVE(2,(#71005,#71006,#71007),.UNSPECIFIED.,.F.,.F.)
B_SPLINE_CURVE_WITH_KNOTS((3,3),(0.367644516946555,0.373830527582529),
 .UNSPECIFIED.)
CURVE()
GEOMETRIC_REPRESENTATION_ITEM()
RATIONAL_B_SPLINE_CURVE((1.13426390111303,1.13389822901296,1.13348223894562))
REPRESENTATION_ITEM('')
);
#1323=(
BOUNDED_CURVE()
B_SPLINE_CURVE(2,(#71011,#71012,#71013),.UNSPECIFIED.,.F.,.F.)
B_SPLINE_CURVE_WITH_KNOTS((3,3),(0.271548216895927,0.277734227531913),
 .UNSPECIFIED.)
CURVE()
GEOMETRIC_REPRESENTATION_ITEM()
RATIONAL_B_SPLINE_CURVE((1.13348223894624,1.13389822901359,1.13426390111366))
REPRESENTATION_ITEM('')
);
#1324=(
BOUNDED_CURVE()
B_SPLINE_CURVE(2,(#71017,#71018,#71019),.UNSPECIFIED.,.F.,.F.)
B_SPLINE_CURVE_WITH_KNOTS((3,3),(0.367644516946557,0.373830527582527),
 .UNSPECIFIED.)
CURVE()
GEOMETRIC_REPRESENTATION_ITEM()
RATIONAL_B_SPLINE_CURVE((1.1342639011131,1.13389822901303,1.13348223894569))
REPRESENTATION_ITEM('')
);
#1325=(
BOUNDED_CURVE()
B_SPLINE_CURVE(2,(#71023,#71024,#71025),.UNSPECIFIED.,.F.,.F.)
B_SPLINE_CURVE_WITH_KNOTS((3,3),(0.27154821689592,0.277734227531904),
 .UNSPECIFIED.)
CURVE()
GEOMETRIC_REPRESENTATION_ITEM()
RATIONAL_B_SPLINE_CURVE((1.13348223894613,1.13389822901348,1.13426390111355))
REPRESENTATION_ITEM('')
);
#1326=(
BOUNDED_CURVE()
B_SPLINE_CURVE(2,(#71029,#71030,#71031),.UNSPECIFIED.,.F.,.F.)
B_SPLINE_CURVE_WITH_KNOTS((3,3),(0.367644516946566,0.373830527582538),
 .UNSPECIFIED.)
CURVE()
GEOMETRIC_REPRESENTATION_ITEM()
RATIONAL_B_SPLINE_CURVE((1.13426390111301,1.13389822901294,1.1334822389456))
REPRESENTATION_ITEM('')
);
#1327=(
BOUNDED_CURVE()
B_SPLINE_CURVE(2,(#71035,#71036,#71037),.UNSPECIFIED.,.F.,.F.)
B_SPLINE_CURVE_WITH_KNOTS((3,3),(0.27154821689592,0.277734227531902),
 .UNSPECIFIED.)
CURVE()
GEOMETRIC_REPRESENTATION_ITEM()
RATIONAL_B_SPLINE_CURVE((1.1334822389461,1.13389822901344,1.13426390111352))
REPRESENTATION_ITEM('')
);
#1328=(
BOUNDED_CURVE()
B_SPLINE_CURVE(2,(#71041,#71042,#71043),.UNSPECIFIED.,.F.,.F.)
B_SPLINE_CURVE_WITH_KNOTS((3,3),(0.367644516946558,0.373830527582536),
 .UNSPECIFIED.)
CURVE()
GEOMETRIC_REPRESENTATION_ITEM()
RATIONAL_B_SPLINE_CURVE((1.13426390111303,1.13389822901296,1.13348223894562))
REPRESENTATION_ITEM('')
);
#1329=(
BOUNDED_CURVE()
B_SPLINE_CURVE(2,(#71047,#71048,#71049),.UNSPECIFIED.,.F.,.F.)
B_SPLINE_CURVE_WITH_KNOTS((3,3),(0.271548216895916,0.277734227531903),
 .UNSPECIFIED.)
CURVE()
GEOMETRIC_REPRESENTATION_ITEM()
RATIONAL_B_SPLINE_CURVE((1.13348223894608,1.13389822901343,1.1342639011135))
REPRESENTATION_ITEM('')
);
#1330=(
BOUNDED_CURVE()
B_SPLINE_CURVE(2,(#71053,#71054,#71055),.UNSPECIFIED.,.F.,.F.)
B_SPLINE_CURVE_WITH_KNOTS((3,3),(0.367644516946558,0.373830527582538),
 .UNSPECIFIED.)
CURVE()
GEOMETRIC_REPRESENTATION_ITEM()
RATIONAL_B_SPLINE_CURVE((1.13426390111299,1.13389822901292,1.13348223894558))
REPRESENTATION_ITEM('')
);
#1331=(
BOUNDED_CURVE()
B_SPLINE_CURVE(2,(#71059,#71060,#71061),.UNSPECIFIED.,.F.,.F.)
B_SPLINE_CURVE_WITH_KNOTS((3,3),(0.271548216895918,0.277734227531905),
 .UNSPECIFIED.)
CURVE()
GEOMETRIC_REPRESENTATION_ITEM()
RATIONAL_B_SPLINE_CURVE((1.13348223894618,1.13389822901353,1.1342639011136))
REPRESENTATION_ITEM('')
);
#1332=(
BOUNDED_CURVE()
B_SPLINE_CURVE(2,(#71065,#71066,#71067),.UNSPECIFIED.,.F.,.F.)
B_SPLINE_CURVE_WITH_KNOTS((3,3),(0.367644516946549,0.373830527582523),
 .UNSPECIFIED.)
CURVE()
GEOMETRIC_REPRESENTATION_ITEM()
RATIONAL_B_SPLINE_CURVE((1.13426390111313,1.13389822901306,1.13348223894572))
REPRESENTATION_ITEM('')
);
#1333=(
BOUNDED_CURVE()
B_SPLINE_CURVE(2,(#71071,#71072,#71073),.UNSPECIFIED.,.F.,.F.)
B_SPLINE_CURVE_WITH_KNOTS((3,3),(0.271548216895918,0.277734227531904),
 .UNSPECIFIED.)
CURVE()
GEOMETRIC_REPRESENTATION_ITEM()
RATIONAL_B_SPLINE_CURVE((1.13348223894607,1.13389822901342,1.1342639011135))
REPRESENTATION_ITEM('')
);
#1334=(
BOUNDED_CURVE()
B_SPLINE_CURVE(2,(#71077,#71078,#71079),.UNSPECIFIED.,.F.,.F.)
B_SPLINE_CURVE_WITH_KNOTS((3,3),(0.367644516946553,0.373830527582525),
 .UNSPECIFIED.)
CURVE()
GEOMETRIC_REPRESENTATION_ITEM()
RATIONAL_B_SPLINE_CURVE((1.13426390111306,1.133898229013,1.13348223894565))
REPRESENTATION_ITEM('')
);
#1335=(
BOUNDED_CURVE()
B_SPLINE_CURVE(2,(#71083,#71084,#71085),.UNSPECIFIED.,.F.,.F.)
B_SPLINE_CURVE_WITH_KNOTS((3,3),(0.271548216895918,0.277734227531897),
 .UNSPECIFIED.)
CURVE()
GEOMETRIC_REPRESENTATION_ITEM()
RATIONAL_B_SPLINE_CURVE((1.13348223894613,1.13389822901348,1.13426390111355))
REPRESENTATION_ITEM('')
);
#1336=(
BOUNDED_CURVE()
B_SPLINE_CURVE(2,(#71089,#71090,#71091),.UNSPECIFIED.,.F.,.F.)
B_SPLINE_CURVE_WITH_KNOTS((3,3),(0.367644516946551,0.373830527582524),
 .UNSPECIFIED.)
CURVE()
GEOMETRIC_REPRESENTATION_ITEM()
RATIONAL_B_SPLINE_CURVE((1.13426390111309,1.13389822901302,1.13348223894568))
REPRESENTATION_ITEM('')
);
#1337=(
BOUNDED_CURVE()
B_SPLINE_CURVE(2,(#71095,#71096,#71097),.UNSPECIFIED.,.F.,.F.)
B_SPLINE_CURVE_WITH_KNOTS((3,3),(0.271548216895914,0.2777342275319),
 .UNSPECIFIED.)
CURVE()
GEOMETRIC_REPRESENTATION_ITEM()
RATIONAL_B_SPLINE_CURVE((1.13348223894608,1.13389822901343,1.13426390111351))
REPRESENTATION_ITEM('')
);
#1338=(
BOUNDED_CURVE()
B_SPLINE_CURVE(2,(#71101,#71102,#71103),.UNSPECIFIED.,.F.,.F.)
B_SPLINE_CURVE_WITH_KNOTS((3,3),(0.367644516946559,0.373830527582536),
 .UNSPECIFIED.)
CURVE()
GEOMETRIC_REPRESENTATION_ITEM()
RATIONAL_B_SPLINE_CURVE((1.13426390111305,1.13389822901298,1.13348223894564))
REPRESENTATION_ITEM('')
);
#1339=(
BOUNDED_CURVE()
B_SPLINE_CURVE(2,(#71107,#71108,#71109),.UNSPECIFIED.,.F.,.F.)
B_SPLINE_CURVE_WITH_KNOTS((3,3),(0.27154821689591,0.277734227531898),
 .UNSPECIFIED.)
CURVE()
GEOMETRIC_REPRESENTATION_ITEM()
RATIONAL_B_SPLINE_CURVE((1.13348223894607,1.13389822901342,1.1342639011135))
REPRESENTATION_ITEM('')
);
#1340=(
BOUNDED_CURVE()
B_SPLINE_CURVE(2,(#71113,#71114,#71115),.UNSPECIFIED.,.F.,.F.)
B_SPLINE_CURVE_WITH_KNOTS((3,3),(0.367644516946559,0.373830527582532),
 .UNSPECIFIED.)
CURVE()
GEOMETRIC_REPRESENTATION_ITEM()
RATIONAL_B_SPLINE_CURVE((1.13426390111307,1.133898229013,1.13348223894566))
REPRESENTATION_ITEM('')
);
#1341=(
BOUNDED_CURVE()
B_SPLINE_CURVE(2,(#71119,#71120,#71121),.UNSPECIFIED.,.F.,.F.)
B_SPLINE_CURVE_WITH_KNOTS((3,3),(0.271548216895924,0.277734227531905),
 .UNSPECIFIED.)
CURVE()
GEOMETRIC_REPRESENTATION_ITEM()
RATIONAL_B_SPLINE_CURVE((1.13348223894618,1.13389822901353,1.1342639011136))
REPRESENTATION_ITEM('')
);
#1342=(
BOUNDED_CURVE()
B_SPLINE_CURVE(2,(#71125,#71126,#71127),.UNSPECIFIED.,.F.,.F.)
B_SPLINE_CURVE_WITH_KNOTS((3,3),(0.367644516946555,0.373830527582531),
 .UNSPECIFIED.)
CURVE()
GEOMETRIC_REPRESENTATION_ITEM()
RATIONAL_B_SPLINE_CURVE((1.134263901113,1.13389822901293,1.13348223894559))
REPRESENTATION_ITEM('')
);
#1343=(
BOUNDED_CURVE()
B_SPLINE_CURVE(2,(#71131,#71132,#71133),.UNSPECIFIED.,.F.,.F.)
B_SPLINE_CURVE_WITH_KNOTS((3,3),(0.271548216895916,0.277734227531902),
 .UNSPECIFIED.)
CURVE()
GEOMETRIC_REPRESENTATION_ITEM()
RATIONAL_B_SPLINE_CURVE((1.13348223894612,1.13389822901347,1.13426390111355))
REPRESENTATION_ITEM('')
);
#1344=(
BOUNDED_CURVE()
B_SPLINE_CURVE(2,(#71137,#71138,#71139),.UNSPECIFIED.,.F.,.F.)
B_SPLINE_CURVE_WITH_KNOTS((3,3),(0.36764451694656,0.373830527582534),
 .UNSPECIFIED.)
CURVE()
GEOMETRIC_REPRESENTATION_ITEM()
RATIONAL_B_SPLINE_CURVE((1.13426390111302,1.13389822901296,1.13348223894561))
REPRESENTATION_ITEM('')
);
#1345=(
BOUNDED_CURVE()
B_SPLINE_CURVE(2,(#71143,#71144,#71145),.UNSPECIFIED.,.F.,.F.)
B_SPLINE_CURVE_WITH_KNOTS((3,3),(0.271548216895913,0.277734227531896),
 .UNSPECIFIED.)
CURVE()
GEOMETRIC_REPRESENTATION_ITEM()
RATIONAL_B_SPLINE_CURVE((1.13348223894608,1.13389822901343,1.1342639011135))
REPRESENTATION_ITEM('')
);
#1346=(
BOUNDED_CURVE()
B_SPLINE_CURVE(2,(#71149,#71150,#71151),.UNSPECIFIED.,.F.,.F.)
B_SPLINE_CURVE_WITH_KNOTS((3,3),(0.367644516946558,0.373830527582535),
 .UNSPECIFIED.)
CURVE()
GEOMETRIC_REPRESENTATION_ITEM()
RATIONAL_B_SPLINE_CURVE((1.13426390111305,1.13389822901298,1.13348223894563))
REPRESENTATION_ITEM('')
);
#1347=(
BOUNDED_CURVE()
B_SPLINE_CURVE(2,(#71155,#71156,#71157),.UNSPECIFIED.,.F.,.F.)
B_SPLINE_CURVE_WITH_KNOTS((3,3),(0.271548216895911,0.277734227531902),
 .UNSPECIFIED.)
CURVE()
GEOMETRIC_REPRESENTATION_ITEM()
RATIONAL_B_SPLINE_CURVE((1.13348223894613,1.13389822901348,1.13426390111355))
REPRESENTATION_ITEM('')
);
#1348=(
BOUNDED_CURVE()
B_SPLINE_CURVE(2,(#71161,#71162,#71163),.UNSPECIFIED.,.F.,.F.)
B_SPLINE_CURVE_WITH_KNOTS((3,3),(0.367644516946552,0.373830527582527),
 .UNSPECIFIED.)
CURVE()
GEOMETRIC_REPRESENTATION_ITEM()
RATIONAL_B_SPLINE_CURVE((1.13426390111308,1.13389822901301,1.13348223894567))
REPRESENTATION_ITEM('')
);
#1349=(
BOUNDED_CURVE()
B_SPLINE_CURVE(2,(#71167,#71168,#71169),.UNSPECIFIED.,.F.,.F.)
B_SPLINE_CURVE_WITH_KNOTS((3,3),(0.271548216895913,0.277734227531896),
 .UNSPECIFIED.)
CURVE()
GEOMETRIC_REPRESENTATION_ITEM()
RATIONAL_B_SPLINE_CURVE((1.13348223894609,1.13389822901344,1.13426390111351))
REPRESENTATION_ITEM('')
);
#1350=(
BOUNDED_CURVE()
B_SPLINE_CURVE(2,(#71173,#71174,#71175),.UNSPECIFIED.,.F.,.F.)
B_SPLINE_CURVE_WITH_KNOTS((3,3),(0.367644516946554,0.373830527582527),
 .UNSPECIFIED.)
CURVE()
GEOMETRIC_REPRESENTATION_ITEM()
RATIONAL_B_SPLINE_CURVE((1.13426390111307,1.13389822901301,1.13348223894566))
REPRESENTATION_ITEM('')
);
#1351=(
BOUNDED_CURVE()
B_SPLINE_CURVE(2,(#71179,#71180,#71181),.UNSPECIFIED.,.F.,.F.)
B_SPLINE_CURVE_WITH_KNOTS((3,3),(0.271548216895912,0.277734227531901),
 .UNSPECIFIED.)
CURVE()
GEOMETRIC_REPRESENTATION_ITEM()
RATIONAL_B_SPLINE_CURVE((1.13348223894619,1.13389822901354,1.13426390111361))
REPRESENTATION_ITEM('')
);
#1352=(
BOUNDED_CURVE()
B_SPLINE_CURVE(2,(#71185,#71186,#71187),.UNSPECIFIED.,.F.,.F.)
B_SPLINE_CURVE_WITH_KNOTS((3,3),(0.367644516946552,0.373830527582526),
 .UNSPECIFIED.)
CURVE()
GEOMETRIC_REPRESENTATION_ITEM()
RATIONAL_B_SPLINE_CURVE((1.13426390111306,1.13389822901299,1.13348223894565))
REPRESENTATION_ITEM('')
);
#1353=(
BOUNDED_CURVE()
B_SPLINE_CURVE(2,(#71191,#71192,#71193),.UNSPECIFIED.,.F.,.F.)
B_SPLINE_CURVE_WITH_KNOTS((3,3),(0.271548216895908,0.277734227531896),
 .UNSPECIFIED.)
CURVE()
GEOMETRIC_REPRESENTATION_ITEM()
RATIONAL_B_SPLINE_CURVE((1.13348223894609,1.13389822901344,1.13426390111351))
REPRESENTATION_ITEM('')
);
#1354=(
BOUNDED_CURVE()
B_SPLINE_CURVE(2,(#71197,#71198,#71199),.UNSPECIFIED.,.F.,.F.)
B_SPLINE_CURVE_WITH_KNOTS((3,3),(0.367644516946558,0.373830527582532),
 .UNSPECIFIED.)
CURVE()
GEOMETRIC_REPRESENTATION_ITEM()
RATIONAL_B_SPLINE_CURVE((1.13426390111305,1.13389822901298,1.13348223894564))
REPRESENTATION_ITEM('')
);
#1355=(
BOUNDED_CURVE()
B_SPLINE_CURVE(2,(#71203,#71204,#71205),.UNSPECIFIED.,.F.,.F.)
B_SPLINE_CURVE_WITH_KNOTS((3,3),(0.271548216895918,0.27773422753191),
 .UNSPECIFIED.)
CURVE()
GEOMETRIC_REPRESENTATION_ITEM()
RATIONAL_B_SPLINE_CURVE((1.1334822389462,1.13389822901355,1.13426390111362))
REPRESENTATION_ITEM('')
);
#1356=(
BOUNDED_CURVE()
B_SPLINE_CURVE(2,(#71209,#71210,#71211),.UNSPECIFIED.,.F.,.F.)
B_SPLINE_CURVE_WITH_KNOTS((3,3),(0.367644516946559,0.373830527582532),
 .UNSPECIFIED.)
CURVE()
GEOMETRIC_REPRESENTATION_ITEM()
RATIONAL_B_SPLINE_CURVE((1.13426390111305,1.13389822901299,1.13348223894564))
REPRESENTATION_ITEM('')
);
#1357=(
BOUNDED_CURVE()
B_SPLINE_CURVE(2,(#71215,#71216,#71217),.UNSPECIFIED.,.F.,.F.)
B_SPLINE_CURVE_WITH_KNOTS((3,3),(0.271548216895917,0.277734227531899),
 .UNSPECIFIED.)
CURVE()
GEOMETRIC_REPRESENTATION_ITEM()
RATIONAL_B_SPLINE_CURVE((1.13348223894612,1.13389822901347,1.13426390111355))
REPRESENTATION_ITEM('')
);
#1358=(
BOUNDED_CURVE()
B_SPLINE_CURVE(2,(#71221,#71222,#71223),.UNSPECIFIED.,.F.,.F.)
B_SPLINE_CURVE_WITH_KNOTS((3,3),(0.367644516946562,0.373830527582533),
 .UNSPECIFIED.)
CURVE()
GEOMETRIC_REPRESENTATION_ITEM()
RATIONAL_B_SPLINE_CURVE((1.13426390111306,1.13389822901299,1.13348223894564))
REPRESENTATION_ITEM('')
);
#1359=(
BOUNDED_CURVE()
B_SPLINE_CURVE(2,(#71227,#71228,#71229),.UNSPECIFIED.,.F.,.F.)
B_SPLINE_CURVE_WITH_KNOTS((3,3),(0.271548216895905,0.277734227531891),
 .UNSPECIFIED.)
CURVE()
GEOMETRIC_REPRESENTATION_ITEM()
RATIONAL_B_SPLINE_CURVE((1.13348223894609,1.13389822901344,1.13426390111351))
REPRESENTATION_ITEM('')
);
#1360=(
BOUNDED_CURVE()
B_SPLINE_CURVE(2,(#71233,#71234,#71235),.UNSPECIFIED.,.F.,.F.)
B_SPLINE_CURVE_WITH_KNOTS((3,3),(0.367644516946557,0.373830527582533),
 .UNSPECIFIED.)
CURVE()
GEOMETRIC_REPRESENTATION_ITEM()
RATIONAL_B_SPLINE_CURVE((1.13426390111305,1.13389822901299,1.13348223894564))
REPRESENTATION_ITEM('')
);
#1361=(
BOUNDED_CURVE()
B_SPLINE_CURVE(2,(#71239,#71240,#71241),.UNSPECIFIED.,.F.,.F.)
B_SPLINE_CURVE_WITH_KNOTS((3,3),(0.271548216895918,0.277734227531906),
 .UNSPECIFIED.)
CURVE()
GEOMETRIC_REPRESENTATION_ITEM()
RATIONAL_B_SPLINE_CURVE((1.13348223894616,1.13389822901351,1.13426390111358))
REPRESENTATION_ITEM('')
);
#1362=(
BOUNDED_CURVE()
B_SPLINE_CURVE(2,(#71263,#71264,#71265),.UNSPECIFIED.,.F.,.F.)
B_SPLINE_CURVE_WITH_KNOTS((3,3),(0.376641898803529,0.382940702095941),
 .UNSPECIFIED.)
CURVE()
GEOMETRIC_REPRESENTATION_ITEM()
RATIONAL_B_SPLINE_CURVE((1.12071541658433,1.1202411994692,1.11971735964528))
REPRESENTATION_ITEM('')
);
#1363=(
BOUNDED_CURVE()
B_SPLINE_CURVE(2,(#71269,#71270,#71271),.UNSPECIFIED.,.F.,.F.)
B_SPLINE_CURVE_WITH_KNOTS((3,3),(0.249954652430657,0.25625345571807),
 .UNSPECIFIED.)
CURVE()
GEOMETRIC_REPRESENTATION_ITEM()
RATIONAL_B_SPLINE_CURVE((1.1197173596462,1.12024119946966,1.12071541658442))
REPRESENTATION_ITEM('')
);
#1364=(
BOUNDED_CURVE()
B_SPLINE_CURVE(2,(#71275,#71276,#71277),.UNSPECIFIED.,.F.,.F.)
B_SPLINE_CURVE_WITH_KNOTS((3,3),(0.376641898803524,0.382940702095934),
 .UNSPECIFIED.)
CURVE()
GEOMETRIC_REPRESENTATION_ITEM()
RATIONAL_B_SPLINE_CURVE((1.12071541658448,1.12024119946934,1.11971735964542))
REPRESENTATION_ITEM('')
);
#1365=(
BOUNDED_CURVE()
B_SPLINE_CURVE(2,(#71281,#71282,#71283),.UNSPECIFIED.,.F.,.F.)
B_SPLINE_CURVE_WITH_KNOTS((3,3),(0.249954652430655,0.256253455718069),
 .UNSPECIFIED.)
CURVE()
GEOMETRIC_REPRESENTATION_ITEM()
RATIONAL_B_SPLINE_CURVE((1.11971735964613,1.1202411994696,1.12071541658435))
REPRESENTATION_ITEM('')
);
#1366=(
BOUNDED_CURVE()
B_SPLINE_CURVE(2,(#71287,#71288,#71289),.UNSPECIFIED.,.F.,.F.)
B_SPLINE_CURVE_WITH_KNOTS((3,3),(0.376641898803532,0.382940702095944),
 .UNSPECIFIED.)
CURVE()
GEOMETRIC_REPRESENTATION_ITEM()
RATIONAL_B_SPLINE_CURVE((1.12071541658434,1.12024119946921,1.11971735964529))
REPRESENTATION_ITEM('')
);
#1367=(
BOUNDED_CURVE()
B_SPLINE_CURVE(2,(#71293,#71294,#71295),.UNSPECIFIED.,.F.,.F.)
B_SPLINE_CURVE_WITH_KNOTS((3,3),(0.249954652430645,0.256253455718059),
 .UNSPECIFIED.)
CURVE()
GEOMETRIC_REPRESENTATION_ITEM()
RATIONAL_B_SPLINE_CURVE((1.11971735964598,1.12024119946945,1.1207154165842))
REPRESENTATION_ITEM('')
);
#1368=(
BOUNDED_CURVE()
B_SPLINE_CURVE(2,(#71299,#71300,#71301),.UNSPECIFIED.,.F.,.F.)
B_SPLINE_CURVE_WITH_KNOTS((3,3),(0.376641898803521,0.382940702095933),
 .UNSPECIFIED.)
CURVE()
GEOMETRIC_REPRESENTATION_ITEM()
RATIONAL_B_SPLINE_CURVE((1.1207154165845,1.12024119946936,1.11971735964544))
REPRESENTATION_ITEM('')
);
#1369=(
BOUNDED_CURVE()
B_SPLINE_CURVE(2,(#71305,#71306,#71307),.UNSPECIFIED.,.F.,.F.)
B_SPLINE_CURVE_WITH_KNOTS((3,3),(0.249954652430661,0.256253455718076),
 .UNSPECIFIED.)
CURVE()
GEOMETRIC_REPRESENTATION_ITEM()
RATIONAL_B_SPLINE_CURVE((1.1197173596463,1.12024119946977,1.12071541658453))
REPRESENTATION_ITEM('')
);
#1370=(
BOUNDED_CURVE()
B_SPLINE_CURVE(2,(#71311,#71312,#71313),.UNSPECIFIED.,.F.,.F.)
B_SPLINE_CURVE_WITH_KNOTS((3,3),(0.376641898803535,0.382940702095943),
 .UNSPECIFIED.)
CURVE()
GEOMETRIC_REPRESENTATION_ITEM()
RATIONAL_B_SPLINE_CURVE((1.12071541658437,1.12024119946923,1.11971735964532))
REPRESENTATION_ITEM('')
);
#1371=(
BOUNDED_CURVE()
B_SPLINE_CURVE(2,(#71317,#71318,#71319),.UNSPECIFIED.,.F.,.F.)
B_SPLINE_CURVE_WITH_KNOTS((3,3),(0.249954652430645,0.256253455718058),
 .UNSPECIFIED.)
CURVE()
GEOMETRIC_REPRESENTATION_ITEM()
RATIONAL_B_SPLINE_CURVE((1.11971735964609,1.12024119946955,1.12071541658431))
REPRESENTATION_ITEM('')
);
#1372=(
BOUNDED_CURVE()
B_SPLINE_CURVE(2,(#71323,#71324,#71325),.UNSPECIFIED.,.F.,.F.)
B_SPLINE_CURVE_WITH_KNOTS((3,3),(0.376641898803531,0.382940702095942),
 .UNSPECIFIED.)
CURVE()
GEOMETRIC_REPRESENTATION_ITEM()
RATIONAL_B_SPLINE_CURVE((1.12071541658437,1.12024119946923,1.11971735964532))
REPRESENTATION_ITEM('')
);
#1373=(
BOUNDED_CURVE()
B_SPLINE_CURVE(2,(#71329,#71330,#71331),.UNSPECIFIED.,.F.,.F.)
B_SPLINE_CURVE_WITH_KNOTS((3,3),(0.249954652430646,0.256253455718059),
 .UNSPECIFIED.)
CURVE()
GEOMETRIC_REPRESENTATION_ITEM()
RATIONAL_B_SPLINE_CURVE((1.11971735964605,1.12024119946951,1.12071541658427))
REPRESENTATION_ITEM('')
);
#1374=(
BOUNDED_CURVE()
B_SPLINE_CURVE(2,(#71335,#71336,#71337),.UNSPECIFIED.,.F.,.F.)
B_SPLINE_CURVE_WITH_KNOTS((3,3),(0.376641898803521,0.382940702095931),
 .UNSPECIFIED.)
CURVE()
GEOMETRIC_REPRESENTATION_ITEM()
RATIONAL_B_SPLINE_CURVE((1.12071541658451,1.12024119946938,1.11971735964546))
REPRESENTATION_ITEM('')
);
#1375=(
BOUNDED_CURVE()
B_SPLINE_CURVE(2,(#71341,#71342,#71343),.UNSPECIFIED.,.F.,.F.)
B_SPLINE_CURVE_WITH_KNOTS((3,3),(0.249954652430639,0.256253455718052),
 .UNSPECIFIED.)
CURVE()
GEOMETRIC_REPRESENTATION_ITEM()
RATIONAL_B_SPLINE_CURVE((1.11971735964601,1.12024119946948,1.12071541658424))
REPRESENTATION_ITEM('')
);
#1376=(
BOUNDED_CURVE()
B_SPLINE_CURVE(2,(#71347,#71348,#71349),.UNSPECIFIED.,.F.,.F.)
B_SPLINE_CURVE_WITH_KNOTS((3,3),(0.376641898803533,0.382940702095945),
 .UNSPECIFIED.)
CURVE()
GEOMETRIC_REPRESENTATION_ITEM()
RATIONAL_B_SPLINE_CURVE((1.12071541658434,1.1202411994692,1.11971735964528))
REPRESENTATION_ITEM('')
);
#1377=(
BOUNDED_CURVE()
B_SPLINE_CURVE(2,(#71353,#71354,#71355),.UNSPECIFIED.,.F.,.F.)
B_SPLINE_CURVE_WITH_KNOTS((3,3),(0.249954652430659,0.256253455718072),
 .UNSPECIFIED.)
CURVE()
GEOMETRIC_REPRESENTATION_ITEM()
RATIONAL_B_SPLINE_CURVE((1.11971735964624,1.12024119946971,1.12071541658447))
REPRESENTATION_ITEM('')
);
#1378=(
BOUNDED_CURVE()
B_SPLINE_CURVE(2,(#71359,#71360,#71361),.UNSPECIFIED.,.F.,.F.)
B_SPLINE_CURVE_WITH_KNOTS((3,3),(0.376641898803529,0.382940702095948),
 .UNSPECIFIED.)
CURVE()
GEOMETRIC_REPRESENTATION_ITEM()
RATIONAL_B_SPLINE_CURVE((1.12071541658446,1.12024119946932,1.1197173596454))
REPRESENTATION_ITEM('')
);
#1379=(
BOUNDED_CURVE()
B_SPLINE_CURVE(2,(#71365,#71366,#71367),.UNSPECIFIED.,.F.,.F.)
B_SPLINE_CURVE_WITH_KNOTS((3,3),(0.249954652430643,0.256253455718057),
 .UNSPECIFIED.)
CURVE()
GEOMETRIC_REPRESENTATION_ITEM()
RATIONAL_B_SPLINE_CURVE((1.11971735964609,1.12024119946956,1.12071541658432))
REPRESENTATION_ITEM('')
);
#1380=(
BOUNDED_CURVE()
B_SPLINE_CURVE(2,(#71371,#71372,#71373),.UNSPECIFIED.,.F.,.F.)
B_SPLINE_CURVE_WITH_KNOTS((3,3),(0.376641898803523,0.382940702095941),
 .UNSPECIFIED.)
CURVE()
GEOMETRIC_REPRESENTATION_ITEM()
RATIONAL_B_SPLINE_CURVE((1.12071541658451,1.12024119946937,1.11971735964545))
REPRESENTATION_ITEM('')
);
#1381=(
BOUNDED_CURVE()
B_SPLINE_CURVE(2,(#71377,#71378,#71379),.UNSPECIFIED.,.F.,.F.)
B_SPLINE_CURVE_WITH_KNOTS((3,3),(0.249954652430644,0.256253455718058),
 .UNSPECIFIED.)
CURVE()
GEOMETRIC_REPRESENTATION_ITEM()
RATIONAL_B_SPLINE_CURVE((1.11971735964615,1.12024119946961,1.12071541658437))
REPRESENTATION_ITEM('')
);
#1382=(
BOUNDED_CURVE()
B_SPLINE_CURVE(2,(#71383,#71384,#71385),.UNSPECIFIED.,.F.,.F.)
B_SPLINE_CURVE_WITH_KNOTS((3,3),(0.376641898803536,0.382940702095946),
 .UNSPECIFIED.)
CURVE()
GEOMETRIC_REPRESENTATION_ITEM()
RATIONAL_B_SPLINE_CURVE((1.12071541658451,1.12024119946938,1.11971735964546))
REPRESENTATION_ITEM('')
);
#1383=(
BOUNDED_CURVE()
B_SPLINE_CURVE(2,(#71389,#71390,#71391),.UNSPECIFIED.,.F.,.F.)
B_SPLINE_CURVE_WITH_KNOTS((3,3),(0.24995465243065,0.256253455718062),
 .UNSPECIFIED.)
CURVE()
GEOMETRIC_REPRESENTATION_ITEM()
RATIONAL_B_SPLINE_CURVE((1.11971735964599,1.12024119946946,1.12071541658421))
REPRESENTATION_ITEM('')
);
#1384=(
BOUNDED_CURVE()
B_SPLINE_CURVE(2,(#71395,#71396,#71397),.UNSPECIFIED.,.F.,.F.)
B_SPLINE_CURVE_WITH_KNOTS((3,3),(0.376641898803523,0.38294070209593),
 .UNSPECIFIED.)
CURVE()
GEOMETRIC_REPRESENTATION_ITEM()
RATIONAL_B_SPLINE_CURVE((1.1207154165845,1.12024119946936,1.11971735964544))
REPRESENTATION_ITEM('')
);
#1385=(
BOUNDED_CURVE()
B_SPLINE_CURVE(2,(#71401,#71402,#71403),.UNSPECIFIED.,.F.,.F.)
B_SPLINE_CURVE_WITH_KNOTS((3,3),(0.249954652430653,0.256253455718064),
 .UNSPECIFIED.)
CURVE()
GEOMETRIC_REPRESENTATION_ITEM()
RATIONAL_B_SPLINE_CURVE((1.11971735964611,1.12024119946957,1.12071541658433))
REPRESENTATION_ITEM('')
);
#1386=(
BOUNDED_CURVE()
B_SPLINE_CURVE(2,(#71407,#71408,#71409),.UNSPECIFIED.,.F.,.F.)
B_SPLINE_CURVE_WITH_KNOTS((3,3),(0.376641898803521,0.382940702095931),
 .UNSPECIFIED.)
CURVE()
GEOMETRIC_REPRESENTATION_ITEM()
RATIONAL_B_SPLINE_CURVE((1.12071541658461,1.12024119946947,1.11971735964555))
REPRESENTATION_ITEM('')
);
#1387=(
BOUNDED_CURVE()
B_SPLINE_CURVE(2,(#71413,#71414,#71415),.UNSPECIFIED.,.F.,.F.)
B_SPLINE_CURVE_WITH_KNOTS((3,3),(0.249954652430661,0.256253455718072),
 .UNSPECIFIED.)
CURVE()
GEOMETRIC_REPRESENTATION_ITEM()
RATIONAL_B_SPLINE_CURVE((1.11971735964623,1.1202411994697,1.12071541658446))
REPRESENTATION_ITEM('')
);
#1388=(
BOUNDED_CURVE()
B_SPLINE_CURVE(2,(#71419,#71420,#71421),.UNSPECIFIED.,.F.,.F.)
B_SPLINE_CURVE_WITH_KNOTS((3,3),(0.376641898803537,0.382940702095947),
 .UNSPECIFIED.)
CURVE()
GEOMETRIC_REPRESENTATION_ITEM()
RATIONAL_B_SPLINE_CURVE((1.1207154165845,1.12024119946936,1.11971735964544))
REPRESENTATION_ITEM('')
);
#1389=(
BOUNDED_CURVE()
B_SPLINE_CURVE(2,(#71425,#71426,#71427),.UNSPECIFIED.,.F.,.F.)
B_SPLINE_CURVE_WITH_KNOTS((3,3),(0.249954652430645,0.256253455718056),
 .UNSPECIFIED.)
CURVE()
GEOMETRIC_REPRESENTATION_ITEM()
RATIONAL_B_SPLINE_CURVE((1.11971735964613,1.1202411994696,1.12071541658435))
REPRESENTATION_ITEM('')
);
#1390=(
BOUNDED_CURVE()
B_SPLINE_CURVE(2,(#71431,#71432,#71433),.UNSPECIFIED.,.F.,.F.)
B_SPLINE_CURVE_WITH_KNOTS((3,3),(0.376641898803536,0.382940702095954),
 .UNSPECIFIED.)
CURVE()
GEOMETRIC_REPRESENTATION_ITEM()
RATIONAL_B_SPLINE_CURVE((1.12071541658435,1.12024119946922,1.1197173596453))
REPRESENTATION_ITEM('')
);
#1391=(
BOUNDED_CURVE()
B_SPLINE_CURVE(2,(#71437,#71438,#71439),.UNSPECIFIED.,.F.,.F.)
B_SPLINE_CURVE_WITH_KNOTS((3,3),(0.249954652430663,0.256253455718072),
 .UNSPECIFIED.)
CURVE()
GEOMETRIC_REPRESENTATION_ITEM()
RATIONAL_B_SPLINE_CURVE((1.11971735964633,1.1202411994698,1.12071541658456))
REPRESENTATION_ITEM('')
);
#1392=(
BOUNDED_CURVE()
B_SPLINE_CURVE(2,(#71443,#71444,#71445),.UNSPECIFIED.,.F.,.F.)
B_SPLINE_CURVE_WITH_KNOTS((3,3),(0.376641898803512,0.382940702095922),
 .UNSPECIFIED.)
CURVE()
GEOMETRIC_REPRESENTATION_ITEM()
RATIONAL_B_SPLINE_CURVE((1.12071541658461,1.12024119946947,1.11971735964555))
REPRESENTATION_ITEM('')
);
#1393=(
BOUNDED_CURVE()
B_SPLINE_CURVE(2,(#71449,#71450,#71451),.UNSPECIFIED.,.F.,.F.)
B_SPLINE_CURVE_WITH_KNOTS((3,3),(0.249954652430648,0.256253455718062),
 .UNSPECIFIED.)
CURVE()
GEOMETRIC_REPRESENTATION_ITEM()
RATIONAL_B_SPLINE_CURVE((1.11971735964605,1.12024119946951,1.12071541658427))
REPRESENTATION_ITEM('')
);
#1394=(
BOUNDED_CURVE()
B_SPLINE_CURVE(2,(#71455,#71456,#71457),.UNSPECIFIED.,.F.,.F.)
B_SPLINE_CURVE_WITH_KNOTS((3,3),(0.376641898803527,0.382940702095944),
 .UNSPECIFIED.)
CURVE()
GEOMETRIC_REPRESENTATION_ITEM()
RATIONAL_B_SPLINE_CURVE((1.12071541658444,1.12024119946931,1.11971735964539))
REPRESENTATION_ITEM('')
);
#1395=(
BOUNDED_CURVE()
B_SPLINE_CURVE(2,(#71461,#71462,#71463),.UNSPECIFIED.,.F.,.F.)
B_SPLINE_CURVE_WITH_KNOTS((3,3),(0.24995465243065,0.256253455718066),
 .UNSPECIFIED.)
CURVE()
GEOMETRIC_REPRESENTATION_ITEM()
RATIONAL_B_SPLINE_CURVE((1.11971735964612,1.12024119946958,1.12071541658434))
REPRESENTATION_ITEM('')
);
#1396=(
BOUNDED_CURVE()
B_SPLINE_CURVE(2,(#71467,#71468,#71469),.UNSPECIFIED.,.F.,.F.)
B_SPLINE_CURVE_WITH_KNOTS((3,3),(0.37664189880352,0.382940702095936),
 .UNSPECIFIED.)
CURVE()
GEOMETRIC_REPRESENTATION_ITEM()
RATIONAL_B_SPLINE_CURVE((1.12071541658452,1.12024119946938,1.11971735964546))
REPRESENTATION_ITEM('')
);
#1397=(
BOUNDED_CURVE()
B_SPLINE_CURVE(2,(#71473,#71474,#71475),.UNSPECIFIED.,.F.,.F.)
B_SPLINE_CURVE_WITH_KNOTS((3,3),(0.249954652430664,0.25625345571808),
 .UNSPECIFIED.)
CURVE()
GEOMETRIC_REPRESENTATION_ITEM()
RATIONAL_B_SPLINE_CURVE((1.11971735964628,1.12024119946975,1.12071541658451))
REPRESENTATION_ITEM('')
);
#1398=(
BOUNDED_CURVE()
B_SPLINE_CURVE(2,(#71479,#71480,#71481),.UNSPECIFIED.,.F.,.F.)
B_SPLINE_CURVE_WITH_KNOTS((3,3),(0.376641898803518,0.382940702095937),
 .UNSPECIFIED.)
CURVE()
GEOMETRIC_REPRESENTATION_ITEM()
RATIONAL_B_SPLINE_CURVE((1.12071541658454,1.12024119946941,1.11971735964549))
REPRESENTATION_ITEM('')
);
#1399=(
BOUNDED_CURVE()
B_SPLINE_CURVE(2,(#71485,#71486,#71487),.UNSPECIFIED.,.F.,.F.)
B_SPLINE_CURVE_WITH_KNOTS((3,3),(0.249954652430639,0.256253455718056),
 .UNSPECIFIED.)
CURVE()
GEOMETRIC_REPRESENTATION_ITEM()
RATIONAL_B_SPLINE_CURVE((1.11971735964609,1.12024119946956,1.12071541658432))
REPRESENTATION_ITEM('')
);
#1400=(
BOUNDED_CURVE()
B_SPLINE_CURVE(2,(#71491,#71492,#71493),.UNSPECIFIED.,.F.,.F.)
B_SPLINE_CURVE_WITH_KNOTS((3,3),(0.376641898803522,0.382940702095936),
 .UNSPECIFIED.)
CURVE()
GEOMETRIC_REPRESENTATION_ITEM()
RATIONAL_B_SPLINE_CURVE((1.12071541658447,1.12024119946934,1.11971735964542))
REPRESENTATION_ITEM('')
);
#1401=(
BOUNDED_CURVE()
B_SPLINE_CURVE(2,(#71497,#71498,#71499),.UNSPECIFIED.,.F.,.F.)
B_SPLINE_CURVE_WITH_KNOTS((3,3),(0.249954652430657,0.256253455718066),
 .UNSPECIFIED.)
CURVE()
GEOMETRIC_REPRESENTATION_ITEM()
RATIONAL_B_SPLINE_CURVE((1.11971735964622,1.12024119946968,1.12071541658444))
REPRESENTATION_ITEM('')
);
#1402=(
BOUNDED_CURVE()
B_SPLINE_CURVE(2,(#71503,#71504,#71505),.UNSPECIFIED.,.F.,.F.)
B_SPLINE_CURVE_WITH_KNOTS((3,3),(0.376641898803533,0.38294070209594),
 .UNSPECIFIED.)
CURVE()
GEOMETRIC_REPRESENTATION_ITEM()
RATIONAL_B_SPLINE_CURVE((1.12071541658433,1.1202411994692,1.11971735964528))
REPRESENTATION_ITEM('')
);
#1403=(
BOUNDED_CURVE()
B_SPLINE_CURVE(2,(#71509,#71510,#71511),.UNSPECIFIED.,.F.,.F.)
B_SPLINE_CURVE_WITH_KNOTS((3,3),(0.249954652430642,0.256253455718055),
 .UNSPECIFIED.)
CURVE()
GEOMETRIC_REPRESENTATION_ITEM()
RATIONAL_B_SPLINE_CURVE((1.11971735964602,1.12024119946948,1.12071541658424))
REPRESENTATION_ITEM('')
);
#1404=(
BOUNDED_CURVE()
B_SPLINE_CURVE(2,(#71515,#71516,#71517),.UNSPECIFIED.,.F.,.F.)
B_SPLINE_CURVE_WITH_KNOTS((3,3),(0.376641898803547,0.382940702095962),
 .UNSPECIFIED.)
CURVE()
GEOMETRIC_REPRESENTATION_ITEM()
RATIONAL_B_SPLINE_CURVE((1.12071541658418,1.12024119946904,1.11971735964512))
REPRESENTATION_ITEM('')
);
#1405=(
BOUNDED_CURVE()
B_SPLINE_CURVE(2,(#71521,#71522,#71523),.UNSPECIFIED.,.F.,.F.)
B_SPLINE_CURVE_WITH_KNOTS((3,3),(0.249954652430658,0.256253455718078),
 .UNSPECIFIED.)
CURVE()
GEOMETRIC_REPRESENTATION_ITEM()
RATIONAL_B_SPLINE_CURVE((1.1197173596463,1.12024119946977,1.12071541658453))
REPRESENTATION_ITEM('')
);
#1406=(
BOUNDED_CURVE()
B_SPLINE_CURVE(2,(#71527,#71528,#71529),.UNSPECIFIED.,.F.,.F.)
B_SPLINE_CURVE_WITH_KNOTS((3,3),(0.376641898803522,0.382940702095938),
 .UNSPECIFIED.)
CURVE()
GEOMETRIC_REPRESENTATION_ITEM()
RATIONAL_B_SPLINE_CURVE((1.12071541658451,1.12024119946937,1.11971735964545))
REPRESENTATION_ITEM('')
);
#1407=(
BOUNDED_CURVE()
B_SPLINE_CURVE(2,(#71533,#71534,#71535),.UNSPECIFIED.,.F.,.F.)
B_SPLINE_CURVE_WITH_KNOTS((3,3),(0.249954652430655,0.25625345571807),
 .UNSPECIFIED.)
CURVE()
GEOMETRIC_REPRESENTATION_ITEM()
RATIONAL_B_SPLINE_CURVE((1.11971735964625,1.12024119946971,1.12071541658447))
REPRESENTATION_ITEM('')
);
#1408=(
BOUNDED_CURVE()
B_SPLINE_CURVE(2,(#71539,#71540,#71541),.UNSPECIFIED.,.F.,.F.)
B_SPLINE_CURVE_WITH_KNOTS((3,3),(0.376641898803531,0.382940702095945),
 .UNSPECIFIED.)
CURVE()
GEOMETRIC_REPRESENTATION_ITEM()
RATIONAL_B_SPLINE_CURVE((1.12071541658432,1.12024119946919,1.11971735964527))
REPRESENTATION_ITEM('')
);
#1409=(
BOUNDED_CURVE()
B_SPLINE_CURVE(2,(#71545,#71546,#71547),.UNSPECIFIED.,.F.,.F.)
B_SPLINE_CURVE_WITH_KNOTS((3,3),(0.249954652430637,0.256253455718055),
 .UNSPECIFIED.)
CURVE()
GEOMETRIC_REPRESENTATION_ITEM()
RATIONAL_B_SPLINE_CURVE((1.11971735964599,1.12024119946945,1.12071541658421))
REPRESENTATION_ITEM('')
);
#1410=(
BOUNDED_CURVE()
B_SPLINE_CURVE(2,(#71551,#71552,#71553),.UNSPECIFIED.,.F.,.F.)
B_SPLINE_CURVE_WITH_KNOTS((3,3),(0.376641898803544,0.382940702095957),
 .UNSPECIFIED.)
CURVE()
GEOMETRIC_REPRESENTATION_ITEM()
RATIONAL_B_SPLINE_CURVE((1.12071541658422,1.12024119946908,1.11971735964516))
REPRESENTATION_ITEM('')
);
#1411=(
BOUNDED_CURVE()
B_SPLINE_CURVE(2,(#71557,#71558,#71559),.UNSPECIFIED.,.F.,.F.)
B_SPLINE_CURVE_WITH_KNOTS((3,3),(0.249954652430653,0.256253455718062),
 .UNSPECIFIED.)
CURVE()
GEOMETRIC_REPRESENTATION_ITEM()
RATIONAL_B_SPLINE_CURVE((1.11971735964616,1.12024119946962,1.12071541658438))
REPRESENTATION_ITEM('')
);
#1412=(
BOUNDED_CURVE()
B_SPLINE_CURVE(2,(#71563,#71564,#71565),.UNSPECIFIED.,.F.,.F.)
B_SPLINE_CURVE_WITH_KNOTS((3,3),(0.376641898803539,0.38294070209595),
 .UNSPECIFIED.)
CURVE()
GEOMETRIC_REPRESENTATION_ITEM()
RATIONAL_B_SPLINE_CURVE((1.12071541658449,1.12024119946935,1.11971735964543))
REPRESENTATION_ITEM('')
);
#1413=(
BOUNDED_CURVE()
B_SPLINE_CURVE(2,(#71569,#71570,#71571),.UNSPECIFIED.,.F.,.F.)
B_SPLINE_CURVE_WITH_KNOTS((3,3),(0.249954652430653,0.256253455718071),
 .UNSPECIFIED.)
CURVE()
GEOMETRIC_REPRESENTATION_ITEM()
RATIONAL_B_SPLINE_CURVE((1.11971735964627,1.12024119946973,1.12071541658449))
REPRESENTATION_ITEM('')
);
#1414=(
BOUNDED_CURVE()
B_SPLINE_CURVE(2,(#71575,#71576,#71577),.UNSPECIFIED.,.F.,.F.)
B_SPLINE_CURVE_WITH_KNOTS((3,3),(0.376641898803533,0.382940702095944),
 .UNSPECIFIED.)
CURVE()
GEOMETRIC_REPRESENTATION_ITEM()
RATIONAL_B_SPLINE_CURVE((1.12071541658435,1.12024119946922,1.1197173596453))
REPRESENTATION_ITEM('')
);
#1415=(
BOUNDED_CURVE()
B_SPLINE_CURVE(2,(#71581,#71582,#71583),.UNSPECIFIED.,.F.,.F.)
B_SPLINE_CURVE_WITH_KNOTS((3,3),(0.249954652430647,0.256253455718059),
 .UNSPECIFIED.)
CURVE()
GEOMETRIC_REPRESENTATION_ITEM()
RATIONAL_B_SPLINE_CURVE((1.11971735964614,1.12024119946961,1.12071541658437))
REPRESENTATION_ITEM('')
);
#1416=(
BOUNDED_CURVE()
B_SPLINE_CURVE(2,(#71587,#71588,#71589),.UNSPECIFIED.,.F.,.F.)
B_SPLINE_CURVE_WITH_KNOTS((3,3),(0.376641898803539,0.382940702095955),
 .UNSPECIFIED.)
CURVE()
GEOMETRIC_REPRESENTATION_ITEM()
RATIONAL_B_SPLINE_CURVE((1.12071541658434,1.1202411994692,1.11971735964528))
REPRESENTATION_ITEM('')
);
#1417=(
BOUNDED_CURVE()
B_SPLINE_CURVE(2,(#71593,#71594,#71595),.UNSPECIFIED.,.F.,.F.)
B_SPLINE_CURVE_WITH_KNOTS((3,3),(0.249954652430656,0.256253455718067),
 .UNSPECIFIED.)
CURVE()
GEOMETRIC_REPRESENTATION_ITEM()
RATIONAL_B_SPLINE_CURVE((1.11971735964622,1.12024119946969,1.12071541658444))
REPRESENTATION_ITEM('')
);
#1418=(
BOUNDED_CURVE()
B_SPLINE_CURVE(2,(#71599,#71600,#71601),.UNSPECIFIED.,.F.,.F.)
B_SPLINE_CURVE_WITH_KNOTS((3,3),(0.376641898803524,0.382940702095936),
 .UNSPECIFIED.)
CURVE()
GEOMETRIC_REPRESENTATION_ITEM()
RATIONAL_B_SPLINE_CURVE((1.12071541658457,1.12024119946943,1.11971735964551))
REPRESENTATION_ITEM('')
);
#1419=(
BOUNDED_CURVE()
B_SPLINE_CURVE(2,(#71605,#71606,#71607),.UNSPECIFIED.,.F.,.F.)
B_SPLINE_CURVE_WITH_KNOTS((3,3),(0.249954652430651,0.256253455718065),
 .UNSPECIFIED.)
CURVE()
GEOMETRIC_REPRESENTATION_ITEM()
RATIONAL_B_SPLINE_CURVE((1.11971735964615,1.12024119946961,1.12071541658437))
REPRESENTATION_ITEM('')
);
#1420=(
BOUNDED_CURVE()
B_SPLINE_CURVE(2,(#71611,#71612,#71613),.UNSPECIFIED.,.F.,.F.)
B_SPLINE_CURVE_WITH_KNOTS((3,3),(0.376641898803518,0.382940702095931),
 .UNSPECIFIED.)
CURVE()
GEOMETRIC_REPRESENTATION_ITEM()
RATIONAL_B_SPLINE_CURVE((1.12071541658449,1.12024119946936,1.11971735964544))
REPRESENTATION_ITEM('')
);
#1421=(
BOUNDED_CURVE()
B_SPLINE_CURVE(2,(#71617,#71618,#71619),.UNSPECIFIED.,.F.,.F.)
B_SPLINE_CURVE_WITH_KNOTS((3,3),(0.249954652430648,0.256253455718058),
 .UNSPECIFIED.)
CURVE()
GEOMETRIC_REPRESENTATION_ITEM()
RATIONAL_B_SPLINE_CURVE((1.11971735964614,1.1202411994696,1.12071541658436))
REPRESENTATION_ITEM('')
);
#1422=(
BOUNDED_CURVE()
B_SPLINE_CURVE(2,(#71623,#71624,#71625),.UNSPECIFIED.,.F.,.F.)
B_SPLINE_CURVE_WITH_KNOTS((3,3),(0.376641898803531,0.382940702095945),
 .UNSPECIFIED.)
CURVE()
GEOMETRIC_REPRESENTATION_ITEM()
RATIONAL_B_SPLINE_CURVE((1.12071541658451,1.12024119946937,1.11971735964545))
REPRESENTATION_ITEM('')
);
#1423=(
BOUNDED_CURVE()
B_SPLINE_CURVE(2,(#71629,#71630,#71631),.UNSPECIFIED.,.F.,.F.)
B_SPLINE_CURVE_WITH_KNOTS((3,3),(0.249954652430648,0.256253455718067),
 .UNSPECIFIED.)
CURVE()
GEOMETRIC_REPRESENTATION_ITEM()
RATIONAL_B_SPLINE_CURVE((1.11971735964618,1.12024119946964,1.1207154165844))
REPRESENTATION_ITEM('')
);
#1424=(
BOUNDED_CURVE()
B_SPLINE_CURVE(2,(#71635,#71636,#71637),.UNSPECIFIED.,.F.,.F.)
B_SPLINE_CURVE_WITH_KNOTS((3,3),(0.376641898803536,0.382940702095949),
 .UNSPECIFIED.)
CURVE()
GEOMETRIC_REPRESENTATION_ITEM()
RATIONAL_B_SPLINE_CURVE((1.12071541658431,1.12024119946918,1.11971735964526))
REPRESENTATION_ITEM('')
);
#1425=(
BOUNDED_CURVE()
B_SPLINE_CURVE(2,(#71641,#71642,#71643),.UNSPECIFIED.,.F.,.F.)
B_SPLINE_CURVE_WITH_KNOTS((3,3),(0.249954652430665,0.256253455718077),
 .UNSPECIFIED.)
CURVE()
GEOMETRIC_REPRESENTATION_ITEM()
RATIONAL_B_SPLINE_CURVE((1.11971735964631,1.12024119946977,1.12071541658453))
REPRESENTATION_ITEM('')
);
#1426=(
BOUNDED_CURVE()
B_SPLINE_CURVE(2,(#71647,#71648,#71649),.UNSPECIFIED.,.F.,.F.)
B_SPLINE_CURVE_WITH_KNOTS((3,3),(0.376641898803534,0.382940702095945),
 .UNSPECIFIED.)
CURVE()
GEOMETRIC_REPRESENTATION_ITEM()
RATIONAL_B_SPLINE_CURVE((1.12071541658427,1.12024119946914,1.11971735964522))
REPRESENTATION_ITEM('')
);
#1427=(
BOUNDED_CURVE()
B_SPLINE_CURVE(2,(#71653,#71654,#71655),.UNSPECIFIED.,.F.,.F.)
B_SPLINE_CURVE_WITH_KNOTS((3,3),(0.249954652430654,0.256253455718069),
 .UNSPECIFIED.)
CURVE()
GEOMETRIC_REPRESENTATION_ITEM()
RATIONAL_B_SPLINE_CURVE((1.11971735964621,1.12024119946968,1.12071541658444))
REPRESENTATION_ITEM('')
);
#1428=(
BOUNDED_CURVE()
B_SPLINE_CURVE(2,(#71659,#71660,#71661),.UNSPECIFIED.,.F.,.F.)
B_SPLINE_CURVE_WITH_KNOTS((3,3),(0.376641898803532,0.382940702095944),
 .UNSPECIFIED.)
CURVE()
GEOMETRIC_REPRESENTATION_ITEM()
RATIONAL_B_SPLINE_CURVE((1.12071541658432,1.12024119946919,1.11971735964527))
REPRESENTATION_ITEM('')
);
#1429=(
BOUNDED_CURVE()
B_SPLINE_CURVE(2,(#71665,#71666,#71667),.UNSPECIFIED.,.F.,.F.)
B_SPLINE_CURVE_WITH_KNOTS((3,3),(0.249954652430654,0.256253455718072),
 .UNSPECIFIED.)
CURVE()
GEOMETRIC_REPRESENTATION_ITEM()
RATIONAL_B_SPLINE_CURVE((1.11971735964625,1.12024119946971,1.12071541658447))
REPRESENTATION_ITEM('')
);
#1430=(
BOUNDED_CURVE()
B_SPLINE_CURVE(2,(#71671,#71672,#71673),.UNSPECIFIED.,.F.,.F.)
B_SPLINE_CURVE_WITH_KNOTS((3,3),(0.376641898803539,0.382940702095952),
 .UNSPECIFIED.)
CURVE()
GEOMETRIC_REPRESENTATION_ITEM()
RATIONAL_B_SPLINE_CURVE((1.1207154165844,1.12024119946926,1.11971735964534))
REPRESENTATION_ITEM('')
);
#1431=(
BOUNDED_CURVE()
B_SPLINE_CURVE(2,(#71677,#71678,#71679),.UNSPECIFIED.,.F.,.F.)
B_SPLINE_CURVE_WITH_KNOTS((3,3),(0.249954652430648,0.256253455718062),
 .UNSPECIFIED.)
CURVE()
GEOMETRIC_REPRESENTATION_ITEM()
RATIONAL_B_SPLINE_CURVE((1.11971735964618,1.12024119946965,1.12071541658441))
REPRESENTATION_ITEM('')
);
#1432=(
BOUNDED_CURVE()
B_SPLINE_CURVE(2,(#71683,#71684,#71685),.UNSPECIFIED.,.F.,.F.)
B_SPLINE_CURVE_WITH_KNOTS((3,3),(0.376641898803519,0.382940702095932),
 .UNSPECIFIED.)
CURVE()
GEOMETRIC_REPRESENTATION_ITEM()
RATIONAL_B_SPLINE_CURVE((1.12071541658452,1.12024119946938,1.11971735964546))
REPRESENTATION_ITEM('')
);
#1433=(
BOUNDED_CURVE()
B_SPLINE_CURVE(2,(#71689,#71690,#71691),.UNSPECIFIED.,.F.,.F.)
B_SPLINE_CURVE_WITH_KNOTS((3,3),(0.249954652430659,0.256253455718071),
 .UNSPECIFIED.)
CURVE()
GEOMETRIC_REPRESENTATION_ITEM()
RATIONAL_B_SPLINE_CURVE((1.11971735964627,1.12024119946974,1.1207154165845))
REPRESENTATION_ITEM('')
);
#1434=(
BOUNDED_CURVE()
B_SPLINE_CURVE(2,(#71695,#71696,#71697),.UNSPECIFIED.,.F.,.F.)
B_SPLINE_CURVE_WITH_KNOTS((3,3),(0.376641898803527,0.382940702095942),
 .UNSPECIFIED.)
CURVE()
GEOMETRIC_REPRESENTATION_ITEM()
RATIONAL_B_SPLINE_CURVE((1.12071541658453,1.1202411994694,1.11971735964547))
REPRESENTATION_ITEM('')
);
#1435=(
BOUNDED_CURVE()
B_SPLINE_CURVE(2,(#71701,#71702,#71703),.UNSPECIFIED.,.F.,.F.)
B_SPLINE_CURVE_WITH_KNOTS((3,3),(0.249954652430662,0.256253455718075),
 .UNSPECIFIED.)
CURVE()
GEOMETRIC_REPRESENTATION_ITEM()
RATIONAL_B_SPLINE_CURVE((1.11971735964629,1.12024119946976,1.12071541658452))
REPRESENTATION_ITEM('')
);
#1436=(
BOUNDED_CURVE()
B_SPLINE_CURVE(2,(#71707,#71708,#71709),.UNSPECIFIED.,.F.,.F.)
B_SPLINE_CURVE_WITH_KNOTS((3,3),(0.376641898803543,0.382940702095954),
 .UNSPECIFIED.)
CURVE()
GEOMETRIC_REPRESENTATION_ITEM()
RATIONAL_B_SPLINE_CURVE((1.12071541658423,1.1202411994691,1.11971735964518))
REPRESENTATION_ITEM('')
);
#1437=(
BOUNDED_CURVE()
B_SPLINE_CURVE(2,(#71713,#71714,#71715),.UNSPECIFIED.,.F.,.F.)
B_SPLINE_CURVE_WITH_KNOTS((3,3),(0.249954652430648,0.256253455718061),
 .UNSPECIFIED.)
CURVE()
GEOMETRIC_REPRESENTATION_ITEM()
RATIONAL_B_SPLINE_CURVE((1.11971735964609,1.12024119946956,1.12071541658431))
REPRESENTATION_ITEM('')
);
#1438=(
BOUNDED_CURVE()
B_SPLINE_CURVE(2,(#71719,#71720,#71721),.UNSPECIFIED.,.F.,.F.)
B_SPLINE_CURVE_WITH_KNOTS((3,3),(0.376641898803529,0.382940702095943),
 .UNSPECIFIED.)
CURVE()
GEOMETRIC_REPRESENTATION_ITEM()
RATIONAL_B_SPLINE_CURVE((1.12071541658438,1.12024119946925,1.11971735964533))
REPRESENTATION_ITEM('')
);
#1439=(
BOUNDED_CURVE()
B_SPLINE_CURVE(2,(#71725,#71726,#71727),.UNSPECIFIED.,.F.,.F.)
B_SPLINE_CURVE_WITH_KNOTS((3,3),(0.249954652430657,0.256253455718069),
 .UNSPECIFIED.)
CURVE()
GEOMETRIC_REPRESENTATION_ITEM()
RATIONAL_B_SPLINE_CURVE((1.11971735964625,1.12024119946971,1.12071541658447))
REPRESENTATION_ITEM('')
);
#1440=(
BOUNDED_CURVE()
B_SPLINE_CURVE(2,(#71731,#71732,#71733),.UNSPECIFIED.,.F.,.F.)
B_SPLINE_CURVE_WITH_KNOTS((3,3),(0.376641898803529,0.382940702095941),
 .UNSPECIFIED.)
CURVE()
GEOMETRIC_REPRESENTATION_ITEM()
RATIONAL_B_SPLINE_CURVE((1.12071541658439,1.12024119946925,1.11971735964533))
REPRESENTATION_ITEM('')
);
#1441=(
BOUNDED_CURVE()
B_SPLINE_CURVE(2,(#71737,#71738,#71739),.UNSPECIFIED.,.F.,.F.)
B_SPLINE_CURVE_WITH_KNOTS((3,3),(0.24995465243065,0.256253455718062),
 .UNSPECIFIED.)
CURVE()
GEOMETRIC_REPRESENTATION_ITEM()
RATIONAL_B_SPLINE_CURVE((1.11971735964607,1.12024119946954,1.12071541658429))
REPRESENTATION_ITEM('')
);
#1442=(
BOUNDED_CURVE()
B_SPLINE_CURVE(2,(#71743,#71744,#71745),.UNSPECIFIED.,.F.,.F.)
B_SPLINE_CURVE_WITH_KNOTS((3,3),(0.376641898803544,0.382940702095955),
 .UNSPECIFIED.)
CURVE()
GEOMETRIC_REPRESENTATION_ITEM()
RATIONAL_B_SPLINE_CURVE((1.12071541658421,1.12024119946907,1.11971735964515))
REPRESENTATION_ITEM('')
);
#1443=(
BOUNDED_CURVE()
B_SPLINE_CURVE(2,(#71749,#71750,#71751),.UNSPECIFIED.,.F.,.F.)
B_SPLINE_CURVE_WITH_KNOTS((3,3),(0.249954652430658,0.256253455718075),
 .UNSPECIFIED.)
CURVE()
GEOMETRIC_REPRESENTATION_ITEM()
RATIONAL_B_SPLINE_CURVE((1.11971735964629,1.12024119946976,1.12071541658452))
REPRESENTATION_ITEM('')
);
#1444=(
BOUNDED_CURVE()
B_SPLINE_CURVE(2,(#71755,#71756,#71757),.UNSPECIFIED.,.F.,.F.)
B_SPLINE_CURVE_WITH_KNOTS((3,3),(0.376641898803543,0.382940702095958),
 .UNSPECIFIED.)
CURVE()
GEOMETRIC_REPRESENTATION_ITEM()
RATIONAL_B_SPLINE_CURVE((1.12071541658432,1.12024119946919,1.11971735964527))
REPRESENTATION_ITEM('')
);
#1445=(
BOUNDED_CURVE()
B_SPLINE_CURVE(2,(#71761,#71762,#71763),.UNSPECIFIED.,.F.,.F.)
B_SPLINE_CURVE_WITH_KNOTS((3,3),(0.249954652430663,0.256253455718076),
 .UNSPECIFIED.)
CURVE()
GEOMETRIC_REPRESENTATION_ITEM()
RATIONAL_B_SPLINE_CURVE((1.11971735964633,1.12024119946979,1.12071541658455))
REPRESENTATION_ITEM('')
);
#1446=(
BOUNDED_CURVE()
B_SPLINE_CURVE(2,(#71767,#71768,#71769),.UNSPECIFIED.,.F.,.F.)
B_SPLINE_CURVE_WITH_KNOTS((3,3),(0.37664189880352,0.382940702095933),
 .UNSPECIFIED.)
CURVE()
GEOMETRIC_REPRESENTATION_ITEM()
RATIONAL_B_SPLINE_CURVE((1.1207154165845,1.12024119946936,1.11971735964544))
REPRESENTATION_ITEM('')
);
#1447=(
BOUNDED_CURVE()
B_SPLINE_CURVE(2,(#71773,#71774,#71775),.UNSPECIFIED.,.F.,.F.)
B_SPLINE_CURVE_WITH_KNOTS((3,3),(0.249954652430661,0.256253455718074),
 .UNSPECIFIED.)
CURVE()
GEOMETRIC_REPRESENTATION_ITEM()
RATIONAL_B_SPLINE_CURVE((1.11971735964627,1.12024119946973,1.12071541658449))
REPRESENTATION_ITEM('')
);
#1448=(
BOUNDED_CURVE()
B_SPLINE_CURVE(2,(#71779,#71780,#71781),.UNSPECIFIED.,.F.,.F.)
B_SPLINE_CURVE_WITH_KNOTS((3,3),(0.376641898803524,0.382940702095942),
 .UNSPECIFIED.)
CURVE()
GEOMETRIC_REPRESENTATION_ITEM()
RATIONAL_B_SPLINE_CURVE((1.12071541658449,1.12024119946935,1.11971735964543))
REPRESENTATION_ITEM('')
);
#1449=(
BOUNDED_CURVE()
B_SPLINE_CURVE(2,(#71785,#71786,#71787),.UNSPECIFIED.,.F.,.F.)
B_SPLINE_CURVE_WITH_KNOTS((3,3),(0.249954652430645,0.256253455718058),
 .UNSPECIFIED.)
CURVE()
GEOMETRIC_REPRESENTATION_ITEM()
RATIONAL_B_SPLINE_CURVE((1.11971735964602,1.12024119946949,1.12071541658425))
REPRESENTATION_ITEM('')
);
#1450=(
BOUNDED_CURVE()
B_SPLINE_CURVE(2,(#71791,#71792,#71793),.UNSPECIFIED.,.F.,.F.)
B_SPLINE_CURVE_WITH_KNOTS((3,3),(0.376641898803526,0.382940702095943),
 .UNSPECIFIED.)
CURVE()
GEOMETRIC_REPRESENTATION_ITEM()
RATIONAL_B_SPLINE_CURVE((1.12071541658447,1.12024119946934,1.11971735964542))
REPRESENTATION_ITEM('')
);
#1451=(
BOUNDED_CURVE()
B_SPLINE_CURVE(2,(#71797,#71798,#71799),.UNSPECIFIED.,.F.,.F.)
B_SPLINE_CURVE_WITH_KNOTS((3,3),(0.249954652430656,0.25625345571807),
 .UNSPECIFIED.)
CURVE()
GEOMETRIC_REPRESENTATION_ITEM()
RATIONAL_B_SPLINE_CURVE((1.11971735964623,1.12024119946969,1.12071541658445))
REPRESENTATION_ITEM('')
);
#1452=(
BOUNDED_CURVE()
B_SPLINE_CURVE(2,(#71803,#71804,#71805),.UNSPECIFIED.,.F.,.F.)
B_SPLINE_CURVE_WITH_KNOTS((3,3),(0.376641898803539,0.382940702095953),
 .UNSPECIFIED.)
CURVE()
GEOMETRIC_REPRESENTATION_ITEM()
RATIONAL_B_SPLINE_CURVE((1.12071541658437,1.12024119946923,1.11971735964531))
REPRESENTATION_ITEM('')
);
#1453=(
BOUNDED_CURVE()
B_SPLINE_CURVE(2,(#71809,#71810,#71811),.UNSPECIFIED.,.F.,.F.)
B_SPLINE_CURVE_WITH_KNOTS((3,3),(0.249954652430661,0.256253455718075),
 .UNSPECIFIED.)
CURVE()
GEOMETRIC_REPRESENTATION_ITEM()
RATIONAL_B_SPLINE_CURVE((1.11971735964628,1.12024119946974,1.1207154165845))
REPRESENTATION_ITEM('')
);
#1454=(
BOUNDED_CURVE()
B_SPLINE_CURVE(2,(#71815,#71816,#71817),.UNSPECIFIED.,.F.,.F.)
B_SPLINE_CURVE_WITH_KNOTS((3,3),(0.376641898803538,0.382940702095948),
 .UNSPECIFIED.)
CURVE()
GEOMETRIC_REPRESENTATION_ITEM()
RATIONAL_B_SPLINE_CURVE((1.12071541658433,1.1202411994692,1.11971735964528))
REPRESENTATION_ITEM('')
);
#1455=(
BOUNDED_CURVE()
B_SPLINE_CURVE(2,(#71821,#71822,#71823),.UNSPECIFIED.,.F.,.F.)
B_SPLINE_CURVE_WITH_KNOTS((3,3),(0.249954652430662,0.256253455718076),
 .UNSPECIFIED.)
CURVE()
GEOMETRIC_REPRESENTATION_ITEM()
RATIONAL_B_SPLINE_CURVE((1.11971735964622,1.12024119946968,1.12071541658444))
REPRESENTATION_ITEM('')
);
#1456=(
BOUNDED_CURVE()
B_SPLINE_CURVE(2,(#71827,#71828,#71829),.UNSPECIFIED.,.F.,.F.)
B_SPLINE_CURVE_WITH_KNOTS((3,3),(0.37664189880352,0.382940702095935),
 .UNSPECIFIED.)
CURVE()
GEOMETRIC_REPRESENTATION_ITEM()
RATIONAL_B_SPLINE_CURVE((1.12071541658454,1.12024119946941,1.11971735964549))
REPRESENTATION_ITEM('')
);
#1457=(
BOUNDED_CURVE()
B_SPLINE_CURVE(2,(#71833,#71834,#71835),.UNSPECIFIED.,.F.,.F.)
B_SPLINE_CURVE_WITH_KNOTS((3,3),(0.24995465243066,0.256253455718075),
 .UNSPECIFIED.)
CURVE()
GEOMETRIC_REPRESENTATION_ITEM()
RATIONAL_B_SPLINE_CURVE((1.1197173596463,1.12024119946976,1.12071541658452))
REPRESENTATION_ITEM('')
);
#1458=(
BOUNDED_CURVE()
B_SPLINE_CURVE(2,(#71839,#71840,#71841),.UNSPECIFIED.,.F.,.F.)
B_SPLINE_CURVE_WITH_KNOTS((3,3),(0.376641898803523,0.382940702095934),
 .UNSPECIFIED.)
CURVE()
GEOMETRIC_REPRESENTATION_ITEM()
RATIONAL_B_SPLINE_CURVE((1.12071541658448,1.12024119946934,1.11971735964542))
REPRESENTATION_ITEM('')
);
#1459=(
BOUNDED_CURVE()
B_SPLINE_CURVE(2,(#71845,#71846,#71847),.UNSPECIFIED.,.F.,.F.)
B_SPLINE_CURVE_WITH_KNOTS((3,3),(0.249954652430663,0.256253455718077),
 .UNSPECIFIED.)
CURVE()
GEOMETRIC_REPRESENTATION_ITEM()
RATIONAL_B_SPLINE_CURVE((1.11971735964627,1.12024119946973,1.12071541658449))
REPRESENTATION_ITEM('')
);
#1460=(
BOUNDED_CURVE()
B_SPLINE_CURVE(2,(#71851,#71852,#71853),.UNSPECIFIED.,.F.,.F.)
B_SPLINE_CURVE_WITH_KNOTS((3,3),(0.376641898803548,0.382940702095957),
 .UNSPECIFIED.)
CURVE()
GEOMETRIC_REPRESENTATION_ITEM()
RATIONAL_B_SPLINE_CURVE((1.12071541658418,1.12024119946905,1.11971735964513))
REPRESENTATION_ITEM('')
);
#1461=(
BOUNDED_CURVE()
B_SPLINE_CURVE(2,(#71857,#71858,#71859),.UNSPECIFIED.,.F.,.F.)
B_SPLINE_CURVE_WITH_KNOTS((3,3),(0.249954652430651,0.256253455718065),
 .UNSPECIFIED.)
CURVE()
GEOMETRIC_REPRESENTATION_ITEM()
RATIONAL_B_SPLINE_CURVE((1.1197173596461,1.12024119946956,1.12071541658432))
REPRESENTATION_ITEM('')
);
#1462=(
BOUNDED_CURVE()
B_SPLINE_CURVE(2,(#71863,#71864,#71865),.UNSPECIFIED.,.F.,.F.)
B_SPLINE_CURVE_WITH_KNOTS((3,3),(0.376641898803522,0.382940702095932),
 .UNSPECIFIED.)
CURVE()
GEOMETRIC_REPRESENTATION_ITEM()
RATIONAL_B_SPLINE_CURVE((1.12071541658448,1.12024119946934,1.11971735964542))
REPRESENTATION_ITEM('')
);
#1463=(
BOUNDED_CURVE()
B_SPLINE_CURVE(2,(#71869,#71870,#71871),.UNSPECIFIED.,.F.,.F.)
B_SPLINE_CURVE_WITH_KNOTS((3,3),(0.249954652430654,0.256253455718068),
 .UNSPECIFIED.)
CURVE()
GEOMETRIC_REPRESENTATION_ITEM()
RATIONAL_B_SPLINE_CURVE((1.11971735964629,1.12024119946976,1.12071541658452))
REPRESENTATION_ITEM('')
);
#1464=(
BOUNDED_CURVE()
B_SPLINE_CURVE(2,(#71875,#71876,#71877),.UNSPECIFIED.,.F.,.F.)
B_SPLINE_CURVE_WITH_KNOTS((3,3),(0.376641898803521,0.382940702095935),
 .UNSPECIFIED.)
CURVE()
GEOMETRIC_REPRESENTATION_ITEM()
RATIONAL_B_SPLINE_CURVE((1.12071541658442,1.12024119946928,1.11971735964536))
REPRESENTATION_ITEM('')
);
#1465=(
BOUNDED_CURVE()
B_SPLINE_CURVE(2,(#71881,#71882,#71883),.UNSPECIFIED.,.F.,.F.)
B_SPLINE_CURVE_WITH_KNOTS((3,3),(0.24995465243066,0.256253455718076),
 .UNSPECIFIED.)
CURVE()
GEOMETRIC_REPRESENTATION_ITEM()
RATIONAL_B_SPLINE_CURVE((1.11971735964628,1.12024119946975,1.12071541658451))
REPRESENTATION_ITEM('')
);
#1466=(
BOUNDED_CURVE()
B_SPLINE_CURVE(2,(#71887,#71888,#71889),.UNSPECIFIED.,.F.,.F.)
B_SPLINE_CURVE_WITH_KNOTS((3,3),(0.37664189880352,0.382940702095931),
 .UNSPECIFIED.)
CURVE()
GEOMETRIC_REPRESENTATION_ITEM()
RATIONAL_B_SPLINE_CURVE((1.12071541658452,1.12024119946938,1.11971735964546))
REPRESENTATION_ITEM('')
);
#1467=(
BOUNDED_CURVE()
B_SPLINE_CURVE(2,(#71893,#71894,#71895),.UNSPECIFIED.,.F.,.F.)
B_SPLINE_CURVE_WITH_KNOTS((3,3),(0.249954652430663,0.25625345571808),
 .UNSPECIFIED.)
CURVE()
GEOMETRIC_REPRESENTATION_ITEM()
RATIONAL_B_SPLINE_CURVE((1.11971735964629,1.12024119946975,1.12071541658451))
REPRESENTATION_ITEM('')
);
#1468=(
BOUNDED_CURVE()
B_SPLINE_CURVE(2,(#71899,#71900,#71901),.UNSPECIFIED.,.F.,.F.)
B_SPLINE_CURVE_WITH_KNOTS((3,3),(0.376641898803514,0.382940702095925),
 .UNSPECIFIED.)
CURVE()
GEOMETRIC_REPRESENTATION_ITEM()
RATIONAL_B_SPLINE_CURVE((1.12071541658449,1.12024119946936,1.11971735964544))
REPRESENTATION_ITEM('')
);
#1469=(
BOUNDED_CURVE()
B_SPLINE_CURVE(2,(#71905,#71906,#71907),.UNSPECIFIED.,.F.,.F.)
B_SPLINE_CURVE_WITH_KNOTS((3,3),(0.249954652430668,0.25625345571808),
 .UNSPECIFIED.)
CURVE()
GEOMETRIC_REPRESENTATION_ITEM()
RATIONAL_B_SPLINE_CURVE((1.11971735964628,1.12024119946974,1.1207154165845))
REPRESENTATION_ITEM('')
);
#1470=(
BOUNDED_CURVE()
B_SPLINE_CURVE(2,(#71911,#71912,#71913),.UNSPECIFIED.,.F.,.F.)
B_SPLINE_CURVE_WITH_KNOTS((3,3),(0.376641898803516,0.382940702095925),
 .UNSPECIFIED.)
CURVE()
GEOMETRIC_REPRESENTATION_ITEM()
RATIONAL_B_SPLINE_CURVE((1.1207154165845,1.12024119946936,1.11971735964544))
REPRESENTATION_ITEM('')
);
#1471=(
BOUNDED_CURVE()
B_SPLINE_CURVE(2,(#71917,#71918,#71919),.UNSPECIFIED.,.F.,.F.)
B_SPLINE_CURVE_WITH_KNOTS((3,3),(0.24995465243065,0.256253455718064),
 .UNSPECIFIED.)
CURVE()
GEOMETRIC_REPRESENTATION_ITEM()
RATIONAL_B_SPLINE_CURVE((1.11971735964608,1.12024119946955,1.1207154165843))
REPRESENTATION_ITEM('')
);
#1472=(
BOUNDED_CURVE()
B_SPLINE_CURVE(2,(#71923,#71924,#71925),.UNSPECIFIED.,.F.,.F.)
B_SPLINE_CURVE_WITH_KNOTS((3,3),(0.376641898803537,0.382940702095953),
 .UNSPECIFIED.)
CURVE()
GEOMETRIC_REPRESENTATION_ITEM()
RATIONAL_B_SPLINE_CURVE((1.12071541658421,1.12024119946908,1.11971735964516))
REPRESENTATION_ITEM('')
);
#1473=(
BOUNDED_CURVE()
B_SPLINE_CURVE(2,(#71929,#71930,#71931),.UNSPECIFIED.,.F.,.F.)
B_SPLINE_CURVE_WITH_KNOTS((3,3),(0.249954652430652,0.256253455718068),
 .UNSPECIFIED.)
CURVE()
GEOMETRIC_REPRESENTATION_ITEM()
RATIONAL_B_SPLINE_CURVE((1.11971735964626,1.12024119946972,1.12071541658448))
REPRESENTATION_ITEM('')
);
#1474=(
BOUNDED_CURVE()
B_SPLINE_CURVE(2,(#71935,#71936,#71937),.UNSPECIFIED.,.F.,.F.)
B_SPLINE_CURVE_WITH_KNOTS((3,3),(0.376641898803534,0.382940702095941),
 .UNSPECIFIED.)
CURVE()
GEOMETRIC_REPRESENTATION_ITEM()
RATIONAL_B_SPLINE_CURVE((1.12071541658423,1.1202411994691,1.11971735964518))
REPRESENTATION_ITEM('')
);
#1475=(
BOUNDED_CURVE()
B_SPLINE_CURVE(2,(#71941,#71942,#71943),.UNSPECIFIED.,.F.,.F.)
B_SPLINE_CURVE_WITH_KNOTS((3,3),(0.249954652430639,0.256253455718054),
 .UNSPECIFIED.)
CURVE()
GEOMETRIC_REPRESENTATION_ITEM()
RATIONAL_B_SPLINE_CURVE((1.11971735964598,1.12024119946944,1.1207154165842))
REPRESENTATION_ITEM('')
);
#1476=(
BOUNDED_CURVE()
B_SPLINE_CURVE(2,(#71947,#71948,#71949),.UNSPECIFIED.,.F.,.F.)
B_SPLINE_CURVE_WITH_KNOTS((3,3),(0.376641898803521,0.382940702095926),
 .UNSPECIFIED.)
CURVE()
GEOMETRIC_REPRESENTATION_ITEM()
RATIONAL_B_SPLINE_CURVE((1.12071541658441,1.12024119946928,1.11971735964536))
REPRESENTATION_ITEM('')
);
#1477=(
BOUNDED_CURVE()
B_SPLINE_CURVE(2,(#71953,#71954,#71955),.UNSPECIFIED.,.F.,.F.)
B_SPLINE_CURVE_WITH_KNOTS((3,3),(0.249954652430644,0.256253455718059),
 .UNSPECIFIED.)
CURVE()
GEOMETRIC_REPRESENTATION_ITEM()
RATIONAL_B_SPLINE_CURVE((1.11971735964605,1.12024119946951,1.12071541658427))
REPRESENTATION_ITEM('')
);
#1478=(
BOUNDED_CURVE()
B_SPLINE_CURVE(2,(#71959,#71960,#71961),.UNSPECIFIED.,.F.,.F.)
B_SPLINE_CURVE_WITH_KNOTS((3,3),(0.376641898803522,0.382940702095933),
 .UNSPECIFIED.)
CURVE()
GEOMETRIC_REPRESENTATION_ITEM()
RATIONAL_B_SPLINE_CURVE((1.12071541658452,1.12024119946939,1.11971735964547))
REPRESENTATION_ITEM('')
);
#1479=(
BOUNDED_CURVE()
B_SPLINE_CURVE(2,(#71965,#71966,#71967),.UNSPECIFIED.,.F.,.F.)
B_SPLINE_CURVE_WITH_KNOTS((3,3),(0.249954652430652,0.256253455718069),
 .UNSPECIFIED.)
CURVE()
GEOMETRIC_REPRESENTATION_ITEM()
RATIONAL_B_SPLINE_CURVE((1.11971735964616,1.12024119946962,1.12071541658438))
REPRESENTATION_ITEM('')
);
#1480=(
BOUNDED_CURVE()
B_SPLINE_CURVE(2,(#71971,#71972,#71973),.UNSPECIFIED.,.F.,.F.)
B_SPLINE_CURVE_WITH_KNOTS((3,3),(0.376641898803538,0.38294070209595),
 .UNSPECIFIED.)
CURVE()
GEOMETRIC_REPRESENTATION_ITEM()
RATIONAL_B_SPLINE_CURVE((1.12071541658426,1.12024119946913,1.11971735964521))
REPRESENTATION_ITEM('')
);
#1481=(
BOUNDED_CURVE()
B_SPLINE_CURVE(2,(#71976,#71977,#71978),.UNSPECIFIED.,.F.,.F.)
B_SPLINE_CURVE_WITH_KNOTS((3,3),(0.249954652430655,0.256253455718073),
 .UNSPECIFIED.)
CURVE()
GEOMETRIC_REPRESENTATION_ITEM()
RATIONAL_B_SPLINE_CURVE((1.11971735964623,1.1202411994697,1.12071541658446))
REPRESENTATION_ITEM('')
);
#1482=(
BOUNDED_CURVE()
B_SPLINE_CURVE(2,(#71980,#71981,#71982),.UNSPECIFIED.,.F.,.F.)
B_SPLINE_CURVE_WITH_KNOTS((3,3),(0.376641898803523,0.38294070209594),
 .UNSPECIFIED.)
CURVE()
GEOMETRIC_REPRESENTATION_ITEM()
RATIONAL_B_SPLINE_CURVE((1.12071541658441,1.12024119946928,1.11971735964536))
REPRESENTATION_ITEM('')
);
#1483=(
BOUNDED_CURVE()
B_SPLINE_CURVE(2,(#71985,#71986,#71987),.UNSPECIFIED.,.F.,.F.)
B_SPLINE_CURVE_WITH_KNOTS((3,3),(0.249954652430659,0.256253455718073),
 .UNSPECIFIED.)
CURVE()
GEOMETRIC_REPRESENTATION_ITEM()
RATIONAL_B_SPLINE_CURVE((1.11971735964623,1.12024119946969,1.12071541658445))
REPRESENTATION_ITEM('')
);
#1484=(
BOUNDED_CURVE()
B_SPLINE_CURVE(2,(#71989,#71990,#71991),.UNSPECIFIED.,.F.,.F.)
B_SPLINE_CURVE_WITH_KNOTS((3,3),(0.376641898803521,0.382940702095929),
 .UNSPECIFIED.)
CURVE()
GEOMETRIC_REPRESENTATION_ITEM()
RATIONAL_B_SPLINE_CURVE((1.12071541658454,1.1202411994694,1.11971735964548))
REPRESENTATION_ITEM('')
);
#1485=(
BOUNDED_CURVE()
B_SPLINE_CURVE(2,(#71994,#71995,#71996),.UNSPECIFIED.,.F.,.F.)
B_SPLINE_CURVE_WITH_KNOTS((3,3),(0.249954652430646,0.256253455718056),
 .UNSPECIFIED.)
CURVE()
GEOMETRIC_REPRESENTATION_ITEM()
RATIONAL_B_SPLINE_CURVE((1.11971735964596,1.12024119946942,1.12071541658418))
REPRESENTATION_ITEM('')
);
#1486=(
BOUNDED_CURVE()
B_SPLINE_CURVE(2,(#71998,#71999,#72000),.UNSPECIFIED.,.F.,.F.)
B_SPLINE_CURVE_WITH_KNOTS((3,3),(0.376641898803528,0.382940702095943),
 .UNSPECIFIED.)
CURVE()
GEOMETRIC_REPRESENTATION_ITEM()
RATIONAL_B_SPLINE_CURVE((1.12071541658433,1.1202411994692,1.11971735964528))
REPRESENTATION_ITEM('')
);
#1487=(
BOUNDED_CURVE()
B_SPLINE_CURVE(2,(#72003,#72004,#72005),.UNSPECIFIED.,.F.,.F.)
B_SPLINE_CURVE_WITH_KNOTS((3,3),(0.24995465243066,0.256253455718077),
 .UNSPECIFIED.)
CURVE()
GEOMETRIC_REPRESENTATION_ITEM()
RATIONAL_B_SPLINE_CURVE((1.11971735964636,1.12024119946983,1.12071541658459))
REPRESENTATION_ITEM('')
);
#1488=(
BOUNDED_CURVE()
B_SPLINE_CURVE(2,(#72007,#72008,#72009),.UNSPECIFIED.,.F.,.F.)
B_SPLINE_CURVE_WITH_KNOTS((3,3),(0.376641898803527,0.382940702095942),
 .UNSPECIFIED.)
CURVE()
GEOMETRIC_REPRESENTATION_ITEM()
RATIONAL_B_SPLINE_CURVE((1.12071541658443,1.12024119946929,1.11971735964537))
REPRESENTATION_ITEM('')
);
#1489=(
BOUNDED_CURVE()
B_SPLINE_CURVE(2,(#72012,#72013,#72014),.UNSPECIFIED.,.F.,.F.)
B_SPLINE_CURVE_WITH_KNOTS((3,3),(0.249954652430663,0.256253455718073),
 .UNSPECIFIED.)
CURVE()
GEOMETRIC_REPRESENTATION_ITEM()
RATIONAL_B_SPLINE_CURVE((1.11971735964622,1.12024119946969,1.12071541658445))
REPRESENTATION_ITEM('')
);
#1490=(
BOUNDED_CURVE()
B_SPLINE_CURVE(2,(#72016,#72017,#72018),.UNSPECIFIED.,.F.,.F.)
B_SPLINE_CURVE_WITH_KNOTS((3,3),(0.376641898803534,0.382940702095947),
 .UNSPECIFIED.)
CURVE()
GEOMETRIC_REPRESENTATION_ITEM()
RATIONAL_B_SPLINE_CURVE((1.12071541658425,1.12024119946912,1.1197173596452))
REPRESENTATION_ITEM('')
);
#1491=(
BOUNDED_CURVE()
B_SPLINE_CURVE(2,(#72021,#72022,#72023),.UNSPECIFIED.,.F.,.F.)
B_SPLINE_CURVE_WITH_KNOTS((3,3),(0.249954652430658,0.256253455718067),
 .UNSPECIFIED.)
CURVE()
GEOMETRIC_REPRESENTATION_ITEM()
RATIONAL_B_SPLINE_CURVE((1.1197173596462,1.12024119946966,1.12071541658442))
REPRESENTATION_ITEM('')
);
#1492=(
BOUNDED_CURVE()
B_SPLINE_CURVE(2,(#72025,#72026,#72027),.UNSPECIFIED.,.F.,.F.)
B_SPLINE_CURVE_WITH_KNOTS((3,3),(0.376641898803512,0.382940702095926),
 .UNSPECIFIED.)
CURVE()
GEOMETRIC_REPRESENTATION_ITEM()
RATIONAL_B_SPLINE_CURVE((1.12071541658454,1.12024119946941,1.11971735964549))
REPRESENTATION_ITEM('')
);
#1493=(
BOUNDED_CURVE()
B_SPLINE_CURVE(2,(#72030,#72031,#72032),.UNSPECIFIED.,.F.,.F.)
B_SPLINE_CURVE_WITH_KNOTS((3,3),(0.249954652430648,0.256253455718064),
 .UNSPECIFIED.)
CURVE()
GEOMETRIC_REPRESENTATION_ITEM()
RATIONAL_B_SPLINE_CURVE((1.11971735964605,1.12024119946951,1.12071541658427))
REPRESENTATION_ITEM('')
);
#1494=(
BOUNDED_CURVE()
B_SPLINE_CURVE(2,(#72034,#72035,#72036),.UNSPECIFIED.,.F.,.F.)
B_SPLINE_CURVE_WITH_KNOTS((3,3),(0.37664189880353,0.382940702095945),
 .UNSPECIFIED.)
CURVE()
GEOMETRIC_REPRESENTATION_ITEM()
RATIONAL_B_SPLINE_CURVE((1.12071541658432,1.12024119946919,1.11971735964527))
REPRESENTATION_ITEM('')
);
#1495=(
BOUNDED_CURVE()
B_SPLINE_CURVE(2,(#72039,#72040,#72041),.UNSPECIFIED.,.F.,.F.)
B_SPLINE_CURVE_WITH_KNOTS((3,3),(0.24995465243065,0.256253455718062),
 .UNSPECIFIED.)
CURVE()
GEOMETRIC_REPRESENTATION_ITEM()
RATIONAL_B_SPLINE_CURVE((1.1197173596462,1.12024119946966,1.12071541658442))
REPRESENTATION_ITEM('')
);
#1496=(
BOUNDED_CURVE()
B_SPLINE_CURVE(2,(#72043,#72044,#72045),.UNSPECIFIED.,.F.,.F.)
B_SPLINE_CURVE_WITH_KNOTS((3,3),(0.376641898803514,0.382940702095926),
 .UNSPECIFIED.)
CURVE()
GEOMETRIC_REPRESENTATION_ITEM()
RATIONAL_B_SPLINE_CURVE((1.12071541658458,1.12024119946944,1.11971735964552))
REPRESENTATION_ITEM('')
);
#1497=(
BOUNDED_CURVE()
B_SPLINE_CURVE(2,(#72048,#72049,#72050),.UNSPECIFIED.,.F.,.F.)
B_SPLINE_CURVE_WITH_KNOTS((3,3),(0.249954652430654,0.256253455718075),
 .UNSPECIFIED.)
CURVE()
GEOMETRIC_REPRESENTATION_ITEM()
RATIONAL_B_SPLINE_CURVE((1.11971735964632,1.12024119946978,1.12071541658454))
REPRESENTATION_ITEM('')
);
#1498=(
BOUNDED_CURVE()
B_SPLINE_CURVE(2,(#72052,#72053,#72054),.UNSPECIFIED.,.F.,.F.)
B_SPLINE_CURVE_WITH_KNOTS((3,3),(0.376641898803524,0.382940702095939),
 .UNSPECIFIED.)
CURVE()
GEOMETRIC_REPRESENTATION_ITEM()
RATIONAL_B_SPLINE_CURVE((1.12071541658443,1.1202411994693,1.11971735964538))
REPRESENTATION_ITEM('')
);
#1499=(
BOUNDED_CURVE()
B_SPLINE_CURVE(2,(#72057,#72058,#72059),.UNSPECIFIED.,.F.,.F.)
B_SPLINE_CURVE_WITH_KNOTS((3,3),(0.249954652430651,0.256253455718065),
 .UNSPECIFIED.)
CURVE()
GEOMETRIC_REPRESENTATION_ITEM()
RATIONAL_B_SPLINE_CURVE((1.11971735964614,1.12024119946961,1.12071541658437))
REPRESENTATION_ITEM('')
);
#1500=(
BOUNDED_CURVE()
B_SPLINE_CURVE(2,(#72061,#72062,#72063),.UNSPECIFIED.,.F.,.F.)
B_SPLINE_CURVE_WITH_KNOTS((3,3),(0.376641898803524,0.382940702095937),
 .UNSPECIFIED.)
CURVE()
GEOMETRIC_REPRESENTATION_ITEM()
RATIONAL_B_SPLINE_CURVE((1.12071541658443,1.1202411994693,1.11971735964538))
REPRESENTATION_ITEM('')
);
#1501=(
BOUNDED_CURVE()
B_SPLINE_CURVE(2,(#72066,#72067,#72068),.UNSPECIFIED.,.F.,.F.)
B_SPLINE_CURVE_WITH_KNOTS((3,3),(0.24995465243066,0.256253455718078),
 .UNSPECIFIED.)
CURVE()
GEOMETRIC_REPRESENTATION_ITEM()
RATIONAL_B_SPLINE_CURVE((1.11971735964625,1.12024119946971,1.12071541658447))
REPRESENTATION_ITEM('')
);
#1502=(
BOUNDED_CURVE()
B_SPLINE_CURVE(2,(#72070,#72071,#72072),.UNSPECIFIED.,.F.,.F.)
B_SPLINE_CURVE_WITH_KNOTS((3,3),(0.376641898803522,0.382940702095931),
 .UNSPECIFIED.)
CURVE()
GEOMETRIC_REPRESENTATION_ITEM()
RATIONAL_B_SPLINE_CURVE((1.1207154165845,1.12024119946936,1.11971735964544))
REPRESENTATION_ITEM('')
);
#1503=(
BOUNDED_CURVE()
B_SPLINE_CURVE(2,(#72075,#72076,#72077),.UNSPECIFIED.,.F.,.F.)
B_SPLINE_CURVE_WITH_KNOTS((3,3),(0.249954652430652,0.256253455718071),
 .UNSPECIFIED.)
CURVE()
GEOMETRIC_REPRESENTATION_ITEM()
RATIONAL_B_SPLINE_CURVE((1.11971735964614,1.12024119946961,1.12071541658437))
REPRESENTATION_ITEM('')
);
#1504=(
BOUNDED_CURVE()
B_SPLINE_CURVE(2,(#72079,#72080,#72081),.UNSPECIFIED.,.F.,.F.)
B_SPLINE_CURVE_WITH_KNOTS((3,3),(0.376641898803528,0.382940702095942),
 .UNSPECIFIED.)
CURVE()
GEOMETRIC_REPRESENTATION_ITEM()
RATIONAL_B_SPLINE_CURVE((1.12071541658436,1.12024119946922,1.1197173596453))
REPRESENTATION_ITEM('')
);
#1505=(
BOUNDED_CURVE()
B_SPLINE_CURVE(2,(#72084,#72085,#72086),.UNSPECIFIED.,.F.,.F.)
B_SPLINE_CURVE_WITH_KNOTS((3,3),(0.249954652430651,0.256253455718071),
 .UNSPECIFIED.)
CURVE()
GEOMETRIC_REPRESENTATION_ITEM()
RATIONAL_B_SPLINE_CURVE((1.11971735964609,1.12024119946955,1.12071541658431))
REPRESENTATION_ITEM('')
);
#1506=(
BOUNDED_CURVE()
B_SPLINE_CURVE(2,(#72088,#72089,#72090),.UNSPECIFIED.,.F.,.F.)
B_SPLINE_CURVE_WITH_KNOTS((3,3),(0.376641898803537,0.382940702095949),
 .UNSPECIFIED.)
CURVE()
GEOMETRIC_REPRESENTATION_ITEM()
RATIONAL_B_SPLINE_CURVE((1.12071541658424,1.1202411994691,1.11971735964519))
REPRESENTATION_ITEM('')
);
#1507=(
BOUNDED_CURVE()
B_SPLINE_CURVE(2,(#72093,#72094,#72095),.UNSPECIFIED.,.F.,.F.)
B_SPLINE_CURVE_WITH_KNOTS((3,3),(0.249954652430663,0.256253455718077),
 .UNSPECIFIED.)
CURVE()
GEOMETRIC_REPRESENTATION_ITEM()
RATIONAL_B_SPLINE_CURVE((1.11971735964627,1.12024119946974,1.1207154165845))
REPRESENTATION_ITEM('')
);
#1508=(
BOUNDED_CURVE()
B_SPLINE_CURVE(2,(#72097,#72098,#72099),.UNSPECIFIED.,.F.,.F.)
B_SPLINE_CURVE_WITH_KNOTS((3,3),(0.376641898803535,0.382940702095948),
 .UNSPECIFIED.)
CURVE()
GEOMETRIC_REPRESENTATION_ITEM()
RATIONAL_B_SPLINE_CURVE((1.12071541658433,1.1202411994692,1.11971735964528))
REPRESENTATION_ITEM('')
);
#1509=(
BOUNDED_CURVE()
B_SPLINE_CURVE(2,(#72102,#72103,#72104),.UNSPECIFIED.,.F.,.F.)
B_SPLINE_CURVE_WITH_KNOTS((3,3),(0.249954652430657,0.256253455718068),
 .UNSPECIFIED.)
CURVE()
GEOMETRIC_REPRESENTATION_ITEM()
RATIONAL_B_SPLINE_CURVE((1.11971735964623,1.1202411994697,1.12071541658445))
REPRESENTATION_ITEM('')
);
#1510=(
BOUNDED_CURVE()
B_SPLINE_CURVE(2,(#72106,#72107,#72108),.UNSPECIFIED.,.F.,.F.)
B_SPLINE_CURVE_WITH_KNOTS((3,3),(0.376641898803534,0.382940702095946),
 .UNSPECIFIED.)
CURVE()
GEOMETRIC_REPRESENTATION_ITEM()
RATIONAL_B_SPLINE_CURVE((1.12071541658428,1.12024119946915,1.11971735964523))
REPRESENTATION_ITEM('')
);
#1511=(
BOUNDED_CURVE()
B_SPLINE_CURVE(2,(#72112,#72113,#72114),.UNSPECIFIED.,.F.,.F.)
B_SPLINE_CURVE_WITH_KNOTS((3,3),(0.249954652430652,0.256253455718065),
 .UNSPECIFIED.)
CURVE()
GEOMETRIC_REPRESENTATION_ITEM()
RATIONAL_B_SPLINE_CURVE((1.11971735964615,1.12024119946961,1.12071541658437))
REPRESENTATION_ITEM('')
);
#1512=(
BOUNDED_CURVE()
B_SPLINE_CURVE(2,(#72118,#72119,#72120),.UNSPECIFIED.,.F.,.F.)
B_SPLINE_CURVE_WITH_KNOTS((3,3),(0.376641898803528,0.38294070209594),
 .UNSPECIFIED.)
CURVE()
GEOMETRIC_REPRESENTATION_ITEM()
RATIONAL_B_SPLINE_CURVE((1.12071541658438,1.12024119946925,1.11971735964533))
REPRESENTATION_ITEM('')
);
#1513=(
BOUNDED_CURVE()
B_SPLINE_CURVE(2,(#72124,#72125,#72126),.UNSPECIFIED.,.F.,.F.)
B_SPLINE_CURVE_WITH_KNOTS((3,3),(0.249954652430646,0.256253455718057),
 .UNSPECIFIED.)
CURVE()
GEOMETRIC_REPRESENTATION_ITEM()
RATIONAL_B_SPLINE_CURVE((1.11971735964604,1.12024119946951,1.12071541658426))
REPRESENTATION_ITEM('')
);
#1514=(
BOUNDED_CURVE()
B_SPLINE_CURVE(2,(#72130,#72131,#72132),.UNSPECIFIED.,.F.,.F.)
B_SPLINE_CURVE_WITH_KNOTS((3,3),(0.376641898803525,0.382940702095939),
 .UNSPECIFIED.)
CURVE()
GEOMETRIC_REPRESENTATION_ITEM()
RATIONAL_B_SPLINE_CURVE((1.12071541658443,1.1202411994693,1.11971735964538))
REPRESENTATION_ITEM('')
);
#1515=(
BOUNDED_CURVE()
B_SPLINE_CURVE(2,(#72136,#72137,#72138),.UNSPECIFIED.,.F.,.F.)
B_SPLINE_CURVE_WITH_KNOTS((3,3),(0.249954652430639,0.256253455718051),
 .UNSPECIFIED.)
CURVE()
GEOMETRIC_REPRESENTATION_ITEM()
RATIONAL_B_SPLINE_CURVE((1.11971735964598,1.12024119946945,1.1207154165842))
REPRESENTATION_ITEM('')
);
#1516=(
BOUNDED_CURVE()
B_SPLINE_CURVE(2,(#72142,#72143,#72144),.UNSPECIFIED.,.F.,.F.)
B_SPLINE_CURVE_WITH_KNOTS((3,3),(0.376641898803521,0.382940702095934),
 .UNSPECIFIED.)
CURVE()
GEOMETRIC_REPRESENTATION_ITEM()
RATIONAL_B_SPLINE_CURVE((1.12071541658441,1.12024119946928,1.11971735964536))
REPRESENTATION_ITEM('')
);
#1517=(
BOUNDED_CURVE()
B_SPLINE_CURVE(2,(#72148,#72149,#72150),.UNSPECIFIED.,.F.,.F.)
B_SPLINE_CURVE_WITH_KNOTS((3,3),(0.249954652430652,0.256253455718065),
 .UNSPECIFIED.)
CURVE()
GEOMETRIC_REPRESENTATION_ITEM()
RATIONAL_B_SPLINE_CURVE((1.11971735964616,1.12024119946962,1.12071541658438))
REPRESENTATION_ITEM('')
);
#1518=(
BOUNDED_CURVE()
B_SPLINE_CURVE(2,(#72154,#72155,#72156),.UNSPECIFIED.,.F.,.F.)
B_SPLINE_CURVE_WITH_KNOTS((3,3),(0.376641898803544,0.382940702095957),
 .UNSPECIFIED.)
CURVE()
GEOMETRIC_REPRESENTATION_ITEM()
RATIONAL_B_SPLINE_CURVE((1.12071541658424,1.1202411994691,1.11971735964518))
REPRESENTATION_ITEM('')
);
#1519=(
BOUNDED_CURVE()
B_SPLINE_CURVE(2,(#72160,#72161,#72162),.UNSPECIFIED.,.F.,.F.)
B_SPLINE_CURVE_WITH_KNOTS((3,3),(0.249954652430643,0.256253455718053),
 .UNSPECIFIED.)
CURVE()
GEOMETRIC_REPRESENTATION_ITEM()
RATIONAL_B_SPLINE_CURVE((1.11971735964601,1.12024119946947,1.12071541658423))
REPRESENTATION_ITEM('')
);
#1520=(
BOUNDED_CURVE()
B_SPLINE_CURVE(2,(#72166,#72167,#72168),.UNSPECIFIED.,.F.,.F.)
B_SPLINE_CURVE_WITH_KNOTS((3,3),(0.376641898803543,0.382940702095953),
 .UNSPECIFIED.)
CURVE()
GEOMETRIC_REPRESENTATION_ITEM()
RATIONAL_B_SPLINE_CURVE((1.12071541658425,1.12024119946911,1.1197173596452))
REPRESENTATION_ITEM('')
);
#1521=(
BOUNDED_CURVE()
B_SPLINE_CURVE(2,(#72172,#72173,#72174),.UNSPECIFIED.,.F.,.F.)
B_SPLINE_CURVE_WITH_KNOTS((3,3),(0.249954652430649,0.256253455718062),
 .UNSPECIFIED.)
CURVE()
GEOMETRIC_REPRESENTATION_ITEM()
RATIONAL_B_SPLINE_CURVE((1.11971735964607,1.12024119946954,1.12071541658429))
REPRESENTATION_ITEM('')
);
#2478=ELLIPSE('',#35028,0.0195162536838815,0.0137573643715162);
#2479=ELLIPSE('',#35029,0.0195162536830269,0.0137573643713391);
#2480=ELLIPSE('',#35031,0.0195162536835621,0.0137573643714695);
#2481=ELLIPSE('',#35032,0.019516253683001,0.0137573643713521);
#2482=ELLIPSE('',#35034,0.0195162536836977,0.0137573643714721);
#2483=ELLIPSE('',#35035,0.0195162536830636,0.0137573643713535);
#2484=ELLIPSE('',#35037,0.0195162536837443,0.0137573643714943);
#2485=ELLIPSE('',#35038,0.0195162536831223,0.0137573643713688);
#2486=ELLIPSE('',#35040,0.019516253683803,0.013757364371504);
#2487=ELLIPSE('',#35041,0.0195162536829111,0.0137573643713217);
#2488=ELLIPSE('',#35043,0.0195162536837688,0.0137573643714986);
#2489=ELLIPSE('',#35044,0.0195162536830749,0.0137573643713556);
#2490=ELLIPSE('',#35046,0.0195162536837257,0.0137573643714922);
#2491=ELLIPSE('',#35047,0.0195162536830703,0.0137573643713494);
#2492=ELLIPSE('',#35049,0.0195162536838104,0.013757364371505);
#2493=ELLIPSE('',#35050,0.0195162536830614,0.0137573643713493);
#2494=ELLIPSE('',#35052,0.0195162536837473,0.0137573643714877);
#2495=ELLIPSE('',#35053,0.0195162536830537,0.0137573643713548);
#2496=ELLIPSE('',#35055,0.0195162536838422,0.0137573643715182);
#2497=ELLIPSE('',#35056,0.0195162536831755,0.0137573643713807);
#2498=ELLIPSE('',#35058,0.0195162536837639,0.0137573643714952);
#2499=ELLIPSE('',#35059,0.0195162536830792,0.0137573643713542);
#2500=ELLIPSE('',#35061,0.0195162536835653,0.0137573643714501);
#2501=ELLIPSE('',#35062,0.0195162536831025,0.0137573643713567);
#2502=ELLIPSE('',#35064,0.0195162536835776,0.0137573643714587);
#2503=ELLIPSE('',#35065,0.0195162536828947,0.01375736437132);
#2504=ELLIPSE('',#35067,0.0195162536837483,0.0137573643714995);
#2505=ELLIPSE('',#35068,0.0195162536831204,0.0137573643713664);
#2506=ELLIPSE('',#35070,0.0195162536835793,0.0137573643714601);
#2507=ELLIPSE('',#35071,0.0195162536830448,0.0137573643713492);
#2508=ELLIPSE('',#35080,0.0195034997306777,0.013754915723726);
#2509=ELLIPSE('',#35082,0.0195030685020683,0.0137548403891227);
#2510=ELLIPSE('',#35084,0.0195027524929284,0.0137547851848027);
#2511=ELLIPSE('',#35086,0.0195025132809572,0.0137547433941177);
#2512=ELLIPSE('',#35088,0.0195023280193677,0.0137547110253133);
#2513=ELLIPSE('',#35090,0.0195021823053853,0.0137546855626127);
#2514=ELLIPSE('',#35092,0.0195020666474465,0.0137546653482711);
#2515=ELLIPSE('',#35094,0.0195019745733047,0.0137546492518586);
#2516=ELLIPSE('',#35096,0.0195019015620118,0.0137546364836367);
#2517=ELLIPSE('',#35098,0.0195018443987318,0.0137546264818649);
#2518=ELLIPSE('',#35100,0.0195018007910573,0.0137546188457545);
#2519=ELLIPSE('',#35102,0.0195017691158091,0.0137546132912077);
#2520=ELLIPSE('',#35104,0.0195017482624769,0.0137546096234092);
#2521=ELLIPSE('',#35106,0.0195017375337946,0.0137546077193674);
#2522=ELLIPSE('',#35108,0.0195017365885567,0.0137546075177427);
#2523=ELLIPSE('',#35110,0.0195017454175912,0.0137546090143427);
#2524=ELLIPSE('',#35112,0.0195017643506138,0.0137546122627749);
#2525=ELLIPSE('',#35114,0.0195017941005044,0.0137546173811011);
#2526=ELLIPSE('',#35116,0.0195018358641676,0.0137546245672221);
#2527=ELLIPSE('',#35118,0.0195018727625836,0.013754631431718);
#2528=ELLIPSE('',#35120,0.0195034997306828,0.0137549157237274);
#2529=ELLIPSE('',#35122,0.0195030685021256,0.0137548403891337);
#2530=ELLIPSE('',#35124,0.0195027524929019,0.0137547851847966);
#2531=ELLIPSE('',#35126,0.0195025132809425,0.0137547433941156);
#2532=ELLIPSE('',#35128,0.0195023280193708,0.0137547110253143);
#2533=ELLIPSE('',#35130,0.0195021823053841,0.0137546855626124);
#2534=ELLIPSE('',#35132,0.0195020666474398,0.0137546653482691);
#2535=ELLIPSE('',#35134,0.0195019745733335,0.0137546492518631);
#2536=ELLIPSE('',#35136,0.0195019015619959,0.0137546364836322);
#2537=ELLIPSE('',#35138,0.0195018443987879,0.0137546264818748);
#2538=ELLIPSE('',#35140,0.0195018007910457,0.0137546188457536);
#2539=ELLIPSE('',#35142,0.0195017691158159,0.0137546132912084);
#2540=ELLIPSE('',#35144,0.0195017482624727,0.013754609623408);
#2541=ELLIPSE('',#35146,0.0195017375337736,0.0137546077193644);
#2542=ELLIPSE('',#35148,0.0195017365885347,0.0137546075177382);
#2543=ELLIPSE('',#35150,0.019501745417596,0.0137546090143437);
#2544=ELLIPSE('',#35152,0.0195017643505816,0.0137546122627688);
#2545=ELLIPSE('',#35154,0.0195017941005605,0.0137546173811125);
#2546=ELLIPSE('',#35156,0.019501835864167,0.0137546245672222);
#2547=ELLIPSE('',#35158,0.0195162536830855,0.0137573643713537);
#2548=ELLIPSE('',#35160,0.0195034997307414,0.013754915723739);
#2549=ELLIPSE('',#35162,0.0195030685021161,0.0137548403891323);
#2550=ELLIPSE('',#35164,0.0195027524929008,0.0137547851847961);
#2551=ELLIPSE('',#35166,0.0195025132809546,0.0137547433941189);
#2552=ELLIPSE('',#35168,0.0195023280193482,0.0137547110253084);
#2553=ELLIPSE('',#35185,0.0195034997306463,0.0137549157237206);
#2554=ELLIPSE('',#35187,0.0195030685021557,0.0137548403891397);
#2555=ELLIPSE('',#35189,0.0195027524928776,0.0137547851847918);
#2556=ELLIPSE('',#35191,0.0195025132809776,0.0137547433941213);
#2557=ELLIPSE('',#35193,0.019502328019347,0.0137547110253081);
#2558=ELLIPSE('',#35195,0.0195021823053738,0.0137546855626116);
#2559=ELLIPSE('',#35197,0.0195020666474525,0.0137546653482711);
#2560=ELLIPSE('',#35199,0.0195019745733739,0.013754649251872);
#2561=ELLIPSE('',#35201,0.0195019015619764,0.0137546364836293);
#2562=ELLIPSE('',#35203,0.0195018443987816,0.0137546264818739);
#2563=ELLIPSE('',#35205,0.0195018007910337,0.0137546188457504);
#2564=ELLIPSE('',#35207,0.0195017691158341,0.0137546132912121);
#2565=ELLIPSE('',#35209,0.0195017482624509,0.0137546096234037);
#2566=ELLIPSE('',#35211,0.0195017375337853,0.0137546077193653);
#2567=ELLIPSE('',#35213,0.0195017365886309,0.0137546075177561);
#2568=ELLIPSE('',#35215,0.0195017454176055,0.0137546090143461);
#2569=ELLIPSE('',#35217,0.0195017643505986,0.0137546122627731);
#2570=ELLIPSE('',#35219,0.0195017941005311,0.0137546173811059);
#2571=ELLIPSE('',#35221,0.0195018358641241,0.0137546245672129);
#2572=ELLIPSE('',#35225,0.0195034997306858,0.0137549157237271);
#2573=ELLIPSE('',#35227,0.0195030685021635,0.0137548403891432);
#2574=ELLIPSE('',#35229,0.019502752492881,0.0137547851847926);
#2575=ELLIPSE('',#35231,0.0195025132809236,0.0137547433941134);
#2576=ELLIPSE('',#35233,0.0195023280193679,0.0137547110253125);
#2577=ELLIPSE('',#35235,0.0195021823054267,0.0137546855626225);
#2578=ELLIPSE('',#35237,0.0195020666474927,0.0137546653482813);
#2579=ELLIPSE('',#35239,0.019501974573308,0.0137546492518591);
#2580=ELLIPSE('',#35241,0.0195019015619601,0.0137546364836262);
#2581=ELLIPSE('',#35243,0.0195018443987825,0.0137546264818736);
#2582=ELLIPSE('',#35245,0.0195018007910841,0.0137546188457617);
#2583=ELLIPSE('',#35247,0.0195017691158046,0.0137546132912069);
#2584=ELLIPSE('',#35249,0.0195017482624746,0.0137546096234107);
#2585=ELLIPSE('',#35251,0.0195017375337627,0.0137546077193623);
#2586=ELLIPSE('',#35253,0.0195017365885639,0.0137546075177438);
#2587=ELLIPSE('',#35255,0.0195017454175912,0.0137546090143448);
#2588=ELLIPSE('',#35257,0.0195017643506125,0.0137546122627745);
#2589=ELLIPSE('',#35259,0.0195017941005712,0.0137546173811145);
#2590=ELLIPSE('',#35261,0.0195018358641553,0.013754624567221);
#2591=ELLIPSE('',#35263,0.0195018727626295,0.0137546314317287);
#2592=ELLIPSE('',#35265,0.0195034997307231,0.0137549157237351);
#2593=ELLIPSE('',#35267,0.0195030685021692,0.0137548403891432);
#2594=ELLIPSE('',#35269,0.0195027524928953,0.013754785184795);
#2595=ELLIPSE('',#35271,0.0195025132809505,0.0137547433941165);
#2596=ELLIPSE('',#35273,0.0195023280194302,0.0137547110253254);
#2597=ELLIPSE('',#35275,0.019502182305463,0.0137546855626286);
#2598=ELLIPSE('',#35277,0.0195020666474861,0.0137546653482797);
#2599=ELLIPSE('',#35279,0.0195019745732981,0.0137546492518571);
#2600=ELLIPSE('',#35281,0.019501901562003,0.0137546364836345);
#2601=ELLIPSE('',#35283,0.0195018443988218,0.0137546264818824);
#2602=ELLIPSE('',#35285,0.0195018007911448,0.0137546188457728);
#2603=ELLIPSE('',#35287,0.0195017691157916,0.0137546132912057);
#2604=ELLIPSE('',#35289,0.0195017482624564,0.013754609623407);
#2605=ELLIPSE('',#35291,0.0195017375338029,0.0137546077193704);
#2606=ELLIPSE('',#35293,0.0195017365886144,0.0137546075177533);
#2607=ELLIPSE('',#35295,0.0195017454176306,0.0137546090143512);
#2608=ELLIPSE('',#35297,0.0195017643505891,0.0137546122627708);
#2609=ELLIPSE('',#35299,0.0195017941005193,0.013754617381105);
#2610=ELLIPSE('',#35301,0.0195018358642213,0.0137546245672329);
#2611=ELLIPSE('',#35303,0.0195162536837232,0.0137573643714884);
#2612=ELLIPSE('',#35305,0.0195034997306679,0.0137549157237246);
#2613=ELLIPSE('',#35307,0.0195030685021047,0.0137548403891311);
#2614=ELLIPSE('',#35309,0.0195027524929266,0.0137547851848028);
#2615=ELLIPSE('',#35311,0.0195025132809874,0.0137547433941253);
#2616=ELLIPSE('',#35313,0.0195023280194086,0.013754711025321);
#2617=ELLIPSE('',#35315,0.0195021823054203,0.0137546855626212);
#2618=ELLIPSE('',#35317,0.0195020666475111,0.0137546653482846);
#2619=ELLIPSE('',#35319,0.0195019745733549,0.0137546492518684);
#2620=ELLIPSE('',#35321,0.0195019015619592,0.0137546364836273);
#2621=ELLIPSE('',#35323,0.0195018443988324,0.0137546264818843);
#2622=ELLIPSE('',#35325,0.0195018007910703,0.0137546188457585);
#2623=ELLIPSE('',#35327,0.0195017691158645,0.0137546132912193);
#2624=ELLIPSE('',#35329,0.0195017482624579,0.0137546096234066);
#2625=ELLIPSE('',#35331,0.0195017375338027,0.0137546077193706);
#2626=ELLIPSE('',#35333,0.0195017365886083,0.0137546075177516);
#2627=ELLIPSE('',#35335,0.019501745417535,0.0137546090143326);
#2628=ELLIPSE('',#35337,0.0195017643506093,0.0137546122627733);
#2629=ELLIPSE('',#35339,0.0195017941005168,0.013754617381103);
#2630=ELLIPSE('',#35341,0.0195018358640787,0.0137546245672056);
#2631=ELLIPSE('',#35358,0.0195017365886013,0.0137546075177502);
#2632=ELLIPSE('',#35360,0.0195017454175941,0.0137546090143434);
#2633=ELLIPSE('',#35362,0.0195017643505789,0.0137546122627681);
#2634=ELLIPSE('',#35364,0.0195017941005255,0.0137546173811058);
#2635=ELLIPSE('',#35366,0.0195018358641318,0.0137546245672154);
#2636=ELLIPSE('',#35382,0.051274964768551,0.0469971417993774);
#2637=ELLIPSE('',#35384,0.0512707788579671,0.0469842741354326);
#2638=ELLIPSE('',#35386,0.0512707788562332,0.0469842741344865);
#2639=ELLIPSE('',#35387,0.0512749647685533,0.0469971417993787);
#2640=ELLIPSE('',#35390,0.0512707788571307,0.0469842741349983);
#2641=ELLIPSE('',#35391,0.0512749647672664,0.0469971417987026);
#2642=ELLIPSE('',#35394,0.0512707788571389,0.0469842741349856);
#2643=ELLIPSE('',#35395,0.0512749647681367,0.0469971417991575);
#2644=ELLIPSE('',#35398,0.0512707788569124,0.0469842741348335);
#2645=ELLIPSE('',#35399,0.051274964768467,0.0469971417993732);
#2646=ELLIPSE('',#35402,0.051270778857559,0.0469842741351648);
#2647=ELLIPSE('',#35403,0.0512749647697504,0.0469971418000396);
#2648=ELLIPSE('',#35406,0.051270778857562,0.0469842741352078);
#2649=ELLIPSE('',#35407,0.0512749647676798,0.0469971417989218);
#2650=ELLIPSE('',#35410,0.0512707788610954,0.0469842741371193);
#2651=ELLIPSE('',#35411,0.0512749647674827,0.0469971417988075);
#2652=ELLIPSE('',#35414,0.0512707788555596,0.0469842741341208);
#2653=ELLIPSE('',#35415,0.0512749647677061,0.0469971417989105);
#2654=ELLIPSE('',#35418,0.0512707788650729,0.0469842741392919);
#2655=ELLIPSE('',#35419,0.0512749647702881,0.0469971418003199);
#2656=ELLIPSE('',#35422,0.0512707788560203,0.0469842741343728);
#2657=ELLIPSE('',#35423,0.0512749647689969,0.0469971417996401);
#2658=ELLIPSE('',#35426,0.0512707788567884,0.046984274134799);
#2659=ELLIPSE('',#35427,0.0512749647681247,0.0469971417991492);
#2660=ELLIPSE('',#35430,0.0512707788573083,0.0469842741350659);
#2661=ELLIPSE('',#35431,0.0512749647690658,0.0469971417996437);
#2662=ELLIPSE('',#35434,0.0512707788615306,0.046984274137359);
#2663=ELLIPSE('',#35435,0.051274964767619,0.0469971417988856);
#2664=ELLIPSE('',#35438,0.0512707788928482,0.0469842741544496);
#2665=ELLIPSE('',#35439,0.0512749647695684,0.0469971417999069);
#2666=ELLIPSE('',#35442,0.051270778857717,0.0469842741353091);
#2667=ELLIPSE('',#35443,0.0512749647683041,0.0469971417992544);
#2668=ELLIPSE('',#35446,0.051270778855901,0.046984274134278);
#2669=ELLIPSE('',#35447,0.0512749647692079,0.0469971417997307);
#2670=ELLIPSE('',#35450,0.0512707788585063,0.0469842741357279);
#2671=ELLIPSE('',#35451,0.0512749647681597,0.0469971417991513);
#2672=ELLIPSE('',#35454,0.0512707788568602,0.0469842741348085);
#2673=ELLIPSE('',#35455,0.0512749647674443,0.0469971417987893);
#2674=ELLIPSE('',#35458,0.0512707788568387,0.0469842741347804);
#2675=ELLIPSE('',#35459,0.0512749647678151,0.0469971417990189);
#2676=ELLIPSE('',#35462,0.0512707788582789,0.0469842741356006);
#2677=ELLIPSE('',#35463,0.05127496476906,0.0469971417996405);
#2678=ELLIPSE('',#35466,0.051270778856965,0.0469842741348763);
#2679=ELLIPSE('',#35467,0.0512749647686908,0.046997141799481);
#2680=ELLIPSE('',#35470,0.0512707788563555,0.0469842741344815);
#2681=ELLIPSE('',#35471,0.0512749647673275,0.0469971417987118);
#2682=ELLIPSE('',#35474,0.0512707788571547,0.0469842741350112);
#2683=ELLIPSE('',#35475,0.0512749647685426,0.046997141799397);
#2684=ELLIPSE('',#35478,0.0512707788556612,0.0469842741341707);
#2685=ELLIPSE('',#35479,0.0512749647699517,0.0469971418001559);
#2686=ELLIPSE('',#35482,0.0512707788576472,0.0469842741352346);
#2687=ELLIPSE('',#35483,0.0512749647672529,0.0469971417986806);
#2688=ELLIPSE('',#35486,0.0512707788618793,0.0469842741375491);
#2689=ELLIPSE('',#35487,0.0512749647679756,0.0469971417990623);
#2690=ELLIPSE('',#35490,0.0512707788555002,0.0469842741340957);
#2691=ELLIPSE('',#35491,0.0512749647688844,0.046997141799544);
#2692=ELLIPSE('',#35494,0.0512707788566344,0.0469842741346946);
#2693=ELLIPSE('',#35495,0.051274964769648,0.046997141799953);
#2694=ELLIPSE('',#35498,0.0512707788584597,0.0469842741356599);
#2695=ELLIPSE('',#35499,0.0512749647679757,0.0469971417990702);
#2696=ELLIPSE('',#35502,0.0512707788568172,0.0469842741347837);
#2697=ELLIPSE('',#35503,0.051274964767697,0.0469971417989173);
#2698=ELLIPSE('',#35506,0.0512707788670663,0.0469842741404324);
#2699=ELLIPSE('',#35507,0.0512749647689531,0.0469971417995761);
#2700=ELLIPSE('',#35510,0.0512707788557115,0.0469842741341769);
#2701=ELLIPSE('',#35511,0.0512749647694815,0.0469971417999415);
#2702=ELLIPSE('',#35514,0.0512707788568934,0.0469842741348491);
#2703=ELLIPSE('',#35515,0.0512749647661315,0.0469971417980767);
#2704=ELLIPSE('',#35518,0.0512707788572177,0.0469842741350563);
#2705=ELLIPSE('',#35519,0.0512749647680353,0.0469971417991282);
#2706=ELLIPSE('',#35522,0.0512707788587383,0.046984274135853);
#2707=ELLIPSE('',#35523,0.0512749647684727,0.0469971417993084);
#2708=ELLIPSE('',#35526,0.0512707788631157,0.0469842741382362);
#2709=ELLIPSE('',#35527,0.0512749647685272,0.0469971417993756);
#2710=ELLIPSE('',#35530,0.0512707788564907,0.0469842741346169);
#2711=ELLIPSE('',#35531,0.0512749647685682,0.0469971417994032);
#2712=ELLIPSE('',#35534,0.0512707788585969,0.0469842741357701);
#2713=ELLIPSE('',#35535,0.0512749647676235,0.0469971417988947);
#2714=ELLIPSE('',#35538,0.0512707788751318,0.0469842741447984);
#2715=ELLIPSE('',#35539,0.0512749647678178,0.0469971417990053);
#2716=ELLIPSE('',#35542,0.0512707788575899,0.0469842741352132);
#2717=ELLIPSE('',#35543,0.0512749647677413,0.0469971417989442);
#2718=ELLIPSE('',#35546,0.0512707788579549,0.0469842741354182);
#2719=ELLIPSE('',#35547,0.0512749647704146,0.0469971418003949);
#2720=ELLIPSE('',#35550,0.0512707788581164,0.0469842741355277);
#2721=ELLIPSE('',#35551,0.0512749647678976,0.0469971417990442);
#2722=ELLIPSE('',#35554,0.0512707788570414,0.0469842741348829);
#2723=ELLIPSE('',#35555,0.0512749647696248,0.0469971417999634);
#2724=ELLIPSE('',#35558,0.0512707789395351,0.0469842741799766);
#2725=ELLIPSE('',#35559,0.0512749647687745,0.0469971417995203);
#2726=ELLIPSE('',#35562,0.0512707788562593,0.0469842741344864);
#2727=ELLIPSE('',#35563,0.0512749647684955,0.046997141799316);
#2728=ELLIPSE('',#35566,0.0512707788603725,0.0469842741367327);
#2729=ELLIPSE('',#35567,0.0512749647690289,0.0469971417996681);
#2730=ELLIPSE('',#35570,0.0512707788577797,0.0469842741353011);
#2731=ELLIPSE('',#35571,0.0512749647683414,0.0469971417992803);
#2732=ELLIPSE('',#35574,0.051270778856875,0.0469842741348193);
#2733=ELLIPSE('',#35575,0.0512749647684586,0.0469971417993373);
#2734=ELLIPSE('',#35578,0.051270778920832,0.0469842741697548);
#2735=ELLIPSE('',#35579,0.0512749647689089,0.0469971417995588);
#2736=ELLIPSE('',#35582,0.0512707788568015,0.0469842741347871);
#2737=ELLIPSE('',#35583,0.0512749647679381,0.0469971417990666);
#2738=ELLIPSE('',#35586,0.0512707788566487,0.046984274134668);
#2739=ELLIPSE('',#35587,0.0512749647684683,0.0469971417993365);
#2740=ELLIPSE('',#35590,0.051270778856618,0.0469842741346731);
#2741=ELLIPSE('',#35591,0.0512749647693393,0.0469971417998184);
#2742=ELLIPSE('',#35594,0.0512707788568358,0.0469842741348282);
#2743=ELLIPSE('',#35595,0.0512749647674564,0.0469971417987839);
#2744=ELLIPSE('',#35598,0.0512707788557633,0.0469842741342339);
#2745=ELLIPSE('',#35599,0.0512749647690638,0.0469971417996539);
#2746=ELLIPSE('',#35602,0.0512707788566786,0.0469842741346996);
#2747=ELLIPSE('',#35603,0.0512749647672967,0.0469971417987006);
#2748=ELLIPSE('',#35606,0.0512707788621377,0.0469842741376985);
#2749=ELLIPSE('',#35607,0.0512749647686591,0.046997141799446);
#2750=ELLIPSE('',#35610,0.0512707788564809,0.0469842741346051);
#2751=ELLIPSE('',#35611,0.0512749647682497,0.0469971417992212);
#2752=ELLIPSE('',#35614,0.0512707788573564,0.0469842741350646);
#2753=ELLIPSE('',#35615,0.0512749647687658,0.0469971417994997);
#2754=ELLIPSE('',#35618,0.051270778874813,0.0469842741446368);
#2755=ELLIPSE('',#35619,0.0512749647675386,0.046997141798832);
#2756=ELLIPSE('',#35622,0.0512707788565269,0.0469842741346491);
#2757=ELLIPSE('',#35623,0.0512749647691996,0.0469971417997275);
#2758=ELLIPSE('',#35626,0.0512707788580797,0.0469842741354721);
#2759=ELLIPSE('',#35627,0.0512749647681002,0.0469971417991393);
#2760=ELLIPSE('',#35630,0.0512707788579047,0.0469842741354009);
#2761=ELLIPSE('',#35631,0.0512749647678865,0.0469971417990283);
#2762=ELLIPSE('',#35634,0.0512707788574115,0.046984274135125);
#2763=ELLIPSE('',#35635,0.0512749647671369,0.0469971417986091);
#2764=ELLIPSE('',#35638,0.0512749647690318,0.0469971417996552);
#2765=ELLIPSE('',#35640,0.0512707788566348,0.0469842741346708);
#2766=ELLIPSE('',#35642,0.0512749647679538,0.0469971417990534);
#2767=ELLIPSE('',#35644,0.0512707788562212,0.0469842741344524);
#2768=ELLIPSE('',#35646,0.051274964768521,0.0469971417993772);
#2769=ELLIPSE('',#35648,0.051270778856042,0.0469842741343731);
#2770=ELLIPSE('',#35650,0.0512749647675581,0.0469971417988677);
#2771=ELLIPSE('',#35652,0.0512707788559885,0.0469842741343514);
#2772=ELLIPSE('',#35654,0.0512749647693218,0.0469971417997968);
#2773=ELLIPSE('',#35656,0.0512707788571387,0.0469842741349643);
#2774=ELLIPSE('',#35658,0.0512749647679417,0.0469971417990759);
#2775=ELLIPSE('',#35660,0.0512707788922353,0.0469842741541131);
#2776=ELLIPSE('',#35662,0.051274964769059,0.046997141799664);
#2777=ELLIPSE('',#35664,0.0512707788612464,0.0469842741372165);
#2778=ELLIPSE('',#35666,0.0512749647686166,0.0469971417994078);
#2779=ELLIPSE('',#35668,0.0512707788558472,0.0469842741342397);
#2780=ELLIPSE('',#35670,0.0512749647686363,0.0469971417994427);
#2781=ELLIPSE('',#35672,0.0512707788567449,0.0469842741347651);
#2782=ELLIPSE('',#35674,0.0512749647684367,0.0469971417993216);
#2783=ELLIPSE('',#35676,0.0512707788561666,0.0469842741344253);
#2784=ELLIPSE('',#35678,0.0512749647683517,0.046997141799283);
#2785=ELLIPSE('',#35680,0.0512707788648064,0.0469842741391505);
#2786=ELLIPSE('',#35682,0.0512749647688174,0.0469971417995523);
#2787=ELLIPSE('',#35684,0.051270778857567,0.0469842741352074);
#2788=ELLIPSE('',#35686,0.0512749647694904,0.0469971417998601);
#2789=ELLIPSE('',#35688,0.0512707788575527,0.0469842741351904);
#2790=ELLIPSE('',#35690,0.0512749647677225,0.0469971417989513);
#2791=ELLIPSE('',#35692,0.0512707788585909,0.0469842741357571);
#2792=ELLIPSE('',#35694,0.051270778940575,0.0469842741805314);
#2793=ELLIPSE('',#35695,0.0512749647683344,0.0469971417992899);
#2794=ELLIPSE('',#35856,0.0512707788678624,0.04698427414088);
#2795=ELLIPSE('',#35857,0.0512749647679163,0.0469971417991227);
#2796=ELLIPSE('',#35859,0.0512749647654335,0.0469971417977818);
#2797=ELLIPSE('',#35860,0.0512707788568347,0.0469842741348514);
#2798=ELLIPSE('',#35862,0.0512749647672852,0.0469971417988039);
#2799=ELLIPSE('',#35863,0.0512707788564686,0.0469842741346539);
#2800=ELLIPSE('',#35865,0.0512749647659393,0.0469971417980464);
#2801=ELLIPSE('',#35866,0.0512707788556944,0.0469842741342504);
#2802=ELLIPSE('',#35868,0.0512749647686629,0.0469971417995544);
#2803=ELLIPSE('',#35869,0.0512707788564297,0.0469842741346479);
#2804=ELLIPSE('',#35871,0.0512749647671486,0.0469971417987065);
#2805=ELLIPSE('',#35872,0.0512707788597197,0.0469842741364453);
#2806=ELLIPSE('',#35874,0.0512749647666077,0.0469971417984174);
#2807=ELLIPSE('',#35875,0.0512707788555701,0.0469842741341628);
#2808=ELLIPSE('',#35877,0.0512749647679515,0.0469971417991682);
#2809=ELLIPSE('',#35878,0.0512707788587403,0.0469842741359266);
#2810=ELLIPSE('',#35880,0.0512749647675462,0.0469971417988912);
#2811=ELLIPSE('',#35881,0.0512707788561996,0.0469842741345216);
#2812=ELLIPSE('',#35883,0.0512749647665171,0.0469971417983294);
#2813=ELLIPSE('',#35884,0.0512707788563593,0.0469842741346364);
#2814=ELLIPSE('',#35886,0.0512749647671419,0.0469971417986936);
#2815=ELLIPSE('',#35887,0.0512707788554834,0.0469842741341348);
#2816=ELLIPSE('',#35889,0.0512749647679126,0.0469971417991247);
#2817=ELLIPSE('',#35890,0.0512707788566136,0.0469842741347507);
#2818=ELLIPSE('',#35892,0.051274964765861,0.0469971417980122);
#2819=ELLIPSE('',#35893,0.0512707788569887,0.0469842741349521);
#2820=ELLIPSE('',#35895,0.0512749647673257,0.046997141798794);
#2821=ELLIPSE('',#35896,0.0512707788578384,0.0469842741354011);
#2822=ELLIPSE('',#35898,0.0512749647685051,0.046997141799409);
#2823=ELLIPSE('',#35899,0.0512707788566497,0.0469842741347448);
#2824=ELLIPSE('',#35901,0.0512749647664023,0.0469971417983194);
#2825=ELLIPSE('',#35902,0.0512707788557973,0.0469842741343033);
#2826=ELLIPSE('',#35904,0.0512749647657081,0.0469971417979273);
#2827=ELLIPSE('',#35905,0.0512707788560454,0.0469842741344356);
#2828=ELLIPSE('',#35907,0.0512749647672847,0.0469971417988018);
#2829=ELLIPSE('',#35908,0.0512707788908472,0.0469842741534398);
#2830=ELLIPSE('',#35910,0.0512749647656979,0.0469971417979225);
#2831=ELLIPSE('',#35911,0.0512707788619598,0.0469842741376821);
#2832=ELLIPSE('',#35913,0.0512749647673844,0.0469971417987892);
#2833=ELLIPSE('',#35914,0.0512707788554361,0.0469842741341347);
#2834=ELLIPSE('',#35916,0.0512749647665351,0.0469971417983737);
#2835=ELLIPSE('',#35917,0.051270778857401,0.0469842741351899);
#2836=ELLIPSE('',#35919,0.0512749647648224,0.0469971417974593);
#2837=ELLIPSE('',#35920,0.051270778857135,0.0469842741350546);
#2838=ELLIPSE('',#35922,0.051274964767923,0.046997141799147);
#2839=ELLIPSE('',#35923,0.0512707788632245,0.0469842741383353);
#2840=ELLIPSE('',#35925,0.0512749647670837,0.0469971417986601);
#2841=ELLIPSE('',#35926,0.0512707788575274,0.0469842741352789);
#2842=ELLIPSE('',#35928,0.0512749647661063,0.046997141798163);
#2843=ELLIPSE('',#35929,0.0512707788614728,0.0469842741374068);
#2844=ELLIPSE('',#35931,0.0512749647661745,0.0469971417981727);
#2845=ELLIPSE('',#35932,0.0512707788561374,0.0469842741344828);
#2846=ELLIPSE('',#35934,0.0512749647684627,0.0469971417993818);
#2847=ELLIPSE('',#35935,0.0512707788547222,0.0469842741337518);
#2848=ELLIPSE('',#35937,0.0512749647675423,0.0469971417989238);
#2849=ELLIPSE('',#35938,0.0512707788556497,0.0469842741342235);
#2850=ELLIPSE('',#35940,0.0512749647674664,0.0469971417988657);
#2851=ELLIPSE('',#35941,0.0512707788563694,0.0469842741346094);
#2852=ELLIPSE('',#35943,0.0512749647689012,0.0469971417996608);
#2853=ELLIPSE('',#35944,0.0512707788554915,0.0469842741341037);
#2854=ELLIPSE('',#35946,0.0512749647674053,0.0469971417988339);
#2855=ELLIPSE('',#35947,0.0512707788551391,0.0469842741339346);
#2856=ELLIPSE('',#35949,0.051274964767584,0.046997141798928);
#2857=ELLIPSE('',#35950,0.0512707788578603,0.0469842741354062);
#2858=ELLIPSE('',#35952,0.0512749647667973,0.046997141798492);
#2859=ELLIPSE('',#35953,0.0512707788554342,0.0469842741340614);
#2860=ELLIPSE('',#35955,0.0512749647663277,0.0469971417982546);
#2861=ELLIPSE('',#35956,0.051270778856014,0.0469842741344105);
#2862=ELLIPSE('',#35958,0.0512749647644558,0.0469971417972658);
#2863=ELLIPSE('',#35959,0.051270778856549,0.046984274134693);
#2864=ELLIPSE('',#35961,0.0512749647655728,0.0469971417978321);
#2865=ELLIPSE('',#35962,0.0512707788565064,0.0469842741346634);
#2866=ELLIPSE('',#35964,0.0512749647677657,0.0469971417990299);
#2867=ELLIPSE('',#35965,0.0512707788566898,0.0469842741347819);
#2868=ELLIPSE('',#35967,0.0512749647676116,0.0469971417989766);
#2869=ELLIPSE('',#35968,0.0512707788912617,0.0469842741536714);
#2870=ELLIPSE('',#35970,0.0512749647664018,0.0469971417982991);
#2871=ELLIPSE('',#35971,0.0512707788616718,0.0469842741375278);
#2872=ELLIPSE('',#35973,0.0512749647667201,0.046997141798501);
#2873=ELLIPSE('',#35974,0.0512707788559321,0.046984274134359);
#2874=ELLIPSE('',#35976,0.0512749647688712,0.0469971417996063);
#2875=ELLIPSE('',#35977,0.0512707788570311,0.0469842741349509);
#2876=ELLIPSE('',#35979,0.0512749647675863,0.0469971417989162);
#2877=ELLIPSE('',#35980,0.0512707788563448,0.0469842741345939);
#2878=ELLIPSE('',#35982,0.0512749647671262,0.0469971417987068);
#2879=ELLIPSE('',#35983,0.0512707788650867,0.0469842741393638);
#2880=ELLIPSE('',#35985,0.0512749647686962,0.0469971417995509);
#2881=ELLIPSE('',#35986,0.0512707788567886,0.0469842741348241);
#2882=ELLIPSE('',#35988,0.0512749647672976,0.0469971417987731);
#2883=ELLIPSE('',#35989,0.0512707788570162,0.0469842741349496);
#2884=ELLIPSE('',#35991,0.0512749647667697,0.0469971417984931);
#2885=ELLIPSE('',#35992,0.0512707788584097,0.0469842741357168);
#2886=ELLIPSE('',#35994,0.0512749647672832,0.0469971417987584);
#2887=ELLIPSE('',#35995,0.0512707788570115,0.0469842741349691);
#2888=ELLIPSE('',#35997,0.0512749647672073,0.0469971417987249);
#2889=ELLIPSE('',#35998,0.0512707789405328,0.0469842741805533);
#2890=ELLIPSE('',#36000,0.0512749647662809,0.0469971417982346);
#2891=ELLIPSE('',#36001,0.0512707788564733,0.0469842741346687);
#2892=ELLIPSE('',#36003,0.0512749647659994,0.0469971417980507);
#2893=ELLIPSE('',#36004,0.0512707788571204,0.0469842741349872);
#2894=ELLIPSE('',#36006,0.0512749647671319,0.0469971417987083);
#2895=ELLIPSE('',#36007,0.0512707788566097,0.0469842741347329);
#2896=ELLIPSE('',#36009,0.0512749647668497,0.0469971417985515);
#2897=ELLIPSE('',#36010,0.0512707788560048,0.0469842741344256);
#2898=ELLIPSE('',#36012,0.051274964765999,0.0469971417980718);
#2899=ELLIPSE('',#36013,0.0512707788746663,0.0469842741446355);
#2900=ELLIPSE('',#36015,0.0512749647672519,0.0469971417987563);
#2901=ELLIPSE('',#36016,0.051270778855846,0.0469842741343271);
#2902=ELLIPSE('',#36018,0.0512749647662359,0.0469971417982146);
#2903=ELLIPSE('',#36019,0.0512707788574978,0.0469842741352291);
#2904=ELLIPSE('',#36021,0.0512749647668179,0.0469971417985263);
#2905=ELLIPSE('',#36022,0.0512707788607044,0.0469842741369976);
#2906=ELLIPSE('',#36024,0.0512749647674441,0.0469971417988379);
#2907=ELLIPSE('',#36025,0.0512707788568965,0.0469842741348871);
#2908=ELLIPSE('',#36027,0.0512749647672645,0.0469971417987703);
#2909=ELLIPSE('',#36028,0.0512707788559945,0.0469842741344026);
#2910=ELLIPSE('',#36030,0.0512749647680151,0.0469971417991764);
#2911=ELLIPSE('',#36031,0.0512707788560419,0.04698427413443);
#2912=ELLIPSE('',#36033,0.0512749647667931,0.0469971417984966);
#2913=ELLIPSE('',#36034,0.0512707788563537,0.0469842741346079);
#2914=ELLIPSE('',#36036,0.0512749647674696,0.0469971417988977);
#2915=ELLIPSE('',#36037,0.0512707788571896,0.0469842741350665);
#2916=ELLIPSE('',#36039,0.0512749647673948,0.046997141798837);
#2917=ELLIPSE('',#36040,0.0512707788555549,0.0469842741341569);
#2918=ELLIPSE('',#36042,0.0512749647668783,0.0469971417985539);
#2919=ELLIPSE('',#36043,0.0512707789210852,0.0469842741699459);
#2920=ELLIPSE('',#36045,0.0512749647677305,0.0469971417990099);
#2921=ELLIPSE('',#36046,0.0512707788552415,0.0469842741340032);
#2922=ELLIPSE('',#36048,0.0512707788564181,0.0469842741346374);
#2923=ELLIPSE('',#36049,0.0512749647669761,0.0469971417985938);
#2924=ELLIPSE('',#36051,0.051270778856969,0.0469842741349151);
#2925=ELLIPSE('',#36052,0.0512749647670935,0.046997141798684);
#2926=ELLIPSE('',#36054,0.0512707788562384,0.0469842741345515);
#2927=ELLIPSE('',#36055,0.0512749647675247,0.0469971417988957);
#2928=ELLIPSE('',#36057,0.0512707788573216,0.0469842741351317);
#2929=ELLIPSE('',#36058,0.0512749647668487,0.046997141798569);
#2930=ELLIPSE('',#36060,0.0512707788622439,0.0469842741378278);
#2931=ELLIPSE('',#36061,0.0512749647677751,0.0469971417990674);
#2932=ELLIPSE('',#36063,0.0512707788576837,0.046984274135325);
#2933=ELLIPSE('',#36064,0.0512749647668911,0.0469971417985504);
#2934=ELLIPSE('',#36066,0.0512707788569353,0.0469842741349273);
#2935=ELLIPSE('',#36067,0.0512749647675315,0.0469971417989158);
#2936=ELLIPSE('',#36069,0.0512707788759282,0.0469842741452617);
#2937=ELLIPSE('',#36070,0.0512749647661136,0.0469971417981488);
#2938=ELLIPSE('',#36072,0.0512707788557471,0.0469842741342912);
#2939=ELLIPSE('',#36073,0.051274964767063,0.0469971417986624);
#2940=ELLIPSE('',#36075,0.0512707788562218,0.0469842741345251);
#2941=ELLIPSE('',#36076,0.0512749647674796,0.0469971417988927);
#2942=ELLIPSE('',#36078,0.0512707788562634,0.0469842741345331);
#2943=ELLIPSE('',#36079,0.0512749647672643,0.0469971417987429);
#2944=ELLIPSE('',#36081,0.0512707788550995,0.0469842741339394);
#2945=ELLIPSE('',#36082,0.0512749647667936,0.0469971417984887);
#2946=ELLIPSE('',#36084,0.0512707789393949,0.0469842741799506);
#2947=ELLIPSE('',#36085,0.0512749647666032,0.0469971417983921);
#2948=ELLIPSE('',#36087,0.0512707788579345,0.0469842741354427);
#2949=ELLIPSE('',#36088,0.0512749647659267,0.0469971417980537);
#2950=ELLIPSE('',#36090,0.0512749647694732,0.0469971417999488);
#2951=ELLIPSE('',#36091,0.0512707788565522,0.0469842741347113);
#2952=ELLIPSE('',#36095,0.0512707788554107,0.0469842741340208);
#2953=ELLIPSE('',#36096,0.0512749647674929,0.0469971417988238);
#2954=ELLIPSE('',#36101,0.0512749647664458,0.0469971417983288);
#2955=ELLIPSE('',#36102,0.0512707788586759,0.0469842741358754);
#2968=CONICAL_SURFACE('',#34988,1.17524047358084,0.785398163397443);
#2969=CONICAL_SURFACE('',#35023,1.17524047358084,0.785398163397443);
#2970=CONICAL_SURFACE('',#35072,1.55162884844711,0.78539816339745);
#2971=CONICAL_SURFACE('',#35078,2.73627063036812,0.785398163397448);
#2972=CONICAL_SURFACE('',#35223,2.68872936963188,0.785398163397435);
#2973=CONICAL_SURFACE('',#36111,1732.05080756885,1.04719755119659);
#3226=B_SPLINE_CURVE_WITH_KNOTS('',3,(#65626,#65627,#65628,#65629,#65630,
#65631,#65632,#65633,#65634,#65635,#65636,#65637,#65638,#65639,#65640,#65641,
#65642,#65643,#65644,#65645,#65646,#65647,#65648,#65649,#65650,#65651,#65652,
#65653,#65654,#65655,#65656,#65657,#65658,#65659,#65660,#65661),
 .UNSPECIFIED.,.F.,.F.,(4,2,2,2,2,2,2,2,2,2,2,2,2,2,2,2,2,4),(-0.945073641183675,
-0.895238035194944,-0.83625541046657,-0.779319325111488,-0.719695813140934,
-0.661359932358853,-0.603989382535731,-0.544046656752618,-0.486380595229568,
-0.427463950957105,-0.368285170516134,-0.311258814957492,-0.251615042406746,
-0.193080680180277,-0.135881569867343,-0.0757214675349668,-0.0372079607299379,
-9.99999995143774E-7),.UNSPECIFIED.);
#3227=B_SPLINE_CURVE_WITH_KNOTS('',3,(#65667,#65668,#65669,#65670,#65671,
#65672,#65673,#65674,#65675,#65676,#65677,#65678,#65679,#65680,#65681,#65682,
#65683,#65684,#65685,#65686,#65687,#65688,#65689,#65690,#65691,#65692,#65693,
#65694,#65695,#65696,#65697,#65698,#65699,#65700),.UNSPECIFIED.,.F.,.F.,
(4,2,2,2,2,2,2,2,2,2,2,2,2,2,2,2,4),(-27.258759550315,-27.2281298462553,
-27.1982051538512,-27.1403355656588,-27.0801605899845,-27.0231066733285,
-26.9645639497272,-26.9050010855415,-26.8479917157334,-26.7888070303952,
-26.7302213719406,-26.6725610910419,-26.6126177738291,-26.5554428144319,
-26.4971129260297,-26.4375855046171,-26.4315188069733),.UNSPECIFIED.);
#3228=B_SPLINE_CURVE_WITH_KNOTS('',3,(#65705,#65706,#65707,#65708,#65709,
#65710,#65711,#65712,#65713,#65714,#65715,#65716,#65717,#65718,#65719,#65720,
#65721,#65722,#65723,#65724,#65725,#65726,#65727,#65728,#65729,#65730,#65731,
#65732,#65733,#65734,#65735,#65736,#65737,#65738,#65739,#65740),
 .UNSPECIFIED.,.F.,.F.,(4,2,2,2,2,2,2,2,2,2,2,2,2,2,2,2,2,4),(-1.89025095676006,
-1.83161362612537,-1.77291723413503,-1.71588088128378,-1.65621305093223,
-1.59816806724067,-1.54019307596245,-1.48057902624682,-1.42320721251111,
-1.36315245228605,-1.30433237640506,-1.24738924893859,-1.18775702178512,
-1.12958586526634,-1.07195013380193,-1.0121910944455,-0.954689933605391,
-0.945073641183675),.UNSPECIFIED.);
#3229=B_SPLINE_CURVE_WITH_KNOTS('',3,(#65741,#65742,#65743,#65744,#65745,
#65746,#65747,#65748,#65749,#65750,#65751,#65752,#65753,#65754,#65755,#65756,
#65757,#65758,#65759,#65760,#65761,#65762,#65763,#65764,#65765,#65766,#65767,
#65768,#65769,#65770,#65771,#65772,#65773,#65774,#65775,#65776),
 .UNSPECIFIED.,.F.,.F.,(4,2,2,2,2,2,2,2,2,2,2,2,2,2,2,2,2,4),(-26.4315188069733,
-26.3807149169946,-26.3217404209326,-26.2626652889544,-26.2051855221022,
-26.1454428390691,-26.08804784233,-26.0298996832198,-25.970377539516,-25.9135472636022,
-25.8547523829465,-25.7951046336945,-25.7377721236726,-25.6781939173096,
-25.6204935481626,-25.5624909627037,-25.5029463840743,-25.4881909358829),
 .UNSPECIFIED.);
#3230=B_SPLINE_CURVE_WITH_KNOTS('',3,(#65781,#65782,#65783,#65784,#65785,
#65786,#65787,#65788,#65789,#65790,#65791,#65792,#65793,#65794,#65795,#65796,
#65797,#65798,#65799,#65800,#65801,#65802,#65803,#65804,#65805,#65806,#65807,
#65808,#65809,#65810,#65811,#65812,#65813,#65814,#65815,#65816,#65817,#65818),
 .UNSPECIFIED.,.F.,.F.,(4,2,2,2,2,2,2,2,2,2,2,2,2,2,2,2,2,2,4),(-2.83625896355377,
-2.82853093222041,-2.76886611006394,-2.71046756100465,-2.65308502383756,
-2.59307616772703,-2.5353480705631,-2.47645222776391,-2.41720668492958,
-2.36012338869581,-2.30043449435393,-2.24183347940531,-2.1846099393252,
-2.12437972037366,-2.06645193254166,-2.00798057621261,-1.94850769470731,
-1.89126109663031,-1.89025095676006),.UNSPECIFIED.);
#3231=B_SPLINE_CURVE_WITH_KNOTS('',3,(#65819,#65820,#65821,#65822,#65823,
#65824,#65825,#65826,#65827,#65828,#65829,#65830,#65831,#65832,#65833,#65834,
#65835,#65836,#65837,#65838,#65839,#65840,#65841,#65842,#65843,#65844,#65845,
#65846,#65847,#65848,#65849,#65850,#65851,#65852,#65853,#65854),
 .UNSPECIFIED.,.F.,.F.,(4,2,2,2,2,2,2,2,2,2,2,2,2,2,2,2,2,4),(-25.4881909358829,
-25.4460636732589,-25.3874120918811,-25.3278816537184,-25.2706841301686,
-25.2112575632321,-25.1531186176646,-25.0952452143788,-25.0350644348795,
-24.9780430196917,-24.9194961959997,-24.8599520194551,-24.8029424006809,
-24.7437542679059,-24.6852489172368,-24.6275880933991,-24.5676424609794,
-24.544394043377),.UNSPECIFIED.);
#3232=B_SPLINE_CURVE_WITH_KNOTS('',3,(#65859,#65860,#65861,#65862,#65863,
#65864,#65865,#65866,#65867,#65868,#65869,#65870,#65871,#65872,#65873,#65874,
#65875,#65876,#65877,#65878,#65879,#65880,#65881,#65882,#65883,#65884,#65885,
#65886,#65887,#65888,#65889,#65890,#65891,#65892,#65893,#65894),
 .UNSPECIFIED.,.F.,.F.,(4,2,2,2,2,2,2,2,2,2,2,2,2,2,2,2,2,4),(-3.78192035948685,
-3.76562796298537,-3.70592564973338,-3.6478278361799,-3.5898592957152,-3.53018901929876,
-3.47276427223133,-3.41274694188657,-3.3538687217505,-3.29689298752725,
-3.2372230084892,-3.17899386626536,-3.12135698149028,-3.06153650613278,
-3.00397762776562,-2.94455692608413,-2.88551146939021,-2.83625896355377),
 .UNSPECIFIED.);
#3233=B_SPLINE_CURVE_WITH_KNOTS('',3,(#65895,#65896,#65897,#65898,#65899,
#65900,#65901,#65902,#65903,#65904,#65905,#65906,#65907,#65908,#65909,#65910,
#65911,#65912,#65913,#65914,#65915,#65916,#65917,#65918,#65919,#65920,#65921,
#65922,#65923,#65924,#65925,#65926,#65927,#65928,#65929,#65930),
 .UNSPECIFIED.,.F.,.F.,(4,2,2,2,2,2,2,2,2,2,2,2,2,2,2,2,2,4),(-24.544394043377,
-24.5105131978097,-24.4521827141638,-24.3926780124691,-24.3358195936076,
-24.2768451471733,-24.2178632708879,-24.1603868788961,-24.1006461200198,
-24.0433090290329,-23.9851645307063,-23.9256688814307,-23.8688632830925,
-23.8100726156683,-23.7505272749807,-23.6932025949219,-23.6336311604901,
-23.6014349735858),.UNSPECIFIED.);
#3234=B_SPLINE_CURVE_WITH_KNOTS('',3,(#65935,#65936,#65937,#65938,#65939,
#65940,#65941,#65942,#65943,#65944,#65945,#65946,#65947,#65948,#65949,#65950,
#65951,#65952,#65953,#65954,#65955,#65956,#65957,#65958,#65959,#65960,#65961,
#65962,#65963,#65964,#65965,#65966,#65967,#65968,#65969,#65970),
 .UNSPECIFIED.,.F.,.F.,(4,2,2,2,2,2,2,2,2,2,2,2,2,2,2,2,2,4),(-4.72839430207058,
-4.70337431740566,-4.64331595464347,-4.58554178921411,-4.52667966073054,
-4.4673838894256,-4.41025831032806,-4.35054027250619,-4.29188896156004,
-4.23465469260147,-4.17437122548907,-4.11639389057874,-4.05794278357937,
-3.99841660337735,-3.94111979450562,-3.88143640467257,-3.82268708479341,
-3.78192035948685),.UNSPECIFIED.);
#3235=B_SPLINE_CURVE_WITH_KNOTS('',3,(#65971,#65972,#65973,#65974,#65975,
#65976,#65977,#65978,#65979,#65980,#65981,#65982,#65983,#65984,#65985,#65986,
#65987,#65988,#65989,#65990,#65991,#65992,#65993,#65994,#65995,#65996,#65997,
#65998,#65999,#66000,#66001,#66002,#66003,#66004,#66005,#66006),
 .UNSPECIFIED.,.F.,.F.,(4,2,2,2,2,2,2,2,2,2,2,2,2,2,2,2,2,4),(-23.6014349735858,
-23.5759985868542,-23.5180045036599,-23.458489879113,-23.4016430359386,
-23.3430005479742,-23.2834982736845,-23.226310920464,-23.166893628097,-23.1088378874003,
-23.0509758826866,-22.9908049952875,-22.9338319947597,-22.8752964277514,
-22.8157879004539,-22.7587920199088,-22.6996160282244,-22.6581171675807),
 .UNSPECIFIED.);
#3236=B_SPLINE_CURVE_WITH_KNOTS('',3,(#66011,#66012,#66013,#66014,#66015,
#66016,#66017,#66018,#66019,#66020,#66021,#66022,#66023,#66024,#66025,#66026,
#66027,#66028,#66029,#66030,#66031,#66032,#66033,#66034,#66035,#66036,#66037,
#66038,#66039,#66040,#66041,#66042,#66043,#66044,#66045,#66046),
 .UNSPECIFIED.,.F.,.F.,(4,2,2,2,2,2,2,2,2,2,2,2,2,2,2,2,2,4),(-5.67439159596968,
-5.64047766140835,-5.58076721688331,-5.52330498546526,-5.4633387313466,
-5.40441833910885,-5.34742402529794,-5.28773207490788,-5.22946075409439,
-5.17183622553644,-5.11197061930769,-5.05436969869878,-4.99499338073396,
-4.9359013779351,-4.878890651626,-4.8192004273671,-4.76075532631967,-4.72839430207058),
 .UNSPECIFIED.);
#3237=B_SPLINE_CURVE_WITH_KNOTS('',3,(#66047,#66048,#66049,#66050,#66051,
#66052,#66053,#66054,#66055,#66056,#66057,#66058,#66059,#66060,#66061,#66062,
#66063,#66064,#66065,#66066,#66067,#66068,#66069,#66070,#66071,#66072,#66073,
#66074,#66075,#66076,#66077,#66078,#66079,#66080,#66081,#66082),
 .UNSPECIFIED.,.F.,.F.,(4,2,2,2,2,2,2,2,2,2,2,2,2,2,2,2,2,4),(-22.6581171675807,
-22.6412102410835,-22.5835641689142,-22.5236319902899,-22.4665652482388,
-22.4082496043878,-22.3487848861067,-22.2919531828174,-22.2329943725634,
-22.1741263229248,-22.1166686457465,-22.0569456248039,-21.9996842855768,
-21.9415589369491,-21.8821072544915,-21.8253417468782,-21.7665709936596,
-21.7157628302399),.UNSPECIFIED.);
#3238=B_SPLINE_CURVE_WITH_KNOTS('',3,(#66087,#66088,#66089,#66090,#66091,
#66092,#66093,#66094,#66095,#66096,#66097,#66098,#66099,#66100,#66101,#66102,
#66103,#66104,#66105,#66106,#66107,#66108,#66109,#66110,#66111,#66112,#66113,
#66114,#66115,#66116,#66117,#66118,#66119,#66120,#66121,#66122),
 .UNSPECIFIED.,.F.,.F.,(4,2,2,2,2,2,2,2,2,2,2,2,2,2,2,2,2,4),(-6.62109380521341,
-6.57761768259959,-6.51828740763027,-6.46113362202641,-6.40140207096381,
-6.34271600715298,-6.28548482095171,-6.22516410228413,-6.16715260360109,
-6.10873547077658,-6.04917186097877,-5.99184011673613,-5.93213648107799,
-5.8733499659965,-5.81628212661826,-5.75656105013342,-5.69842598086126,
-5.67439159596968),.UNSPECIFIED.);
#3239=B_SPLINE_CURVE_WITH_KNOTS('',3,(#66123,#66124,#66125,#66126,#66127,
#66128,#66129,#66130,#66131,#66132,#66133,#66134,#66135,#66136,#66137,#66138,
#66139,#66140,#66141,#66142,#66143,#66144,#66145,#66146,#66147,#66148,#66149,
#66150,#66151,#66152,#66153,#66154,#66155,#66156,#66157,#66158),
 .UNSPECIFIED.,.F.,.F.,(4,2,2,2,2,2,2,2,2,2,2,2,2,2,2,2,2,4),(-21.7157628302399,
-21.7071499734112,-21.6498486291818,-21.5902999589255,-21.5327541629797,
-21.4747842600729,-21.4153173211779,-21.3585227590009,-21.2999052492263,
-21.2398720875173,-21.1826905454483,-21.1232764692568,-21.065378520901,
-21.0075245508875,-20.9480158554619,-20.8911101904613,-20.8326059984683,
-20.7731793950157),.UNSPECIFIED.);
#3240=B_SPLINE_CURVE_WITH_KNOTS('',3,(#66163,#66164,#66165,#66166,#66167,
#66168,#66169,#66170,#66171,#66172,#66173,#66174,#66175,#66176,#66177,#66178,
#66179,#66180,#66181,#66182,#66183,#66184,#66185,#66186,#66187,#66188,#66189,
#66190,#66191,#66192,#66193,#66194,#66195,#66196,#66197,#66198),
 .UNSPECIFIED.,.F.,.F.,(4,2,2,2,2,2,2,2,2,2,2,2,2,2,2,2,2,4),(-7.56721318319246,
-7.51440195941646,-7.4554548070908,-7.39845589958658,-7.33875763160917,
-7.28045937419718,-7.22286133868259,-7.16296628560166,-7.10533842940707,
-7.04602095897405,-6.9868979771895,-6.92987099130527,-6.87017100691209,
-6.81169474396116,-6.75432913502786,-6.69423710481114,-6.63643211656935,
-6.62109380521341),.UNSPECIFIED.);
#3241=B_SPLINE_CURVE_WITH_KNOTS('',3,(#66199,#66200,#66201,#66202,#66203,
#66204,#66205,#66206,#66207,#66208,#66209,#66210,#66211,#66212,#66213,#66214,
#66215,#66216,#66217,#66218,#66219,#66220,#66221,#66222,#66223,#66224,#66225,
#66226,#66227,#66228,#66229,#66230,#66231,#66232,#66233,#66234,#66235,#66236),
 .UNSPECIFIED.,.F.,.F.,(4,2,2,2,2,2,2,2,2,2,2,2,2,2,2,2,2,2,4),(-20.7731793950157,
-20.7731201315055,-20.7160582025871,-20.6567792566783,-20.5983599289237,
-20.5406164839802,-20.4805811221967,-20.4234656784966,-20.3650514109911,
-20.305511597516,-20.2485949896086,-20.1895371334662,-20.1306696919239,
-20.0731189832228,-20.0132974755221,-19.9560008596223,-19.8977815738613,
-19.8382589546996,-19.8295444030046),.UNSPECIFIED.);
#3242=B_SPLINE_CURVE_WITH_KNOTS('',3,(#66241,#66242,#66243,#66244,#66245,
#66246,#66247,#66248,#66249,#66250,#66251,#66252,#66253,#66254,#66255,#66256,
#66257,#66258,#66259,#66260,#66261,#66262,#66263,#66264,#66265,#66266,#66267,
#66268,#66269,#66270,#66271,#66272,#66273,#66274,#66275,#66276,#66277,#66278),
 .UNSPECIFIED.,.F.,.F.,(4,2,2,2,2,2,2,2,2,2,2,2,2,2,2,2,2,2,4),(-8.51391269073544,
-8.51222365838152,-8.45249428513948,-8.39378861667143,-8.33657472393003,
-8.27623231073072,-8.21820164401039,-8.1598332741766,-8.10024765479814,
-8.04289584139225,-7.98318755401621,-7.92437912604881,-7.86731677437594,
-7.80759259896721,-7.74943539170332,-7.6915218402897,-7.631786775557,-7.57430204194946,
-7.56721318319246),.UNSPECIFIED.);
#3243=B_SPLINE_CURVE_WITH_KNOTS('',3,(#66279,#66280,#66281,#66282,#66283,
#66284,#66285,#66286,#66287,#66288,#66289,#66290,#66291,#66292,#66293,#66294,
#66295,#66296,#66297,#66298,#66299,#66300,#66301,#66302,#66303,#66304,#66305,
#66306,#66307,#66308,#66309,#66310,#66311,#66312,#66313,#66314),
 .UNSPECIFIED.,.F.,.F.,(4,2,2,2,2,2,2,2,2,2,2,2,2,2,2,2,2,4),(-19.8295444030046,
-19.781422440649,-19.7225572817117,-19.6631471763022,-19.6057577545878,
-19.5461159927651,-19.4885461013889,-19.4304876297435,-19.3709535721035,
-19.3141007093386,-19.2553941827952,-19.1953773792029,-19.1381132548424,
-19.0786120692882,-19.0206974716804,-18.9627608300149,-18.9031885891784,
-18.8860416189937),.UNSPECIFIED.);
#3244=B_SPLINE_CURVE_WITH_KNOTS('',3,(#66319,#66320,#66321,#66322,#66323,
#66324,#66325,#66326,#66327,#66328,#66329,#66330,#66331,#66332,#66333,#66334,
#66335,#66336,#66337,#66338,#66339,#66340,#66341,#66342,#66343,#66344,#66345,
#66346,#66347,#66348,#66349,#66350,#66351,#66352,#66353,#66354),
 .UNSPECIFIED.,.F.,.F.,(4,2,2,2,2,2,2,2,2,2,2,2,2,2,2,2,2,4),(-9.4600020867739,
-9.44946097484441,-9.38977226427863,-9.3314620836995,-9.27390543364871,
-9.21399634460654,-9.15635642704838,-9.09711384600216,-9.03797514352587,
-8.98094579786149,-8.92125183936447,-8.86275948675276,-8.8054237975235,
-8.7453135764027,-8.68749269541132,-8.62874128051507,-8.56939184171518,
-8.51391269073544),.UNSPECIFIED.);
#3245=B_SPLINE_CURVE_WITH_KNOTS('',3,(#66355,#66356,#66357,#66358,#66359,
#66360,#66361,#66362,#66363,#66364,#66365,#66366,#66367,#66368,#66369,#66370,
#66371,#66372,#66373,#66374,#66375,#66376,#66377,#66378,#66379,#66380,#66381,
#66382,#66383,#66384,#66385,#66386,#66387,#66388,#66389,#66390),
 .UNSPECIFIED.,.F.,.F.,(4,2,2,2,2,2,2,2,2,2,2,2,2,2,2,2,2,4),(-18.8860416189937,
-18.8462348900712,-18.7876476548069,-18.7280968440835,-18.6709555484027,
-18.6115929558287,-18.5531716016611,-18.495349324202,-18.4352301709226,
-18.3780798368063,-18.319585679885,-18.2599881331103,-18.2030028878512,
-18.1438648978918,-18.0850090800984,-18.0273834680497,-17.9674824112817,
-17.941522876477),.UNSPECIFIED.);
#3246=B_SPLINE_CURVE_WITH_KNOTS('',3,(#66395,#66396,#66397,#66398,#66399,
#66400,#66401,#66402,#66403,#66404,#66405,#66406,#66407,#66408,#66409,#66410,
#66411,#66412,#66413,#66414,#66415,#66416,#66417,#66418,#66419,#66420,#66421,
#66422,#66423,#66424,#66425,#66426,#66427,#66428,#66429,#66430),
 .UNSPECIFIED.,.F.,.F.,(4,2,2,2,2,2,2,2,2,2,2,2,2,2,2,2,2,4),(-10.4063262286273,
-10.387392591544,-10.3270439303512,-10.2690090232558,-10.210705562305,-10.1511132343272,
-10.09375612853,-10.034059046947,-9.97524386932148,-9.91820163035005,-9.8584903134111,
-9.80032595747233,-9.74246277833438,-9.68271846928724,-9.62522607647149,
-9.56540900336133,-9.50645028314585,-9.4600020867739),.UNSPECIFIED.);
#3247=B_SPLINE_CURVE_WITH_KNOTS('',3,(#66431,#66432,#66433,#66434,#66435,
#66436,#66437,#66438,#66439,#66440,#66441,#66442,#66443,#66444,#66445,#66446,
#66447,#66448,#66449,#66450,#66451,#66452,#66453,#66454,#66455,#66456,#66457,
#66458,#66459,#66460,#66461,#66462,#66463,#66464,#66465,#66466),
 .UNSPECIFIED.,.F.,.F.,(4,2,2,2,2,2,2,2,2,2,2,2,2,2,2,2,2,4),(-17.941522876477,
-17.9101636562757,-17.8518687182981,-17.7922922877475,-17.7354001068821,
-17.6764590004862,-17.6170707989498,-17.5596109797981,-17.4998945731994,
-17.4423134048219,-17.3841841685699,-17.3245998970605,-17.2677034424408,
-17.2089258668494,-17.1489368038417,-17.0916073172332,-17.0320369692312,
-16.997272415308),.UNSPECIFIED.);
#3248=B_SPLINE_CURVE_WITH_KNOTS('',3,(#66471,#66472,#66473,#66474,#66475,
#66476,#66477,#66478,#66479,#66480,#66481,#66482,#66483,#66484,#66485,#66486,
#66487,#66488,#66489,#66490,#66491,#66492,#66493,#66494,#66495,#66496,#66497,
#66498,#66499,#66500,#66501,#66502,#66503,#66504,#66505,#66506),
 .UNSPECIFIED.,.F.,.F.,(4,2,2,2,2,2,2,2,2,2,2,2,2,2,2,2,2,4),(-11.3522871924595,
-11.324430394275,-11.264522730746,-11.2068857092522,-11.1477360236872,-11.08859687367,
-11.0315792760543,-10.9719076335357,-10.9134142640608,-10.8561239489264,
-10.796010976838,-10.7381891351563,-10.6795177406942,-10.620164420077,-10.5629956093436,
-10.5032845165816,-10.4445743180876,-10.4063262286273),.UNSPECIFIED.);
#3249=B_SPLINE_CURVE_WITH_KNOTS('',3,(#66507,#66508,#66509,#66510,#66511,
#66512,#66513,#66514,#66515,#66516,#66517,#66518,#66519,#66520,#66521,#66522,
#66523,#66524,#66525,#66526,#66527,#66528,#66529,#66530,#66531,#66532,#66533,
#66534,#66535,#66536,#66537,#66538,#66539,#66540,#66541,#66542),
 .UNSPECIFIED.,.F.,.F.,(4,2,2,2,2,2,2,2,2,2,2,2,2,2,2,2,2,4),(-16.997272415308,
-16.974118579872,-16.9161165902415,-16.8564975009602,-16.7995101512218,
-16.7408573501075,-16.6812582779792,-16.6240545216982,-16.5646258893359,
-16.5062147666311,-16.448330624569,-16.388145391231,-16.3309738020301,-16.2724169024022,
-16.2127779950283,-16.155739296564,-16.0965384948368,-16.052121842989),
 .UNSPECIFIED.);
#3250=B_SPLINE_CURVE_WITH_KNOTS('',3,(#66547,#66548,#66549,#66550,#66551,
#66552,#66553,#66554,#66555,#66556,#66557,#66558,#66559,#66560,#66561,#66562,
#66563,#66564,#66565,#66566,#66567,#66568,#66569,#66570,#66571,#66572,#66573,
#66574,#66575,#66576,#66577,#66578,#66579,#66580,#66581,#66582),
 .UNSPECIFIED.,.F.,.F.,(4,2,2,2,2,2,2,2,2,2,2,2,2,2,2,2,2,4),(-12.2980151684053,
-12.2608049534251,-12.2012214180354,-12.1438740189948,-12.0842046319712,
-12.0253980696236,-11.9683912868138,-11.9087094544592,-11.8505531273409,
-11.7927573534416,-11.7330193273245,-11.6755342944868,-11.6158192576419,
-11.5568642629696,-11.4998992163216,-11.4402365277277,-11.3819295252021,
-11.3522871924595),.UNSPECIFIED.);
#3251=B_SPLINE_CURVE_WITH_KNOTS('',3,(#66583,#66584,#66585,#66586,#66587,
#66588,#66589,#66590,#66591,#66592,#66593,#66594,#66595,#66596,#66597,#66598,
#66599,#66600,#66601,#66602,#66603,#66604,#66605,#66606,#66607,#66608,#66609,
#66610,#66611,#66612,#66613,#66614,#66615,#66616,#66617,#66618),
 .UNSPECIFIED.,.F.,.F.,(4,2,2,2,2,2,2,2,2,2,2,2,2,2,2,2,2,4),(-16.052121842989,
-16.0377063442003,-15.9800225041649,-15.9200592855784,-15.8627316418797,
-15.8043778785959,-15.7447638720137,-15.6878306019307,-15.6288305455336,
-15.5694764347843,-15.5119625793001,-15.452188569769,-15.3946092699113,
-15.3364257590099,-15.2768073817686,-15.2198815508401,-15.1610495793805,
-15.1073443691545),.UNSPECIFIED.);
#3252=B_SPLINE_CURVE_WITH_KNOTS('',3,(#66623,#66624,#66625,#66626,#66627,
#66628,#66629,#66630,#66631,#66632,#66633,#66634,#66635,#66636,#66637,#66638,
#66639,#66640,#66641,#66642,#66643,#66644,#66645,#66646,#66647,#66648,#66649,
#66650,#66651,#66652,#66653,#66654,#66655,#66656,#66657,#66658),
 .UNSPECIFIED.,.F.,.F.,(4,2,2,2,2,2,2,2,2,2,2,2,2,2,2,2,2,4),(-13.2436220538442,
-13.1973293402993,-13.1382053560805,-13.0812140676331,-13.0215819437106,
-12.9631029490451,-12.905874761448,-12.8457747640532,-12.787967213325,-12.7293949980337,
-12.670053341907,-12.6128978517491,-12.5532219431716,-12.494522530246,-12.4373888207658,
-12.3770495663262,-12.3190255916381,-12.2980151684053),.UNSPECIFIED.);
#3253=B_SPLINE_CURVE_WITH_KNOTS('',3,(#66659,#66660,#66661,#66662,#66663,
#66664,#66665,#66666,#66667,#66668,#66669,#66670,#66671,#66672,#66673,#66674,
#66675,#66676,#66677,#66678,#66679,#66680,#66681,#66682,#66683,#66684,#66685,
#66686,#66687,#66688,#66689,#66690,#66691,#66692,#66693,#66694,#66695,#66696),
 .UNSPECIFIED.,.F.,.F.,(4,2,2,2,2,2,2,2,2,2,2,2,2,2,2,2,2,2,4),(-15.1073443691545,
-15.1011008892937,-15.0437220848592,-14.9840992717133,-14.926190394778,
-14.8681392181562,-14.8084892686686,-14.7514823595925,-14.6927803091387,
-14.6331489331619,-14.5758985339276,-14.5164203125443,-14.4580324516964,
-14.4001023522461,-14.339867608388,-14.2826884114687,-14.2240848432797,
-14.1644203791933,-14.161791521072),.UNSPECIFIED.);
#3254=B_SPLINE_CURVE_WITH_KNOTS('',3,(#66701,#66702,#66703,#66704,#66705,
#66706,#66707,#66708,#66709,#66710,#66711,#66712,#66713,#66714,#66715,#66716,
#66717,#66718,#66719,#66720,#66721,#66722,#66723,#66724,#66725,#66726,#66727,
#66728,#66729,#66730,#66731,#66732,#66733,#66734,#66735,#66736),
 .UNSPECIFIED.,.F.,.F.,(4,2,2,2,2,2,2,2,2,2,2,2,2,2,2,2,2,4),(-14.1885859699234,
-14.1330844909293,-14.0738030834317,-14.0151322001193,-13.9573780431577,
-13.8973369154889,-13.8400747014035,-13.781649842778,-13.7220284098382,
-13.6650669338426,-13.6061313895152,-13.5492060305576,-13.4895868440872,
-13.4312985326842,-13.3738747554208,-13.3139843572995,-13.2563655957482,
-13.2436220538442),.UNSPECIFIED.);
#3255=B_SPLINE_CURVE_WITH_KNOTS('',3,(#66737,#66738,#66739,#66740,#66741,
#66742,#66743,#66744,#66745,#66746,#66747,#66748,#66749,#66750,#66751,#66752,
#66753,#66754,#66755,#66756,#66757,#66758,#66759,#66760,#66761,#66762,#66763,
#66764,#66765,#66766,#66767,#66768,#66769,#66770,#66771,#66772),
 .UNSPECIFIED.,.F.,.F.,(4,2,2,2,2,2,2,2,2,2,2,2,2,2,2,2,2,4),(-14.161791521072,
-14.1073426685626,-14.0480953063394,-13.9892999039839,-13.9315735440484,
-13.8715645099561,-13.8142414960538,-13.7558447627025,-13.6962089327002,
-13.6392486779599,-13.5802573437773,-13.5233108369954,-13.4636758610349,
-13.4053314288153,-13.3479464458854,-13.2879951425265,-13.2303206406094,
-13.2166062380566),.UNSPECIFIED.);
#3256=B_SPLINE_CURVE_WITH_KNOTS('',3,(#66777,#66778,#66779,#66780,#66781,
#66782,#66783,#66784,#66785,#66786,#66787,#66788,#66789,#66790,#66791,#66792,
#66793,#66794,#66795,#66796,#66797,#66798,#66799,#66800,#66801,#66802,#66803,
#66804,#66805,#66806,#66807,#66808,#66809,#66810,#66811,#66812,#66813,#66814),
 .UNSPECIFIED.,.F.,.F.,(4,2,2,2,2,2,2,2,2,2,2,2,2,2,2,2,2,2,4),(-15.1341561055544,
-15.1269994338561,-15.0695799723091,-15.0099125340775,-14.9520739190766,
-14.8939828445778,-14.8343297519005,-14.7773366004228,-14.7185951213641,
-14.6589576423824,-14.6016713251844,-14.5421535644632,-14.4838629359255,
-14.4258987192761,-14.3656251166082,-14.3084824988271,-14.2498440170218,
-14.1901865832963,-14.1885859699234),.UNSPECIFIED.);
#3257=B_SPLINE_CURVE_WITH_KNOTS('',3,(#66815,#66816,#66817,#66818,#66819,
#66820,#66821,#66822,#66823,#66824,#66825,#66826,#66827,#66828,#66829,#66830,
#66831,#66832,#66833,#66834,#66835,#66836,#66837,#66838,#66839,#66840,#66841,
#66842,#66843,#66844,#66845,#66846,#66847,#66848,#66849,#66850),
 .UNSPECIFIED.,.F.,.F.,(4,2,2,2,2,2,2,2,2,2,2,2,2,2,2,2,2,4),(-13.2166062380566,
-13.1713851979337,-13.1121981319385,-13.0551628296182,-12.9955080421381,
-12.9369655576865,-12.8797535453401,-12.819585289645,-12.761715189623,-12.7032194250943,
-12.6438086463492,-12.586620577358,-12.5270150261763,-12.4683803900242,
-12.4113696886299,-12.35174219741,-12.2937588655423,-12.2712695292436),
 .UNSPECIFIED.);
#3258=B_SPLINE_CURVE_WITH_KNOTS('',3,(#66855,#66856,#66857,#66858,#66859,
#66860,#66861,#66862,#66863,#66864,#66865,#66866,#66867,#66868,#66869,#66870,
#66871,#66872,#66873,#66874,#66875,#66876,#66877,#66878,#66879,#66880,#66881,
#66882,#66883,#66884,#66885,#66886,#66887,#66888,#66889,#66890),
 .UNSPECIFIED.,.F.,.F.,(4,2,2,2,2,2,2,2,2,2,2,2,2,2,2,2,2,4),(-16.0791645683298,
-16.0637629880179,-16.0060223350212,-15.9459969234656,-15.8887024341941,
-15.8302912537239,-15.7706612508563,-15.7136999051047,-15.654642811055,
-15.5954057874932,-15.5378426704977,-15.4780146687669,-15.4204898319656,
-15.3622571133794,-15.3026293793744,-15.2456979578477,-15.1868171504776,
-15.1341561055544),.UNSPECIFIED.);
#3259=B_SPLINE_CURVE_WITH_KNOTS('',3,(#66891,#66892,#66893,#66894,#66895,
#66896,#66897,#66898,#66899,#66900,#66901,#66902,#66903,#66904,#66905,#66906,
#66907,#66908,#66909,#66910,#66911,#66912,#66913,#66914,#66915,#66916,#66917,
#66918,#66919,#66920,#66921,#66922,#66923,#66924,#66925,#66926),
 .UNSPECIFIED.,.F.,.F.,(4,2,2,2,2,2,2,2,2,2,2,2,2,2,2,2,2,4),(-12.2712695292436,
-12.2357754508004,-12.1762270533728,-12.1189170680661,-12.0588176303639,
-12.0000655464483,-11.943159299172,-11.8835712422689,-11.8254678956475,
-11.7678321870858,-11.708145031833,-11.6507114242844,-11.5912213696332,
-11.5323122460786,-11.4754266605439,-11.4158513420701,-11.3575887654668,
-11.3269908932583),.UNSPECIFIED.);
#3260=B_SPLINE_CURVE_WITH_KNOTS('',3,(#66931,#66932,#66933,#66934,#66935,
#66936,#66937,#66938,#66939,#66940,#66941,#66942,#66943,#66944,#66945,#66946,
#66947,#66948,#66949,#66950,#66951,#66952,#66953,#66954,#66955,#66956,#66957,
#66958,#66959,#66960,#66961,#66962,#66963,#66964,#66965,#66966),
 .UNSPECIFIED.,.F.,.F.,(4,2,2,2,2,2,2,2,2,2,2,2,2,2,2,2,2,4),(-17.0247741151702,
-17.0006922494049,-16.942620899042,-16.8829683888398,-16.8259674619989,
-16.7672454552544,-16.7076101234707,-16.6503415003102,-16.590843286514,
-16.5325014804607,-16.4745540351945,-16.4142996421448,-16.357137434069,
-16.2985161360182,-16.2388539992256,-16.1817640975146,-16.1224994016558,
-16.0791645683298),.UNSPECIFIED.);
#3261=B_SPLINE_CURVE_WITH_KNOTS('',3,(#66967,#66968,#66969,#66970,#66971,
#66972,#66973,#66974,#66975,#66976,#66977,#66978,#66979,#66980,#66981,#66982,
#66983,#66984,#66985,#66986,#66987,#66988,#66989,#66990,#66991,#66992,#66993,
#66994,#66995,#66996,#66997,#66998,#66999,#67000,#67001,#67002),
 .UNSPECIFIED.,.F.,.F.,(4,2,2,2,2,2,2,2,2,2,2,2,2,2,2,2,2,4),(-11.3269908932583,
-11.3002304831747,-11.2403651502537,-11.1827717007332,-11.1238285355636,
-11.064728011521,-11.0077668972893,-10.9481757635054,-10.8897195155163,
-10.8325471683827,-10.7724692707686,-10.7146842840278,-10.6561946025542,
-10.5968740051404,-10.5397395269343,-10.4801014814801,-10.4214223488875,
-10.3822526002173),.UNSPECIFIED.);
#3262=B_SPLINE_CURVE_WITH_KNOTS('',3,(#67007,#67008,#67009,#67010,#67011,
#67012,#67013,#67014,#67015,#67016,#67017,#67018,#67019,#67020,#67021,#67022,
#67023,#67024,#67025,#67026,#67027,#67028,#67029,#67030,#67031,#67032,#67033,
#67034,#67035,#67036,#67037,#67038,#67039,#67040,#67041,#67042),
 .UNSPECIFIED.,.F.,.F.,(4,2,2,2,2,2,2,2,2,2,2,2,2,2,2,2,2,4),(-17.9696970255303,
-17.937289370862,-17.8789069021961,-17.8192841522869,-17.7623368372575,
-17.7033082433986,-17.6440100001385,-17.5864714106887,-17.526670356869,
-17.4691167328281,-17.4109085209012,-17.3512845924667,-17.2943555190345,
-17.2354990142404,-17.1756126480208,-17.1182132969445,-17.0585679978772,
-17.0247741151702),.UNSPECIFIED.);
#3263=B_SPLINE_CURVE_WITH_KNOTS('',3,(#67043,#67044,#67045,#67046,#67047,
#67048,#67049,#67050,#67051,#67052,#67053,#67054,#67055,#67056,#67057,#67058,
#67059,#67060,#67061,#67062,#67063,#67064,#67065,#67066,#67067,#67068,#67069,
#67070,#67071,#67072,#67073,#67074,#67075,#67076,#67077,#67078),
 .UNSPECIFIED.,.F.,.F.,(4,2,2,2,2,2,2,2,2,2,2,2,2,2,2,2,2,4),(-10.3822526002173,
-10.3643343540307,-10.3046400968479,-10.246613334744,-10.1885181147052,
-10.128927402479,-10.0715754084394,-10.011325400927,-9.9525347708931,-9.89556195447909,
-9.83591091083034,-9.77776999750488,-9.72003077893023,-9.66030722303232,
-9.60283704872725,-9.54320316116386,-9.48426076178981,-9.43689892858011),
 .UNSPECIFIED.);
#3264=B_SPLINE_CURVE_WITH_KNOTS('',3,(#67083,#67084,#67085,#67086,#67087,
#67088,#67089,#67090,#67091,#67092,#67093,#67094,#67095,#67096,#67097,#67098,
#67099,#67100,#67101,#67102,#67103,#67104,#67105,#67106,#67107,#67108,#67109,
#67110,#67111,#67112,#67113,#67114,#67115,#67116,#67117,#67118),
 .UNSPECIFIED.,.F.,.F.,(4,2,2,2,2,2,2,2,2,2,2,2,2,2,2,2,2,4),(-18.9151145034862,
-18.8743164654268,-18.8156291548377,-18.7560115648048,-18.6987754493173,
-18.6393121439161,-18.5809341256596,-18.5230183981635,-18.4627987144582,
-18.4056311968295,-18.3470421802252,-18.2873910545073,-18.2303271150055,
-18.171094421965,-18.1123080260466,-18.0545957689432,-17.9946015046478,
-17.9696970255303),.UNSPECIFIED.);
#3265=B_SPLINE_CURVE_WITH_KNOTS('',3,(#67119,#67120,#67121,#67122,#67123,
#67124,#67125,#67126,#67127,#67128,#67129,#67130,#67131,#67132,#67133,#67134,
#67135,#67136,#67137,#67138,#67139,#67140,#67141,#67142,#67143,#67144,#67145,
#67146,#67147,#67148,#67149,#67150,#67151,#67152,#67153,#67154),
 .UNSPECIFIED.,.F.,.F.,(4,2,2,2,2,2,2,2,2,2,2,2,2,2,2,2,2,4),(-9.43689892858011,
-9.42732171849391,-9.36768738295302,-9.30939248028644,-9.25194272911408,
-9.19204622378449,-9.13442101602013,-9.07534568068709,-9.01621630273034,
-8.95921594082851,-8.89957004368503,-8.84108593111714,-8.78383634874988,
-8.72373170856049,-8.6659190669351,-8.60731272480359,-8.54796686813959,
-8.49156038630827),.UNSPECIFIED.);
#3266=B_SPLINE_CURVE_WITH_KNOTS('',3,(#67159,#67160,#67161,#67162,#67163,
#67164,#67165,#67166,#67167,#67168,#67169,#67170,#67171,#67172,#67173,#67174,
#67175,#67176,#67177,#67178,#67179,#67180,#67181,#67182,#67183,#67184,#67185,
#67186,#67187,#67188,#67189,#67190,#67191,#67192,#67193,#67194),
 .UNSPECIFIED.,.F.,.F.,(4,2,2,2,2,2,2,2,2,2,2,2,2,2,2,2,2,4),(-19.8597382210236,
-19.810451373043,-19.7514667566491,-19.6921219719675,-19.6346229403372,
-19.5748644342208,-19.5172962645061,-19.4591277252691,-19.3995232496075,
-19.3426105099162,-19.2837936446735,-19.2238539608265,-19.1664896413472,
-19.1068819617647,-19.0489837573588,-18.9909471893313,-18.9313109305834,
-18.9151145034862),.UNSPECIFIED.);
#3267=B_SPLINE_CURVE_WITH_KNOTS('',3,(#67195,#67196,#67197,#67198,#67199,
#67200,#67201,#67202,#67203,#67204,#67205,#67206,#67207,#67208,#67209,#67210,
#67211,#67212,#67213,#67214,#67215,#67216,#67217,#67218,#67219,#67220,#67221,
#67222,#67223,#67224,#67225,#67226,#67227,#67228,#67229,#67230,#67231,#67232),
 .UNSPECIFIED.,.F.,.F.,(4,2,2,2,2,2,2,2,2,2,2,2,2,2,2,2,2,2,4),(-8.49156038630827,
-8.49080675575303,-8.43111857134256,-8.37241526446117,-8.31526501763932,
-8.25492233706489,-8.19689441801019,-8.13864530142174,-8.07905854481672,
-8.02170761683104,-7.96202852596394,-7.9032187975688,-7.84619976450985,
-7.78650760972943,-7.72834831916545,-7.67052935317836,-7.61078895216033,
-7.55330118212272,-7.54539583975842),.UNSPECIFIED.);
#3268=B_SPLINE_CURVE_WITH_KNOTS('',3,(#67237,#67238,#67239,#67240,#67241,
#67242,#67243,#67244,#67245,#67246,#67247,#67248,#67249,#67250,#67251,#67252,
#67253,#67254,#67255,#67256,#67257,#67258,#67259,#67260,#67261,#67262,#67263,
#67264,#67265,#67266,#67267,#67268,#67269,#67270,#67271,#67272,#67273,#67274),
 .UNSPECIFIED.,.F.,.F.,(4,2,2,2,2,2,2,2,2,2,2,2,2,2,2,2,2,2,4),(-20.8047268284554,
-20.8036363389145,-20.7464479008663,-20.6870352594353,-20.6286348915891,
-20.5707661629285,-20.510597073108,-20.4534380889162,-20.3948967931479,
-20.3352722771837,-20.2782483009287,-20.219063232801,-20.1602410153004,
-20.1025723093681,-20.0426249323872,-19.9853090960203,-19.9269706384341,
-19.867370764855,-19.8597382210236),.UNSPECIFIED.);
#3269=B_SPLINE_CURVE_WITH_KNOTS('',3,(#67275,#67276,#67277,#67278,#67279,
#67280,#67281,#67282,#67283,#67284,#67285,#67286,#67287,#67288,#67289,#67290,
#67291,#67292,#67293,#67294,#67295,#67296,#67297,#67298,#67299,#67300,#67301,
#67302,#67303,#67304,#67305,#67306,#67307,#67308,#67309,#67310),
 .UNSPECIFIED.,.F.,.F.,(4,2,2,2,2,2,2,2,2,2,2,2,2,2,2,2,2,4),(-7.54539583975842,
-7.49355110204946,-7.43459460077228,-7.37762115395009,-7.31794932817515,
-7.25964100917192,-7.20212210603924,-7.14221371611197,-7.08457547245393,
-7.02539392871746,-6.96625468515904,-6.90923296876007,-6.84955345859718,
-6.79106019408235,-6.73375428080265,-6.6736419972573,-6.61582024058893,
-6.59962043014718),.UNSPECIFIED.);
#3270=B_SPLINE_CURVE_WITH_KNOTS('',3,(#67315,#67316,#67317,#67318,#67319,
#67320,#67321,#67322,#67323,#67324,#67325,#67326,#67327,#67328,#67329,#67330,
#67331,#67332,#67333,#67334,#67335,#67336,#67337,#67338,#67339,#67340,#67341,
#67342,#67343,#67344,#67345,#67346,#67347,#67348,#67349,#67350),
 .UNSPECIFIED.,.F.,.F.,(4,2,2,2,2,2,2,2,2,2,2,2,2,2,2,2,2,4),(-21.7489046572791,
-21.7392153866495,-21.6817714549229,-21.6220716583751,-21.5645025223573,
-21.5063893301253,-21.4468200256293,-21.3899376073178,-21.3311762213552,
-21.2711970668162,-21.2138831121422,-21.1543289862749,-21.0964221879644,
-21.0384358621701,-20.9788315240901,-20.9218575630073,-20.8632205676017,
-20.8047268284554),.UNSPECIFIED.);
#3271=B_SPLINE_CURVE_WITH_KNOTS('',3,(#67351,#67352,#67353,#67354,#67355,
#67356,#67357,#67358,#67359,#67360,#67361,#67362,#67363,#67364,#67365,#67366,
#67367,#67368,#67369,#67370,#67371,#67372,#67373,#67374,#67375,#67376,#67377,
#67378,#67379,#67380,#67381,#67382,#67383,#67384,#67385,#67386),
 .UNSPECIFIED.,.F.,.F.,(4,2,2,2,2,2,2,2,2,2,2,2,2,2,2,2,2,4),(-6.59962043014718,
-6.55712143056447,-6.49776917806976,-6.44060046014423,-6.3808828825634,
-6.32217397813377,-6.26498116754636,-6.20463437850135,-6.14660066752985,
-6.0882749718812,-6.02868466855325,-5.9713291133043,-5.91162795849117,-5.85281481524407,
-5.79576557777481,-5.73604961995392,-5.67788743624381,-5.65305968192749),
 .UNSPECIFIED.);
#3272=B_SPLINE_CURVE_WITH_KNOTS('',3,(#67391,#67392,#67393,#67394,#67395,
#67396,#67397,#67398,#67399,#67400,#67401,#67402,#67403,#67404,#67405,#67406,
#67407,#67408,#67409,#67410,#67411,#67412,#67413,#67414,#67415,#67416,#67417,
#67418,#67419,#67420,#67421,#67422,#67423,#67424,#67425,#67426),
 .UNSPECIFIED.,.F.,.F.,(4,2,2,2,2,2,2,2,2,2,2,2,2,2,2,2,2,4),(-22.6930944862137,
-22.6750742815793,-22.6172685137948,-22.5571666469156,-22.5000298336195,
-22.4415523883347,-22.3819703093803,-22.3250007752965,-22.2658796385637,
-22.2070346049225,-22.1494252073759,-22.0895411174023,-22.0322350703383,
-21.9739565284333,-21.9143953015877,-21.8575179583935,-21.7985933937003,
-21.7489046572791),.UNSPECIFIED.);
#3273=B_SPLINE_CURVE_WITH_KNOTS('',3,(#67427,#67428,#67429,#67430,#67431,
#67432,#67433,#67434,#67435,#67436,#67437,#67438,#67439,#67440,#67441,#67442,
#67443,#67444,#67445,#67446,#67447,#67448,#67449,#67450,#67451,#67452,#67453,
#67454,#67455,#67456,#67457,#67458,#67459,#67460,#67461,#67462),
 .UNSPECIFIED.,.F.,.F.,(4,2,2,2,2,2,2,2,2,2,2,2,2,2,2,2,2,4),(-5.65305968192749,
-5.62000697109407,-5.56026553634326,-5.50277548740805,-5.4429300395589,
-5.38397497750277,-5.32698226097639,-5.2672900308627,-5.20898363219345,
-5.15141280935565,-5.09150820934248,-5.03387211917237,-4.97460397585247,
-4.91547032791341,-4.8584416373336,-4.79874535977046,-4.74025819094778,
-4.7070192889843),.UNSPECIFIED.);
#3274=B_SPLINE_CURVE_WITH_KNOTS('',3,(#67467,#67468,#67469,#67470,#67471,
#67472,#67473,#67474,#67475,#67476,#67477,#67478,#67479,#67480,#67481,#67482,
#67483,#67484,#67485,#67486,#67487,#67488,#67489,#67490,#67491,#67492,#67493,
#67494,#67495,#67496,#67497,#67498,#67499,#67500,#67501,#67502),
 .UNSPECIFIED.,.F.,.F.,(4,2,2,2,2,2,2,2,2,2,2,2,2,2,2,2,2,4),(-23.6367224740298,
-23.6102009889967,-23.5521597036553,-23.4926417159663,-23.435803856614,
-23.3771146729451,-23.3171085926091,-23.2598611088234,-23.2003772998387,
-23.1424751745089,-23.0845553127723,-23.0249989156642,-22.9680595588619,
-22.9094892557851,-22.8499543793008,-22.7928294928815,-22.7334840265615,
-22.6930944862137),.UNSPECIFIED.);
#3275=B_SPLINE_CURVE_WITH_KNOTS('',3,(#67503,#67504,#67505,#67506,#67507,
#67508,#67509,#67510,#67511,#67512,#67513,#67514,#67515,#67516,#67517,#67518,
#67519,#67520,#67521,#67522,#67523,#67524,#67525,#67526,#67527,#67528,#67529,
#67530,#67531,#67532,#67533,#67534,#67535,#67536,#67537,#67538),
 .UNSPECIFIED.,.F.,.F.,(4,2,2,2,2,2,2,2,2,2,2,2,2,2,2,2,2,4),(-4.7070192889843,
-4.68291221701188,-4.62280788263384,-4.56499211835275,-4.50621920975702,
-4.44687598188547,-4.3897125228076,-4.32998213906469,-4.27128283566224,
-4.21406294394457,-4.15372759490239,-4.09570314650131,-4.03731813708901,
-3.97773968458231,-3.92039439080922,-3.86068740451247,-3.80188610698126,
-3.76030733114506),.UNSPECIFIED.);
#3276=B_SPLINE_CURVE_WITH_KNOTS('',3,(#67543,#67544,#67545,#67546,#67547,
#67548,#67549,#67550,#67551,#67552,#67553,#67554,#67555,#67556,#67557,#67558,
#67559,#67560,#67561,#67562,#67563,#67564,#67565,#67566,#67567,#67568,#67569,
#67570,#67571,#67572,#67573,#67574,#67575,#67576,#67577,#67578),
 .UNSPECIFIED.,.F.,.F.,(4,2,2,2,2,2,2,2,2,2,2,2,2,2,2,2,2,4),(-24.5799045977848,
-24.544864402261,-24.4864680402579,-24.4269448204466,-24.3700449713328,
-24.3110051741305,-24.2521492970098,-24.1946159613695,-24.1348126294181,
-24.0775296073419,-24.0193278864891,-23.9598215850082,-23.9030009070175,
-23.8441534701742,-23.7847543450619,-23.7273819445697,-23.667757974583,
-23.6367224740298),.UNSPECIFIED.);
#3277=B_SPLINE_CURVE_WITH_KNOTS('',3,(#67579,#67580,#67581,#67582,#67583,
#67584,#67585,#67586,#67587,#67588,#67589,#67590,#67591,#67592,#67593,#67594,
#67595,#67596,#67597,#67598,#67599,#67600,#67601,#67602,#67603,#67604,#67605,
#67606,#67607,#67608,#67609,#67610,#67611,#67612,#67613,#67614),
 .UNSPECIFIED.,.F.,.F.,(4,2,2,2,2,2,2,2,2,2,2,2,2,2,2,2,2,4),(-3.76030733114506,
-3.74482173076156,-3.6850983260828,-3.62694832744347,-3.56902286769636,
-3.50929583899485,-3.45181843527126,-3.39189585023894,-3.33295745069471,
-3.27595993809932,-3.21626352613547,-3.15797408399984,-3.1003669659872,
-3.04048156422391,-2.98286252158158,-2.92352507208656,-2.86441225193454,
-2.81422223630842),.UNSPECIFIED.);
#3278=B_SPLINE_CURVE_WITH_KNOTS('',3,(#67619,#67620,#67621,#67622,#67623,
#67624,#67625,#67626,#67627,#67628,#67629,#67630,#67631,#67632,#67633,#67634,
#67635,#67636,#67637,#67638,#67639,#67640,#67641,#67642,#67643,#67644,#67645,
#67646,#67647,#67648,#67649,#67650,#67651,#67652,#67653,#67654),
 .UNSPECIFIED.,.F.,.F.,(4,2,2,2,2,2,2,2,2,2,2,2,2,2,2,2,2,4),(-25.5227587485597,
-25.47965708315,-25.421058174348,-25.361036462416,-25.3038727637219,-25.2444773184052,
-25.1865926949701,-25.128756714116,-25.0692650147963,-25.0123746718861,
-24.9538886316087,-24.8944198504469,-24.8373755091807,-24.7781149174187,
-24.7197080007783,-24.6619822469935,-24.6019654058989,-24.5799045977848),
 .UNSPECIFIED.);
#3279=B_SPLINE_CURVE_WITH_KNOTS('',3,(#67655,#67656,#67657,#67658,#67659,
#67660,#67661,#67662,#67663,#67664,#67665,#67666,#67667,#67668,#67669,#67670,
#67671,#67672,#67673,#67674,#67675,#67676,#67677,#67678,#67679,#67680,#67681,
#67682,#67683,#67684,#67685,#67686,#67687,#67688,#67689,#67690,#67691,#67692),
 .UNSPECIFIED.,.F.,.F.,(4,2,2,2,2,2,2,2,2,2,2,2,2,2,2,2,2,2,4),(-2.81422223630842,
-2.80739059809379,-2.74769363128926,-2.68922759545975,-2.63185666495599,
-2.57177569602702,-2.51398082031509,-2.45515020591261,-2.39583126811454,
-2.3386868262193,-2.27895955966271,-2.22028492138649,-2.16305256653281,
-2.1027441052407,-2.04474383487291,-1.98631516239258,-1.92676386570169,
-1.86944360522889,-1.86759610747369),.UNSPECIFIED.);
#3280=B_SPLINE_CURVE_WITH_KNOTS('',3,(#67697,#67698,#67699,#67700,#67701,
#67702,#67703,#67704,#67705,#67706,#67707,#67708,#67709,#67710,#67711,#67712,
#67713,#67714,#67715,#67716,#67717,#67718,#67719,#67720,#67721,#67722,#67723,
#67724,#67725,#67726,#67727,#67728,#67729,#67730,#67731,#67732),
 .UNSPECIFIED.,.F.,.F.,(4,2,2,2,2,2,2,2,2,2,2,2,2,2,2,2,2,4),(-26.4647006629411,
-26.4128164821547,-26.3538770628634,-26.295021282913,-26.2375822529352,
-26.1778787398139,-26.1206318744523,-26.0625253754812,-26.0030911980923,
-25.9463425849355,-25.8875908503495,-25.8281815100278,-25.7708984260118,
-25.7113688412011,-25.6538368035759,-25.595885334023,-25.5364356344578,
-25.5227587485597),.UNSPECIFIED.);
#3281=B_SPLINE_CURVE_WITH_KNOTS('',3,(#67733,#67734,#67735,#67736,#67737,
#67738,#67739,#67740,#67741,#67742,#67743,#67744,#67745,#67746,#67747,#67748,
#67749,#67750,#67751,#67752,#67753,#67754,#67755,#67756,#67757,#67758,#67759,
#67760,#67761,#67762,#67763,#67764,#67765,#67766,#67767,#67768),
 .UNSPECIFIED.,.F.,.F.,(4,2,2,2,2,2,2,2,2,2,2,2,2,2,2,2,2,4),(-1.86759610747369,
-1.8097465170722,-1.7509722323765,-1.69390716991027,-1.63419213717573,-1.57606932036452,
-1.51811407870063,-1.45841685307261,-1.40096694869804,-1.34098343757821,
-1.28207692999559,-1.22508871615811,-1.16540388332849,-1.10714645181714,
-1.0495176707267,-0.989666932708261,-0.932079853846146,-0.921606618540025),
 .UNSPECIFIED.);
#3282=B_SPLINE_CURVE_WITH_KNOTS('',3,(#67774,#67775,#67776,#67777,#67778,
#67779,#67780,#67781,#67782,#67783,#67784,#67785,#67786,#67787,#67788,#67789,
#67790,#67791,#67792,#67793),.UNSPECIFIED.,.F.,.F.,(4,2,2,2,2,2,2,2,2,4),
(9.99987117032003E-7,0.0282047267175922,0.0500972781633209,0.077222937740314,
0.107624298477487,0.137340418712146,0.157932276880896,0.175135732483776,
0.191462844907497,0.203440126186273),.UNSPECIFIED.);
#3283=B_SPLINE_CURVE_WITH_KNOTS('',3,(#67799,#67800,#67801,#67802,#67803,
#67804,#67805,#67806),.UNSPECIFIED.,.F.,.F.,(4,2,2,4),(21.4315064013737,
21.4634357935859,21.4930318613417,21.5226265917604),.UNSPECIFIED.);
#3284=B_SPLINE_CURVE_WITH_KNOTS('',3,(#67812,#67813,#67814,#67815,#67816,
#67817,#67818,#67819,#67820,#67821,#67822,#67823,#67824,#67825,#67826,#67827,
#67828,#67829,#67830,#67831,#67832,#67833,#67834,#67835,#67836,#67837,#67838,
#67839,#67840,#67841,#67842,#67843,#67844,#67845,#67846,#67847),
 .UNSPECIFIED.,.F.,.F.,(4,2,2,2,2,2,2,2,2,2,2,2,2,2,2,2,2,4),(20.6936878716818,
20.7322285263897,20.7783057175789,20.8227795047066,20.8693557730982,20.9149428892879,
20.9597524851927,21.0065846852777,21.0516438851204,21.0976519395239,21.1438788790039,
21.188432473727,21.2350392941589,21.2807854576605,21.3254925240272,21.3724982892632,
21.417717724476,21.4315064013737),.UNSPECIFIED.);
#3285=B_SPLINE_CURVE_WITH_KNOTS('',3,(#67848,#67849,#67850,#67851,#67852,
#67853,#67854,#67855,#67856,#67857,#67858,#67859,#67860,#67861,#67862,#67863,
#67864,#67865,#67866,#67867,#67868,#67869,#67870,#67871,#67872,#67873,#67874,
#67875,#67876,#67877,#67878,#67879,#67880,#67881,#67882,#67883),
 .UNSPECIFIED.,.F.,.F.,(4,2,2,2,2,2,2,2,2,2,2,2,2,2,2,2,2,4),(9.99999999753597E-7,
0.0364903991492045,0.0742057367939146,0.120984278340417,0.165716260437277,
0.212135354668823,0.258243398942271,0.303486376579508,0.350510827449709,
0.395451299070227,0.441223703670797,0.487964967533294,0.532602258835938,
0.578864855147042,0.625329100321987,0.670440021753448,0.717320863549735,
0.740262878339932),.UNSPECIFIED.);
#3286=B_SPLINE_CURVE_WITH_KNOTS('',3,(#67888,#67889,#67890,#67891,#67892,
#67893,#67894,#67895,#67896,#67897,#67898,#67899,#67900,#67901,#67902,#67903,
#67904,#67905,#67906,#67907,#67908,#67909,#67910,#67911,#67912,#67913,#67914,
#67915,#67916,#67917,#67918,#67919,#67920,#67921,#67922,#67923),
 .UNSPECIFIED.,.F.,.F.,(4,2,2,2,2,2,2,2,2,2,2,2,2,2,2,2,2,4),(19.9559680414516,
20.0008504784901,20.0467368410681,20.0912761832143,20.1378918451635,20.1832739295335,
20.2285046006904,20.275104513086,20.3199511087905,20.366754624975,20.4127173643503,
20.4571887454312,20.5037686894442,20.5492336658488,20.5942218762843,20.6409180608554,
20.6858523218674,20.6936878716818),.UNSPECIFIED.);
#3287=B_SPLINE_CURVE_WITH_KNOTS('',3,(#67924,#67925,#67926,#67927,#67928,
#67929,#67930,#67931,#67932,#67933,#67934,#67935,#67936,#67937,#67938,#67939,
#67940,#67941,#67942,#67943,#67944,#67945,#67946,#67947,#67948,#67949,#67950,
#67951,#67952,#67953,#67954,#67955,#67956,#67957,#67958,#67959),
 .UNSPECIFIED.,.F.,.F.,(4,2,2,2,2,2,2,2,2,2,2,2,2,2,2,2,2,4),(0.740262878339932,
0.762427102215096,0.808069985401053,0.854808846272841,0.899429812570394,
0.945570872042072,0.992454683227221,1.03747065146669,1.08424743869661,1.12958660656193,
1.175138889682,1.22190780149668,1.26658471043468,1.31264188421903,1.35939848501362,
1.4043392205548,1.45103260193205,1.48067239646651),.UNSPECIFIED.);
#3288=B_SPLINE_CURVE_WITH_KNOTS('',3,(#67964,#67965,#67966,#67967,#67968,
#67969,#67970,#67971,#67972,#67973,#67974,#67975,#67976,#67977,#67978,#67979,
#67980,#67981,#67982,#67983,#67984,#67985,#67986,#67987,#67988,#67989,#67990,
#67991,#67992,#67993,#67994,#67995,#67996,#67997,#67998,#67999,#68000,#68001),
 .UNSPECIFIED.,.F.,.F.,(4,2,2,2,2,2,2,2,2,2,2,2,2,2,2,2,2,2,4),(19.2175408288878,
19.2219373965907,19.2685210725085,19.3141891378125,19.3589248216993,19.4058460198647,
19.4509870738391,19.4968133764095,19.5431350504829,19.5877640910998,19.6343990565288,
19.6802461513431,19.72492597093,19.7720411959568,19.8173618084826,19.8629496498953,
19.9094715861334,19.954248068259,19.9559680414516),.UNSPECIFIED.);
#3289=B_SPLINE_CURVE_WITH_KNOTS('',3,(#68002,#68003,#68004,#68005,#68006,
#68007,#68008,#68009,#68010,#68011,#68012,#68013,#68014,#68015,#68016,#68017,
#68018,#68019,#68020,#68021,#68022,#68023,#68024,#68025,#68026,#68027,#68028,
#68029,#68030,#68031,#68032,#68033,#68034,#68035,#68036,#68037),
 .UNSPECIFIED.,.F.,.F.,(4,2,2,2,2,2,2,2,2,2,2,2,2,2,2,2,2,4),(1.48067239646651,
1.49671326012625,1.54219831558785,1.5894859449329,1.63428944893413,1.68030245144421,
1.72708174969527,1.77186789842175,1.81835464146615,1.86425678940839,1.90955548631379,
1.95664189809396,2.00148568453804,2.0473126858144,2.0940334671172,2.13867975719358,
2.18499121801513,2.22108960850334),.UNSPECIFIED.);
#3290=B_SPLINE_CURVE_WITH_KNOTS('',3,(#68042,#68043,#68044,#68045,#68046,
#68047,#68048,#68049,#68050,#68051,#68052,#68053,#68054,#68055,#68056,#68057,
#68058,#68059,#68060,#68061,#68062,#68063,#68064,#68065,#68066,#68067,#68068,
#68069,#68070,#68071,#68072,#68073,#68074,#68075,#68076,#68077),
 .UNSPECIFIED.,.F.,.F.,(4,2,2,2,2,2,2,2,2,2,2,2,2,2,2,2,2,4),(18.4801374015765,
18.4907658335562,18.5373515680576,18.5827705444335,18.6278503823358,18.6744946234866,
18.7193811539994,18.7659288026933,18.8119468369207,18.8564049550709,18.9029730508313,
18.9484975984601,18.9933693854802,19.0401328543241,19.0851285772229,19.1312801323088,
19.1774331204032,19.2175408288878),.UNSPECIFIED.);
#3291=B_SPLINE_CURVE_WITH_KNOTS('',3,(#68078,#68079,#68080,#68081,#68082,
#68083,#68084,#68085,#68086,#68087,#68088,#68089,#68090,#68091,#68092,#68093,
#68094,#68095,#68096,#68097,#68098,#68099,#68100,#68101,#68102,#68103,#68104,
#68105,#68106,#68107,#68108,#68109,#68110,#68111,#68112,#68113),
 .UNSPECIFIED.,.F.,.F.,(4,2,2,2,2,2,2,2,2,2,2,2,2,2,2,2,2,4),(2.22108960850334,
2.23120408655543,2.27635041769103,2.32327161206725,2.368237212408,2.41391337637609,
2.46061197050217,2.50519713949817,2.5513666691862,2.59796482416004,2.64299465171328,
2.68978881476098,2.73495033654449,2.78051325760178,2.82722340804027,2.87182391079689,
2.91788757586549,2.96056667106229),.UNSPECIFIED.);
#3292=B_SPLINE_CURVE_WITH_KNOTS('',3,(#68118,#68119,#68120,#68121,#68122,
#68123,#68124,#68125,#68126,#68127,#68128,#68129,#68130,#68131,#68132,#68133,
#68134,#68135,#68136,#68137,#68138,#68139,#68140,#68141,#68142,#68143,#68144,
#68145,#68146,#68147,#68148,#68149,#68150,#68151,#68152,#68153),
 .UNSPECIFIED.,.F.,.F.,(4,2,2,2,2,2,2,2,2,2,2,2,2,2,2,2,2,4),(17.7416164546727,
17.7581937026132,17.8052897667917,17.8505949548622,17.8963342504639,17.9428341472151,
17.9875910340227,18.0342105180494,18.0800707723051,18.124652551507,18.1712871824617,
18.2166406572815,18.2619848045744,18.3085503929415,18.3533657882032,18.4003592098579,
18.446278791736,18.4801374015765),.UNSPECIFIED.);
#3293=B_SPLINE_CURVE_WITH_KNOTS('',3,(#68154,#68155,#68156,#68157,#68158,
#68159,#68160,#68161,#68162,#68163,#68164,#68165,#68166,#68167,#68168,#68169,
#68170,#68171,#68172,#68173,#68174,#68175,#68176,#68177,#68178,#68179,#68180,
#68181,#68182,#68183,#68184,#68185,#68186,#68187,#68188,#68189,#68190,#68191),
 .UNSPECIFIED.,.F.,.F.,(4,2,2,2,2,2,2,2,2,2,2,2,2,2,2,2,2,2,4),(2.96056667106229,
2.96492507840458,3.00987622748865,3.05658369115965,3.10200096713613,3.14749048109044,
3.19424386894225,3.23892780465305,3.28492439308362,3.33166335864177,3.3765506531,
3.42318675517329,3.46898366970959,3.51441887461108,3.56165143931351,3.60649480370264,
3.65245839321213,3.69924258617203,3.70124435567),.UNSPECIFIED.);
#3294=B_SPLINE_CURVE_WITH_KNOTS('',3,(#68196,#68197,#68198,#68199,#68200,
#68201,#68202,#68203,#68204,#68205,#68206,#68207,#68208,#68209,#68210,#68211,
#68212,#68213,#68214,#68215,#68216,#68217,#68218,#68219,#68220,#68221,#68222,
#68223,#68224,#68225,#68226,#68227,#68228,#68229,#68230,#68231),
 .UNSPECIFIED.,.F.,.F.,(4,2,2,2,2,2,2,2,2,2,2,2,2,2,2,2,2,4),(17.002935008964,
17.0259159067871,17.0726902796453,17.117698909592,17.1640720079207,17.2102290646699,
17.2547667636235,17.301404789293,17.3470724875982,17.391917818806,17.4388344123328,
17.4839738011972,17.5299894371059,17.5763017108472,17.6209316820209,17.6676058954979,
17.7134384045876,17.7416164546727),.UNSPECIFIED.);
#3295=B_SPLINE_CURVE_WITH_KNOTS('',3,(#68232,#68233,#68234,#68235,#68236,
#68237,#68238,#68239,#68240,#68241,#68242,#68243,#68244,#68245,#68246,#68247,
#68248,#68249,#68250,#68251,#68252,#68253,#68254,#68255,#68256,#68257,#68258,
#68259,#68260,#68261,#68262,#68263,#68264,#68265,#68266,#68267),
 .UNSPECIFIED.,.F.,.F.,(4,2,2,2,2,2,2,2,2,2,2,2,2,2,2,2,2,4),(3.70124435567,
3.74399270352421,3.79043516379055,3.83649298289209,3.88175593971899,3.92880219425985,
3.97372113000247,4.01951325018307,4.0662546751028,4.11089815702418,4.15717909203302,
4.20358177465394,4.24870726106109,4.29560414076508,4.34067748019848,4.38633433906348,
4.43306819834531,4.44139309323576),.UNSPECIFIED.);
#3296=B_SPLINE_CURVE_WITH_KNOTS('',3,(#68272,#68273,#68274,#68275,#68276,
#68277,#68278,#68279,#68280,#68281,#68282,#68283,#68284,#68285,#68286,#68287,
#68288,#68289,#68290,#68291,#68292,#68293,#68294,#68295,#68296,#68297,#68298,
#68299,#68300,#68301,#68302,#68303,#68304,#68305,#68306,#68307),
 .UNSPECIFIED.,.F.,.F.,(4,2,2,2,2,2,2,2,2,2,2,2,2,2,2,2,2,4),(16.2641372477882,
16.2938030439013,16.3403922128616,16.3852327649267,16.4318876926505,16.4778418228271,
16.5224230010358,16.5690903677485,16.6145405429621,16.6597873151308,16.7064589317587,
16.7513738187352,16.7981669545333,16.8442036947422,16.8887271733991,16.9353636748532,
16.9809031318305,17.002935008964),.UNSPECIFIED.);
#3297=B_SPLINE_CURVE_WITH_KNOTS('',3,(#68308,#68309,#68310,#68311,#68312,
#68313,#68314,#68315,#68316,#68317,#68318,#68319,#68320,#68321,#68322,#68323,
#68324,#68325,#68326,#68327,#68328,#68329,#68330,#68331,#68332,#68333,#68334,
#68335,#68336,#68337,#68338,#68339,#68340,#68341,#68342,#68343),
 .UNSPECIFIED.,.F.,.F.,(4,2,2,2,2,2,2,2,2,2,2,2,2,2,2,2,2,4),(4.44139309323576,
4.47768369479005,4.52383758291686,4.57065155177945,4.61567630686354,4.66246297203597,
4.70776020748785,4.7533204420323,4.80007956137218,4.8447406734777,4.8908048094463,
4.93755248955131,4.98249808878681,5.02919719884178,5.0748218415068,5.12031038865077,
5.16760288129374,5.1818539671131),.UNSPECIFIED.);
#3298=B_SPLINE_CURVE_WITH_KNOTS('',3,(#68348,#68349,#68350,#68351,#68352,
#68353,#68354,#68355,#68356,#68357,#68358,#68359,#68360,#68361,#68362,#68363,
#68364,#68365,#68366,#68367,#68368,#68369,#68370,#68371,#68372,#68373,#68374,
#68375,#68376,#68377,#68378,#68379,#68380,#68381,#68382,#68383),
 .UNSPECIFIED.,.F.,.F.,(4,2,2,2,2,2,2,2,2,2,2,2,2,2,2,2,2,4),(15.5253008226521,
15.5614208712953,15.6076307463169,15.6521806514462,15.6988024510405,15.7445285973342,
15.7892808885852,15.8362633798431,15.8814623032694,15.9272761463232,15.9736600003967,
16.0183472154503,16.0650263145743,16.1109370835491,16.1556467547297,16.2028290254408,
16.2482129532865,16.2641372477882),.UNSPECIFIED.);
#3299=B_SPLINE_CURVE_WITH_KNOTS('',3,(#68384,#68385,#68386,#68387,#68388,
#68389,#68390,#68391,#68392,#68393,#68394,#68395,#68396,#68397,#68398,#68399,
#68400,#68401,#68402,#68403,#68404,#68405,#68406,#68407,#68408,#68409,#68410,
#68411,#68412,#68413,#68414,#68415,#68416,#68417,#68418,#68419),
 .UNSPECIFIED.,.F.,.F.,(4,2,2,2,2,2,2,2,2,2,2,2,2,2,2,2,2,4),(5.1818539671131,
5.21237880454505,5.258394968262,5.30515700825967,5.34994371692685,5.39643143835995,
5.44226233196025,5.48755936077848,5.53464520113254,5.57944804045745,5.62527291369698,
5.67197040786348,5.71660500923211,5.76291244064308,5.80904038797896,5.85417959966551,
5.90109443452282,5.92163532828753),.UNSPECIFIED.);
#3300=B_SPLINE_CURVE_WITH_KNOTS('',3,(#68424,#68425,#68426,#68427,#68428,
#68429,#68430,#68431,#68432,#68433,#68434,#68435,#68436,#68437,#68438,#68439,
#68440,#68441,#68442,#68443,#68444,#68445,#68446,#68447,#68448,#68449,#68450,
#68451,#68452,#68453,#68454,#68455,#68456,#68457,#68458,#68459),
 .UNSPECIFIED.,.F.,.F.,(4,2,2,2,2,2,2,2,2,2,2,2,2,2,2,2,2,4),(14.7873695620709,
14.8300506862385,14.8760153817406,14.9205240016754,14.9671371535707,15.0126019576596,
15.0576755801971,15.1043686547149,15.149301357282,15.1958140370104,15.2418832855322,
15.286374482974,15.3329751561295,15.3785518380475,15.4234279626835,15.4702466599603,
15.5152945505239,15.5253008226521),.UNSPECIFIED.);
#3301=B_SPLINE_CURVE_WITH_KNOTS('',3,(#68460,#68461,#68462,#68463,#68464,
#68465,#68466,#68467,#68468,#68469,#68470,#68471,#68472,#68473,#68474,#68475,
#68476,#68477,#68478,#68479,#68480,#68481,#68482,#68483,#68484,#68485,#68486,
#68487,#68488,#68489,#68490,#68491,#68492,#68493,#68494,#68495),
 .UNSPECIFIED.,.F.,.F.,(4,2,2,2,2,2,2,2,2,2,2,2,2,2,2,2,2,4),(5.92163532828753,
5.94600637034905,5.99167472503286,6.03834442621258,6.08290534138804,6.12906543193699,
6.17556776582538,6.22058468374404,6.26736631647045,6.31246290290152,6.358011917132,
6.40468792773244,6.44925237282631,6.4953007135921,6.54223498706927,6.58716711269207,
6.63385553062737,6.66068791027176),.UNSPECIFIED.);
#3302=B_SPLINE_CURVE_WITH_KNOTS('',3,(#68500,#68501,#68502,#68503,#68504,
#68505,#68506,#68507,#68508,#68509,#68510,#68511,#68512,#68513,#68514,#68515,
#68516,#68517,#68518,#68519,#68520,#68521,#68522,#68523,#68524,#68525,#68526,
#68527,#68528,#68529,#68530,#68531,#68532,#68533,#68534,#68535,#68536,#68537),
 .UNSPECIFIED.,.F.,.F.,(4,2,2,2,2,2,2,2,2,2,2,2,2,2,2,2,2,2,4),(14.0482100339955,
14.0502949245492,14.096984232057,14.142851009537,14.1876060347159,14.2347388331608,
14.2800782706825,14.3257899974572,14.3723273782223,14.41711976203,14.463762437258,
14.5096613573186,14.55425504223,14.6009122351073,14.6463049690835,14.6916352778898,
14.7382430334376,14.7830983471007,14.7873695620709),.UNSPECIFIED.);
#3303=B_SPLINE_CURVE_WITH_KNOTS('',3,(#68538,#68539,#68540,#68541,#68542,
#68543,#68544,#68545,#68546,#68547,#68548,#68549,#68550,#68551,#68552,#68553,
#68554,#68555,#68556,#68557,#68558,#68559,#68560,#68561,#68562,#68563,#68564,
#68565,#68566,#68567,#68568,#68569,#68570,#68571,#68572,#68573),
 .UNSPECIFIED.,.F.,.F.,(4,2,2,2,2,2,2,2,2,2,2,2,2,2,2,2,2,4),(6.66068791027176,
6.67919937428358,6.72466854077273,6.77138281680808,6.8160205136328,6.86199546468963,
6.90869606620136,6.95356006101863,7.00017259357045,7.04588152905359,7.09129151458587,
7.13849904618301,7.1832836822818,7.22922137847032,7.27595882272717,7.32067836819823,
7.3670926336791,7.40074313214862),.UNSPECIFIED.);
#3304=B_SPLINE_CURVE_WITH_KNOTS('',3,(#68578,#68579,#68580,#68581,#68582,
#68583,#68584,#68585,#68586,#68587,#68588,#68589,#68590,#68591,#68592,#68593,
#68594,#68595,#68596,#68597,#68598,#68599,#68600,#68601,#68602,#68603,#68604,
#68605,#68606,#68607,#68608,#68609,#68610,#68611,#68612,#68613),
 .UNSPECIFIED.,.F.,.F.,(4,2,2,2,2,2,2,2,2,2,2,2,2,2,2,2,2,4),(13.3095464675158,
13.3179418806692,13.3645829204745,13.4101456027589,13.4551345123131,13.5019343594699,
13.5469666402861,13.5932875705783,13.6394722908042,13.6840250076321,13.7306726518614,
13.7763692796775,13.8212020202917,13.8681498816812,13.9133183606713,13.9592929931832,
14.0056379903772,14.0482100339955),.UNSPECIFIED.);
#3305=B_SPLINE_CURVE_WITH_KNOTS('',3,(#68614,#68615,#68616,#68617,#68618,
#68619,#68620,#68621,#68622,#68623,#68624,#68625,#68626,#68627,#68628,#68629,
#68630,#68631,#68632,#68633,#68634,#68635,#68636,#68637,#68638,#68639,#68640,
#68641,#68642,#68643,#68644,#68645,#68646,#68647,#68648,#68649),
 .UNSPECIFIED.,.F.,.F.,(4,2,2,2,2,2,2,2,2,2,2,2,2,2,2,2,2,4),(7.40074313214862,
7.41304791193527,7.45828058796883,7.50529645981043,7.55014367964178,7.59590467610001,
7.64259365979734,7.68719438829927,7.73344217485688,7.77972977945611,7.82481959518803,
7.87168035903332,7.91667006179515,7.96229014337893,8.00896624300127,8.05352690669973,
8.09964223179755,8.13994719566162),.UNSPECIFIED.);
#3306=B_SPLINE_CURVE_WITH_KNOTS('',3,(#68654,#68655,#68656,#68657,#68658,
#68659,#68660,#68661,#68662,#68663,#68664,#68665,#68666,#68667,#68668,#68669,
#68670,#68671,#68672,#68673,#68674,#68675,#68676,#68677,#68678,#68679,#68680,
#68681,#68682,#68683,#68684,#68685,#68686,#68687,#68688,#68689),
 .UNSPECIFIED.,.F.,.F.,(4,2,2,2,2,2,2,2,2,2,2,2,2,2,2,2,2,4),(12.5705412100685,
12.5848546363202,12.6320513419363,12.6774479779185,12.7229914291377,12.7695957874756,
12.8144503148156,12.8611058709474,12.9070763074098,12.951650697705,12.9983178350321,
13.0437851961517,13.0889992823918,13.1356902587469,13.1806230630583,13.2273560115123,
13.2734149408359,13.3095464675158),.UNSPECIFIED.);
#3307=B_SPLINE_CURVE_WITH_KNOTS('',3,(#68690,#68691,#68692,#68693,#68694,
#68695,#68696,#68697,#68698,#68699,#68700,#68701,#68702,#68703,#68704,#68705,
#68706,#68707,#68708,#68709,#68710,#68711,#68712,#68713,#68714,#68715,#68716,
#68717,#68718,#68719,#68720,#68721,#68722,#68723,#68724,#68725,#68726,#68727),
 .UNSPECIFIED.,.F.,.F.,(4,2,2,2,2,2,2,2,2,2,2,2,2,2,2,2,2,2,4),(8.13994719566162,
8.1463316268328,8.19131496388372,8.2380593874591,8.28326280667136,8.33020598996195,
8.37537161294956,8.42146167930536,8.46779890512908,8.51245656585315,8.55916791039741,
8.60502388501555,8.64982522039719,8.69694438308839,8.7422725099988,8.78807715134522,
8.83459899420235,8.87937738670119,8.87958134265245),.UNSPECIFIED.);
#3308=B_SPLINE_CURVE_WITH_KNOTS('',3,(#68732,#68733,#68734,#68735,#68736,
#68737,#68738,#68739,#68740,#68741,#68742,#68743,#68744,#68745,#68746,#68747,
#68748,#68749,#68750,#68751,#68752,#68753,#68754,#68755,#68756,#68757,#68758,
#68759,#68760,#68761,#68762,#68763,#68764,#68765,#68766,#68767),
 .UNSPECIFIED.,.F.,.F.,(4,2,2,2,2,2,2,2,2,2,2,2,2,2,2,2,2,4),(11.8321815561307,
11.8527802750529,11.8996021687833,11.9446521456017,11.9907033317147,12.0369186139489,
12.0814657613186,12.1280739153687,12.1738072480122,12.2185277557899,12.2655192350349,
12.3107256977114,12.3564778448273,12.4028721237148,12.4475687949672,12.4942402335744,
12.5401634891127,12.5705412100685),.UNSPECIFIED.);
#3309=B_SPLINE_CURVE_WITH_KNOTS('',3,(#68768,#68769,#68770,#68771,#68772,
#68773,#68774,#68775,#68776,#68777,#68778,#68779,#68780,#68781,#68782,#68783,
#68784,#68785,#68786,#68787,#68788,#68789,#68790,#68791,#68792,#68793,#68794,
#68795,#68796,#68797,#68798,#68799,#68800,#68801,#68802,#68803),
 .UNSPECIFIED.,.F.,.F.,(4,2,2,2,2,2,2,2,2,2,2,2,2,2,2,2,2,4),(8.87958134265245,
8.92602852613987,8.97190922554665,9.01652860508801,9.06319528540556,9.10856829663463,
9.15396816684055,9.20055253946269,9.24538645185148,9.29245567553163,9.33839133852289,
9.38290947461184,9.42952391977244,9.47495799934766,9.52008834525836,9.56674688093536,
9.6116477128901,9.61793661341104),.UNSPECIFIED.);
#3310=B_SPLINE_CURVE_WITH_KNOTS('',3,(#68808,#68809,#68810,#68811,#68812,
#68813,#68814,#68815,#68816,#68817,#68818,#68819,#68820,#68821,#68822,#68823,
#68824,#68825,#68826,#68827,#68828,#68829,#68830,#68831,#68832,#68833,#68834,
#68835,#68836,#68837,#68838,#68839,#68840,#68841,#68842,#68843),
 .UNSPECIFIED.,.F.,.F.,(4,2,2,2,2,2,2,2,2,2,2,2,2,2,2,2,2,4),(11.0945157929649,
11.1213867420797,11.1679850354348,11.212830558321,11.2596899586864,11.3056487691199,
11.3501304725593,11.3967192229775,11.4421794409724,11.4871976310158,11.5338877382452,
11.5788167443302,11.6252436424475,11.6713128846608,11.7157888443594,11.7623703136435,
11.8079484981885,11.8321815561307),.UNSPECIFIED.);
#3311=B_SPLINE_CURVE_WITH_KNOTS('',3,(#68844,#68845,#68846,#68847,#68848,
#68849,#68850,#68851,#68852,#68853,#68854,#68855,#68856,#68857,#68858,#68859,
#68860,#68861,#68862,#68863,#68864,#68865,#68866,#68867,#68868,#68869,#68870,
#68871,#68872,#68873,#68874,#68875,#68876,#68877,#68878,#68879),
 .UNSPECIFIED.,.F.,.F.,(4,2,2,2,2,2,2,2,2,2,2,2,2,2,2,2,2,4),(9.61793661341104,
9.65826687912693,9.70429689093938,9.74877836477337,9.79537166131895,9.84090708321871,
9.88582218876157,9.93259567749554,9.97760169196064,10.0238180381891,10.0699792278232,
10.1144983947581,10.1611035398683,10.2067785301348,10.2515491657397,10.2984763720027,
10.3436239452287,10.3558181882677),.UNSPECIFIED.);
#3312=B_SPLINE_CURVE_WITH_KNOTS('',3,(#68884,#68885,#68886,#68887,#68888,
#68889,#68890,#68891,#68892,#68893,#68894,#68895,#68896,#68897,#68898,#68899,
#68900,#68901,#68902,#68903,#68904,#68905,#68906,#68907,#68908,#68909,#68910,
#68911,#68912,#68913,#68914,#68915,#68916,#68917,#68918,#68919),
 .UNSPECIFIED.,.F.,.F.,(4,2,2,2,2,2,2,2,2,2,2,2,2,2,2,2,2,4),(10.3558181865992,
10.3895062288278,10.4358326314552,10.4804680791543,10.5271205064737,10.5729708577389,
10.6176765737363,10.6647940480184,10.710117621532,10.7557512885806,10.8022746889798,
10.8470530120057,10.8936670905081,10.9395538338801,10.9841105681321,11.0307384394129,
11.0761201700909,11.0945157929649),.UNSPECIFIED.);
#3313=B_SPLINE_CURVE_WITH_KNOTS('',3,(#68920,#68921,#68922,#68923,#68924,
#68925,#68926,#68927,#68928,#68929,#68930,#68931,#68932,#68933,#68934,#68935,
#68936,#68937,#68938,#68939,#68940,#68941,#68942,#68943,#68944,#68945,#68946,
#68947,#68948,#68949,#68950,#68951,#68952,#68953,#68954,#68955),
 .UNSPECIFIED.,.F.,.F.,(4,2,2,2,2,2,2,2,2,2,2,2,2,2,2,2,2,4),(10.3558181882677,
10.3895062304569,10.4358326331012,10.4804680808162,10.5271205081509,10.572970859433,
10.6176765754436,10.6647940497431,10.7101176232735,10.7557512903329,10.8022746907493,
10.8470530137919,10.8936670923103,10.9395538356998,10.9841105699663,11.0307384412633,
11.0761201719588,11.0945157948807),.UNSPECIFIED.);
#3314=B_SPLINE_CURVE_WITH_KNOTS('',3,(#68960,#68961,#68962,#68963,#68964,
#68965,#68966,#68967,#68968,#68969,#68970,#68971,#68972,#68973,#68974,#68975,
#68976,#68977,#68978,#68979,#68980,#68981,#68982,#68983,#68984,#68985,#68986,
#68987,#68988,#68989,#68990,#68991,#68992,#68993,#68994,#68995),
 .UNSPECIFIED.,.F.,.F.,(4,2,2,2,2,2,2,2,2,2,2,2,2,2,2,2,2,4),(9.61793661197057,
9.65826687772365,9.7042968895204,9.74877836334091,9.79537165987244,9.84090708175655,
9.88582218728856,9.93259567600637,9.977601690456,10.0238180366761,10.069979226294,
10.1144983932143,10.16110353831,10.2067785285603,10.2515491641532,10.2984763703993,
10.3436239436092,10.3558181865992),.UNSPECIFIED.);
#3315=B_SPLINE_CURVE_WITH_KNOTS('',3,(#68996,#68997,#68998,#68999,#69000,
#69001,#69002,#69003,#69004,#69005,#69006,#69007,#69008,#69009,#69010,#69011,
#69012,#69013,#69014,#69015,#69016,#69017,#69018,#69019,#69020,#69021,#69022,
#69023,#69024,#69025,#69026,#69027,#69028,#69029,#69030,#69031),
 .UNSPECIFIED.,.F.,.F.,(4,2,2,2,2,2,2,2,2,2,2,2,2,2,2,2,2,4),(11.0945157948807,
11.1213867439599,11.1679850373331,11.2128305602366,11.2596899606121,11.3056487710637,
11.3501304745185,11.3967192249533,11.4421794429662,11.4871976330225,11.5338877402705,
11.5788167463733,11.625243644501,11.6713128867326,11.7157888464474,11.762370315748,
11.8079485003112,11.8321815583089),.UNSPECIFIED.);
#3316=B_SPLINE_CURVE_WITH_KNOTS('',3,(#69036,#69037,#69038,#69039,#69040,
#69041,#69042,#69043,#69044,#69045,#69046,#69047,#69048,#69049,#69050,#69051,
#69052,#69053,#69054,#69055,#69056,#69057,#69058,#69059,#69060,#69061,#69062,
#69063,#69064,#69065,#69066,#69067,#69068,#69069,#69070,#69071),
 .UNSPECIFIED.,.F.,.F.,(4,2,2,2,2,2,2,2,2,2,2,2,2,2,2,2,2,4),(8.87958134142251,
8.92602852493827,8.97190922433066,9.01652860386053,9.06319528416507,9.10856829537987,
9.15396816557657,9.20055253818396,9.24538645055861,9.29245567423173,9.33839133720815,
9.38290947328484,9.42952391843202,9.47495799799238,9.5200883438932,9.56674687955462,
9.61164771149445,9.61793661197057),.UNSPECIFIED.);
#3317=B_SPLINE_CURVE_WITH_KNOTS('',3,(#69072,#69073,#69074,#69075,#69076,
#69077,#69078,#69079,#69080,#69081,#69082,#69083,#69084,#69085,#69086,#69087,
#69088,#69089,#69090,#69091,#69092,#69093,#69094,#69095,#69096,#69097,#69098,
#69099,#69100,#69101,#69102,#69103,#69104,#69105,#69106,#69107),
 .UNSPECIFIED.,.F.,.F.,(4,2,2,2,2,2,2,2,2,2,2,2,2,2,2,2,2,4),(11.8321815583089,
11.8527802771891,11.8996021709384,11.9446521477749,11.9907033338989,12.0369186161519,
12.0814657635389,12.128073917606,12.1738072502682,12.2185277580605,12.2655192373249,
12.31072570002,12.3564778471481,12.402872126055,12.4475687973262,12.4942402359512,
12.5401634915089,12.5705412125212),.UNSPECIFIED.);
#3318=B_SPLINE_CURVE_WITH_KNOTS('',3,(#69112,#69113,#69114,#69115,#69116,
#69117,#69118,#69119,#69120,#69121,#69122,#69123,#69124,#69125,#69126,#69127,
#69128,#69129,#69130,#69131,#69132,#69133,#69134,#69135,#69136,#69137,#69138,
#69139,#69140,#69141,#69142,#69143,#69144,#69145,#69146,#69147,#69148,#69149),
 .UNSPECIFIED.,.F.,.F.,(4,2,2,2,2,2,2,2,2,2,2,2,2,2,2,2,2,2,4),(8.13994719462425,
8.14633162583834,8.19131496287961,8.23805938644507,8.28326280564246,8.33020598891935,
8.37537161189387,8.42146167824292,8.46779890405304,8.51245656476452,8.55916790929672,
8.60502388390122,8.64982521927269,8.69694438194964,8.74227250884644,8.78807715018487,
8.83459899302762,8.87937738551268,8.87958134142251),.UNSPECIFIED.);
#3319=B_SPLINE_CURVE_WITH_KNOTS('',3,(#69150,#69151,#69152,#69153,#69154,
#69155,#69156,#69157,#69158,#69159,#69160,#69161,#69162,#69163,#69164,#69165,
#69166,#69167,#69168,#69169,#69170,#69171,#69172,#69173,#69174,#69175,#69176,
#69177,#69178,#69179,#69180,#69181,#69182,#69183,#69184,#69185),
 .UNSPECIFIED.,.F.,.F.,(4,2,2,2,2,2,2,2,2,2,2,2,2,2,2,2,2,4),(12.5705412125212,
12.5848546387325,12.6320513443688,12.6774479803703,12.7229914316032,12.7695957899609,
12.81445031732,12.8611058734703,12.9070763099523,12.9516507002645,12.99831783761,
13.0437851987491,13.0889992850039,13.1356902613794,13.1806230657103,13.2273560141773,
13.2734149435215,13.3095464702606),.UNSPECIFIED.);
#3320=B_SPLINE_CURVE_WITH_KNOTS('',3,(#69190,#69191,#69192,#69193,#69194,
#69195,#69196,#69197,#69198,#69199,#69200,#69201,#69202,#69203,#69204,#69205,
#69206,#69207,#69208,#69209,#69210,#69211,#69212,#69213,#69214,#69215,#69216,
#69217,#69218,#69219,#69220,#69221,#69222,#69223,#69224,#69225),
 .UNSPECIFIED.,.F.,.F.,(4,2,2,2,2,2,2,2,2,2,2,2,2,2,2,2,2,4),(7.4007431312885,
7.41304791111891,7.45828058714382,7.50529645897655,7.55014367879521,7.59590467524459,
7.64259365893083,7.68719438742294,7.73344217397141,7.7797297785534,7.82481959427612,
7.87168035811193,7.91667006085986,7.96229014243438,8.00896624204524,8.05352690573283,
8.09964223082121,8.13994719462425),.UNSPECIFIED.);
#3321=B_SPLINE_CURVE_WITH_KNOTS('',3,(#69226,#69227,#69228,#69229,#69230,
#69231,#69232,#69233,#69234,#69235,#69236,#69237,#69238,#69239,#69240,#69241,
#69242,#69243,#69244,#69245,#69246,#69247,#69248,#69249,#69250,#69251,#69252,
#69253,#69254,#69255,#69256,#69257,#69258,#69259,#69260,#69261),
 .UNSPECIFIED.,.F.,.F.,(4,2,2,2,2,2,2,2,2,2,2,2,2,2,2,2,2,4),(13.3095464702606,
13.317941883373,13.3645829231975,13.4101456055024,13.4551345150724,13.5019343622502,
13.5469666430868,13.5932875733925,13.6394722936394,13.6840250104865,13.7306726547352,
13.7763692825722,13.8212020232032,13.8681498846145,13.9133183636254,13.9592929961519,
14.0056379933677,14.0482100370503),.UNSPECIFIED.);
#3322=B_SPLINE_CURVE_WITH_KNOTS('',3,(#69266,#69267,#69268,#69269,#69270,
#69271,#69272,#69273,#69274,#69275,#69276,#69277,#69278,#69279,#69280,#69281,
#69282,#69283,#69284,#69285,#69286,#69287,#69288,#69289,#69290,#69291,#69292,
#69293,#69294,#69295,#69296,#69297,#69298,#69299,#69300,#69301),
 .UNSPECIFIED.,.F.,.F.,(4,2,2,2,2,2,2,2,2,2,2,2,2,2,2,2,2,4),(6.66068790957161,
6.67919937362265,6.72466854010414,6.77138281612983,6.81602051294445,6.86199546399339,
6.90869606549543,6.95356006030469,7.00017259284827,7.04588152831696,7.09129151384102,
7.13849904542972,7.18328368151711,7.22922137769738,7.27595882194379,7.32067836740631,
7.36709263287862,7.4007431312885),.UNSPECIFIED.);
#3323=B_SPLINE_CURVE_WITH_KNOTS('',3,(#69302,#69303,#69304,#69305,#69306,
#69307,#69308,#69309,#69310,#69311,#69312,#69313,#69314,#69315,#69316,#69317,
#69318,#69319,#69320,#69321,#69322,#69323,#69324,#69325,#69326,#69327,#69328,
#69329,#69330,#69331,#69332,#69333,#69334,#69335,#69336,#69337,#69338,#69339),
 .UNSPECIFIED.,.F.,.F.,(4,2,2,2,2,2,2,2,2,2,2,2,2,2,2,2,2,2,4),(14.0482100370503,
14.0502949275604,14.0969842350884,14.1428510125903,14.1876060377872,14.2347388362546,
14.2800782737978,14.3257900005883,14.3723273813755,14.4171197652046,14.4637624404534,
14.5096613605359,14.5542550454664,14.6009122383646,14.6463049723626,14.6916352811859,
14.7382430367566,14.7830983504416,14.7873695654535),.UNSPECIFIED.);
#3324=B_SPLINE_CURVE_WITH_KNOTS('',3,(#69344,#69345,#69346,#69347,#69348,
#69349,#69350,#69351,#69352,#69353,#69354,#69355,#69356,#69357,#69358,#69359,
#69360,#69361,#69362,#69363,#69364,#69365,#69366,#69367,#69368,#69369,#69370,
#69371,#69372,#69373,#69374,#69375,#69376,#69377,#69378,#69379),
 .UNSPECIFIED.,.F.,.F.,(4,2,2,2,2,2,2,2,2,2,2,2,2,2,2,2,2,4),(5.92163532773223,
5.94600636983764,5.99167472451486,6.03834442568581,6.08290534085326,6.12906543139539,
6.17556776526837,6.22058468317993,6.26736631589905,6.31246290231792,6.35801191654115,
6.40468792713218,6.44925237221679,6.49530071297518,6.5422349864363,6.58716711205166,
6.6338555299793,6.66068790957161),.UNSPECIFIED.);
#3325=B_SPLINE_CURVE_WITH_KNOTS('',3,(#69380,#69381,#69382,#69383,#69384,
#69385,#69386,#69387,#69388,#69389,#69390,#69391,#69392,#69393,#69394,#69395,
#69396,#69397,#69398,#69399,#69400,#69401,#69402,#69403,#69404,#69405,#69406,
#69407,#69408,#69409,#69410,#69411,#69412,#69413,#69414,#69415),
 .UNSPECIFIED.,.F.,.F.,(4,2,2,2,2,2,2,2,2,2,2,2,2,2,2,2,2,4),(14.7873695654535,
14.8300506895943,14.8760153851188,14.9205240050731,14.9671371569893,15.0126019611003,
15.057675583655,15.1043686581955,15.1493013607845,15.1958140405279,15.2418832890724,
15.2863744865348,15.3329751597116,15.3785518416522,15.4234279663063,15.4702466636066,
15.5152945541928,15.52530082637),.UNSPECIFIED.);
#3326=B_SPLINE_CURVE_WITH_KNOTS('',3,(#69420,#69421,#69422,#69423,#69424,
#69425,#69426,#69427,#69428,#69429,#69430,#69431,#69432,#69433,#69434,#69435,
#69436,#69437,#69438,#69439,#69440,#69441,#69442,#69443,#69444,#69445,#69446,
#69447,#69448,#69449,#69450,#69451,#69452,#69453,#69454,#69455),
 .UNSPECIFIED.,.F.,.F.,(4,2,2,2,2,2,2,2,2,2,2,2,2,2,2,2,2,4),(5.18185396668694,
5.21237880416024,5.25839496787151,5.30515700786141,5.34994371652288,5.39643143795004,
5.44226233153737,5.48755936034949,5.53464520069729,5.57944804001234,5.62527291324563,
5.6719704074037,5.71660500876536,5.76291244016987,5.80904038749152,5.85417959917163,
5.90109443402236,5.92163532773223),.UNSPECIFIED.);
#3327=B_SPLINE_CURVE_WITH_KNOTS('',3,(#69456,#69457,#69458,#69459,#69460,
#69461,#69462,#69463,#69464,#69465,#69466,#69467,#69468,#69469,#69470,#69471,
#69472,#69473,#69474,#69475,#69476,#69477,#69478,#69479,#69480,#69481,#69482,
#69483,#69484,#69485,#69486,#69487,#69488,#69489,#69490,#69491),
 .UNSPECIFIED.,.F.,.F.,(4,2,2,2,2,2,2,2,2,2,2,2,2,2,2,2,2,4),(15.52530082637,
15.5614208749801,15.6076307500252,15.6521806551763,15.6988024547926,15.7445286011097,
15.7892808923799,15.8362633836619,15.8814623071114,15.927276150182,15.9736600042795,
16.0183472193562,16.0650263185026,16.1109370875013,16.1556467587023,16.2028290294383,
16.2482129573077,16.2641372518591),.UNSPECIFIED.);
#3328=B_SPLINE_CURVE_WITH_KNOTS('',3,(#69496,#69497,#69498,#69499,#69500,
#69501,#69502,#69503,#69504,#69505,#69506,#69507,#69508,#69509,#69510,#69511,
#69512,#69513,#69514,#69515,#69516,#69517,#69518,#69519,#69520,#69521,#69522,
#69523,#69524,#69525,#69526,#69527,#69528,#69529,#69530,#69531),
 .UNSPECIFIED.,.F.,.F.,(4,2,2,2,2,2,2,2,2,2,2,2,2,2,2,2,2,4),(4.44139309291887,
4.4776836945143,4.52383758263681,4.5706515514869,4.61567630656631,4.66246297173395,
4.70776020717613,4.75332044171567,4.80007956104877,4.84474067314722,4.89080480911077,
4.93755248920882,4.9824980884388,5.02919719848812,5.0748218411417,5.12031038828011,
5.16760288091741,5.18185396668694),.UNSPECIFIED.);
#3329=B_SPLINE_CURVE_WITH_KNOTS('',3,(#69532,#69533,#69534,#69535,#69536,
#69537,#69538,#69539,#69540,#69541,#69542,#69543,#69544,#69545,#69546,#69547,
#69548,#69549,#69550,#69551,#69552,#69553,#69554,#69555,#69556,#69557,#69558,
#69559,#69560,#69561,#69562,#69563,#69564,#69565,#69566,#69567),
 .UNSPECIFIED.,.F.,.F.,(4,2,2,2,2,2,2,2,2,2,2,2,2,2,2,2,2,4),(16.2641372518591,
16.2938030479407,16.3403922169256,16.3852327690144,16.4318876967614,16.4778418269624,
16.5224230051924,16.5690903719281,16.6145405471659,16.6597873193538,16.7064589360066,
16.7513738230071,16.7981669588227,16.8442036990566,16.8887271777361,16.9353636792139,
16.9809031362162,17.002935013404),.UNSPECIFIED.);
#3330=B_SPLINE_CURVE_WITH_KNOTS('',3,(#69572,#69573,#69574,#69575,#69576,
#69577,#69578,#69579,#69580,#69581,#69582,#69583,#69584,#69585,#69586,#69587,
#69588,#69589,#69590,#69591,#69592,#69593,#69594,#69595,#69596,#69597,#69598,
#69599,#69600,#69601,#69602,#69603,#69604,#69605,#69606,#69607),
 .UNSPECIFIED.,.F.,.F.,(4,2,2,2,2,2,2,2,2,2,2,2,2,2,2,2,2,4),(3.70124435544509,
3.74399270334172,3.79043516360456,3.83649298269546,3.88175593951858,3.92880219405563,
3.97372112979052,4.0195132499672,4.06625467488101,4.11089815679736,4.15717909180209,
4.20358177441128,4.24870726081431,4.29560414051408,4.34067747993884,4.38633433879972,
4.43306819807542,4.44139309291887),.UNSPECIFIED.);
#3331=B_SPLINE_CURVE_WITH_KNOTS('',3,(#69608,#69609,#69610,#69611,#69612,
#69613,#69614,#69615,#69616,#69617,#69618,#69619,#69620,#69621,#69622,#69623,
#69624,#69625,#69626,#69627,#69628,#69629,#69630,#69631,#69632,#69633,#69634,
#69635,#69636,#69637,#69638,#69639,#69640,#69641,#69642,#69643),
 .UNSPECIFIED.,.F.,.F.,(4,2,2,2,2,2,2,2,2,2,2,2,2,2,2,2,2,4),(17.002935013404,
17.025915911193,17.072690284077,17.1176989140485,17.1640720123954,17.2102290691703,
17.2547667681474,17.3014047938411,17.3470724921718,17.3919178234011,17.4388344169549,
17.4839738058451,17.5299894417733,17.576301715541,17.6209316867396,17.6676059002416,
17.7134384093576,17.7416164595014),.UNSPECIFIED.);
#3332=B_SPLINE_CURVE_WITH_KNOTS('',3,(#69648,#69649,#69650,#69651,#69652,
#69653,#69654,#69655,#69656,#69657,#69658,#69659,#69660,#69661,#69662,#69663,
#69664,#69665,#69666,#69667,#69668,#69669,#69670,#69671,#69672,#69673,#69674,
#69675,#69676,#69677,#69678,#69679,#69680,#69681,#69682,#69683,#69684,#69685),
 .UNSPECIFIED.,.F.,.F.,(4,2,2,2,2,2,2,2,2,2,2,2,2,2,2,2,2,2,4),(2.96056667091537,
2.96492507829847,3.00987622737974,3.05658369104791,3.10200096701632,3.14749048096761,
3.19424386881459,3.23892780451988,3.28492439294727,3.33166335850067,3.37655065295563,
3.42318675502558,3.46898366955253,3.51441887445073,3.56165143914983,3.60649480353247,
3.65245839303867,3.69924258599329,3.70124435544509),.UNSPECIFIED.);
#3333=B_SPLINE_CURVE_WITH_KNOTS('',3,(#69686,#69687,#69688,#69689,#69690,
#69691,#69692,#69693,#69694,#69695,#69696,#69697,#69698,#69699,#69700,#69701,
#69702,#69703,#69704,#69705,#69706,#69707,#69708,#69709,#69710,#69711,#69712,
#69713,#69714,#69715,#69716,#69717,#69718,#69719,#69720,#69721),
 .UNSPECIFIED.,.F.,.F.,(4,2,2,2,2,2,2,2,2,2,2,2,2,2,2,2,2,4),(17.7416164595014,
17.7581937074056,17.8052897716113,17.8505949597077,17.8963342553297,17.9428341521077,
17.9875910389412,18.0342105229933,18.0800707772756,18.1246525565008,18.1712871874809,
18.216640662327,18.2619848096412,18.3085503980356,18.3533657933236,18.400359214998,
18.4462787969036,18.4801374068086),.UNSPECIFIED.);
#3334=B_SPLINE_CURVE_WITH_KNOTS('',3,(#69726,#69727,#69728,#69729,#69730,
#69731,#69732,#69733,#69734,#69735,#69736,#69737,#69738,#69739,#69740,#69741,
#69742,#69743,#69744,#69745,#69746,#69747,#69748,#69749,#69750,#69751,#69752,
#69753,#69754,#69755,#69756,#69757,#69758,#69759,#69760,#69761),
 .UNSPECIFIED.,.F.,.F.,(4,2,2,2,2,2,2,2,2,2,2,2,2,2,2,2,2,4),(2.22108960842022,
2.23120408651738,2.27635041765121,2.32327161202571,2.36823721236016,2.41391337632635,
2.46061197044848,2.50519713944098,2.5513666691269,2.59796482409036,2.64299465164124,
2.68978881468655,2.73495033646277,2.78051325751773,2.82722340795193,2.87182391070409,
2.91788757577027,2.96056667091537),.UNSPECIFIED.);
#3335=B_SPLINE_CURVE_WITH_KNOTS('',3,(#69762,#69763,#69764,#69765,#69766,
#69767,#69768,#69769,#69770,#69771,#69772,#69773,#69774,#69775,#69776,#69777,
#69778,#69779,#69780,#69781,#69782,#69783,#69784,#69785,#69786,#69787,#69788,
#69789,#69790,#69791,#69792,#69793,#69794,#69795,#69796,#69797),
 .UNSPECIFIED.,.F.,.F.,(4,2,2,2,2,2,2,2,2,2,2,2,2,2,2,2,2,4),(18.4801374068086,
18.4907658387484,18.5373515732759,18.5827705496792,18.6278503876037,18.6744946287827,
18.7193811593225,18.7659288080364,18.8119468422919,18.8564049604675,18.9029730562544,
18.9484976039111,18.9933693909541,19.040132859827,19.0851285827534,19.1312801378602,
19.1774331259836,19.2175408345414),.UNSPECIFIED.);
#3336=B_SPLINE_CURVE_WITH_KNOTS('',3,(#69802,#69803,#69804,#69805,#69806,
#69807,#69808,#69809,#69810,#69811,#69812,#69813,#69814,#69815,#69816,#69817,
#69818,#69819,#69820,#69821,#69822,#69823,#69824,#69825,#69826,#69827,#69828,
#69829,#69830,#69831,#69832,#69833,#69834,#69835,#69836,#69837),
 .UNSPECIFIED.,.F.,.F.,(4,2,2,2,2,2,2,2,2,2,2,2,2,2,2,2,2,4),(1.48067239643092,
1.4967132601331,1.54219831559389,1.58948594493822,1.63428944893559,1.68030245144475,
1.72708174969294,1.77186789841824,1.81835464146151,1.86425678939566,1.90955548629973,
1.95664189807863,2.00148568451759,2.04731268579268,2.09403346709215,2.13867975716629,
2.18499121798638,2.22108960842022),.UNSPECIFIED.);
#3337=B_SPLINE_CURVE_WITH_KNOTS('',3,(#69838,#69839,#69840,#69841,#69842,
#69843,#69844,#69845,#69846,#69847,#69848,#69849,#69850,#69851,#69852,#69853,
#69854,#69855,#69856,#69857,#69858,#69859,#69860,#69861,#69862,#69863,#69864,
#69865,#69866,#69867,#69868,#69869,#69870,#69871,#69872,#69873,#69874,#69875),
 .UNSPECIFIED.,.F.,.F.,(4,2,2,2,2,2,2,2,2,2,2,2,2,2,2,2,2,2,4),(19.2175408345414,
19.221937402198,19.2685210781433,19.3141891434761,19.3589248273872,19.4058460255822,
19.4509870795851,19.4968133821774,19.5431350562803,19.5877640969252,19.634399062382,
19.6802461572256,19.724925976838,19.7720412018952,19.81736181445,19.862949655886,
19.9094715921544,19.954248074309,19.955968047547),.UNSPECIFIED.);
#3338=B_SPLINE_CURVE_WITH_KNOTS('',3,(#69880,#69881,#69882,#69883,#69884,
#69885,#69886,#69887,#69888,#69889,#69890,#69891,#69892,#69893,#69894,#69895,
#69896,#69897,#69898,#69899,#69900,#69901,#69902,#69903,#69904,#69905,#69906,
#69907,#69908,#69909,#69910,#69911,#69912,#69913,#69914,#69915),
 .UNSPECIFIED.,.F.,.F.,(4,2,2,2,2,2,2,2,2,2,2,2,2,2,2,2,2,4),(0.740262878330326,
0.76242710224918,0.808069985435835,0.854808846306471,0.899429812602798,
0.94557087207502,0.992454683252572,1.03747065149212,1.08424743872217,1.12958660658263,
1.17513888970271,1.22190780151563,1.26658471045133,1.31264188423565,1.35939848502835,
1.40433922056887,1.45103260194552,1.48067239643092),.UNSPECIFIED.);
#3339=B_SPLINE_CURVE_WITH_KNOTS('',3,(#69916,#69917,#69918,#69919,#69920,
#69921,#69922,#69923,#69924,#69925,#69926,#69927,#69928,#69929,#69930,#69931,
#69932,#69933,#69934,#69935,#69936,#69937,#69938,#69939,#69940,#69941,#69942,
#69943,#69944,#69945,#69946,#69947,#69948,#69949,#69950,#69951),
 .UNSPECIFIED.,.F.,.F.,(4,2,2,2,2,2,2,2,2,2,2,2,2,2,2,2,2,4),(19.955968047547,
20.000850484569,20.0467368471769,20.0912761893499,20.1378918513278,20.1832739357276,
20.2285046069091,20.2751045193351,20.3199511150685,20.3667546312751,20.4127173706803,
20.4571887517883,20.5037686958299,20.5492336722642,20.5942218827244,20.6409180673264,
20.685852328368,20.6936878782319),.UNSPECIFIED.);
#3340=B_SPLINE_CURVE_WITH_KNOTS('',3,(#69956,#69957,#69958,#69959,#69960,
#69961,#69962,#69963,#69964,#69965,#69966,#69967,#69968,#69969,#69970,#69971,
#69972,#69973,#69974,#69975,#69976,#69977,#69978,#69979,#69980,#69981,#69982,
#69983,#69984,#69985,#69986,#69987,#69988,#69989,#69990,#69991),
 .UNSPECIFIED.,.F.,.F.,(4,2,2,2,2,2,2,2,2,2,2,2,2,2,2,2,2,4),(1.00000014275486E-6,
0.0364903991724837,0.0742057368406976,0.120984278386942,0.16571626048475,
0.212135354717781,0.258243398985401,0.303486376623694,0.350510827495094,
0.395451299112592,0.441223703714196,0.487964967575798,0.532602258878132,
0.578864855190162,0.62532910035835,0.67044002179057,0.717320863587734,0.740262878330326),
 .UNSPECIFIED.);
#3341=B_SPLINE_CURVE_WITH_KNOTS('',3,(#69992,#69993,#69994,#69995,#69996,
#69997,#69998,#69999,#70000,#70001,#70002,#70003,#70004,#70005,#70006,#70007,
#70008,#70009,#70010,#70011,#70012,#70013,#70014,#70015,#70016,#70017,#70018,
#70019,#70020,#70021,#70022,#70023,#70024,#70025,#70026,#70027),
 .UNSPECIFIED.,.F.,.F.,(4,2,2,2,2,2,2,2,2,2,2,2,2,2,2,2,2,4),(20.6936878782319,
20.732228532913,20.778305724133,20.8227795112891,20.8693557797099,20.9149428959302,
20.9597524918607,21.0065846919771,21.0516438918501,21.0976519462771,21.1438788857884,
21.188432480541,21.2350393010027,21.2807854645354,21.325492530929,21.3724982961973,
21.417717731441,21.4315064083924),.UNSPECIFIED.);
#3342=B_SPLINE_CURVE_WITH_KNOTS('',3,(#70030,#70031,#70032,#70033,#70034,
#70035,#70036,#70037),.UNSPECIFIED.,.F.,.F.,(4,2,2,4),(21.4315064083924,
21.4634358005757,21.493031868375,21.522626598838),.UNSPECIFIED.);
#3343=B_SPLINE_CURVE_WITH_KNOTS('',3,(#70042,#70043,#70044,#70045,#70046,
#70047,#70048,#70049,#70050,#70051,#70052,#70053),.UNSPECIFIED.,.F.,.F.,
(4,2,2,2,2,4),(-0.220493779628296,-0.188155373461082,-0.153829429857051,
-0.103952453260852,-0.0536656706932583,-1.00000014990886E-6),
 .UNSPECIFIED.);
#3344=B_SPLINE_CURVE_WITH_KNOTS('',3,(#70056,#70057,#70058,#70059,#70060,
#70061,#70062,#70063,#70064,#70065,#70066,#70067,#70068,#70069,#70070,#70071,
#70072,#70073,#70074,#70075,#70076,#70077),.UNSPECIFIED.,.F.,.F.,(4,2,2,
2,2,2,2,2,2,2,4),(0.203440126186273,0.213167596868103,0.241856386112924,
0.272211919544501,0.305118112000406,0.341399456620154,0.378879659132554,
0.40534149334872,0.429291364608543,0.44378295238274,0.459192789470913),
 .UNSPECIFIED.);
#3345=B_SPLINE_CURVE_WITH_KNOTS('',3,(#70079,#70080,#70081,#70082,#70083,
#70084,#70085,#70086,#70087,#70088,#70089,#70090,#70091,#70092,#70093,#70094,
#70095,#70096,#70097,#70098,#70099,#70100,#70101,#70102,#70103,#70104,#70105,
#70106,#70107,#70108,#70109,#70110,#70111,#70112),.UNSPECIFIED.,.F.,.F.,
(4,2,2,2,2,2,2,2,2,2,2,2,2,2,2,2,4),(-0.921606618540025,-0.872688627355351,
-0.813612023857313,-0.756611351546357,-0.69692945872276,-0.638499761548747,
-0.581118209737007,-0.521076231967445,-0.463317306881228,-0.4044438926574,
-0.345164740388026,-0.288053249414949,-0.228344796882901,-0.169710130792356,
-0.112479424024743,-0.0563089256119929,-9.99999990258793E-7),
 .UNSPECIFIED.);
#3346=B_SPLINE_CURVE_WITH_KNOTS('',3,(#70113,#70114,#70115,#70116,#70117,
#70118,#70119,#70120,#70121,#70122,#70123,#70124,#70125,#70126,#70127,#70128,
#70129,#70130,#70131,#70132,#70133,#70134,#70135,#70136,#70137,#70138,#70139,
#70140,#70141,#70142,#70143,#70144),.UNSPECIFIED.,.F.,.F.,(4,2,2,2,2,2,
2,2,2,2,2,2,2,2,2,4),(-27.2675995337344,-27.2205810783644,-27.1716030839864,
-27.1114524980469,-27.0544959346273,-26.9959799991961,-26.9364896777515,
-26.8795127522937,-26.8203565510693,-26.7619639947482,-26.7043369916545,
-26.6444247756288,-26.5873734790364,-26.5290771329393,-26.4696302887724,
-26.4647006629411),.UNSPECIFIED.);
#3347=B_SPLINE_CURVE_WITH_KNOTS('',3,(#70321,#70322,#70323,#70324,#70325,
#70326,#70327,#70328),.UNSPECIFIED.,.F.,.F.,(4,2,2,4),(-0.00426615559741139,
-0.00353262795509977,-0.00302253710286643,-0.00251244625063308),
 .UNSPECIFIED.);
#3348=B_SPLINE_CURVE_WITH_KNOTS('',3,(#71242,#71243,#71244,#71245,#71246,
#71247,#71248,#71249),.UNSPECIFIED.,.F.,.F.,(4,2,2,4),(-0.00251244625063308,
-0.00200235539839974,-0.0014922645461664,-0.000758736903856822),
 .UNSPECIFIED.);
#3349=B_SPLINE_CURVE_WITH_KNOTS('',3,(#71254,#71255,#71256,#71257,#71258,
#71259,#71260,#71261),.UNSPECIFIED.,.F.,.F.,(4,2,2,4),(-0.00932716297425779,
-0.00859363533194745,-0.0080835444797141,-0.00757345362748076),
 .UNSPECIFIED.);
#3350=B_SPLINE_CURVE_WITH_KNOTS('',3,(#72175,#72176,#72177,#72178,#72179,
#72180,#72181,#72182),.UNSPECIFIED.,.F.,.F.,(4,2,2,4),(-0.00757345362748076,
-0.00706336277524741,-0.00655327192301407,-0.00581974428070595),
 .UNSPECIFIED.);
#3351=B_SPLINE_CURVE_WITH_KNOTS('',3,(#74178,#74179,#74180,#74181,#74182,
#74183,#74184,#74185,#74186,#74187,#74188,#74189,#74190,#74191,#74192,#74193,
#74194,#74195,#74196,#74197,#74198,#74199,#74200,#74201,#74202,#74203,#74204,
#74205),.UNSPECIFIED.,.F.,.F.,(4,2,2,2,2,2,2,2,2,2,2,2,2,4),(1.00000052656661E-6,
0.0405527857266322,0.0799421814660319,0.1262631587317,0.186952165234641,
0.270820823781497,0.348937293245129,0.459507052180891,0.623823282878412,
0.790896670749941,0.927459468885873,1.05843758188768,1.16179395572833,1.24835467272154),
 .UNSPECIFIED.);
#3362=SHAPE_REPRESENTATION_RELATIONSHIP('SRR','None',#75375,#3370);
#3370=ADVANCED_BREP_SHAPE_REPRESENTATION('',(#3386),#75335);
#3378=STYLED_ITEM('',(#75419),#3386);
#3386=MANIFOLD_SOLID_BREP('Body1',#32028);
#3398=FACE_BOUND('',#8360,.T.);
#3399=FACE_BOUND('',#8365,.T.);
#4115=CIRCLE('',#34959,1.5);
#4116=CIRCLE('',#34960,1.5);
#4117=CIRCLE('',#34989,1.17524047358084);
#4118=CIRCLE('',#34991,1.17524047358084);
#4119=CIRCLE('',#35022,1.1752404735812);
#4120=CIRCLE('',#35024,1.17524047358084);
#4121=CIRCLE('',#35025,1.5);
#4122=CIRCLE('',#35073,1.55162884844711);
#4123=CIRCLE('',#35075,2.61372936963188);
#4124=CIRCLE('',#35076,0.0468749999999982);
#4125=CIRCLE('',#35077,2.58058373926377);
#4126=CIRCLE('',#35079,2.73627063036812);
#4127=CIRCLE('',#35081,2.73627063036812);
#4128=CIRCLE('',#35083,2.73627063036812);
#4129=CIRCLE('',#35085,2.73627063036812);
#4130=CIRCLE('',#35087,2.73627063036812);
#4131=CIRCLE('',#35089,2.73627063036812);
#4132=CIRCLE('',#35091,2.73627063036812);
#4133=CIRCLE('',#35093,2.73627063036812);
#4134=CIRCLE('',#35095,2.73627063036812);
#4135=CIRCLE('',#35097,2.73627063036812);
#4136=CIRCLE('',#35099,2.73627063036812);
#4137=CIRCLE('',#35101,2.73627063036812);
#4138=CIRCLE('',#35103,2.73627063036812);
#4139=CIRCLE('',#35105,2.73627063036812);
#4140=CIRCLE('',#35107,2.73627063036812);
#4141=CIRCLE('',#35109,2.73627063036812);
#4142=CIRCLE('',#35111,2.73627063036812);
#4143=CIRCLE('',#35113,2.73627063036812);
#4144=CIRCLE('',#35115,2.73627063036812);
#4145=CIRCLE('',#35117,2.73627063036812);
#4146=CIRCLE('',#35119,2.73627063036812);
#4147=CIRCLE('',#35121,2.73627063036812);
#4148=CIRCLE('',#35123,2.73627063036812);
#4149=CIRCLE('',#35125,2.73627063036812);
#4150=CIRCLE('',#35127,2.73627063036812);
#4151=CIRCLE('',#35129,2.73627063036812);
#4152=CIRCLE('',#35131,2.73627063036812);
#4153=CIRCLE('',#35133,2.73627063036812);
#4154=CIRCLE('',#35135,2.73627063036812);
#4155=CIRCLE('',#35137,2.73627063036812);
#4156=CIRCLE('',#35139,2.73627063036812);
#4157=CIRCLE('',#35141,2.73627063036812);
#4158=CIRCLE('',#35143,2.73627063036812);
#4159=CIRCLE('',#35145,2.73627063036812);
#4160=CIRCLE('',#35147,2.73627063036812);
#4161=CIRCLE('',#35149,2.73627063036812);
#4162=CIRCLE('',#35151,2.73627063036812);
#4163=CIRCLE('',#35153,2.73627063036812);
#4164=CIRCLE('',#35155,2.73627063036812);
#4165=CIRCLE('',#35157,2.73627063036812);
#4166=CIRCLE('',#35159,2.73627063036812);
#4167=CIRCLE('',#35161,2.73627063036812);
#4168=CIRCLE('',#35163,2.73627063036812);
#4169=CIRCLE('',#35165,2.73627063036812);
#4170=CIRCLE('',#35167,2.73627063036812);
#4171=CIRCLE('',#35169,2.73627063036812);
#4172=CIRCLE('',#35170,2.73627063036812);
#4173=CIRCLE('',#35171,2.73627063036812);
#4174=CIRCLE('',#35172,2.73627063036812);
#4175=CIRCLE('',#35173,2.73627063036812);
#4176=CIRCLE('',#35174,2.73627063036812);
#4177=CIRCLE('',#35175,2.73627063036812);
#4178=CIRCLE('',#35176,2.73627063036812);
#4179=CIRCLE('',#35177,2.73627063036812);
#4180=CIRCLE('',#35178,2.73627063036812);
#4181=CIRCLE('',#35179,2.73627063036812);
#4182=CIRCLE('',#35180,2.73627063036812);
#4183=CIRCLE('',#35181,2.73627063036812);
#4184=CIRCLE('',#35182,2.73627063036812);
#4185=CIRCLE('',#35183,2.73627063036812);
#4186=CIRCLE('',#35184,2.73627063036812);
#4187=CIRCLE('',#35186,2.73627063036812);
#4188=CIRCLE('',#35188,2.73627063036812);
#4189=CIRCLE('',#35190,2.73627063036812);
#4190=CIRCLE('',#35192,2.73627063036812);
#4191=CIRCLE('',#35194,2.73627063036812);
#4192=CIRCLE('',#35196,2.73627063036812);
#4193=CIRCLE('',#35198,2.73627063036812);
#4194=CIRCLE('',#35200,2.73627063036812);
#4195=CIRCLE('',#35202,2.73627063036812);
#4196=CIRCLE('',#35204,2.73627063036812);
#4197=CIRCLE('',#35206,2.73627063036812);
#4198=CIRCLE('',#35208,2.73627063036812);
#4199=CIRCLE('',#35210,2.73627063036812);
#4200=CIRCLE('',#35212,2.73627063036812);
#4201=CIRCLE('',#35214,2.73627063036812);
#4202=CIRCLE('',#35216,2.73627063036812);
#4203=CIRCLE('',#35218,2.73627063036812);
#4204=CIRCLE('',#35220,2.73627063036812);
#4205=CIRCLE('',#35222,2.73627063036812);
#4206=CIRCLE('',#35224,2.73627063036812);
#4207=CIRCLE('',#35226,2.73627063036812);
#4208=CIRCLE('',#35228,2.73627063036812);
#4209=CIRCLE('',#35230,2.73627063036812);
#4210=CIRCLE('',#35232,2.73627063036812);
#4211=CIRCLE('',#35234,2.73627063036812);
#4212=CIRCLE('',#35236,2.73627063036812);
#4213=CIRCLE('',#35238,2.73627063036812);
#4214=CIRCLE('',#35240,2.73627063036812);
#4215=CIRCLE('',#35242,2.73627063036812);
#4216=CIRCLE('',#35244,2.73627063036812);
#4217=CIRCLE('',#35246,2.73627063036812);
#4218=CIRCLE('',#35248,2.73627063036812);
#4219=CIRCLE('',#35250,2.73627063036812);
#4220=CIRCLE('',#35252,2.73627063036812);
#4221=CIRCLE('',#35254,2.73627063036812);
#4222=CIRCLE('',#35256,2.73627063036812);
#4223=CIRCLE('',#35258,2.73627063036812);
#4224=CIRCLE('',#35260,2.73627063036812);
#4225=CIRCLE('',#35262,2.73627063036812);
#4226=CIRCLE('',#35264,2.73627063036812);
#4227=CIRCLE('',#35266,2.73627063036812);
#4228=CIRCLE('',#35268,2.73627063036812);
#4229=CIRCLE('',#35270,2.73627063036812);
#4230=CIRCLE('',#35272,2.73627063036812);
#4231=CIRCLE('',#35274,2.73627063036812);
#4232=CIRCLE('',#35276,2.73627063036812);
#4233=CIRCLE('',#35278,2.73627063036812);
#4234=CIRCLE('',#35280,2.73627063036812);
#4235=CIRCLE('',#35282,2.73627063036812);
#4236=CIRCLE('',#35284,2.73627063036812);
#4237=CIRCLE('',#35286,2.73627063036812);
#4238=CIRCLE('',#35288,2.73627063036812);
#4239=CIRCLE('',#35290,2.73627063036812);
#4240=CIRCLE('',#35292,2.73627063036812);
#4241=CIRCLE('',#35294,2.73627063036812);
#4242=CIRCLE('',#35296,2.73627063036812);
#4243=CIRCLE('',#35298,2.73627063036812);
#4244=CIRCLE('',#35300,2.73627063036812);
#4245=CIRCLE('',#35302,2.73627063036812);
#4246=CIRCLE('',#35304,2.73627063036812);
#4247=CIRCLE('',#35306,2.73627063036812);
#4248=CIRCLE('',#35308,2.73627063036812);
#4249=CIRCLE('',#35310,2.73627063036812);
#4250=CIRCLE('',#35312,2.73627063036812);
#4251=CIRCLE('',#35314,2.73627063036812);
#4252=CIRCLE('',#35316,2.73627063036812);
#4253=CIRCLE('',#35318,2.73627063036812);
#4254=CIRCLE('',#35320,2.73627063036812);
#4255=CIRCLE('',#35322,2.73627063036812);
#4256=CIRCLE('',#35324,2.73627063036812);
#4257=CIRCLE('',#35326,2.73627063036812);
#4258=CIRCLE('',#35328,2.73627063036812);
#4259=CIRCLE('',#35330,2.73627063036812);
#4260=CIRCLE('',#35332,2.73627063036812);
#4261=CIRCLE('',#35334,2.73627063036812);
#4262=CIRCLE('',#35336,2.73627063036812);
#4263=CIRCLE('',#35338,2.73627063036812);
#4264=CIRCLE('',#35340,2.73627063036812);
#4265=CIRCLE('',#35342,2.73627063036812);
#4266=CIRCLE('',#35343,2.73627063036812);
#4267=CIRCLE('',#35344,2.73627063036812);
#4268=CIRCLE('',#35345,2.73627063036812);
#4269=CIRCLE('',#35346,2.73627063036812);
#4270=CIRCLE('',#35347,2.73627063036812);
#4271=CIRCLE('',#35348,2.73627063036812);
#4272=CIRCLE('',#35349,2.73627063036812);
#4273=CIRCLE('',#35350,2.73627063036812);
#4274=CIRCLE('',#35351,2.73627063036812);
#4275=CIRCLE('',#35352,2.73627063036812);
#4276=CIRCLE('',#35353,2.73627063036812);
#4277=CIRCLE('',#35354,2.73627063036812);
#4278=CIRCLE('',#35355,2.73627063036812);
#4279=CIRCLE('',#35356,2.73627063036812);
#4280=CIRCLE('',#35357,2.73627063036812);
#4281=CIRCLE('',#35359,2.73627063036812);
#4282=CIRCLE('',#35361,2.73627063036812);
#4283=CIRCLE('',#35363,2.73627063036812);
#4284=CIRCLE('',#35365,2.73627063036812);
#4285=CIRCLE('',#35367,2.73627063036812);
#4286=CIRCLE('',#35368,2.68872936963188);
#4287=CIRCLE('',#35369,2.68872936963188);
#4288=CIRCLE('',#35371,2.675);
#4289=CIRCLE('',#35372,0.0468749999999996);
#4290=CIRCLE('',#35374,2.675);
#4291=CIRCLE('',#35376,2.60625);
#4292=CIRCLE('',#35377,0.0687500000000002);
#4293=CIRCLE('',#35379,0.15);
#4294=CIRCLE('',#35380,1.65);
#4295=CIRCLE('',#35383,2.75);
#4296=CIRCLE('',#35388,2.75);
#4297=CIRCLE('',#35392,2.75);
#4298=CIRCLE('',#35396,2.75);
#4299=CIRCLE('',#35400,2.75);
#4300=CIRCLE('',#35404,2.75);
#4301=CIRCLE('',#35408,2.75);
#4302=CIRCLE('',#35412,2.75);
#4303=CIRCLE('',#35416,2.75);
#4304=CIRCLE('',#35420,2.75);
#4305=CIRCLE('',#35424,2.75);
#4306=CIRCLE('',#35428,2.75);
#4307=CIRCLE('',#35432,2.75);
#4308=CIRCLE('',#35436,2.75);
#4309=CIRCLE('',#35440,2.75);
#4310=CIRCLE('',#35444,2.75);
#4311=CIRCLE('',#35448,2.75);
#4312=CIRCLE('',#35452,2.75);
#4313=CIRCLE('',#35456,2.75);
#4314=CIRCLE('',#35460,2.75);
#4315=CIRCLE('',#35464,2.75);
#4316=CIRCLE('',#35468,2.75);
#4317=CIRCLE('',#35472,2.75);
#4318=CIRCLE('',#35476,2.75);
#4319=CIRCLE('',#35480,2.75);
#4320=CIRCLE('',#35484,2.75);
#4321=CIRCLE('',#35488,2.75);
#4322=CIRCLE('',#35492,2.75);
#4323=CIRCLE('',#35496,2.75);
#4324=CIRCLE('',#35500,2.75);
#4325=CIRCLE('',#35504,2.75);
#4326=CIRCLE('',#35508,2.75);
#4327=CIRCLE('',#35512,2.75);
#4328=CIRCLE('',#35516,2.75);
#4329=CIRCLE('',#35520,2.75);
#4330=CIRCLE('',#35524,2.75);
#4331=CIRCLE('',#35528,2.75);
#4332=CIRCLE('',#35532,2.75);
#4333=CIRCLE('',#35536,2.75);
#4334=CIRCLE('',#35540,2.75);
#4335=CIRCLE('',#35544,2.75);
#4336=CIRCLE('',#35548,2.75);
#4337=CIRCLE('',#35552,2.75);
#4338=CIRCLE('',#35556,2.75);
#4339=CIRCLE('',#35560,2.75);
#4340=CIRCLE('',#35564,2.75);
#4341=CIRCLE('',#35568,2.75);
#4342=CIRCLE('',#35572,2.75);
#4343=CIRCLE('',#35576,2.75);
#4344=CIRCLE('',#35580,2.75);
#4345=CIRCLE('',#35584,2.75);
#4346=CIRCLE('',#35588,2.75);
#4347=CIRCLE('',#35592,2.75);
#4348=CIRCLE('',#35596,2.75);
#4349=CIRCLE('',#35600,2.75);
#4350=CIRCLE('',#35604,2.75);
#4351=CIRCLE('',#35608,2.75);
#4352=CIRCLE('',#35612,2.75);
#4353=CIRCLE('',#35616,2.75);
#4354=CIRCLE('',#35620,2.75);
#4355=CIRCLE('',#35624,2.75);
#4356=CIRCLE('',#35628,2.75);
#4357=CIRCLE('',#35632,2.75);
#4358=CIRCLE('',#35636,2.75);
#4359=CIRCLE('',#35639,2.75);
#4360=CIRCLE('',#35643,2.75);
#4361=CIRCLE('',#35647,2.75);
#4362=CIRCLE('',#35651,2.75);
#4363=CIRCLE('',#35655,2.75);
#4364=CIRCLE('',#35659,2.75);
#4365=CIRCLE('',#35663,2.75);
#4366=CIRCLE('',#35667,2.75);
#4367=CIRCLE('',#35671,2.75);
#4368=CIRCLE('',#35675,2.75);
#4369=CIRCLE('',#35679,2.75);
#4370=CIRCLE('',#35683,2.75);
#4371=CIRCLE('',#35687,2.75);
#4372=CIRCLE('',#35691,2.75);
#4373=CIRCLE('',#35696,2.75);
#4374=CIRCLE('',#35698,2.75);
#4375=CIRCLE('',#35700,2.75);
#4376=CIRCLE('',#35702,2.75);
#4377=CIRCLE('',#35704,2.75);
#4378=CIRCLE('',#35706,2.75);
#4379=CIRCLE('',#35708,2.75);
#4380=CIRCLE('',#35710,2.75);
#4381=CIRCLE('',#35712,2.75);
#4382=CIRCLE('',#35714,2.75);
#4383=CIRCLE('',#35716,2.75);
#4384=CIRCLE('',#35718,2.75);
#4385=CIRCLE('',#35720,2.75);
#4386=CIRCLE('',#35722,2.75);
#4387=CIRCLE('',#35724,2.75);
#4388=CIRCLE('',#35726,2.75);
#4389=CIRCLE('',#35728,2.75);
#4390=CIRCLE('',#35730,2.75);
#4391=CIRCLE('',#35732,2.75);
#4392=CIRCLE('',#35734,2.75);
#4393=CIRCLE('',#35736,2.75);
#4394=CIRCLE('',#35738,2.75);
#4395=CIRCLE('',#35740,2.75);
#4396=CIRCLE('',#35742,2.75);
#4397=CIRCLE('',#35744,2.75);
#4398=CIRCLE('',#35746,2.75);
#4399=CIRCLE('',#35748,2.75);
#4400=CIRCLE('',#35750,2.75);
#4401=CIRCLE('',#35752,2.75);
#4402=CIRCLE('',#35754,2.75);
#4403=CIRCLE('',#35756,2.75);
#4404=CIRCLE('',#35758,2.75);
#4405=CIRCLE('',#35760,2.75);
#4406=CIRCLE('',#35762,2.75);
#4407=CIRCLE('',#35764,2.75);
#4408=CIRCLE('',#35766,2.75);
#4409=CIRCLE('',#35768,2.75);
#4410=CIRCLE('',#35770,2.75);
#4411=CIRCLE('',#35772,2.75);
#4412=CIRCLE('',#35774,2.75);
#4413=CIRCLE('',#35776,2.75);
#4414=CIRCLE('',#35778,2.75);
#4415=CIRCLE('',#35780,2.75);
#4416=CIRCLE('',#35782,2.75);
#4417=CIRCLE('',#35784,2.75);
#4418=CIRCLE('',#35786,2.75);
#4419=CIRCLE('',#35788,2.75);
#4420=CIRCLE('',#35790,2.75);
#4421=CIRCLE('',#35792,2.75);
#4422=CIRCLE('',#35794,2.75);
#4423=CIRCLE('',#35796,2.75);
#4424=CIRCLE('',#35798,2.75);
#4425=CIRCLE('',#35800,2.75);
#4426=CIRCLE('',#35802,2.75);
#4427=CIRCLE('',#35804,2.75);
#4428=CIRCLE('',#35806,2.75);
#4429=CIRCLE('',#35808,2.75);
#4430=CIRCLE('',#35810,2.75);
#4431=CIRCLE('',#35812,2.75);
#4432=CIRCLE('',#35814,2.75);
#4433=CIRCLE('',#35816,2.75);
#4434=CIRCLE('',#35818,2.75);
#4435=CIRCLE('',#35820,2.75);
#4436=CIRCLE('',#35822,2.75);
#4437=CIRCLE('',#35824,2.75);
#4438=CIRCLE('',#35826,2.75);
#4439=CIRCLE('',#35828,2.75);
#4440=CIRCLE('',#35830,2.75);
#4441=CIRCLE('',#35832,2.75);
#4442=CIRCLE('',#35834,2.75);
#4443=CIRCLE('',#35836,2.75);
#4444=CIRCLE('',#35838,2.75);
#4445=CIRCLE('',#35840,2.75);
#4446=CIRCLE('',#35842,2.75);
#4447=CIRCLE('',#35844,2.75);
#4448=CIRCLE('',#35846,2.75);
#4449=CIRCLE('',#35848,2.75);
#4450=CIRCLE('',#35850,2.75);
#4451=CIRCLE('',#35852,2.75);
#4452=CIRCLE('',#35854,2.75);
#4453=CIRCLE('',#36097,2.75);
#4454=CIRCLE('',#36099,2.75);
#4913=CYLINDRICAL_SURFACE('',#34958,1.5);
#4914=CYLINDRICAL_SURFACE('',#34961,1.5);
#4915=CYLINDRICAL_SURFACE('',#34962,1.5);
#4916=CYLINDRICAL_SURFACE('',#34963,1.5);
#4917=CYLINDRICAL_SURFACE('',#34964,1.5);
#4918=CYLINDRICAL_SURFACE('',#34965,1.5);
#4919=CYLINDRICAL_SURFACE('',#34966,1.5);
#4920=CYLINDRICAL_SURFACE('',#34967,1.5);
#4921=CYLINDRICAL_SURFACE('',#34968,1.5);
#4922=CYLINDRICAL_SURFACE('',#34969,1.5);
#4923=CYLINDRICAL_SURFACE('',#34970,1.5);
#4924=CYLINDRICAL_SURFACE('',#34971,1.5);
#4925=CYLINDRICAL_SURFACE('',#34972,1.5);
#4926=CYLINDRICAL_SURFACE('',#34973,1.5);
#4927=CYLINDRICAL_SURFACE('',#34974,1.5);
#4928=CYLINDRICAL_SURFACE('',#34975,1.5);
#4929=CYLINDRICAL_SURFACE('',#34976,1.5);
#4930=CYLINDRICAL_SURFACE('',#34977,1.5);
#4931=CYLINDRICAL_SURFACE('',#34978,1.5);
#4932=CYLINDRICAL_SURFACE('',#34979,1.5);
#4933=CYLINDRICAL_SURFACE('',#34980,1.5);
#4934=CYLINDRICAL_SURFACE('',#34981,1.5);
#4935=CYLINDRICAL_SURFACE('',#34982,1.5);
#4936=CYLINDRICAL_SURFACE('',#34983,1.5);
#4937=CYLINDRICAL_SURFACE('',#34984,1.5);
#4938=CYLINDRICAL_SURFACE('',#34985,1.5);
#4939=CYLINDRICAL_SURFACE('',#34986,1.5);
#4940=CYLINDRICAL_SURFACE('',#34987,1.5);
#4941=CYLINDRICAL_SURFACE('',#34990,1.17524047358084);
#4942=CYLINDRICAL_SURFACE('',#34992,1.17524047358084);
#4943=CYLINDRICAL_SURFACE('',#34993,1.17524047358084);
#4944=CYLINDRICAL_SURFACE('',#34994,1.17524047358084);
#4945=CYLINDRICAL_SURFACE('',#34995,1.17524047358084);
#4946=CYLINDRICAL_SURFACE('',#34996,1.17524047358084);
#4947=CYLINDRICAL_SURFACE('',#34997,1.17524047358084);
#4948=CYLINDRICAL_SURFACE('',#34998,1.17524047358084);
#4949=CYLINDRICAL_SURFACE('',#34999,1.17524047358084);
#4950=CYLINDRICAL_SURFACE('',#35000,1.17524047358084);
#4951=CYLINDRICAL_SURFACE('',#35001,1.17524047358084);
#4952=CYLINDRICAL_SURFACE('',#35002,1.17524047358084);
#4953=CYLINDRICAL_SURFACE('',#35003,1.17524047358084);
#4954=CYLINDRICAL_SURFACE('',#35004,1.17524047358084);
#4955=CYLINDRICAL_SURFACE('',#35005,1.17524047358084);
#4956=CYLINDRICAL_SURFACE('',#35006,1.17524047358084);
#4957=CYLINDRICAL_SURFACE('',#35007,1.17524047358084);
#4958=CYLINDRICAL_SURFACE('',#35008,1.17524047358084);
#4959=CYLINDRICAL_SURFACE('',#35009,1.17524047358084);
#4960=CYLINDRICAL_SURFACE('',#35010,1.17524047358084);
#4961=CYLINDRICAL_SURFACE('',#35011,1.17524047358084);
#4962=CYLINDRICAL_SURFACE('',#35012,1.17524047358084);
#4963=CYLINDRICAL_SURFACE('',#35013,1.17524047358084);
#4964=CYLINDRICAL_SURFACE('',#35014,1.17524047358084);
#4965=CYLINDRICAL_SURFACE('',#35015,1.17524047358084);
#4966=CYLINDRICAL_SURFACE('',#35016,1.17524047358084);
#4967=CYLINDRICAL_SURFACE('',#35017,1.17524047358084);
#4968=CYLINDRICAL_SURFACE('',#35018,1.17524047358084);
#4969=CYLINDRICAL_SURFACE('',#35019,1.17524047358084);
#4970=CYLINDRICAL_SURFACE('',#35020,1.17524047358084);
#4971=CYLINDRICAL_SURFACE('',#35021,1.17524047358084);
#4972=CYLINDRICAL_SURFACE('',#35026,1.5);
#4973=CYLINDRICAL_SURFACE('',#35027,0.0137499999999999);
#4974=CYLINDRICAL_SURFACE('',#35030,0.0137499999999999);
#4975=CYLINDRICAL_SURFACE('',#35033,0.0137499999999999);
#4976=CYLINDRICAL_SURFACE('',#35036,0.0137499999999999);
#4977=CYLINDRICAL_SURFACE('',#35039,0.0137499999999999);
#4978=CYLINDRICAL_SURFACE('',#35042,0.0137499999999999);
#4979=CYLINDRICAL_SURFACE('',#35045,0.0137499999999999);
#4980=CYLINDRICAL_SURFACE('',#35048,0.0137499999999999);
#4981=CYLINDRICAL_SURFACE('',#35051,0.0137499999999999);
#4982=CYLINDRICAL_SURFACE('',#35054,0.0137499999999999);
#4983=CYLINDRICAL_SURFACE('',#35057,0.0137499999999997);
#4984=CYLINDRICAL_SURFACE('',#35060,0.0137499999999997);
#4985=CYLINDRICAL_SURFACE('',#35063,0.0137499999999997);
#4986=CYLINDRICAL_SURFACE('',#35066,0.0137499999999997);
#4987=CYLINDRICAL_SURFACE('',#35069,0.0137499999999997);
#4988=CYLINDRICAL_SURFACE('',#35373,2.675);
#4989=CYLINDRICAL_SURFACE('',#35697,2.75);
#4990=CYLINDRICAL_SURFACE('',#35699,2.75);
#4991=CYLINDRICAL_SURFACE('',#35701,2.75);
#4992=CYLINDRICAL_SURFACE('',#35703,2.75);
#4993=CYLINDRICAL_SURFACE('',#35705,2.75);
#4994=CYLINDRICAL_SURFACE('',#35707,2.75);
#4995=CYLINDRICAL_SURFACE('',#35709,2.75);
#4996=CYLINDRICAL_SURFACE('',#35711,2.75);
#4997=CYLINDRICAL_SURFACE('',#35713,2.75);
#4998=CYLINDRICAL_SURFACE('',#35715,2.75);
#4999=CYLINDRICAL_SURFACE('',#35717,2.75);
#5000=CYLINDRICAL_SURFACE('',#35719,2.75);
#5001=CYLINDRICAL_SURFACE('',#35721,2.75);
#5002=CYLINDRICAL_SURFACE('',#35723,2.75);
#5003=CYLINDRICAL_SURFACE('',#35725,2.75);
#5004=CYLINDRICAL_SURFACE('',#35727,2.75);
#5005=CYLINDRICAL_SURFACE('',#35729,2.75);
#5006=CYLINDRICAL_SURFACE('',#35731,2.75);
#5007=CYLINDRICAL_SURFACE('',#35733,2.75);
#5008=CYLINDRICAL_SURFACE('',#35735,2.75);
#5009=CYLINDRICAL_SURFACE('',#35737,2.75);
#5010=CYLINDRICAL_SURFACE('',#35739,2.75);
#5011=CYLINDRICAL_SURFACE('',#35741,2.75);
#5012=CYLINDRICAL_SURFACE('',#35743,2.75);
#5013=CYLINDRICAL_SURFACE('',#35745,2.75);
#5014=CYLINDRICAL_SURFACE('',#35747,2.75);
#5015=CYLINDRICAL_SURFACE('',#35749,2.75);
#5016=CYLINDRICAL_SURFACE('',#35751,2.75);
#5017=CYLINDRICAL_SURFACE('',#35753,2.75);
#5018=CYLINDRICAL_SURFACE('',#35755,2.75);
#5019=CYLINDRICAL_SURFACE('',#35757,2.75);
#5020=CYLINDRICAL_SURFACE('',#35759,2.75);
#5021=CYLINDRICAL_SURFACE('',#35761,2.75);
#5022=CYLINDRICAL_SURFACE('',#35763,2.75);
#5023=CYLINDRICAL_SURFACE('',#35765,2.75);
#5024=CYLINDRICAL_SURFACE('',#35767,2.75);
#5025=CYLINDRICAL_SURFACE('',#35769,2.75);
#5026=CYLINDRICAL_SURFACE('',#35771,2.75);
#5027=CYLINDRICAL_SURFACE('',#35773,2.75);
#5028=CYLINDRICAL_SURFACE('',#35775,2.75);
#5029=CYLINDRICAL_SURFACE('',#35777,2.75);
#5030=CYLINDRICAL_SURFACE('',#35779,2.75);
#5031=CYLINDRICAL_SURFACE('',#35781,2.75);
#5032=CYLINDRICAL_SURFACE('',#35783,2.75);
#5033=CYLINDRICAL_SURFACE('',#35785,2.75);
#5034=CYLINDRICAL_SURFACE('',#35787,2.75);
#5035=CYLINDRICAL_SURFACE('',#35789,2.75);
#5036=CYLINDRICAL_SURFACE('',#35791,2.75);
#5037=CYLINDRICAL_SURFACE('',#35793,2.75);
#5038=CYLINDRICAL_SURFACE('',#35795,2.75);
#5039=CYLINDRICAL_SURFACE('',#35797,2.75);
#5040=CYLINDRICAL_SURFACE('',#35799,2.75);
#5041=CYLINDRICAL_SURFACE('',#35801,2.75);
#5042=CYLINDRICAL_SURFACE('',#35803,2.75);
#5043=CYLINDRICAL_SURFACE('',#35805,2.75);
#5044=CYLINDRICAL_SURFACE('',#35807,2.75);
#5045=CYLINDRICAL_SURFACE('',#35809,2.75);
#5046=CYLINDRICAL_SURFACE('',#35811,2.75);
#5047=CYLINDRICAL_SURFACE('',#35813,2.75);
#5048=CYLINDRICAL_SURFACE('',#35815,2.75);
#5049=CYLINDRICAL_SURFACE('',#35817,2.75);
#5050=CYLINDRICAL_SURFACE('',#35819,2.75);
#5051=CYLINDRICAL_SURFACE('',#35821,2.75);
#5052=CYLINDRICAL_SURFACE('',#35823,2.75);
#5053=CYLINDRICAL_SURFACE('',#35825,2.75);
#5054=CYLINDRICAL_SURFACE('',#35827,2.75);
#5055=CYLINDRICAL_SURFACE('',#35829,2.75);
#5056=CYLINDRICAL_SURFACE('',#35831,2.75);
#5057=CYLINDRICAL_SURFACE('',#35833,2.75);
#5058=CYLINDRICAL_SURFACE('',#35835,2.75);
#5059=CYLINDRICAL_SURFACE('',#35837,2.75);
#5060=CYLINDRICAL_SURFACE('',#35839,2.75);
#5061=CYLINDRICAL_SURFACE('',#35841,2.75);
#5062=CYLINDRICAL_SURFACE('',#35843,2.75);
#5063=CYLINDRICAL_SURFACE('',#35845,2.75);
#5064=CYLINDRICAL_SURFACE('',#35847,2.75);
#5065=CYLINDRICAL_SURFACE('',#35849,2.75);
#5066=CYLINDRICAL_SURFACE('',#35851,2.75);
#5067=CYLINDRICAL_SURFACE('',#35853,2.75);
#5068=CYLINDRICAL_SURFACE('',#36098,2.75);
#5069=CYLINDRICAL_SURFACE('',#36113,0.0137499999999997);
#5070=CYLINDRICAL_SURFACE('',#36116,0.0137499999999997);
#5071=CYLINDRICAL_SURFACE('',#36119,0.0137499999999997);
#5072=CYLINDRICAL_SURFACE('',#36122,0.0137499999999997);
#5073=CYLINDRICAL_SURFACE('',#36125,0.0137499999999998);
#5074=CYLINDRICAL_SURFACE('',#36128,0.0137499999999998);
#5075=CYLINDRICAL_SURFACE('',#36131,0.0137499999999997);
#5076=CYLINDRICAL_SURFACE('',#36152,0.0137499999999997);
#5077=CYLINDRICAL_SURFACE('',#36155,0.0137499999999998);
#5078=CYLINDRICAL_SURFACE('',#36158,0.0137499999999998);
#5079=CYLINDRICAL_SURFACE('',#36161,0.0137499999999997);
#5080=CYLINDRICAL_SURFACE('',#36164,0.0137499999999997);
#5081=CYLINDRICAL_SURFACE('',#36167,0.0137499999999997);
#5082=CYLINDRICAL_SURFACE('',#36170,0.0137499999999997);
#5083=CYLINDRICAL_SURFACE('',#36173,0.0137499999999997);
#5084=CYLINDRICAL_SURFACE('',#36176,0.0137499999999997);
#5085=CYLINDRICAL_SURFACE('',#36179,0.0137499999999999);
#5086=CYLINDRICAL_SURFACE('',#36182,0.0137499999999999);
#5087=CYLINDRICAL_SURFACE('',#36185,0.0137499999999999);
#5088=CYLINDRICAL_SURFACE('',#36188,0.0137499999999999);
#5089=CYLINDRICAL_SURFACE('',#36191,0.0137499999999999);
#5090=CYLINDRICAL_SURFACE('',#36194,0.0137499999999999);
#5091=CYLINDRICAL_SURFACE('',#36197,0.0137499999999999);
#5092=CYLINDRICAL_SURFACE('',#36200,0.0137499999999999);
#5093=CYLINDRICAL_SURFACE('',#36203,0.0137499999999999);
#5094=CYLINDRICAL_SURFACE('',#36206,0.0137499999999997);
#5095=CYLINDRICAL_SURFACE('',#36209,0.0137499999999997);
#5096=CYLINDRICAL_SURFACE('',#36212,0.0137499999999997);
#5097=CYLINDRICAL_SURFACE('',#36215,0.0137499999999998);
#5098=CYLINDRICAL_SURFACE('',#36218,0.0137499999999998);
#5099=CYLINDRICAL_SURFACE('',#36221,0.0137499999999997);
#5100=CYLINDRICAL_SURFACE('',#36224,0.0137499999999997);
#5101=CYLINDRICAL_SURFACE('',#36227,0.0137499999999997);
#5102=CYLINDRICAL_SURFACE('',#36230,0.0137499999999997);
#5103=CYLINDRICAL_SURFACE('',#36233,0.0137499999999997);
#5104=CYLINDRICAL_SURFACE('',#36236,0.0137499999999997);
#5105=CYLINDRICAL_SURFACE('',#36239,0.0137499999999999);
#5106=CYLINDRICAL_SURFACE('',#36242,0.0137499999999999);
#5107=CYLINDRICAL_SURFACE('',#36245,0.0137499999999999);
#5108=CYLINDRICAL_SURFACE('',#36248,0.0137499999999999);
#5109=CYLINDRICAL_SURFACE('',#36251,0.0137499999999999);
#5110=CYLINDRICAL_SURFACE('',#36254,0.0137499999999999);
#5111=CYLINDRICAL_SURFACE('',#36257,0.0137499999999999);
#5112=CYLINDRICAL_SURFACE('',#36260,0.0137499999999999);
#5113=CYLINDRICAL_SURFACE('',#36263,0.0137499999999999);
#5114=CYLINDRICAL_SURFACE('',#36266,0.0137499999999999);
#5115=CYLINDRICAL_SURFACE('',#36269,0.0137499999999999);
#5116=CYLINDRICAL_SURFACE('',#36272,0.0137499999999999);
#5117=CYLINDRICAL_SURFACE('',#36275,0.0137499999999999);
#5118=CYLINDRICAL_SURFACE('',#36278,0.0137499999999999);
#5119=CYLINDRICAL_SURFACE('',#36281,0.0137499999999999);
#5120=CYLINDRICAL_SURFACE('',#36284,0.0137499999999999);
#5121=CYLINDRICAL_SURFACE('',#36287,0.0137499999999999);
#5122=CYLINDRICAL_SURFACE('',#36290,0.0137499999999999);
#5123=CYLINDRICAL_SURFACE('',#36293,0.0137499999999999);
#5124=CYLINDRICAL_SURFACE('',#36296,0.0137499999999997);
#5125=CYLINDRICAL_SURFACE('',#36299,0.0137499999999997);
#5126=CYLINDRICAL_SURFACE('',#36302,0.0137499999999997);
#5127=CYLINDRICAL_SURFACE('',#36305,0.0137499999999997);
#5128=CYLINDRICAL_SURFACE('',#36308,0.0137499999999997);
#5129=CYLINDRICAL_SURFACE('',#36311,0.0137499999999997);
#5130=CYLINDRICAL_SURFACE('',#36314,0.0137499999999998);
#5131=CYLINDRICAL_SURFACE('',#36317,0.0137499999999998);
#5132=CYLINDRICAL_SURFACE('',#36320,0.0137499999999997);
#5133=CYLINDRICAL_SURFACE('',#36323,0.0137499999999997);
#6298=FACE_OUTER_BOUND('',#8036,.T.);
#6299=FACE_OUTER_BOUND('',#8037,.T.);
#6300=FACE_OUTER_BOUND('',#8038,.T.);
#6301=FACE_OUTER_BOUND('',#8039,.T.);
#6302=FACE_OUTER_BOUND('',#8040,.T.);
#6303=FACE_OUTER_BOUND('',#8041,.T.);
#6304=FACE_OUTER_BOUND('',#8042,.T.);
#6305=FACE_OUTER_BOUND('',#8043,.T.);
#6306=FACE_OUTER_BOUND('',#8044,.T.);
#6307=FACE_OUTER_BOUND('',#8045,.T.);
#6308=FACE_OUTER_BOUND('',#8046,.T.);
#6309=FACE_OUTER_BOUND('',#8047,.T.);
#6310=FACE_OUTER_BOUND('',#8048,.T.);
#6311=FACE_OUTER_BOUND('',#8049,.T.);
#6312=FACE_OUTER_BOUND('',#8050,.T.);
#6313=FACE_OUTER_BOUND('',#8051,.T.);
#6314=FACE_OUTER_BOUND('',#8052,.T.);
#6315=FACE_OUTER_BOUND('',#8053,.T.);
#6316=FACE_OUTER_BOUND('',#8054,.T.);
#6317=FACE_OUTER_BOUND('',#8055,.T.);
#6318=FACE_OUTER_BOUND('',#8056,.T.);
#6319=FACE_OUTER_BOUND('',#8057,.T.);
#6320=FACE_OUTER_BOUND('',#8058,.T.);
#6321=FACE_OUTER_BOUND('',#8059,.T.);
#6322=FACE_OUTER_BOUND('',#8060,.T.);
#6323=FACE_OUTER_BOUND('',#8061,.T.);
#6324=FACE_OUTER_BOUND('',#8062,.T.);
#6325=FACE_OUTER_BOUND('',#8063,.T.);
#6326=FACE_OUTER_BOUND('',#8064,.T.);
#6327=FACE_OUTER_BOUND('',#8065,.T.);
#6328=FACE_OUTER_BOUND('',#8066,.T.);
#6329=FACE_OUTER_BOUND('',#8067,.T.);
#6330=FACE_OUTER_BOUND('',#8068,.T.);
#6331=FACE_OUTER_BOUND('',#8069,.T.);
#6332=FACE_OUTER_BOUND('',#8070,.T.);
#6333=FACE_OUTER_BOUND('',#8071,.T.);
#6334=FACE_OUTER_BOUND('',#8072,.T.);
#6335=FACE_OUTER_BOUND('',#8073,.T.);
#6336=FACE_OUTER_BOUND('',#8074,.T.);
#6337=FACE_OUTER_BOUND('',#8075,.T.);
#6338=FACE_OUTER_BOUND('',#8076,.T.);
#6339=FACE_OUTER_BOUND('',#8077,.T.);
#6340=FACE_OUTER_BOUND('',#8078,.T.);
#6341=FACE_OUTER_BOUND('',#8079,.T.);
#6342=FACE_OUTER_BOUND('',#8080,.T.);
#6343=FACE_OUTER_BOUND('',#8081,.T.);
#6344=FACE_OUTER_BOUND('',#8082,.T.);
#6345=FACE_OUTER_BOUND('',#8083,.T.);
#6346=FACE_OUTER_BOUND('',#8084,.T.);
#6347=FACE_OUTER_BOUND('',#8085,.T.);
#6348=FACE_OUTER_BOUND('',#8086,.T.);
#6349=FACE_OUTER_BOUND('',#8087,.T.);
#6350=FACE_OUTER_BOUND('',#8088,.T.);
#6351=FACE_OUTER_BOUND('',#8089,.T.);
#6352=FACE_OUTER_BOUND('',#8090,.T.);
#6353=FACE_OUTER_BOUND('',#8091,.T.);
#6354=FACE_OUTER_BOUND('',#8092,.T.);
#6355=FACE_OUTER_BOUND('',#8093,.T.);
#6356=FACE_OUTER_BOUND('',#8094,.T.);
#6357=FACE_OUTER_BOUND('',#8095,.T.);
#6358=FACE_OUTER_BOUND('',#8096,.T.);
#6359=FACE_OUTER_BOUND('',#8097,.T.);
#6360=FACE_OUTER_BOUND('',#8098,.T.);
#6361=FACE_OUTER_BOUND('',#8099,.T.);
#6362=FACE_OUTER_BOUND('',#8100,.T.);
#6363=FACE_OUTER_BOUND('',#8101,.T.);
#6364=FACE_OUTER_BOUND('',#8102,.T.);
#6365=FACE_OUTER_BOUND('',#8103,.T.);
#6366=FACE_OUTER_BOUND('',#8104,.T.);
#6367=FACE_OUTER_BOUND('',#8105,.T.);
#6368=FACE_OUTER_BOUND('',#8106,.T.);
#6369=FACE_OUTER_BOUND('',#8107,.T.);
#6370=FACE_OUTER_BOUND('',#8108,.T.);
#6371=FACE_OUTER_BOUND('',#8109,.T.);
#6372=FACE_OUTER_BOUND('',#8110,.T.);
#6373=FACE_OUTER_BOUND('',#8111,.T.);
#6374=FACE_OUTER_BOUND('',#8112,.T.);
#6375=FACE_OUTER_BOUND('',#8113,.T.);
#6376=FACE_OUTER_BOUND('',#8114,.T.);
#6377=FACE_OUTER_BOUND('',#8115,.T.);
#6378=FACE_OUTER_BOUND('',#8116,.T.);
#6379=FACE_OUTER_BOUND('',#8117,.T.);
#6380=FACE_OUTER_BOUND('',#8118,.T.);
#6381=FACE_OUTER_BOUND('',#8119,.T.);
#6382=FACE_OUTER_BOUND('',#8120,.T.);
#6383=FACE_OUTER_BOUND('',#8121,.T.);
#6384=FACE_OUTER_BOUND('',#8122,.T.);
#6385=FACE_OUTER_BOUND('',#8123,.T.);
#6386=FACE_OUTER_BOUND('',#8124,.T.);
#6387=FACE_OUTER_BOUND('',#8125,.T.);
#6388=FACE_OUTER_BOUND('',#8126,.T.);
#6389=FACE_OUTER_BOUND('',#8127,.T.);
#6390=FACE_OUTER_BOUND('',#8128,.T.);
#6391=FACE_OUTER_BOUND('',#8129,.T.);
#6392=FACE_OUTER_BOUND('',#8130,.T.);
#6393=FACE_OUTER_BOUND('',#8131,.T.);
#6394=FACE_OUTER_BOUND('',#8132,.T.);
#6395=FACE_OUTER_BOUND('',#8133,.T.);
#6396=FACE_OUTER_BOUND('',#8134,.T.);
#6397=FACE_OUTER_BOUND('',#8135,.T.);
#6398=FACE_OUTER_BOUND('',#8136,.T.);
#6399=FACE_OUTER_BOUND('',#8137,.T.);
#6400=FACE_OUTER_BOUND('',#8138,.T.);
#6401=FACE_OUTER_BOUND('',#8139,.T.);
#6402=FACE_OUTER_BOUND('',#8140,.T.);
#6403=FACE_OUTER_BOUND('',#8141,.T.);
#6404=FACE_OUTER_BOUND('',#8142,.T.);
#6405=FACE_OUTER_BOUND('',#8143,.T.);
#6406=FACE_OUTER_BOUND('',#8144,.T.);
#6407=FACE_OUTER_BOUND('',#8145,.T.);
#6408=FACE_OUTER_BOUND('',#8146,.T.);
#6409=FACE_OUTER_BOUND('',#8147,.T.);
#6410=FACE_OUTER_BOUND('',#8148,.T.);
#6411=FACE_OUTER_BOUND('',#8149,.T.);
#6412=FACE_OUTER_BOUND('',#8150,.T.);
#6413=FACE_OUTER_BOUND('',#8151,.T.);
#6414=FACE_OUTER_BOUND('',#8152,.T.);
#6415=FACE_OUTER_BOUND('',#8153,.T.);
#6416=FACE_OUTER_BOUND('',#8154,.T.);
#6417=FACE_OUTER_BOUND('',#8155,.T.);
#6418=FACE_OUTER_BOUND('',#8156,.T.);
#6419=FACE_OUTER_BOUND('',#8157,.T.);
#6420=FACE_OUTER_BOUND('',#8158,.T.);
#6421=FACE_OUTER_BOUND('',#8159,.T.);
#6422=FACE_OUTER_BOUND('',#8160,.T.);
#6423=FACE_OUTER_BOUND('',#8161,.T.);
#6424=FACE_OUTER_BOUND('',#8162,.T.);
#6425=FACE_OUTER_BOUND('',#8163,.T.);
#6426=FACE_OUTER_BOUND('',#8164,.T.);
#6427=FACE_OUTER_BOUND('',#8165,.T.);
#6428=FACE_OUTER_BOUND('',#8166,.T.);
#6429=FACE_OUTER_BOUND('',#8167,.T.);
#6430=FACE_OUTER_BOUND('',#8168,.T.);
#6431=FACE_OUTER_BOUND('',#8169,.T.);
#6432=FACE_OUTER_BOUND('',#8170,.T.);
#6433=FACE_OUTER_BOUND('',#8171,.T.);
#6434=FACE_OUTER_BOUND('',#8172,.T.);
#6435=FACE_OUTER_BOUND('',#8173,.T.);
#6436=FACE_OUTER_BOUND('',#8174,.T.);
#6437=FACE_OUTER_BOUND('',#8175,.T.);
#6438=FACE_OUTER_BOUND('',#8176,.T.);
#6439=FACE_OUTER_BOUND('',#8177,.T.);
#6440=FACE_OUTER_BOUND('',#8178,.T.);
#6441=FACE_OUTER_BOUND('',#8179,.T.);
#6442=FACE_OUTER_BOUND('',#8180,.T.);
#6443=FACE_OUTER_BOUND('',#8181,.T.);
#6444=FACE_OUTER_BOUND('',#8182,.T.);
#6445=FACE_OUTER_BOUND('',#8183,.T.);
#6446=FACE_OUTER_BOUND('',#8184,.T.);
#6447=FACE_OUTER_BOUND('',#8185,.T.);
#6448=FACE_OUTER_BOUND('',#8186,.T.);
#6449=FACE_OUTER_BOUND('',#8187,.T.);
#6450=FACE_OUTER_BOUND('',#8188,.T.);
#6451=FACE_OUTER_BOUND('',#8189,.T.);
#6452=FACE_OUTER_BOUND('',#8190,.T.);
#6453=FACE_OUTER_BOUND('',#8191,.T.);
#6454=FACE_OUTER_BOUND('',#8192,.T.);
#6455=FACE_OUTER_BOUND('',#8193,.T.);
#6456=FACE_OUTER_BOUND('',#8194,.T.);
#6457=FACE_OUTER_BOUND('',#8195,.T.);
#6458=FACE_OUTER_BOUND('',#8196,.T.);
#6459=FACE_OUTER_BOUND('',#8197,.T.);
#6460=FACE_OUTER_BOUND('',#8198,.T.);
#6461=FACE_OUTER_BOUND('',#8199,.T.);
#6462=FACE_OUTER_BOUND('',#8200,.T.);
#6463=FACE_OUTER_BOUND('',#8201,.T.);
#6464=FACE_OUTER_BOUND('',#8202,.T.);
#6465=FACE_OUTER_BOUND('',#8203,.T.);
#6466=FACE_OUTER_BOUND('',#8204,.T.);
#6467=FACE_OUTER_BOUND('',#8205,.T.);
#6468=FACE_OUTER_BOUND('',#8206,.T.);
#6469=FACE_OUTER_BOUND('',#8207,.T.);
#6470=FACE_OUTER_BOUND('',#8208,.T.);
#6471=FACE_OUTER_BOUND('',#8209,.T.);
#6472=FACE_OUTER_BOUND('',#8210,.T.);
#6473=FACE_OUTER_BOUND('',#8211,.T.);
#6474=FACE_OUTER_BOUND('',#8212,.T.);
#6475=FACE_OUTER_BOUND('',#8213,.T.);
#6476=FACE_OUTER_BOUND('',#8214,.T.);
#6477=FACE_OUTER_BOUND('',#8215,.T.);
#6478=FACE_OUTER_BOUND('',#8216,.T.);
#6479=FACE_OUTER_BOUND('',#8217,.T.);
#6480=FACE_OUTER_BOUND('',#8218,.T.);
#6481=FACE_OUTER_BOUND('',#8219,.T.);
#6482=FACE_OUTER_BOUND('',#8220,.T.);
#6483=FACE_OUTER_BOUND('',#8221,.T.);
#6484=FACE_OUTER_BOUND('',#8222,.T.);
#6485=FACE_OUTER_BOUND('',#8223,.T.);
#6486=FACE_OUTER_BOUND('',#8224,.T.);
#6487=FACE_OUTER_BOUND('',#8225,.T.);
#6488=FACE_OUTER_BOUND('',#8226,.T.);
#6489=FACE_OUTER_BOUND('',#8227,.T.);
#6490=FACE_OUTER_BOUND('',#8228,.T.);
#6491=FACE_OUTER_BOUND('',#8229,.T.);
#6492=FACE_OUTER_BOUND('',#8230,.T.);
#6493=FACE_OUTER_BOUND('',#8231,.T.);
#6494=FACE_OUTER_BOUND('',#8232,.T.);
#6495=FACE_OUTER_BOUND('',#8233,.T.);
#6496=FACE_OUTER_BOUND('',#8234,.T.);
#6497=FACE_OUTER_BOUND('',#8235,.T.);
#6498=FACE_OUTER_BOUND('',#8236,.T.);
#6499=FACE_OUTER_BOUND('',#8237,.T.);
#6500=FACE_OUTER_BOUND('',#8238,.T.);
#6501=FACE_OUTER_BOUND('',#8239,.T.);
#6502=FACE_OUTER_BOUND('',#8240,.T.);
#6503=FACE_OUTER_BOUND('',#8241,.T.);
#6504=FACE_OUTER_BOUND('',#8242,.T.);
#6505=FACE_OUTER_BOUND('',#8243,.T.);
#6506=FACE_OUTER_BOUND('',#8244,.T.);
#6507=FACE_OUTER_BOUND('',#8245,.T.);
#6508=FACE_OUTER_BOUND('',#8246,.T.);
#6509=FACE_OUTER_BOUND('',#8247,.T.);
#6510=FACE_OUTER_BOUND('',#8248,.T.);
#6511=FACE_OUTER_BOUND('',#8249,.T.);
#6512=FACE_OUTER_BOUND('',#8250,.T.);
#6513=FACE_OUTER_BOUND('',#8251,.T.);
#6514=FACE_OUTER_BOUND('',#8252,.T.);
#6515=FACE_OUTER_BOUND('',#8253,.T.);
#6516=FACE_OUTER_BOUND('',#8254,.T.);
#6517=FACE_OUTER_BOUND('',#8255,.T.);
#6518=FACE_OUTER_BOUND('',#8256,.T.);
#6519=FACE_OUTER_BOUND('',#8257,.T.);
#6520=FACE_OUTER_BOUND('',#8258,.T.);
#6521=FACE_OUTER_BOUND('',#8259,.T.);
#6522=FACE_OUTER_BOUND('',#8260,.T.);
#6523=FACE_OUTER_BOUND('',#8261,.T.);
#6524=FACE_OUTER_BOUND('',#8262,.T.);
#6525=FACE_OUTER_BOUND('',#8263,.T.);
#6526=FACE_OUTER_BOUND('',#8264,.T.);
#6527=FACE_OUTER_BOUND('',#8265,.T.);
#6528=FACE_OUTER_BOUND('',#8266,.T.);
#6529=FACE_OUTER_BOUND('',#8267,.T.);
#6530=FACE_OUTER_BOUND('',#8268,.T.);
#6531=FACE_OUTER_BOUND('',#8269,.T.);
#6532=FACE_OUTER_BOUND('',#8270,.T.);
#6533=FACE_OUTER_BOUND('',#8271,.T.);
#6534=FACE_OUTER_BOUND('',#8272,.T.);
#6535=FACE_OUTER_BOUND('',#8273,.T.);
#6536=FACE_OUTER_BOUND('',#8274,.T.);
#6537=FACE_OUTER_BOUND('',#8275,.T.);
#6538=FACE_OUTER_BOUND('',#8276,.T.);
#6539=FACE_OUTER_BOUND('',#8277,.T.);
#6540=FACE_OUTER_BOUND('',#8278,.T.);
#6541=FACE_OUTER_BOUND('',#8279,.T.);
#6542=FACE_OUTER_BOUND('',#8280,.T.);
#6543=FACE_OUTER_BOUND('',#8281,.T.);
#6544=FACE_OUTER_BOUND('',#8282,.T.);
#6545=FACE_OUTER_BOUND('',#8283,.T.);
#6546=FACE_OUTER_BOUND('',#8284,.T.);
#6547=FACE_OUTER_BOUND('',#8285,.T.);
#6548=FACE_OUTER_BOUND('',#8286,.T.);
#6549=FACE_OUTER_BOUND('',#8287,.T.);
#6550=FACE_OUTER_BOUND('',#8288,.T.);
#6551=FACE_OUTER_BOUND('',#8289,.T.);
#6552=FACE_OUTER_BOUND('',#8290,.T.);
#6553=FACE_OUTER_BOUND('',#8291,.T.);
#6554=FACE_OUTER_BOUND('',#8292,.T.);
#6555=FACE_OUTER_BOUND('',#8293,.T.);
#6556=FACE_OUTER_BOUND('',#8294,.T.);
#6557=FACE_OUTER_BOUND('',#8295,.T.);
#6558=FACE_OUTER_BOUND('',#8296,.T.);
#6559=FACE_OUTER_BOUND('',#8297,.T.);
#6560=FACE_OUTER_BOUND('',#8298,.T.);
#6561=FACE_OUTER_BOUND('',#8299,.T.);
#6562=FACE_OUTER_BOUND('',#8300,.T.);
#6563=FACE_OUTER_BOUND('',#8301,.T.);
#6564=FACE_OUTER_BOUND('',#8302,.T.);
#6565=FACE_OUTER_BOUND('',#8303,.T.);
#6566=FACE_OUTER_BOUND('',#8304,.T.);
#6567=FACE_OUTER_BOUND('',#8305,.T.);
#6568=FACE_OUTER_BOUND('',#8306,.T.);
#6569=FACE_OUTER_BOUND('',#8307,.T.);
#6570=FACE_OUTER_BOUND('',#8308,.T.);
#6571=FACE_OUTER_BOUND('',#8309,.T.);
#6572=FACE_OUTER_BOUND('',#8310,.T.);
#6573=FACE_OUTER_BOUND('',#8311,.T.);
#6574=FACE_OUTER_BOUND('',#8312,.T.);
#6575=FACE_OUTER_BOUND('',#8313,.T.);
#6576=FACE_OUTER_BOUND('',#8314,.T.);
#6577=FACE_OUTER_BOUND('',#8315,.T.);
#6578=FACE_OUTER_BOUND('',#8316,.T.);
#6579=FACE_OUTER_BOUND('',#8317,.T.);
#6580=FACE_OUTER_BOUND('',#8318,.T.);
#6581=FACE_OUTER_BOUND('',#8319,.T.);
#6582=FACE_OUTER_BOUND('',#8320,.T.);
#6583=FACE_OUTER_BOUND('',#8321,.T.);
#6584=FACE_OUTER_BOUND('',#8322,.T.);
#6585=FACE_OUTER_BOUND('',#8323,.T.);
#6586=FACE_OUTER_BOUND('',#8324,.T.);
#6587=FACE_OUTER_BOUND('',#8325,.T.);
#6588=FACE_OUTER_BOUND('',#8326,.T.);
#6589=FACE_OUTER_BOUND('',#8327,.T.);
#6590=FACE_OUTER_BOUND('',#8328,.T.);
#6591=FACE_OUTER_BOUND('',#8329,.T.);
#6592=FACE_OUTER_BOUND('',#8330,.T.);
#6593=FACE_OUTER_BOUND('',#8331,.T.);
#6594=FACE_OUTER_BOUND('',#8332,.T.);
#6595=FACE_OUTER_BOUND('',#8333,.T.);
#6596=FACE_OUTER_BOUND('',#8334,.T.);
#6597=FACE_OUTER_BOUND('',#8335,.T.);
#6598=FACE_OUTER_BOUND('',#8336,.T.);
#6599=FACE_OUTER_BOUND('',#8337,.T.);
#6600=FACE_OUTER_BOUND('',#8338,.T.);
#6601=FACE_OUTER_BOUND('',#8339,.T.);
#6602=FACE_OUTER_BOUND('',#8340,.T.);
#6603=FACE_OUTER_BOUND('',#8341,.T.);
#6604=FACE_OUTER_BOUND('',#8342,.T.);
#6605=FACE_OUTER_BOUND('',#8343,.T.);
#6606=FACE_OUTER_BOUND('',#8344,.T.);
#6607=FACE_OUTER_BOUND('',#8345,.T.);
#6608=FACE_OUTER_BOUND('',#8346,.T.);
#6609=FACE_OUTER_BOUND('',#8347,.T.);
#6610=FACE_OUTER_BOUND('',#8348,.T.);
#6611=FACE_OUTER_BOUND('',#8349,.T.);
#6612=FACE_OUTER_BOUND('',#8350,.T.);
#6613=FACE_OUTER_BOUND('',#8351,.T.);
#6614=FACE_OUTER_BOUND('',#8352,.T.);
#6615=FACE_OUTER_BOUND('',#8353,.T.);
#6616=FACE_OUTER_BOUND('',#8354,.T.);
#6617=FACE_OUTER_BOUND('',#8355,.T.);
#6618=FACE_OUTER_BOUND('',#8356,.T.);
#6619=FACE_OUTER_BOUND('',#8357,.T.);
#6620=FACE_OUTER_BOUND('',#8358,.T.);
#6621=FACE_OUTER_BOUND('',#8359,.T.);
#6622=FACE_OUTER_BOUND('',#8361,.T.);
#6623=FACE_OUTER_BOUND('',#8362,.T.);
#6624=FACE_OUTER_BOUND('',#8363,.T.);
#6625=FACE_OUTER_BOUND('',#8364,.T.);
#6626=FACE_OUTER_BOUND('',#8366,.T.);
#6627=FACE_OUTER_BOUND('',#8367,.T.);
#6628=FACE_OUTER_BOUND('',#8368,.T.);
#6629=FACE_OUTER_BOUND('',#8369,.T.);
#6630=FACE_OUTER_BOUND('',#8370,.T.);
#6631=FACE_OUTER_BOUND('',#8371,.T.);
#6632=FACE_OUTER_BOUND('',#8372,.T.);
#6633=FACE_OUTER_BOUND('',#8373,.T.);
#6634=FACE_OUTER_BOUND('',#8374,.T.);
#6635=FACE_OUTER_BOUND('',#8375,.T.);
#6636=FACE_OUTER_BOUND('',#8376,.T.);
#6637=FACE_OUTER_BOUND('',#8377,.T.);
#6638=FACE_OUTER_BOUND('',#8378,.T.);
#6639=FACE_OUTER_BOUND('',#8379,.T.);
#6640=FACE_OUTER_BOUND('',#8380,.T.);
#6641=FACE_OUTER_BOUND('',#8381,.T.);
#6642=FACE_OUTER_BOUND('',#8382,.T.);
#6643=FACE_OUTER_BOUND('',#8383,.T.);
#6644=FACE_OUTER_BOUND('',#8384,.T.);
#6645=FACE_OUTER_BOUND('',#8385,.T.);
#6646=FACE_OUTER_BOUND('',#8386,.T.);
#6647=FACE_OUTER_BOUND('',#8387,.T.);
#6648=FACE_OUTER_BOUND('',#8388,.T.);
#6649=FACE_OUTER_BOUND('',#8389,.T.);
#6650=FACE_OUTER_BOUND('',#8390,.T.);
#6651=FACE_OUTER_BOUND('',#8391,.T.);
#6652=FACE_OUTER_BOUND('',#8392,.T.);
#6653=FACE_OUTER_BOUND('',#8393,.T.);
#6654=FACE_OUTER_BOUND('',#8394,.T.);
#6655=FACE_OUTER_BOUND('',#8395,.T.);
#6656=FACE_OUTER_BOUND('',#8396,.T.);
#6657=FACE_OUTER_BOUND('',#8397,.T.);
#6658=FACE_OUTER_BOUND('',#8398,.T.);
#6659=FACE_OUTER_BOUND('',#8399,.T.);
#6660=FACE_OUTER_BOUND('',#8400,.T.);
#6661=FACE_OUTER_BOUND('',#8401,.T.);
#6662=FACE_OUTER_BOUND('',#8402,.T.);
#6663=FACE_OUTER_BOUND('',#8403,.T.);
#6664=FACE_OUTER_BOUND('',#8404,.T.);
#6665=FACE_OUTER_BOUND('',#8405,.T.);
#6666=FACE_OUTER_BOUND('',#8406,.T.);
#6667=FACE_OUTER_BOUND('',#8407,.T.);
#6668=FACE_OUTER_BOUND('',#8408,.T.);
#6669=FACE_OUTER_BOUND('',#8409,.T.);
#6670=FACE_OUTER_BOUND('',#8410,.T.);
#6671=FACE_OUTER_BOUND('',#8411,.T.);
#6672=FACE_OUTER_BOUND('',#8412,.T.);
#6673=FACE_OUTER_BOUND('',#8413,.T.);
#6674=FACE_OUTER_BOUND('',#8414,.T.);
#6675=FACE_OUTER_BOUND('',#8415,.T.);
#6676=FACE_OUTER_BOUND('',#8416,.T.);
#6677=FACE_OUTER_BOUND('',#8417,.T.);
#6678=FACE_OUTER_BOUND('',#8418,.T.);
#6679=FACE_OUTER_BOUND('',#8419,.T.);
#6680=FACE_OUTER_BOUND('',#8420,.T.);
#6681=FACE_OUTER_BOUND('',#8421,.T.);
#6682=FACE_OUTER_BOUND('',#8422,.T.);
#6683=FACE_OUTER_BOUND('',#8423,.T.);
#6684=FACE_OUTER_BOUND('',#8424,.T.);
#6685=FACE_OUTER_BOUND('',#8425,.T.);
#6686=FACE_OUTER_BOUND('',#8426,.T.);
#6687=FACE_OUTER_BOUND('',#8427,.T.);
#6688=FACE_OUTER_BOUND('',#8428,.T.);
#6689=FACE_OUTER_BOUND('',#8429,.T.);
#6690=FACE_OUTER_BOUND('',#8430,.T.);
#6691=FACE_OUTER_BOUND('',#8431,.T.);
#6692=FACE_OUTER_BOUND('',#8432,.T.);
#6693=FACE_OUTER_BOUND('',#8433,.T.);
#6694=FACE_OUTER_BOUND('',#8434,.T.);
#6695=FACE_OUTER_BOUND('',#8435,.T.);
#6696=FACE_OUTER_BOUND('',#8436,.T.);
#6697=FACE_OUTER_BOUND('',#8437,.T.);
#6698=FACE_OUTER_BOUND('',#8438,.T.);
#6699=FACE_OUTER_BOUND('',#8439,.T.);
#6700=FACE_OUTER_BOUND('',#8440,.T.);
#6701=FACE_OUTER_BOUND('',#8441,.T.);
#6702=FACE_OUTER_BOUND('',#8442,.T.);
#6703=FACE_OUTER_BOUND('',#8443,.T.);
#6704=FACE_OUTER_BOUND('',#8444,.T.);
#6705=FACE_OUTER_BOUND('',#8445,.T.);
#6706=FACE_OUTER_BOUND('',#8446,.T.);
#6707=FACE_OUTER_BOUND('',#8447,.T.);
#6708=FACE_OUTER_BOUND('',#8448,.T.);
#6709=FACE_OUTER_BOUND('',#8449,.T.);
#6710=FACE_OUTER_BOUND('',#8450,.T.);
#6711=FACE_OUTER_BOUND('',#8451,.T.);
#6712=FACE_OUTER_BOUND('',#8452,.T.);
#6713=FACE_OUTER_BOUND('',#8453,.T.);
#6714=FACE_OUTER_BOUND('',#8454,.T.);
#6715=FACE_OUTER_BOUND('',#8455,.T.);
#6716=FACE_OUTER_BOUND('',#8456,.T.);
#6717=FACE_OUTER_BOUND('',#8457,.T.);
#6718=FACE_OUTER_BOUND('',#8458,.T.);
#6719=FACE_OUTER_BOUND('',#8459,.T.);
#6720=FACE_OUTER_BOUND('',#8460,.T.);
#6721=FACE_OUTER_BOUND('',#8461,.T.);
#6722=FACE_OUTER_BOUND('',#8462,.T.);
#6723=FACE_OUTER_BOUND('',#8463,.T.);
#6724=FACE_OUTER_BOUND('',#8464,.T.);
#6725=FACE_OUTER_BOUND('',#8465,.T.);
#6726=FACE_OUTER_BOUND('',#8466,.T.);
#6727=FACE_OUTER_BOUND('',#8467,.T.);
#6728=FACE_OUTER_BOUND('',#8468,.T.);
#6729=FACE_OUTER_BOUND('',#8469,.T.);
#6730=FACE_OUTER_BOUND('',#8470,.T.);
#6731=FACE_OUTER_BOUND('',#8471,.T.);
#6732=FACE_OUTER_BOUND('',#8472,.T.);
#6733=FACE_OUTER_BOUND('',#8473,.T.);
#6734=FACE_OUTER_BOUND('',#8474,.T.);
#6735=FACE_OUTER_BOUND('',#8475,.T.);
#6736=FACE_OUTER_BOUND('',#8476,.T.);
#6737=FACE_OUTER_BOUND('',#8477,.T.);
#6738=FACE_OUTER_BOUND('',#8478,.T.);
#6739=FACE_OUTER_BOUND('',#8479,.T.);
#6740=FACE_OUTER_BOUND('',#8480,.T.);
#6741=FACE_OUTER_BOUND('',#8481,.T.);
#6742=FACE_OUTER_BOUND('',#8482,.T.);
#6743=FACE_OUTER_BOUND('',#8483,.T.);
#6744=FACE_OUTER_BOUND('',#8484,.T.);
#6745=FACE_OUTER_BOUND('',#8485,.T.);
#6746=FACE_OUTER_BOUND('',#8486,.T.);
#6747=FACE_OUTER_BOUND('',#8487,.T.);
#6748=FACE_OUTER_BOUND('',#8488,.T.);
#6749=FACE_OUTER_BOUND('',#8489,.T.);
#6750=FACE_OUTER_BOUND('',#8490,.T.);
#6751=FACE_OUTER_BOUND('',#8491,.T.);
#6752=FACE_OUTER_BOUND('',#8492,.T.);
#6753=FACE_OUTER_BOUND('',#8493,.T.);
#6754=FACE_OUTER_BOUND('',#8494,.T.);
#6755=FACE_OUTER_BOUND('',#8495,.T.);
#6756=FACE_OUTER_BOUND('',#8496,.T.);
#6757=FACE_OUTER_BOUND('',#8497,.T.);
#6758=FACE_OUTER_BOUND('',#8498,.T.);
#6759=FACE_OUTER_BOUND('',#8499,.T.);
#6760=FACE_OUTER_BOUND('',#8500,.T.);
#6761=FACE_OUTER_BOUND('',#8501,.T.);
#6762=FACE_OUTER_BOUND('',#8502,.T.);
#6763=FACE_OUTER_BOUND('',#8503,.T.);
#6764=FACE_OUTER_BOUND('',#8504,.T.);
#6765=FACE_OUTER_BOUND('',#8505,.T.);
#6766=FACE_OUTER_BOUND('',#8506,.T.);
#6767=FACE_OUTER_BOUND('',#8507,.T.);
#6768=FACE_OUTER_BOUND('',#8508,.T.);
#6769=FACE_OUTER_BOUND('',#8509,.T.);
#6770=FACE_OUTER_BOUND('',#8510,.T.);
#6771=FACE_OUTER_BOUND('',#8511,.T.);
#6772=FACE_OUTER_BOUND('',#8512,.T.);
#6773=FACE_OUTER_BOUND('',#8513,.T.);
#6774=FACE_OUTER_BOUND('',#8514,.T.);
#6775=FACE_OUTER_BOUND('',#8515,.T.);
#6776=FACE_OUTER_BOUND('',#8516,.T.);
#6777=FACE_OUTER_BOUND('',#8517,.T.);
#6778=FACE_OUTER_BOUND('',#8518,.T.);
#6779=FACE_OUTER_BOUND('',#8519,.T.);
#6780=FACE_OUTER_BOUND('',#8520,.T.);
#6781=FACE_OUTER_BOUND('',#8521,.T.);
#6782=FACE_OUTER_BOUND('',#8522,.T.);
#6783=FACE_OUTER_BOUND('',#8523,.T.);
#6784=FACE_OUTER_BOUND('',#8524,.T.);
#6785=FACE_OUTER_BOUND('',#8525,.T.);
#6786=FACE_OUTER_BOUND('',#8526,.T.);
#6787=FACE_OUTER_BOUND('',#8527,.T.);
#6788=FACE_OUTER_BOUND('',#8528,.T.);
#6789=FACE_OUTER_BOUND('',#8529,.T.);
#6790=FACE_OUTER_BOUND('',#8530,.T.);
#6791=FACE_OUTER_BOUND('',#8531,.T.);
#6792=FACE_OUTER_BOUND('',#8532,.T.);
#6793=FACE_OUTER_BOUND('',#8533,.T.);
#6794=FACE_OUTER_BOUND('',#8534,.T.);
#6795=FACE_OUTER_BOUND('',#8535,.T.);
#6796=FACE_OUTER_BOUND('',#8536,.T.);
#6797=FACE_OUTER_BOUND('',#8537,.T.);
#6798=FACE_OUTER_BOUND('',#8538,.T.);
#6799=FACE_OUTER_BOUND('',#8539,.T.);
#6800=FACE_OUTER_BOUND('',#8540,.T.);
#6801=FACE_OUTER_BOUND('',#8541,.T.);
#6802=FACE_OUTER_BOUND('',#8542,.T.);
#6803=FACE_OUTER_BOUND('',#8543,.T.);
#6804=FACE_OUTER_BOUND('',#8544,.T.);
#6805=FACE_OUTER_BOUND('',#8545,.T.);
#6806=FACE_OUTER_BOUND('',#8546,.T.);
#6807=FACE_OUTER_BOUND('',#8547,.T.);
#6808=FACE_OUTER_BOUND('',#8548,.T.);
#6809=FACE_OUTER_BOUND('',#8549,.T.);
#6810=FACE_OUTER_BOUND('',#8550,.T.);
#6811=FACE_OUTER_BOUND('',#8551,.T.);
#6812=FACE_OUTER_BOUND('',#8552,.T.);
#6813=FACE_OUTER_BOUND('',#8553,.T.);
#6814=FACE_OUTER_BOUND('',#8554,.T.);
#6815=FACE_OUTER_BOUND('',#8555,.T.);
#6816=FACE_OUTER_BOUND('',#8556,.T.);
#6817=FACE_OUTER_BOUND('',#8557,.T.);
#6818=FACE_OUTER_BOUND('',#8558,.T.);
#6819=FACE_OUTER_BOUND('',#8559,.T.);
#6820=FACE_OUTER_BOUND('',#8560,.T.);
#6821=FACE_OUTER_BOUND('',#8561,.T.);
#6822=FACE_OUTER_BOUND('',#8562,.T.);
#6823=FACE_OUTER_BOUND('',#8563,.T.);
#6824=FACE_OUTER_BOUND('',#8564,.T.);
#6825=FACE_OUTER_BOUND('',#8565,.T.);
#6826=FACE_OUTER_BOUND('',#8566,.T.);
#6827=FACE_OUTER_BOUND('',#8567,.T.);
#6828=FACE_OUTER_BOUND('',#8568,.T.);
#6829=FACE_OUTER_BOUND('',#8569,.T.);
#6830=FACE_OUTER_BOUND('',#8570,.T.);
#6831=FACE_OUTER_BOUND('',#8571,.T.);
#6832=FACE_OUTER_BOUND('',#8572,.T.);
#6833=FACE_OUTER_BOUND('',#8573,.T.);
#6834=FACE_OUTER_BOUND('',#8574,.T.);
#6835=FACE_OUTER_BOUND('',#8575,.T.);
#6836=FACE_OUTER_BOUND('',#8576,.T.);
#6837=FACE_OUTER_BOUND('',#8577,.T.);
#6838=FACE_OUTER_BOUND('',#8578,.T.);
#6839=FACE_OUTER_BOUND('',#8579,.T.);
#6840=FACE_OUTER_BOUND('',#8580,.T.);
#6841=FACE_OUTER_BOUND('',#8581,.T.);
#6842=FACE_OUTER_BOUND('',#8582,.T.);
#6843=FACE_OUTER_BOUND('',#8583,.T.);
#6844=FACE_OUTER_BOUND('',#8584,.T.);
#6845=FACE_OUTER_BOUND('',#8585,.T.);
#6846=FACE_OUTER_BOUND('',#8586,.T.);
#6847=FACE_OUTER_BOUND('',#8587,.T.);
#6848=FACE_OUTER_BOUND('',#8588,.T.);
#6849=FACE_OUTER_BOUND('',#8589,.T.);
#6850=FACE_OUTER_BOUND('',#8590,.T.);
#6851=FACE_OUTER_BOUND('',#8591,.T.);
#6852=FACE_OUTER_BOUND('',#8592,.T.);
#6853=FACE_OUTER_BOUND('',#8593,.T.);
#6854=FACE_OUTER_BOUND('',#8594,.T.);
#6855=FACE_OUTER_BOUND('',#8595,.T.);
#6856=FACE_OUTER_BOUND('',#8596,.T.);
#6857=FACE_OUTER_BOUND('',#8597,.T.);
#6858=FACE_OUTER_BOUND('',#8598,.T.);
#6859=FACE_OUTER_BOUND('',#8599,.T.);
#6860=FACE_OUTER_BOUND('',#8600,.T.);
#8036=EDGE_LOOP('',(#26429,#26430,#26431,#26432,#26433,#26434,#26435));
#8037=EDGE_LOOP('',(#26436,#26437,#26438,#26439));
#8038=EDGE_LOOP('',(#26440,#26441,#26442,#26443));
#8039=EDGE_LOOP('',(#26444,#26445,#26446,#26447));
#8040=EDGE_LOOP('',(#26448,#26449,#26450,#26451));
#8041=EDGE_LOOP('',(#26452,#26453,#26454,#26455));
#8042=EDGE_LOOP('',(#26456,#26457,#26458,#26459));
#8043=EDGE_LOOP('',(#26460,#26461,#26462,#26463));
#8044=EDGE_LOOP('',(#26464,#26465,#26466,#26467));
#8045=EDGE_LOOP('',(#26468,#26469,#26470,#26471));
#8046=EDGE_LOOP('',(#26472,#26473,#26474,#26475));
#8047=EDGE_LOOP('',(#26476,#26477,#26478,#26479));
#8048=EDGE_LOOP('',(#26480,#26481,#26482,#26483));
#8049=EDGE_LOOP('',(#26484,#26485,#26486,#26487));
#8050=EDGE_LOOP('',(#26488,#26489,#26490,#26491));
#8051=EDGE_LOOP('',(#26492,#26493,#26494,#26495));
#8052=EDGE_LOOP('',(#26496,#26497,#26498,#26499));
#8053=EDGE_LOOP('',(#26500,#26501,#26502,#26503));
#8054=EDGE_LOOP('',(#26504,#26505,#26506,#26507));
#8055=EDGE_LOOP('',(#26508,#26509,#26510,#26511));
#8056=EDGE_LOOP('',(#26512,#26513,#26514,#26515));
#8057=EDGE_LOOP('',(#26516,#26517,#26518,#26519));
#8058=EDGE_LOOP('',(#26520,#26521,#26522,#26523));
#8059=EDGE_LOOP('',(#26524,#26525,#26526,#26527));
#8060=EDGE_LOOP('',(#26528,#26529,#26530,#26531));
#8061=EDGE_LOOP('',(#26532,#26533,#26534,#26535));
#8062=EDGE_LOOP('',(#26536,#26537,#26538,#26539));
#8063=EDGE_LOOP('',(#26540,#26541,#26542,#26543));
#8064=EDGE_LOOP('',(#26544,#26545,#26546));
#8065=EDGE_LOOP('',(#26547,#26548,#26549));
#8066=EDGE_LOOP('',(#26550,#26551,#26552,#26553));
#8067=EDGE_LOOP('',(#26554,#26555,#26556,#26557));
#8068=EDGE_LOOP('',(#26558,#26559,#26560,#26561));
#8069=EDGE_LOOP('',(#26562,#26563,#26564,#26565));
#8070=EDGE_LOOP('',(#26566,#26567,#26568,#26569));
#8071=EDGE_LOOP('',(#26570,#26571,#26572,#26573));
#8072=EDGE_LOOP('',(#26574,#26575,#26576,#26577));
#8073=EDGE_LOOP('',(#26578,#26579,#26580,#26581));
#8074=EDGE_LOOP('',(#26582,#26583,#26584,#26585));
#8075=EDGE_LOOP('',(#26586,#26587,#26588,#26589));
#8076=EDGE_LOOP('',(#26590,#26591,#26592,#26593));
#8077=EDGE_LOOP('',(#26594,#26595,#26596,#26597));
#8078=EDGE_LOOP('',(#26598,#26599,#26600,#26601));
#8079=EDGE_LOOP('',(#26602,#26603,#26604,#26605));
#8080=EDGE_LOOP('',(#26606,#26607,#26608,#26609));
#8081=EDGE_LOOP('',(#26610,#26611,#26612,#26613));
#8082=EDGE_LOOP('',(#26614,#26615,#26616,#26617));
#8083=EDGE_LOOP('',(#26618,#26619,#26620,#26621));
#8084=EDGE_LOOP('',(#26622,#26623,#26624,#26625));
#8085=EDGE_LOOP('',(#26626,#26627,#26628,#26629));
#8086=EDGE_LOOP('',(#26630,#26631,#26632,#26633));
#8087=EDGE_LOOP('',(#26634,#26635,#26636,#26637));
#8088=EDGE_LOOP('',(#26638,#26639,#26640,#26641));
#8089=EDGE_LOOP('',(#26642,#26643,#26644,#26645));
#8090=EDGE_LOOP('',(#26646,#26647,#26648,#26649));
#8091=EDGE_LOOP('',(#26650,#26651,#26652,#26653));
#8092=EDGE_LOOP('',(#26654,#26655,#26656,#26657));
#8093=EDGE_LOOP('',(#26658,#26659,#26660,#26661));
#8094=EDGE_LOOP('',(#26662,#26663,#26664,#26665));
#8095=EDGE_LOOP('',(#26666,#26667,#26668));
#8096=EDGE_LOOP('',(#26669,#26670,#26671,#26672,#26673));
#8097=EDGE_LOOP('',(#26674,#26675,#26676,#26677));
#8098=EDGE_LOOP('',(#26678,#26679,#26680,#26681));
#8099=EDGE_LOOP('',(#26682,#26683,#26684,#26685));
#8100=EDGE_LOOP('',(#26686,#26687,#26688,#26689));
#8101=EDGE_LOOP('',(#26690,#26691,#26692,#26693));
#8102=EDGE_LOOP('',(#26694,#26695,#26696,#26697));
#8103=EDGE_LOOP('',(#26698,#26699,#26700,#26701));
#8104=EDGE_LOOP('',(#26702,#26703,#26704,#26705));
#8105=EDGE_LOOP('',(#26706,#26707,#26708,#26709));
#8106=EDGE_LOOP('',(#26710,#26711,#26712,#26713));
#8107=EDGE_LOOP('',(#26714,#26715,#26716,#26717));
#8108=EDGE_LOOP('',(#26718,#26719,#26720,#26721));
#8109=EDGE_LOOP('',(#26722,#26723,#26724,#26725));
#8110=EDGE_LOOP('',(#26726,#26727,#26728,#26729));
#8111=EDGE_LOOP('',(#26730,#26731,#26732,#26733));
#8112=EDGE_LOOP('',(#26734,#26735,#26736,#26737));
#8113=EDGE_LOOP('',(#26738,#26739,#26740,#26741,#26742,#26743,#26744,#26745,
#26746,#26747));
#8114=EDGE_LOOP('',(#26748,#26749,#26750,#26751));
#8115=EDGE_LOOP('',(#26752,#26753,#26754,#26755,#26756,#26757,#26758,#26759,
#26760,#26761,#26762,#26763,#26764,#26765,#26766,#26767,#26768,#26769,#26770,
#26771,#26772,#26773,#26774,#26775,#26776,#26777,#26778,#26779,#26780,#26781,
#26782,#26783,#26784,#26785,#26786,#26787,#26788,#26789,#26790,#26791,#26792,
#26793,#26794,#26795,#26796,#26797,#26798,#26799,#26800,#26801,#26802,#26803,
#26804,#26805,#26806,#26807,#26808,#26809,#26810,#26811,#26812,#26813,#26814,
#26815,#26816,#26817,#26818,#26819,#26820,#26821,#26822,#26823,#26824,#26825,
#26826,#26827,#26828,#26829,#26830,#26831,#26832,#26833,#26834,#26835,#26836,
#26837,#26838,#26839,#26840,#26841,#26842,#26843,#26844,#26845,#26846,#26847,
#26848,#26849,#26850,#26851,#26852,#26853,#26854,#26855,#26856,#26857,#26858,
#26859,#26860,#26861,#26862,#26863,#26864,#26865,#26866,#26867,#26868,#26869,
#26870,#26871,#26872,#26873,#26874,#26875,#26876,#26877,#26878,#26879,#26880,
#26881,#26882,#26883,#26884,#26885,#26886,#26887,#26888,#26889,#26890,#26891,
#26892,#26893,#26894,#26895,#26896,#26897,#26898,#26899,#26900,#26901,#26902,
#26903,#26904,#26905,#26906,#26907,#26908,#26909,#26910,#26911,#26912,#26913,
#26914,#26915,#26916,#26917,#26918,#26919,#26920,#26921,#26922,#26923,#26924,
#26925,#26926,#26927,#26928,#26929,#26930,#26931,#26932,#26933,#26934,#26935,
#26936,#26937,#26938,#26939,#26940,#26941,#26942,#26943,#26944,#26945,#26946,
#26947,#26948,#26949,#26950,#26951,#26952,#26953,#26954,#26955,#26956,#26957,
#26958,#26959,#26960,#26961,#26962,#26963,#26964,#26965,#26966,#26967,#26968,
#26969,#26970,#26971,#26972,#26973,#26974,#26975,#26976,#26977,#26978,#26979,
#26980,#26981,#26982,#26983,#26984,#26985,#26986,#26987,#26988,#26989,#26990,
#26991,#26992,#26993,#26994,#26995,#26996,#26997,#26998,#26999,#27000,#27001,
#27002,#27003,#27004,#27005,#27006,#27007,#27008,#27009,#27010,#27011,#27012,
#27013,#27014,#27015,#27016,#27017,#27018,#27019,#27020,#27021,#27022,#27023,
#27024,#27025,#27026,#27027,#27028,#27029,#27030,#27031,#27032,#27033,#27034,
#27035,#27036,#27037,#27038,#27039,#27040,#27041,#27042,#27043,#27044,#27045,
#27046,#27047,#27048,#27049,#27050,#27051,#27052,#27053,#27054,#27055,#27056,
#27057,#27058,#27059,#27060,#27061,#27062,#27063,#27064,#27065,#27066,#27067,
#27068,#27069,#27070,#27071,#27072,#27073,#27074,#27075));
#8116=EDGE_LOOP('',(#27076,#27077,#27078,#27079,#27080,#27081,#27082,#27083,
#27084,#27085,#27086,#27087,#27088,#27089,#27090,#27091,#27092,#27093,#27094,
#27095,#27096,#27097,#27098,#27099,#27100,#27101,#27102,#27103,#27104,#27105,
#27106,#27107,#27108,#27109,#27110,#27111,#27112,#27113,#27114,#27115,#27116,
#27117,#27118,#27119,#27120,#27121,#27122,#27123,#27124,#27125,#27126,#27127,
#27128,#27129,#27130,#27131,#27132,#27133,#27134,#27135,#27136,#27137,#27138,
#27139,#27140,#27141,#27142,#27143,#27144,#27145,#27146,#27147,#27148,#27149,
#27150,#27151,#27152,#27153,#27154,#27155,#27156,#27157,#27158,#27159,#27160,
#27161,#27162,#27163,#27164,#27165,#27166,#27167,#27168,#27169,#27170,#27171,
#27172,#27173,#27174,#27175,#27176,#27177,#27178,#27179,#27180,#27181,#27182,
#27183,#27184,#27185,#27186,#27187,#27188,#27189,#27190,#27191,#27192,#27193,
#27194,#27195,#27196,#27197,#27198,#27199,#27200,#27201,#27202,#27203,#27204,
#27205,#27206,#27207,#27208,#27209,#27210,#27211,#27212,#27213,#27214,#27215,
#27216,#27217,#27218,#27219,#27220,#27221,#27222,#27223,#27224,#27225,#27226,
#27227,#27228,#27229,#27230,#27231,#27232,#27233,#27234,#27235,#27236,#27237,
#27238,#27239,#27240,#27241,#27242,#27243,#27244,#27245,#27246,#27247,#27248,
#27249,#27250,#27251,#27252,#27253,#27254,#27255,#27256,#27257,#27258,#27259,
#27260,#27261,#27262,#27263,#27264,#27265,#27266,#27267,#27268,#27269,#27270,
#27271,#27272,#27273,#27274,#27275,#27276,#27277,#27278,#27279,#27280,#27281,
#27282,#27283,#27284,#27285,#27286,#27287,#27288,#27289,#27290,#27291,#27292,
#27293,#27294,#27295,#27296,#27297,#27298,#27299,#27300,#27301,#27302,#27303,
#27304,#27305,#27306,#27307,#27308,#27309,#27310,#27311,#27312,#27313,#27314,
#27315,#27316,#27317,#27318,#27319,#27320,#27321,#27322,#27323,#27324,#27325,
#27326,#27327,#27328,#27329,#27330,#27331,#27332,#27333,#27334,#27335,#27336,
#27337,#27338,#27339,#27340,#27341,#27342,#27343,#27344,#27345,#27346,#27347,
#27348,#27349,#27350,#27351,#27352,#27353,#27354,#27355,#27356,#27357,#27358,
#27359,#27360,#27361,#27362,#27363,#27364,#27365,#27366,#27367,#27368,#27369,
#27370,#27371,#27372,#27373,#27374,#27375,#27376,#27377,#27378,#27379,#27380,
#27381,#27382,#27383,#27384,#27385,#27386,#27387,#27388,#27389,#27390,#27391,
#27392,#27393,#27394,#27395,#27396,#27397,#27398,#27399,#27400));
#8117=EDGE_LOOP('',(#27401,#27402,#27403,#27404,#27405));
#8118=EDGE_LOOP('',(#27406,#27407,#27408,#27409));
#8119=EDGE_LOOP('',(#27410,#27411,#27412,#27413));
#8120=EDGE_LOOP('',(#27414,#27415,#27416,#27417));
#8121=EDGE_LOOP('',(#27418,#27419,#27420,#27421));
#8122=EDGE_LOOP('',(#27422,#27423,#27424,#27425));
#8123=EDGE_LOOP('',(#27426,#27427,#27428,#27429));
#8124=EDGE_LOOP('',(#27430,#27431,#27432,#27433));
#8125=EDGE_LOOP('',(#27434,#27435,#27436,#27437));
#8126=EDGE_LOOP('',(#27438,#27439,#27440,#27441));
#8127=EDGE_LOOP('',(#27442,#27443,#27444,#27445));
#8128=EDGE_LOOP('',(#27446,#27447,#27448,#27449));
#8129=EDGE_LOOP('',(#27450,#27451,#27452,#27453));
#8130=EDGE_LOOP('',(#27454,#27455,#27456,#27457));
#8131=EDGE_LOOP('',(#27458,#27459,#27460,#27461));
#8132=EDGE_LOOP('',(#27462,#27463,#27464,#27465));
#8133=EDGE_LOOP('',(#27466,#27467,#27468,#27469));
#8134=EDGE_LOOP('',(#27470,#27471,#27472,#27473));
#8135=EDGE_LOOP('',(#27474,#27475,#27476,#27477));
#8136=EDGE_LOOP('',(#27478,#27479,#27480,#27481));
#8137=EDGE_LOOP('',(#27482,#27483,#27484,#27485));
#8138=EDGE_LOOP('',(#27486,#27487,#27488,#27489));
#8139=EDGE_LOOP('',(#27490,#27491,#27492,#27493));
#8140=EDGE_LOOP('',(#27494,#27495,#27496,#27497));
#8141=EDGE_LOOP('',(#27498,#27499,#27500,#27501));
#8142=EDGE_LOOP('',(#27502,#27503,#27504,#27505));
#8143=EDGE_LOOP('',(#27506,#27507,#27508,#27509));
#8144=EDGE_LOOP('',(#27510,#27511,#27512,#27513));
#8145=EDGE_LOOP('',(#27514,#27515,#27516,#27517));
#8146=EDGE_LOOP('',(#27518,#27519,#27520,#27521));
#8147=EDGE_LOOP('',(#27522,#27523,#27524,#27525));
#8148=EDGE_LOOP('',(#27526,#27527,#27528,#27529));
#8149=EDGE_LOOP('',(#27530,#27531,#27532,#27533));
#8150=EDGE_LOOP('',(#27534,#27535,#27536,#27537));
#8151=EDGE_LOOP('',(#27538,#27539,#27540,#27541));
#8152=EDGE_LOOP('',(#27542,#27543,#27544,#27545));
#8153=EDGE_LOOP('',(#27546,#27547,#27548,#27549));
#8154=EDGE_LOOP('',(#27550,#27551,#27552,#27553));
#8155=EDGE_LOOP('',(#27554,#27555,#27556,#27557));
#8156=EDGE_LOOP('',(#27558,#27559,#27560,#27561));
#8157=EDGE_LOOP('',(#27562,#27563,#27564,#27565));
#8158=EDGE_LOOP('',(#27566,#27567,#27568,#27569));
#8159=EDGE_LOOP('',(#27570,#27571,#27572,#27573));
#8160=EDGE_LOOP('',(#27574,#27575,#27576,#27577));
#8161=EDGE_LOOP('',(#27578,#27579,#27580,#27581));
#8162=EDGE_LOOP('',(#27582,#27583,#27584,#27585));
#8163=EDGE_LOOP('',(#27586,#27587,#27588,#27589));
#8164=EDGE_LOOP('',(#27590,#27591,#27592,#27593));
#8165=EDGE_LOOP('',(#27594,#27595,#27596,#27597));
#8166=EDGE_LOOP('',(#27598,#27599,#27600,#27601));
#8167=EDGE_LOOP('',(#27602,#27603,#27604,#27605));
#8168=EDGE_LOOP('',(#27606,#27607,#27608,#27609));
#8169=EDGE_LOOP('',(#27610,#27611,#27612,#27613));
#8170=EDGE_LOOP('',(#27614,#27615,#27616,#27617));
#8171=EDGE_LOOP('',(#27618,#27619,#27620,#27621));
#8172=EDGE_LOOP('',(#27622,#27623,#27624,#27625));
#8173=EDGE_LOOP('',(#27626,#27627,#27628,#27629));
#8174=EDGE_LOOP('',(#27630,#27631,#27632,#27633));
#8175=EDGE_LOOP('',(#27634,#27635,#27636,#27637));
#8176=EDGE_LOOP('',(#27638,#27639,#27640,#27641));
#8177=EDGE_LOOP('',(#27642,#27643,#27644,#27645));
#8178=EDGE_LOOP('',(#27646,#27647,#27648,#27649));
#8179=EDGE_LOOP('',(#27650,#27651,#27652,#27653));
#8180=EDGE_LOOP('',(#27654,#27655,#27656,#27657));
#8181=EDGE_LOOP('',(#27658,#27659,#27660,#27661));
#8182=EDGE_LOOP('',(#27662,#27663,#27664,#27665));
#8183=EDGE_LOOP('',(#27666,#27667,#27668,#27669));
#8184=EDGE_LOOP('',(#27670,#27671,#27672,#27673));
#8185=EDGE_LOOP('',(#27674,#27675,#27676,#27677));
#8186=EDGE_LOOP('',(#27678,#27679,#27680,#27681));
#8187=EDGE_LOOP('',(#27682,#27683,#27684,#27685));
#8188=EDGE_LOOP('',(#27686,#27687,#27688,#27689));
#8189=EDGE_LOOP('',(#27690,#27691,#27692,#27693));
#8190=EDGE_LOOP('',(#27694,#27695,#27696,#27697));
#8191=EDGE_LOOP('',(#27698,#27699,#27700,#27701));
#8192=EDGE_LOOP('',(#27702,#27703,#27704,#27705));
#8193=EDGE_LOOP('',(#27706,#27707,#27708,#27709));
#8194=EDGE_LOOP('',(#27710,#27711,#27712,#27713));
#8195=EDGE_LOOP('',(#27714,#27715,#27716,#27717));
#8196=EDGE_LOOP('',(#27718,#27719,#27720,#27721));
#8197=EDGE_LOOP('',(#27722,#27723,#27724,#27725));
#8198=EDGE_LOOP('',(#27726,#27727,#27728,#27729));
#8199=EDGE_LOOP('',(#27730,#27731,#27732,#27733));
#8200=EDGE_LOOP('',(#27734,#27735,#27736,#27737));
#8201=EDGE_LOOP('',(#27738,#27739,#27740,#27741));
#8202=EDGE_LOOP('',(#27742,#27743,#27744,#27745));
#8203=EDGE_LOOP('',(#27746,#27747,#27748,#27749));
#8204=EDGE_LOOP('',(#27750,#27751,#27752,#27753));
#8205=EDGE_LOOP('',(#27754,#27755,#27756,#27757));
#8206=EDGE_LOOP('',(#27758,#27759,#27760,#27761));
#8207=EDGE_LOOP('',(#27762,#27763,#27764,#27765));
#8208=EDGE_LOOP('',(#27766,#27767,#27768,#27769));
#8209=EDGE_LOOP('',(#27770,#27771,#27772,#27773));
#8210=EDGE_LOOP('',(#27774,#27775,#27776,#27777));
#8211=EDGE_LOOP('',(#27778,#27779,#27780,#27781));
#8212=EDGE_LOOP('',(#27782,#27783,#27784,#27785));
#8213=EDGE_LOOP('',(#27786,#27787,#27788,#27789));
#8214=EDGE_LOOP('',(#27790,#27791,#27792,#27793));
#8215=EDGE_LOOP('',(#27794,#27795,#27796,#27797));
#8216=EDGE_LOOP('',(#27798,#27799,#27800,#27801));
#8217=EDGE_LOOP('',(#27802,#27803,#27804,#27805));
#8218=EDGE_LOOP('',(#27806,#27807,#27808,#27809));
#8219=EDGE_LOOP('',(#27810,#27811,#27812,#27813));
#8220=EDGE_LOOP('',(#27814,#27815,#27816,#27817));
#8221=EDGE_LOOP('',(#27818,#27819,#27820,#27821));
#8222=EDGE_LOOP('',(#27822,#27823,#27824,#27825));
#8223=EDGE_LOOP('',(#27826,#27827,#27828,#27829));
#8224=EDGE_LOOP('',(#27830,#27831,#27832,#27833));
#8225=EDGE_LOOP('',(#27834,#27835,#27836,#27837));
#8226=EDGE_LOOP('',(#27838,#27839,#27840,#27841));
#8227=EDGE_LOOP('',(#27842,#27843,#27844,#27845));
#8228=EDGE_LOOP('',(#27846,#27847,#27848,#27849));
#8229=EDGE_LOOP('',(#27850,#27851,#27852,#27853));
#8230=EDGE_LOOP('',(#27854,#27855,#27856,#27857));
#8231=EDGE_LOOP('',(#27858,#27859,#27860,#27861));
#8232=EDGE_LOOP('',(#27862,#27863,#27864,#27865));
#8233=EDGE_LOOP('',(#27866,#27867,#27868,#27869));
#8234=EDGE_LOOP('',(#27870,#27871,#27872,#27873));
#8235=EDGE_LOOP('',(#27874,#27875,#27876,#27877));
#8236=EDGE_LOOP('',(#27878,#27879,#27880,#27881));
#8237=EDGE_LOOP('',(#27882,#27883,#27884,#27885));
#8238=EDGE_LOOP('',(#27886,#27887,#27888,#27889));
#8239=EDGE_LOOP('',(#27890,#27891,#27892,#27893));
#8240=EDGE_LOOP('',(#27894,#27895,#27896,#27897));
#8241=EDGE_LOOP('',(#27898,#27899,#27900,#27901));
#8242=EDGE_LOOP('',(#27902,#27903,#27904,#27905));
#8243=EDGE_LOOP('',(#27906,#27907,#27908,#27909));
#8244=EDGE_LOOP('',(#27910,#27911,#27912,#27913));
#8245=EDGE_LOOP('',(#27914,#27915,#27916,#27917));
#8246=EDGE_LOOP('',(#27918,#27919,#27920,#27921));
#8247=EDGE_LOOP('',(#27922,#27923,#27924,#27925));
#8248=EDGE_LOOP('',(#27926,#27927,#27928,#27929));
#8249=EDGE_LOOP('',(#27930,#27931,#27932,#27933));
#8250=EDGE_LOOP('',(#27934,#27935,#27936,#27937));
#8251=EDGE_LOOP('',(#27938,#27939,#27940,#27941));
#8252=EDGE_LOOP('',(#27942,#27943,#27944,#27945));
#8253=EDGE_LOOP('',(#27946,#27947,#27948,#27949));
#8254=EDGE_LOOP('',(#27950,#27951,#27952,#27953));
#8255=EDGE_LOOP('',(#27954,#27955,#27956,#27957));
#8256=EDGE_LOOP('',(#27958,#27959,#27960,#27961));
#8257=EDGE_LOOP('',(#27962,#27963,#27964,#27965));
#8258=EDGE_LOOP('',(#27966,#27967,#27968,#27969));
#8259=EDGE_LOOP('',(#27970,#27971,#27972,#27973));
#8260=EDGE_LOOP('',(#27974,#27975,#27976,#27977));
#8261=EDGE_LOOP('',(#27978,#27979,#27980,#27981));
#8262=EDGE_LOOP('',(#27982,#27983,#27984,#27985));
#8263=EDGE_LOOP('',(#27986,#27987,#27988,#27989));
#8264=EDGE_LOOP('',(#27990,#27991,#27992,#27993));
#8265=EDGE_LOOP('',(#27994,#27995,#27996,#27997));
#8266=EDGE_LOOP('',(#27998,#27999,#28000,#28001));
#8267=EDGE_LOOP('',(#28002,#28003,#28004,#28005));
#8268=EDGE_LOOP('',(#28006,#28007,#28008,#28009));
#8269=EDGE_LOOP('',(#28010,#28011,#28012,#28013));
#8270=EDGE_LOOP('',(#28014,#28015,#28016,#28017));
#8271=EDGE_LOOP('',(#28018,#28019,#28020,#28021));
#8272=EDGE_LOOP('',(#28022,#28023,#28024,#28025));
#8273=EDGE_LOOP('',(#28026,#28027,#28028,#28029));
#8274=EDGE_LOOP('',(#28030,#28031,#28032,#28033));
#8275=EDGE_LOOP('',(#28034,#28035,#28036,#28037));
#8276=EDGE_LOOP('',(#28038,#28039,#28040,#28041));
#8277=EDGE_LOOP('',(#28042,#28043,#28044,#28045));
#8278=EDGE_LOOP('',(#28046,#28047,#28048,#28049));
#8279=EDGE_LOOP('',(#28050,#28051,#28052,#28053));
#8280=EDGE_LOOP('',(#28054,#28055,#28056,#28057));
#8281=EDGE_LOOP('',(#28058,#28059,#28060,#28061));
#8282=EDGE_LOOP('',(#28062,#28063,#28064,#28065));
#8283=EDGE_LOOP('',(#28066,#28067,#28068,#28069));
#8284=EDGE_LOOP('',(#28070,#28071,#28072,#28073));
#8285=EDGE_LOOP('',(#28074,#28075,#28076,#28077));
#8286=EDGE_LOOP('',(#28078,#28079,#28080,#28081));
#8287=EDGE_LOOP('',(#28082,#28083,#28084,#28085));
#8288=EDGE_LOOP('',(#28086,#28087,#28088,#28089));
#8289=EDGE_LOOP('',(#28090,#28091,#28092,#28093));
#8290=EDGE_LOOP('',(#28094,#28095,#28096,#28097));
#8291=EDGE_LOOP('',(#28098,#28099,#28100,#28101));
#8292=EDGE_LOOP('',(#28102,#28103,#28104,#28105));
#8293=EDGE_LOOP('',(#28106,#28107,#28108,#28109));
#8294=EDGE_LOOP('',(#28110,#28111,#28112,#28113));
#8295=EDGE_LOOP('',(#28114,#28115,#28116,#28117));
#8296=EDGE_LOOP('',(#28118,#28119,#28120,#28121));
#8297=EDGE_LOOP('',(#28122,#28123,#28124,#28125));
#8298=EDGE_LOOP('',(#28126,#28127,#28128,#28129));
#8299=EDGE_LOOP('',(#28130,#28131,#28132,#28133));
#8300=EDGE_LOOP('',(#28134,#28135,#28136,#28137));
#8301=EDGE_LOOP('',(#28138,#28139,#28140,#28141));
#8302=EDGE_LOOP('',(#28142,#28143,#28144,#28145));
#8303=EDGE_LOOP('',(#28146,#28147,#28148,#28149));
#8304=EDGE_LOOP('',(#28150,#28151,#28152,#28153));
#8305=EDGE_LOOP('',(#28154,#28155,#28156,#28157));
#8306=EDGE_LOOP('',(#28158,#28159,#28160,#28161));
#8307=EDGE_LOOP('',(#28162,#28163,#28164,#28165));
#8308=EDGE_LOOP('',(#28166,#28167,#28168,#28169));
#8309=EDGE_LOOP('',(#28170,#28171,#28172,#28173));
#8310=EDGE_LOOP('',(#28174,#28175,#28176,#28177));
#8311=EDGE_LOOP('',(#28178,#28179,#28180,#28181));
#8312=EDGE_LOOP('',(#28182,#28183,#28184,#28185));
#8313=EDGE_LOOP('',(#28186,#28187,#28188,#28189));
#8314=EDGE_LOOP('',(#28190,#28191,#28192,#28193));
#8315=EDGE_LOOP('',(#28194,#28195,#28196,#28197));
#8316=EDGE_LOOP('',(#28198,#28199,#28200,#28201));
#8317=EDGE_LOOP('',(#28202,#28203,#28204,#28205));
#8318=EDGE_LOOP('',(#28206,#28207,#28208,#28209));
#8319=EDGE_LOOP('',(#28210,#28211,#28212,#28213));
#8320=EDGE_LOOP('',(#28214,#28215,#28216,#28217));
#8321=EDGE_LOOP('',(#28218,#28219,#28220,#28221));
#8322=EDGE_LOOP('',(#28222,#28223,#28224,#28225));
#8323=EDGE_LOOP('',(#28226,#28227,#28228,#28229));
#8324=EDGE_LOOP('',(#28230,#28231,#28232,#28233));
#8325=EDGE_LOOP('',(#28234,#28235,#28236,#28237));
#8326=EDGE_LOOP('',(#28238,#28239,#28240,#28241));
#8327=EDGE_LOOP('',(#28242,#28243,#28244,#28245));
#8328=EDGE_LOOP('',(#28246,#28247,#28248,#28249));
#8329=EDGE_LOOP('',(#28250,#28251,#28252,#28253));
#8330=EDGE_LOOP('',(#28254,#28255,#28256,#28257));
#8331=EDGE_LOOP('',(#28258,#28259,#28260,#28261));
#8332=EDGE_LOOP('',(#28262,#28263,#28264,#28265));
#8333=EDGE_LOOP('',(#28266,#28267,#28268,#28269));
#8334=EDGE_LOOP('',(#28270,#28271,#28272,#28273));
#8335=EDGE_LOOP('',(#28274,#28275,#28276,#28277));
#8336=EDGE_LOOP('',(#28278,#28279,#28280,#28281));
#8337=EDGE_LOOP('',(#28282,#28283,#28284,#28285));
#8338=EDGE_LOOP('',(#28286,#28287,#28288,#28289));
#8339=EDGE_LOOP('',(#28290,#28291,#28292,#28293));
#8340=EDGE_LOOP('',(#28294,#28295,#28296,#28297));
#8341=EDGE_LOOP('',(#28298,#28299,#28300,#28301));
#8342=EDGE_LOOP('',(#28302,#28303,#28304,#28305));
#8343=EDGE_LOOP('',(#28306,#28307,#28308,#28309));
#8344=EDGE_LOOP('',(#28310,#28311,#28312,#28313));
#8345=EDGE_LOOP('',(#28314,#28315,#28316,#28317));
#8346=EDGE_LOOP('',(#28318,#28319,#28320,#28321));
#8347=EDGE_LOOP('',(#28322,#28323,#28324,#28325));
#8348=EDGE_LOOP('',(#28326,#28327,#28328,#28329));
#8349=EDGE_LOOP('',(#28330,#28331,#28332,#28333));
#8350=EDGE_LOOP('',(#28334,#28335,#28336,#28337));
#8351=EDGE_LOOP('',(#28338,#28339,#28340,#28341));
#8352=EDGE_LOOP('',(#28342,#28343,#28344,#28345));
#8353=EDGE_LOOP('',(#28346,#28347,#28348,#28349));
#8354=EDGE_LOOP('',(#28350,#28351,#28352,#28353));
#8355=EDGE_LOOP('',(#28354,#28355,#28356,#28357));
#8356=EDGE_LOOP('',(#28358,#28359,#28360,#28361));
#8357=EDGE_LOOP('',(#28362,#28363,#28364,#28365));
#8358=EDGE_LOOP('',(#28366,#28367,#28368));
#8359=EDGE_LOOP('',(#28369));
#8360=EDGE_LOOP('',(#28370));
#8361=EDGE_LOOP('',(#28371,#28372,#28373,#28374));
#8362=EDGE_LOOP('',(#28375,#28376,#28377,#28378));
#8363=EDGE_LOOP('',(#28379,#28380,#28381,#28382));
#8364=EDGE_LOOP('',(#28383));
#8365=EDGE_LOOP('',(#28384));
#8366=EDGE_LOOP('',(#28385,#28386,#28387,#28388,#28389,#28390));
#8367=EDGE_LOOP('',(#28391,#28392,#28393,#28394));
#8368=EDGE_LOOP('',(#28395,#28396,#28397,#28398));
#8369=EDGE_LOOP('',(#28399,#28400,#28401,#28402));
#8370=EDGE_LOOP('',(#28403,#28404,#28405,#28406,#28407));
#8371=EDGE_LOOP('',(#28408,#28409,#28410,#28411));
#8372=EDGE_LOOP('',(#28412,#28413,#28414,#28415));
#8373=EDGE_LOOP('',(#28416,#28417,#28418,#28419,#28420,#28421,#28422,#28423,
#28424,#28425,#28426,#28427,#28428,#28429,#28430,#28431,#28432,#28433,#28434,
#28435,#28436,#28437,#28438,#28439,#28440,#28441,#28442,#28443,#28444,#28445,
#28446,#28447,#28448,#28449,#28450,#28451,#28452,#28453,#28454,#28455,#28456,
#28457,#28458,#28459,#28460,#28461,#28462,#28463,#28464,#28465,#28466,#28467,
#28468,#28469,#28470,#28471,#28472,#28473,#28474,#28475,#28476,#28477));
#8374=EDGE_LOOP('',(#28478,#28479,#28480,#28481,#28482,#28483,#28484,#28485,
#28486,#28487,#28488,#28489,#28490,#28491,#28492,#28493,#28494,#28495,#28496,
#28497,#28498,#28499,#28500,#28501,#28502,#28503,#28504,#28505,#28506,#28507,
#28508,#28509,#28510,#28511,#28512,#28513,#28514,#28515,#28516,#28517,#28518,
#28519,#28520,#28521,#28522,#28523,#28524,#28525,#28526,#28527,#28528,#28529,
#28530,#28531,#28532,#28533,#28534,#28535,#28536,#28537,#28538));
#8375=EDGE_LOOP('',(#28539,#28540,#28541,#28542));
#8376=EDGE_LOOP('',(#28543,#28544,#28545,#28546,#28547,#28548));
#8377=EDGE_LOOP('',(#28549,#28550,#28551,#28552,#28553));
#8378=EDGE_LOOP('',(#28554,#28555,#28556,#28557,#28558,#28559));
#8379=EDGE_LOOP('',(#28560,#28561,#28562,#28563,#28564,#28565));
#8380=EDGE_LOOP('',(#28566,#28567,#28568,#28569));
#8381=EDGE_LOOP('',(#28570,#28571,#28572,#28573,#28574,#28575));
#8382=EDGE_LOOP('',(#28576,#28577,#28578,#28579,#28580,#28581));
#8383=EDGE_LOOP('',(#28582,#28583,#28584,#28585));
#8384=EDGE_LOOP('',(#28586,#28587,#28588,#28589,#28590,#28591));
#8385=EDGE_LOOP('',(#28592,#28593,#28594,#28595,#28596,#28597));
#8386=EDGE_LOOP('',(#28598,#28599,#28600,#28601));
#8387=EDGE_LOOP('',(#28602,#28603,#28604,#28605,#28606,#28607));
#8388=EDGE_LOOP('',(#28608,#28609,#28610,#28611,#28612,#28613));
#8389=EDGE_LOOP('',(#28614,#28615,#28616,#28617));
#8390=EDGE_LOOP('',(#28618,#28619,#28620,#28621,#28622,#28623));
#8391=EDGE_LOOP('',(#28624,#28625,#28626,#28627,#28628,#28629));
#8392=EDGE_LOOP('',(#28630,#28631,#28632,#28633));
#8393=EDGE_LOOP('',(#28634,#28635,#28636,#28637,#28638,#28639));
#8394=EDGE_LOOP('',(#28640,#28641,#28642,#28643,#28644,#28645));
#8395=EDGE_LOOP('',(#28646,#28647,#28648,#28649));
#8396=EDGE_LOOP('',(#28650,#28651,#28652,#28653,#28654,#28655));
#8397=EDGE_LOOP('',(#28656,#28657,#28658,#28659,#28660,#28661));
#8398=EDGE_LOOP('',(#28662,#28663,#28664,#28665,#28666,#28667));
#8399=EDGE_LOOP('',(#28668,#28669,#28670,#28671,#28672,#28673));
#8400=EDGE_LOOP('',(#28674,#28675,#28676,#28677,#28678,#28679));
#8401=EDGE_LOOP('',(#28680,#28681,#28682,#28683,#28684,#28685));
#8402=EDGE_LOOP('',(#28686,#28687,#28688,#28689,#28690,#28691));
#8403=EDGE_LOOP('',(#28692,#28693,#28694,#28695,#28696,#28697));
#8404=EDGE_LOOP('',(#28698,#28699,#28700,#28701,#28702,#28703));
#8405=EDGE_LOOP('',(#28704,#28705,#28706,#28707,#28708,#28709));
#8406=EDGE_LOOP('',(#28710,#28711,#28712,#28713,#28714,#28715));
#8407=EDGE_LOOP('',(#28716,#28717,#28718,#28719,#28720,#28721));
#8408=EDGE_LOOP('',(#28722,#28723,#28724,#28725,#28726,#28727));
#8409=EDGE_LOOP('',(#28728,#28729,#28730,#28731,#28732,#28733));
#8410=EDGE_LOOP('',(#28734,#28735,#28736,#28737,#28738,#28739));
#8411=EDGE_LOOP('',(#28740,#28741,#28742,#28743,#28744,#28745));
#8412=EDGE_LOOP('',(#28746,#28747,#28748,#28749,#28750,#28751));
#8413=EDGE_LOOP('',(#28752,#28753,#28754,#28755,#28756,#28757));
#8414=EDGE_LOOP('',(#28758,#28759,#28760,#28761,#28762,#28763));
#8415=EDGE_LOOP('',(#28764,#28765,#28766,#28767,#28768,#28769));
#8416=EDGE_LOOP('',(#28770,#28771,#28772,#28773));
#8417=EDGE_LOOP('',(#28774,#28775,#28776,#28777,#28778,#28779));
#8418=EDGE_LOOP('',(#28780,#28781,#28782,#28783,#28784,#28785));
#8419=EDGE_LOOP('',(#28786,#28787,#28788,#28789));
#8420=EDGE_LOOP('',(#28790,#28791,#28792,#28793,#28794,#28795));
#8421=EDGE_LOOP('',(#28796,#28797,#28798,#28799,#28800,#28801));
#8422=EDGE_LOOP('',(#28802,#28803,#28804,#28805));
#8423=EDGE_LOOP('',(#28806,#28807,#28808,#28809,#28810,#28811));
#8424=EDGE_LOOP('',(#28812,#28813,#28814,#28815,#28816,#28817));
#8425=EDGE_LOOP('',(#28818,#28819,#28820,#28821));
#8426=EDGE_LOOP('',(#28822,#28823,#28824,#28825,#28826,#28827));
#8427=EDGE_LOOP('',(#28828,#28829,#28830,#28831,#28832,#28833));
#8428=EDGE_LOOP('',(#28834,#28835,#28836,#28837));
#8429=EDGE_LOOP('',(#28838,#28839,#28840,#28841,#28842,#28843));
#8430=EDGE_LOOP('',(#28844,#28845,#28846,#28847,#28848,#28849));
#8431=EDGE_LOOP('',(#28850,#28851,#28852,#28853));
#8432=EDGE_LOOP('',(#28854,#28855,#28856,#28857,#28858,#28859));
#8433=EDGE_LOOP('',(#28860,#28861,#28862,#28863,#28864,#28865));
#8434=EDGE_LOOP('',(#28866,#28867,#28868,#28869));
#8435=EDGE_LOOP('',(#28870,#28871,#28872,#28873,#28874,#28875));
#8436=EDGE_LOOP('',(#28876,#28877,#28878,#28879,#28880,#28881));
#8437=EDGE_LOOP('',(#28882,#28883,#28884,#28885));
#8438=EDGE_LOOP('',(#28886,#28887,#28888,#28889,#28890,#28891));
#8439=EDGE_LOOP('',(#28892,#28893,#28894,#28895,#28896,#28897));
#8440=EDGE_LOOP('',(#28898,#28899,#28900,#28901));
#8441=EDGE_LOOP('',(#28902,#28903,#28904,#28905,#28906,#28907));
#8442=EDGE_LOOP('',(#28908,#28909,#28910,#28911,#28912,#28913));
#8443=EDGE_LOOP('',(#28914,#28915,#28916,#28917));
#8444=EDGE_LOOP('',(#28918,#28919,#28920,#28921,#28922,#28923));
#8445=EDGE_LOOP('',(#28924,#28925,#28926,#28927,#28928,#28929));
#8446=EDGE_LOOP('',(#28930,#28931,#28932,#28933));
#8447=EDGE_LOOP('',(#28934,#28935,#28936,#28937,#28938,#28939));
#8448=EDGE_LOOP('',(#28940,#28941,#28942,#28943,#28944,#28945));
#8449=EDGE_LOOP('',(#28946,#28947,#28948,#28949));
#8450=EDGE_LOOP('',(#28950,#28951,#28952,#28953,#28954,#28955));
#8451=EDGE_LOOP('',(#28956,#28957,#28958,#28959,#28960,#28961));
#8452=EDGE_LOOP('',(#28962,#28963,#28964,#28965));
#8453=EDGE_LOOP('',(#28966,#28967,#28968,#28969,#28970,#28971));
#8454=EDGE_LOOP('',(#28972,#28973,#28974,#28975,#28976,#28977));
#8455=EDGE_LOOP('',(#28978,#28979,#28980,#28981));
#8456=EDGE_LOOP('',(#28982,#28983,#28984,#28985,#28986,#28987));
#8457=EDGE_LOOP('',(#28988,#28989,#28990,#28991,#28992,#28993));
#8458=EDGE_LOOP('',(#28994,#28995,#28996,#28997));
#8459=EDGE_LOOP('',(#28998,#28999,#29000,#29001,#29002,#29003));
#8460=EDGE_LOOP('',(#29004,#29005,#29006,#29007,#29008,#29009));
#8461=EDGE_LOOP('',(#29010,#29011,#29012,#29013));
#8462=EDGE_LOOP('',(#29014,#29015,#29016,#29017,#29018,#29019));
#8463=EDGE_LOOP('',(#29020,#29021,#29022,#29023,#29024,#29025));
#8464=EDGE_LOOP('',(#29026,#29027,#29028,#29029));
#8465=EDGE_LOOP('',(#29030,#29031,#29032,#29033,#29034,#29035));
#8466=EDGE_LOOP('',(#29036,#29037,#29038,#29039,#29040,#29041));
#8467=EDGE_LOOP('',(#29042,#29043,#29044,#29045));
#8468=EDGE_LOOP('',(#29046,#29047,#29048,#29049,#29050,#29051));
#8469=EDGE_LOOP('',(#29052,#29053,#29054,#29055,#29056,#29057));
#8470=EDGE_LOOP('',(#29058,#29059,#29060,#29061));
#8471=EDGE_LOOP('',(#29062,#29063,#29064,#29065,#29066,#29067));
#8472=EDGE_LOOP('',(#29068,#29069,#29070,#29071,#29072,#29073));
#8473=EDGE_LOOP('',(#29074,#29075,#29076,#29077));
#8474=EDGE_LOOP('',(#29078,#29079,#29080,#29081,#29082,#29083));
#8475=EDGE_LOOP('',(#29084,#29085,#29086,#29087,#29088,#29089));
#8476=EDGE_LOOP('',(#29090,#29091,#29092,#29093));
#8477=EDGE_LOOP('',(#29094,#29095,#29096,#29097,#29098,#29099));
#8478=EDGE_LOOP('',(#29100,#29101,#29102,#29103,#29104,#29105));
#8479=EDGE_LOOP('',(#29106,#29107,#29108,#29109));
#8480=EDGE_LOOP('',(#29110,#29111,#29112,#29113,#29114,#29115));
#8481=EDGE_LOOP('',(#29116,#29117,#29118,#29119,#29120,#29121));
#8482=EDGE_LOOP('',(#29122,#29123,#29124,#29125));
#8483=EDGE_LOOP('',(#29126,#29127,#29128,#29129,#29130,#29131));
#8484=EDGE_LOOP('',(#29132,#29133,#29134,#29135,#29136,#29137));
#8485=EDGE_LOOP('',(#29138,#29139,#29140,#29141));
#8486=EDGE_LOOP('',(#29142,#29143,#29144,#29145,#29146,#29147));
#8487=EDGE_LOOP('',(#29148,#29149,#29150,#29151,#29152,#29153));
#8488=EDGE_LOOP('',(#29154,#29155,#29156,#29157));
#8489=EDGE_LOOP('',(#29158,#29159,#29160,#29161,#29162,#29163));
#8490=EDGE_LOOP('',(#29164,#29165,#29166,#29167,#29168,#29169));
#8491=EDGE_LOOP('',(#29170,#29171,#29172,#29173));
#8492=EDGE_LOOP('',(#29174,#29175,#29176,#29177,#29178,#29179));
#8493=EDGE_LOOP('',(#29180,#29181,#29182,#29183,#29184,#29185));
#8494=EDGE_LOOP('',(#29186,#29187,#29188,#29189));
#8495=EDGE_LOOP('',(#29190,#29191,#29192,#29193,#29194,#29195));
#8496=EDGE_LOOP('',(#29196,#29197,#29198,#29199,#29200,#29201));
#8497=EDGE_LOOP('',(#29202,#29203,#29204,#29205));
#8498=EDGE_LOOP('',(#29206,#29207,#29208,#29209,#29210,#29211));
#8499=EDGE_LOOP('',(#29212,#29213,#29214,#29215,#29216,#29217));
#8500=EDGE_LOOP('',(#29218,#29219,#29220,#29221));
#8501=EDGE_LOOP('',(#29222,#29223,#29224,#29225,#29226,#29227));
#8502=EDGE_LOOP('',(#29228,#29229,#29230,#29231,#29232,#29233));
#8503=EDGE_LOOP('',(#29234,#29235,#29236,#29237));
#8504=EDGE_LOOP('',(#29238,#29239,#29240,#29241,#29242,#29243));
#8505=EDGE_LOOP('',(#29244,#29245,#29246,#29247,#29248,#29249));
#8506=EDGE_LOOP('',(#29250,#29251,#29252,#29253));
#8507=EDGE_LOOP('',(#29254,#29255,#29256,#29257,#29258,#29259));
#8508=EDGE_LOOP('',(#29260,#29261,#29262,#29263,#29264,#29265));
#8509=EDGE_LOOP('',(#29266,#29267,#29268,#29269));
#8510=EDGE_LOOP('',(#29270,#29271,#29272,#29273,#29274,#29275));
#8511=EDGE_LOOP('',(#29276,#29277,#29278,#29279,#29280,#29281));
#8512=EDGE_LOOP('',(#29282,#29283,#29284,#29285));
#8513=EDGE_LOOP('',(#29286,#29287,#29288,#29289,#29290,#29291));
#8514=EDGE_LOOP('',(#29292,#29293,#29294,#29295,#29296,#29297));
#8515=EDGE_LOOP('',(#29298,#29299,#29300,#29301));
#8516=EDGE_LOOP('',(#29302,#29303,#29304,#29305,#29306,#29307));
#8517=EDGE_LOOP('',(#29308,#29309,#29310,#29311,#29312,#29313));
#8518=EDGE_LOOP('',(#29314,#29315,#29316,#29317));
#8519=EDGE_LOOP('',(#29318,#29319,#29320,#29321,#29322,#29323));
#8520=EDGE_LOOP('',(#29324,#29325,#29326,#29327,#29328,#29329));
#8521=EDGE_LOOP('',(#29330,#29331,#29332,#29333));
#8522=EDGE_LOOP('',(#29334,#29335,#29336,#29337,#29338,#29339));
#8523=EDGE_LOOP('',(#29340,#29341,#29342,#29343,#29344,#29345));
#8524=EDGE_LOOP('',(#29346,#29347,#29348,#29349));
#8525=EDGE_LOOP('',(#29350,#29351,#29352,#29353,#29354,#29355));
#8526=EDGE_LOOP('',(#29356,#29357,#29358,#29359,#29360,#29361));
#8527=EDGE_LOOP('',(#29362,#29363,#29364,#29365));
#8528=EDGE_LOOP('',(#29366,#29367,#29368,#29369,#29370,#29371));
#8529=EDGE_LOOP('',(#29372,#29373,#29374,#29375,#29376,#29377));
#8530=EDGE_LOOP('',(#29378,#29379,#29380,#29381,#29382));
#8531=EDGE_LOOP('',(#29383,#29384,#29385,#29386,#29387,#29388));
#8532=EDGE_LOOP('',(#29389,#29390,#29391,#29392,#29393,#29394));
#8533=EDGE_LOOP('',(#29395,#29396,#29397,#29398));
#8534=EDGE_LOOP('',(#29399,#29400,#29401,#29402,#29403,#29404));
#8535=EDGE_LOOP('',(#29405,#29406,#29407,#29408,#29409,#29410));
#8536=EDGE_LOOP('',(#29411,#29412,#29413,#29414));
#8537=EDGE_LOOP('',(#29415,#29416,#29417,#29418,#29419,#29420));
#8538=EDGE_LOOP('',(#29421,#29422,#29423,#29424,#29425,#29426));
#8539=EDGE_LOOP('',(#29427,#29428,#29429,#29430));
#8540=EDGE_LOOP('',(#29431,#29432,#29433,#29434,#29435,#29436));
#8541=EDGE_LOOP('',(#29437,#29438,#29439,#29440,#29441,#29442));
#8542=EDGE_LOOP('',(#29443,#29444,#29445,#29446));
#8543=EDGE_LOOP('',(#29447,#29448,#29449,#29450,#29451,#29452));
#8544=EDGE_LOOP('',(#29453,#29454,#29455,#29456,#29457,#29458));
#8545=EDGE_LOOP('',(#29459,#29460,#29461,#29462));
#8546=EDGE_LOOP('',(#29463,#29464,#29465,#29466,#29467,#29468));
#8547=EDGE_LOOP('',(#29469,#29470,#29471,#29472,#29473,#29474));
#8548=EDGE_LOOP('',(#29475,#29476,#29477,#29478));
#8549=EDGE_LOOP('',(#29479,#29480,#29481,#29482,#29483,#29484));
#8550=EDGE_LOOP('',(#29485,#29486,#29487,#29488,#29489,#29490));
#8551=EDGE_LOOP('',(#29491,#29492,#29493,#29494));
#8552=EDGE_LOOP('',(#29495,#29496,#29497,#29498,#29499,#29500));
#8553=EDGE_LOOP('',(#29501,#29502,#29503,#29504,#29505,#29506));
#8554=EDGE_LOOP('',(#29507,#29508,#29509,#29510));
#8555=EDGE_LOOP('',(#29511,#29512,#29513,#29514,#29515,#29516));
#8556=EDGE_LOOP('',(#29517,#29518,#29519,#29520,#29521,#29522));
#8557=EDGE_LOOP('',(#29523,#29524,#29525,#29526));
#8558=EDGE_LOOP('',(#29527,#29528,#29529,#29530,#29531,#29532));
#8559=EDGE_LOOP('',(#29533,#29534,#29535,#29536,#29537,#29538));
#8560=EDGE_LOOP('',(#29539,#29540,#29541,#29542));
#8561=EDGE_LOOP('',(#29543,#29544,#29545,#29546,#29547,#29548));
#8562=EDGE_LOOP('',(#29549,#29550,#29551,#29552,#29553,#29554));
#8563=EDGE_LOOP('',(#29555,#29556,#29557,#29558));
#8564=EDGE_LOOP('',(#29559,#29560,#29561,#29562,#29563,#29564));
#8565=EDGE_LOOP('',(#29565,#29566,#29567,#29568,#29569,#29570));
#8566=EDGE_LOOP('',(#29571,#29572,#29573,#29574));
#8567=EDGE_LOOP('',(#29575,#29576,#29577,#29578,#29579,#29580));
#8568=EDGE_LOOP('',(#29581,#29582,#29583,#29584,#29585,#29586));
#8569=EDGE_LOOP('',(#29587,#29588,#29589,#29590));
#8570=EDGE_LOOP('',(#29591,#29592,#29593,#29594,#29595,#29596));
#8571=EDGE_LOOP('',(#29597,#29598,#29599,#29600,#29601,#29602));
#8572=EDGE_LOOP('',(#29603,#29604,#29605,#29606));
#8573=EDGE_LOOP('',(#29607,#29608,#29609,#29610,#29611,#29612));
#8574=EDGE_LOOP('',(#29613,#29614,#29615,#29616,#29617,#29618));
#8575=EDGE_LOOP('',(#29619,#29620,#29621,#29622));
#8576=EDGE_LOOP('',(#29623,#29624,#29625,#29626,#29627,#29628));
#8577=EDGE_LOOP('',(#29629,#29630,#29631,#29632,#29633,#29634));
#8578=EDGE_LOOP('',(#29635,#29636,#29637,#29638));
#8579=EDGE_LOOP('',(#29639,#29640,#29641,#29642,#29643,#29644));
#8580=EDGE_LOOP('',(#29645,#29646,#29647,#29648,#29649,#29650));
#8581=EDGE_LOOP('',(#29651,#29652,#29653,#29654));
#8582=EDGE_LOOP('',(#29655,#29656,#29657,#29658,#29659,#29660));
#8583=EDGE_LOOP('',(#29661,#29662,#29663,#29664,#29665,#29666));
#8584=EDGE_LOOP('',(#29667,#29668,#29669,#29670));
#8585=EDGE_LOOP('',(#29671,#29672,#29673,#29674,#29675,#29676));
#8586=EDGE_LOOP('',(#29677,#29678,#29679,#29680,#29681,#29682));
#8587=EDGE_LOOP('',(#29683,#29684,#29685,#29686));
#8588=EDGE_LOOP('',(#29687,#29688,#29689,#29690,#29691,#29692));
#8589=EDGE_LOOP('',(#29693,#29694,#29695,#29696,#29697,#29698));
#8590=EDGE_LOOP('',(#29699,#29700,#29701,#29702,#29703,#29704));
#8591=EDGE_LOOP('',(#29705,#29706,#29707,#29708,#29709,#29710));
#8592=EDGE_LOOP('',(#29711,#29712,#29713,#29714,#29715,#29716));
#8593=EDGE_LOOP('',(#29717,#29718,#29719,#29720,#29721,#29722));
#8594=EDGE_LOOP('',(#29723,#29724,#29725,#29726,#29727,#29728));
#8595=EDGE_LOOP('',(#29729,#29730,#29731,#29732,#29733,#29734));
#8596=EDGE_LOOP('',(#29735,#29736,#29737,#29738,#29739,#29740));
#8597=EDGE_LOOP('',(#29741,#29742,#29743,#29744,#29745,#29746));
#8598=EDGE_LOOP('',(#29747,#29748,#29749,#29750,#29751,#29752));
#8599=EDGE_LOOP('',(#29753,#29754,#29755,#29756,#29757,#29758));
#8600=EDGE_LOOP('',(#29759,#29760,#29761,#29762,#29763,#29764));
#9450=LINE('',#65624,#10696);
#9451=LINE('',#65663,#10697);
#9452=LINE('',#65704,#10698);
#9453=LINE('',#65780,#10699);
#9454=LINE('',#65858,#10700);
#9455=LINE('',#65934,#10701);
#9456=LINE('',#66010,#10702);
#9457=LINE('',#66086,#10703);
#9458=LINE('',#66162,#10704);
#9459=LINE('',#66240,#10705);
#9460=LINE('',#66318,#10706);
#9461=LINE('',#66394,#10707);
#9462=LINE('',#66470,#10708);
#9463=LINE('',#66546,#10709);
#9464=LINE('',#66622,#10710);
#9465=LINE('',#66700,#10711);
#9466=LINE('',#66776,#10712);
#9467=LINE('',#66854,#10713);
#9468=LINE('',#66930,#10714);
#9469=LINE('',#67006,#10715);
#9470=LINE('',#67082,#10716);
#9471=LINE('',#67158,#10717);
#9472=LINE('',#67236,#10718);
#9473=LINE('',#67314,#10719);
#9474=LINE('',#67390,#10720);
#9475=LINE('',#67466,#10721);
#9476=LINE('',#67542,#10722);
#9477=LINE('',#67618,#10723);
#9478=LINE('',#67696,#10724);
#9479=LINE('',#67772,#10725);
#9480=LINE('',#67797,#10726);
#9481=LINE('',#67811,#10727);
#9482=LINE('',#67887,#10728);
#9483=LINE('',#67963,#10729);
#9484=LINE('',#68041,#10730);
#9485=LINE('',#68117,#10731);
#9486=LINE('',#68195,#10732);
#9487=LINE('',#68271,#10733);
#9488=LINE('',#68347,#10734);
#9489=LINE('',#68423,#10735);
#9490=LINE('',#68499,#10736);
#9491=LINE('',#68577,#10737);
#9492=LINE('',#68653,#10738);
#9493=LINE('',#68731,#10739);
#9494=LINE('',#68807,#10740);
#9495=LINE('',#68883,#10741);
#9496=LINE('',#68959,#10742);
#9497=LINE('',#69035,#10743);
#9498=LINE('',#69111,#10744);
#9499=LINE('',#69189,#10745);
#9500=LINE('',#69265,#10746);
#9501=LINE('',#69343,#10747);
#9502=LINE('',#69419,#10748);
#9503=LINE('',#69495,#10749);
#9504=LINE('',#69571,#10750);
#9505=LINE('',#69647,#10751);
#9506=LINE('',#69725,#10752);
#9507=LINE('',#69801,#10753);
#9508=LINE('',#69879,#10754);
#9509=LINE('',#69955,#10755);
#9510=LINE('',#70150,#10756);
#9511=LINE('',#70153,#10757);
#9512=LINE('',#70159,#10758);
#9513=LINE('',#70162,#10759);
#9514=LINE('',#70168,#10760);
#9515=LINE('',#70171,#10761);
#9516=LINE('',#70177,#10762);
#9517=LINE('',#70180,#10763);
#9518=LINE('',#70186,#10764);
#9519=LINE('',#70189,#10765);
#9520=LINE('',#70195,#10766);
#9521=LINE('',#70198,#10767);
#9522=LINE('',#70204,#10768);
#9523=LINE('',#70207,#10769);
#9524=LINE('',#70213,#10770);
#9525=LINE('',#70216,#10771);
#9526=LINE('',#70222,#10772);
#9527=LINE('',#70225,#10773);
#9528=LINE('',#70231,#10774);
#9529=LINE('',#70234,#10775);
#9530=LINE('',#70240,#10776);
#9531=LINE('',#70243,#10777);
#9532=LINE('',#70249,#10778);
#9533=LINE('',#70252,#10779);
#9534=LINE('',#70258,#10780);
#9535=LINE('',#70261,#10781);
#9536=LINE('',#70267,#10782);
#9537=LINE('',#70270,#10783);
#9538=LINE('',#70276,#10784);
#9539=LINE('',#70279,#10785);
#9540=LINE('',#70310,#10786);
#9541=LINE('',#71250,#10787);
#9542=LINE('',#72184,#10788);
#9543=LINE('',#72195,#10789);
#9544=LINE('',#72680,#10790);
#9545=LINE('',#72683,#10791);
#9546=LINE('',#72686,#10792);
#9547=LINE('',#72688,#10793);
#9548=LINE('',#72692,#10794);
#9549=LINE('',#72694,#10795);
#9550=LINE('',#72698,#10796);
#9551=LINE('',#72700,#10797);
#9552=LINE('',#72704,#10798);
#9553=LINE('',#72706,#10799);
#9554=LINE('',#72710,#10800);
#9555=LINE('',#72712,#10801);
#9556=LINE('',#72716,#10802);
#9557=LINE('',#72718,#10803);
#9558=LINE('',#72722,#10804);
#9559=LINE('',#72724,#10805);
#9560=LINE('',#72728,#10806);
#9561=LINE('',#72730,#10807);
#9562=LINE('',#72734,#10808);
#9563=LINE('',#72736,#10809);
#9564=LINE('',#72740,#10810);
#9565=LINE('',#72742,#10811);
#9566=LINE('',#72746,#10812);
#9567=LINE('',#72748,#10813);
#9568=LINE('',#72752,#10814);
#9569=LINE('',#72754,#10815);
#9570=LINE('',#72758,#10816);
#9571=LINE('',#72760,#10817);
#9572=LINE('',#72764,#10818);
#9573=LINE('',#72766,#10819);
#9574=LINE('',#72770,#10820);
#9575=LINE('',#72772,#10821);
#9576=LINE('',#72776,#10822);
#9577=LINE('',#72778,#10823);
#9578=LINE('',#72782,#10824);
#9579=LINE('',#72784,#10825);
#9580=LINE('',#72788,#10826);
#9581=LINE('',#72790,#10827);
#9582=LINE('',#72794,#10828);
#9583=LINE('',#72796,#10829);
#9584=LINE('',#72800,#10830);
#9585=LINE('',#72802,#10831);
#9586=LINE('',#72806,#10832);
#9587=LINE('',#72808,#10833);
#9588=LINE('',#72812,#10834);
#9589=LINE('',#72814,#10835);
#9590=LINE('',#72818,#10836);
#9591=LINE('',#72820,#10837);
#9592=LINE('',#72824,#10838);
#9593=LINE('',#72826,#10839);
#9594=LINE('',#72830,#10840);
#9595=LINE('',#72832,#10841);
#9596=LINE('',#72836,#10842);
#9597=LINE('',#72838,#10843);
#9598=LINE('',#72842,#10844);
#9599=LINE('',#72844,#10845);
#9600=LINE('',#72848,#10846);
#9601=LINE('',#72850,#10847);
#9602=LINE('',#72854,#10848);
#9603=LINE('',#72856,#10849);
#9604=LINE('',#72860,#10850);
#9605=LINE('',#72862,#10851);
#9606=LINE('',#72866,#10852);
#9607=LINE('',#72868,#10853);
#9608=LINE('',#72872,#10854);
#9609=LINE('',#72874,#10855);
#9610=LINE('',#72878,#10856);
#9611=LINE('',#72880,#10857);
#9612=LINE('',#72884,#10858);
#9613=LINE('',#72886,#10859);
#9614=LINE('',#72890,#10860);
#9615=LINE('',#72892,#10861);
#9616=LINE('',#72896,#10862);
#9617=LINE('',#72898,#10863);
#9618=LINE('',#72902,#10864);
#9619=LINE('',#72904,#10865);
#9620=LINE('',#72908,#10866);
#9621=LINE('',#72910,#10867);
#9622=LINE('',#72914,#10868);
#9623=LINE('',#72916,#10869);
#9624=LINE('',#72920,#10870);
#9625=LINE('',#72922,#10871);
#9626=LINE('',#72926,#10872);
#9627=LINE('',#72928,#10873);
#9628=LINE('',#72932,#10874);
#9629=LINE('',#72934,#10875);
#9630=LINE('',#72938,#10876);
#9631=LINE('',#72940,#10877);
#9632=LINE('',#72944,#10878);
#9633=LINE('',#72946,#10879);
#9634=LINE('',#72950,#10880);
#9635=LINE('',#72952,#10881);
#9636=LINE('',#72956,#10882);
#9637=LINE('',#72958,#10883);
#9638=LINE('',#72962,#10884);
#9639=LINE('',#72964,#10885);
#9640=LINE('',#72968,#10886);
#9641=LINE('',#72970,#10887);
#9642=LINE('',#72974,#10888);
#9643=LINE('',#72976,#10889);
#9644=LINE('',#72980,#10890);
#9645=LINE('',#72982,#10891);
#9646=LINE('',#72986,#10892);
#9647=LINE('',#72988,#10893);
#9648=LINE('',#72992,#10894);
#9649=LINE('',#72994,#10895);
#9650=LINE('',#72998,#10896);
#9651=LINE('',#73000,#10897);
#9652=LINE('',#73004,#10898);
#9653=LINE('',#73006,#10899);
#9654=LINE('',#73010,#10900);
#9655=LINE('',#73012,#10901);
#9656=LINE('',#73016,#10902);
#9657=LINE('',#73018,#10903);
#9658=LINE('',#73022,#10904);
#9659=LINE('',#73024,#10905);
#9660=LINE('',#73028,#10906);
#9661=LINE('',#73030,#10907);
#9662=LINE('',#73034,#10908);
#9663=LINE('',#73036,#10909);
#9664=LINE('',#73040,#10910);
#9665=LINE('',#73042,#10911);
#9666=LINE('',#73046,#10912);
#9667=LINE('',#73048,#10913);
#9668=LINE('',#73052,#10914);
#9669=LINE('',#73054,#10915);
#9670=LINE('',#73058,#10916);
#9671=LINE('',#73060,#10917);
#9672=LINE('',#73064,#10918);
#9673=LINE('',#73067,#10919);
#9674=LINE('',#73070,#10920);
#9675=LINE('',#73073,#10921);
#9676=LINE('',#73076,#10922);
#9677=LINE('',#73079,#10923);
#9678=LINE('',#73082,#10924);
#9679=LINE('',#73085,#10925);
#9680=LINE('',#73088,#10926);
#9681=LINE('',#73091,#10927);
#9682=LINE('',#73094,#10928);
#9683=LINE('',#73097,#10929);
#9684=LINE('',#73100,#10930);
#9685=LINE('',#73103,#10931);
#9686=LINE('',#73106,#10932);
#9687=LINE('',#73109,#10933);
#9688=LINE('',#73112,#10934);
#9689=LINE('',#73115,#10935);
#9690=LINE('',#73118,#10936);
#9691=LINE('',#73121,#10937);
#9692=LINE('',#73124,#10938);
#9693=LINE('',#73127,#10939);
#9694=LINE('',#73130,#10940);
#9695=LINE('',#73133,#10941);
#9696=LINE('',#73136,#10942);
#9697=LINE('',#73139,#10943);
#9698=LINE('',#73142,#10944);
#9699=LINE('',#73145,#10945);
#9700=LINE('',#73148,#10946);
#9701=LINE('',#73150,#10947);
#9702=LINE('',#73399,#10948);
#9703=LINE('',#73401,#10949);
#9704=LINE('',#73410,#10950);
#9705=LINE('',#73412,#10951);
#9706=LINE('',#73414,#10952);
#9707=LINE('',#73416,#10953);
#9708=LINE('',#73418,#10954);
#9709=LINE('',#73419,#10955);
#9710=LINE('',#73421,#10956);
#9711=LINE('',#73422,#10957);
#9712=LINE('',#73424,#10958);
#9713=LINE('',#73426,#10959);
#9714=LINE('',#73428,#10960);
#9715=LINE('',#73430,#10961);
#9716=LINE('',#74952,#10962);
#9717=LINE('',#74955,#10963);
#9718=LINE('',#74957,#10964);
#9719=LINE('',#74960,#10965);
#9720=LINE('',#74962,#10966);
#9721=LINE('',#74965,#10967);
#9722=LINE('',#74967,#10968);
#9723=LINE('',#74970,#10969);
#9724=LINE('',#74972,#10970);
#9725=LINE('',#74975,#10971);
#9726=LINE('',#74977,#10972);
#9727=LINE('',#74980,#10973);
#9728=LINE('',#74982,#10974);
#9729=LINE('',#74985,#10975);
#9730=LINE('',#74987,#10976);
#9731=LINE('',#75008,#10977);
#9732=LINE('',#75010,#10978);
#9733=LINE('',#75013,#10979);
#9734=LINE('',#75015,#10980);
#9735=LINE('',#75018,#10981);
#9736=LINE('',#75020,#10982);
#9737=LINE('',#75023,#10983);
#9738=LINE('',#75025,#10984);
#9739=LINE('',#75028,#10985);
#9740=LINE('',#75030,#10986);
#9741=LINE('',#75033,#10987);
#9742=LINE('',#75035,#10988);
#9743=LINE('',#75038,#10989);
#9744=LINE('',#75040,#10990);
#9745=LINE('',#75043,#10991);
#9746=LINE('',#75045,#10992);
#9747=LINE('',#75048,#10993);
#9748=LINE('',#75050,#10994);
#9749=LINE('',#75053,#10995);
#9750=LINE('',#75055,#10996);
#9751=LINE('',#75058,#10997);
#9752=LINE('',#75060,#10998);
#9753=LINE('',#75063,#10999);
#9754=LINE('',#75065,#11000);
#9755=LINE('',#75068,#11001);
#9756=LINE('',#75070,#11002);
#9757=LINE('',#75073,#11003);
#9758=LINE('',#75075,#11004);
#9759=LINE('',#75078,#11005);
#9760=LINE('',#75080,#11006);
#9761=LINE('',#75083,#11007);
#9762=LINE('',#75085,#11008);
#9763=LINE('',#75088,#11009);
#9764=LINE('',#75090,#11010);
#9765=LINE('',#75093,#11011);
#9766=LINE('',#75095,#11012);
#9767=LINE('',#75098,#11013);
#9768=LINE('',#75100,#11014);
#9769=LINE('',#75103,#11015);
#9770=LINE('',#75105,#11016);
#9771=LINE('',#75108,#11017);
#9772=LINE('',#75110,#11018);
#9773=LINE('',#75113,#11019);
#9774=LINE('',#75115,#11020);
#9775=LINE('',#75118,#11021);
#9776=LINE('',#75120,#11022);
#9777=LINE('',#75123,#11023);
#9778=LINE('',#75125,#11024);
#9779=LINE('',#75128,#11025);
#9780=LINE('',#75130,#11026);
#9781=LINE('',#75133,#11027);
#9782=LINE('',#75135,#11028);
#9783=LINE('',#75138,#11029);
#9784=LINE('',#75140,#11030);
#9785=LINE('',#75143,#11031);
#9786=LINE('',#75145,#11032);
#9787=LINE('',#75148,#11033);
#9788=LINE('',#75150,#11034);
#9789=LINE('',#75153,#11035);
#9790=LINE('',#75155,#11036);
#9791=LINE('',#75158,#11037);
#9792=LINE('',#75160,#11038);
#9793=LINE('',#75163,#11039);
#9794=LINE('',#75165,#11040);
#9795=LINE('',#75168,#11041);
#9796=LINE('',#75170,#11042);
#9797=LINE('',#75173,#11043);
#9798=LINE('',#75175,#11044);
#9799=LINE('',#75178,#11045);
#9800=LINE('',#75180,#11046);
#9801=LINE('',#75183,#11047);
#9802=LINE('',#75185,#11048);
#9803=LINE('',#75188,#11049);
#9804=LINE('',#75190,#11050);
#9805=LINE('',#75193,#11051);
#9806=LINE('',#75195,#11052);
#9807=LINE('',#75198,#11053);
#9808=LINE('',#75200,#11054);
#9809=LINE('',#75203,#11055);
#9810=LINE('',#75205,#11056);
#9811=LINE('',#75208,#11057);
#9812=LINE('',#75210,#11058);
#9813=LINE('',#75213,#11059);
#9814=LINE('',#75215,#11060);
#9815=LINE('',#75218,#11061);
#9816=LINE('',#75220,#11062);
#9817=LINE('',#75223,#11063);
#9818=LINE('',#75225,#11064);
#9819=LINE('',#75228,#11065);
#9820=LINE('',#75230,#11066);
#9821=LINE('',#75233,#11067);
#9822=LINE('',#75235,#11068);
#9823=LINE('',#75238,#11069);
#9824=LINE('',#75240,#11070);
#9825=LINE('',#75243,#11071);
#9826=LINE('',#75245,#11072);
#9827=LINE('',#75248,#11073);
#9828=LINE('',#75250,#11074);
#9829=LINE('',#75253,#11075);
#9830=LINE('',#75255,#11076);
#9831=LINE('',#75258,#11077);
#9832=LINE('',#75260,#11078);
#9833=LINE('',#75263,#11079);
#9834=LINE('',#75265,#11080);
#9835=LINE('',#75268,#11081);
#9836=LINE('',#75270,#11082);
#9837=LINE('',#75273,#11083);
#9838=LINE('',#75275,#11084);
#9839=LINE('',#75278,#11085);
#9840=LINE('',#75280,#11086);
#9841=LINE('',#75283,#11087);
#9842=LINE('',#75285,#11088);
#9843=LINE('',#75288,#11089);
#9844=LINE('',#75290,#11090);
#9845=LINE('',#75293,#11091);
#9846=LINE('',#75295,#11092);
#10696=VECTOR('',#42876,1.5);
#10697=VECTOR('',#42877,1.5);
#10698=VECTOR('',#42884,1.5);
#10699=VECTOR('',#42887,1.5);
#10700=VECTOR('',#42890,1.5);
#10701=VECTOR('',#42893,1.5);
#10702=VECTOR('',#42896,1.5);
#10703=VECTOR('',#42899,1.5);
#10704=VECTOR('',#42902,1.5);
#10705=VECTOR('',#42905,1.5);
#10706=VECTOR('',#42908,1.5);
#10707=VECTOR('',#42911,1.5);
#10708=VECTOR('',#42914,1.5);
#10709=VECTOR('',#42917,1.5);
#10710=VECTOR('',#42920,1.5);
#10711=VECTOR('',#42923,1.5);
#10712=VECTOR('',#42926,1.5);
#10713=VECTOR('',#42929,1.5);
#10714=VECTOR('',#42932,1.5);
#10715=VECTOR('',#42935,1.5);
#10716=VECTOR('',#42938,1.5);
#10717=VECTOR('',#42941,1.5);
#10718=VECTOR('',#42944,1.5);
#10719=VECTOR('',#42947,1.5);
#10720=VECTOR('',#42950,1.5);
#10721=VECTOR('',#42953,1.5);
#10722=VECTOR('',#42956,1.5);
#10723=VECTOR('',#42959,1.5);
#10724=VECTOR('',#42962,1.5);
#10725=VECTOR('',#42965,1.17524047358084);
#10726=VECTOR('',#42970,1.17524047358084);
#10727=VECTOR('',#42975,1.17524047358084);
#10728=VECTOR('',#42978,1.17524047358084);
#10729=VECTOR('',#42981,1.17524047358084);
#10730=VECTOR('',#42984,1.17524047358084);
#10731=VECTOR('',#42987,1.17524047358084);
#10732=VECTOR('',#42990,1.17524047358084);
#10733=VECTOR('',#42993,1.17524047358084);
#10734=VECTOR('',#42996,1.17524047358084);
#10735=VECTOR('',#42999,1.17524047358084);
#10736=VECTOR('',#43002,1.17524047358084);
#10737=VECTOR('',#43005,1.17524047358084);
#10738=VECTOR('',#43008,1.17524047358084);
#10739=VECTOR('',#43011,1.17524047358084);
#10740=VECTOR('',#43014,1.17524047358084);
#10741=VECTOR('',#43017,1.17524047358084);
#10742=VECTOR('',#43020,1.17524047358084);
#10743=VECTOR('',#43023,1.17524047358084);
#10744=VECTOR('',#43026,1.17524047358084);
#10745=VECTOR('',#43029,1.17524047358084);
#10746=VECTOR('',#43032,1.17524047358084);
#10747=VECTOR('',#43035,1.17524047358084);
#10748=VECTOR('',#43038,1.17524047358084);
#10749=VECTOR('',#43041,1.17524047358084);
#10750=VECTOR('',#43044,1.17524047358084);
#10751=VECTOR('',#43047,1.17524047358084);
#10752=VECTOR('',#43050,1.17524047358084);
#10753=VECTOR('',#43053,1.17524047358084);
#10754=VECTOR('',#43056,1.17524047358084);
#10755=VECTOR('',#43059,1.17524047358084);
#10756=VECTOR('',#43076,1000.);
#10757=VECTOR('',#43079,1000.);
#10758=VECTOR('',#43084,1000.);
#10759=VECTOR('',#43087,1000.);
#10760=VECTOR('',#43092,1000.);
#10761=VECTOR('',#43095,1000.);
#10762=VECTOR('',#43100,1000.);
#10763=VECTOR('',#43103,1000.);
#10764=VECTOR('',#43108,1000.);
#10765=VECTOR('',#43111,1000.);
#10766=VECTOR('',#43116,1000.);
#10767=VECTOR('',#43119,1000.);
#10768=VECTOR('',#43124,1000.);
#10769=VECTOR('',#43127,1000.);
#10770=VECTOR('',#43132,1000.);
#10771=VECTOR('',#43135,1000.);
#10772=VECTOR('',#43140,1000.);
#10773=VECTOR('',#43143,1000.);
#10774=VECTOR('',#43148,1000.);
#10775=VECTOR('',#43151,1000.);
#10776=VECTOR('',#43156,1000.);
#10777=VECTOR('',#43159,1000.);
#10778=VECTOR('',#43164,1000.);
#10779=VECTOR('',#43167,1000.);
#10780=VECTOR('',#43172,1000.);
#10781=VECTOR('',#43175,1000.);
#10782=VECTOR('',#43180,1000.);
#10783=VECTOR('',#43183,1000.);
#10784=VECTOR('',#43188,1000.);
#10785=VECTOR('',#43191,1000.);
#10786=VECTOR('',#43194,1.55162884844711);
#10787=VECTOR('',#43495,2.73627063036812);
#10788=VECTOR('',#43786,2.68872936963188);
#10789=VECTOR('',#43801,2.675);
#10790=VECTOR('',#44448,1000.);
#10791=VECTOR('',#44451,1000.);
#10792=VECTOR('',#44454,1000.);
#10793=VECTOR('',#44455,1000.);
#10794=VECTOR('',#44460,1000.);
#10795=VECTOR('',#44461,1000.);
#10796=VECTOR('',#44466,1000.);
#10797=VECTOR('',#44467,1000.);
#10798=VECTOR('',#44472,1000.);
#10799=VECTOR('',#44473,1000.);
#10800=VECTOR('',#44478,1000.);
#10801=VECTOR('',#44479,1000.);
#10802=VECTOR('',#44484,1000.);
#10803=VECTOR('',#44485,1000.);
#10804=VECTOR('',#44490,1000.);
#10805=VECTOR('',#44491,1000.);
#10806=VECTOR('',#44496,1000.);
#10807=VECTOR('',#44497,1000.);
#10808=VECTOR('',#44502,1000.);
#10809=VECTOR('',#44503,1000.);
#10810=VECTOR('',#44508,1000.);
#10811=VECTOR('',#44509,1000.);
#10812=VECTOR('',#44514,1000.);
#10813=VECTOR('',#44515,1000.);
#10814=VECTOR('',#44520,1000.);
#10815=VECTOR('',#44521,1000.);
#10816=VECTOR('',#44526,1000.);
#10817=VECTOR('',#44527,1000.);
#10818=VECTOR('',#44532,1000.);
#10819=VECTOR('',#44533,1000.);
#10820=VECTOR('',#44538,1000.);
#10821=VECTOR('',#44539,1000.);
#10822=VECTOR('',#44544,1000.);
#10823=VECTOR('',#44545,1000.);
#10824=VECTOR('',#44550,1000.);
#10825=VECTOR('',#44551,1000.);
#10826=VECTOR('',#44556,1000.);
#10827=VECTOR('',#44557,1000.);
#10828=VECTOR('',#44562,1000.);
#10829=VECTOR('',#44563,1000.);
#10830=VECTOR('',#44568,1000.);
#10831=VECTOR('',#44569,1000.);
#10832=VECTOR('',#44574,1000.);
#10833=VECTOR('',#44575,1000.);
#10834=VECTOR('',#44580,1000.);
#10835=VECTOR('',#44581,1000.);
#10836=VECTOR('',#44586,1000.);
#10837=VECTOR('',#44587,1000.);
#10838=VECTOR('',#44592,1000.);
#10839=VECTOR('',#44593,1000.);
#10840=VECTOR('',#44598,1000.);
#10841=VECTOR('',#44599,1000.);
#10842=VECTOR('',#44604,1000.);
#10843=VECTOR('',#44605,1000.);
#10844=VECTOR('',#44610,1000.);
#10845=VECTOR('',#44611,1000.);
#10846=VECTOR('',#44616,1000.);
#10847=VECTOR('',#44617,1000.);
#10848=VECTOR('',#44622,1000.);
#10849=VECTOR('',#44623,1000.);
#10850=VECTOR('',#44628,1000.);
#10851=VECTOR('',#44629,1000.);
#10852=VECTOR('',#44634,1000.);
#10853=VECTOR('',#44635,1000.);
#10854=VECTOR('',#44640,1000.);
#10855=VECTOR('',#44641,1000.);
#10856=VECTOR('',#44646,1000.);
#10857=VECTOR('',#44647,1000.);
#10858=VECTOR('',#44652,1000.);
#10859=VECTOR('',#44653,1000.);
#10860=VECTOR('',#44658,1000.);
#10861=VECTOR('',#44659,1000.);
#10862=VECTOR('',#44664,1000.);
#10863=VECTOR('',#44665,1000.);
#10864=VECTOR('',#44670,1000.);
#10865=VECTOR('',#44671,1000.);
#10866=VECTOR('',#44676,1000.);
#10867=VECTOR('',#44677,1000.);
#10868=VECTOR('',#44682,1000.);
#10869=VECTOR('',#44683,1000.);
#10870=VECTOR('',#44688,1000.);
#10871=VECTOR('',#44689,1000.);
#10872=VECTOR('',#44694,1000.);
#10873=VECTOR('',#44695,1000.);
#10874=VECTOR('',#44700,1000.);
#10875=VECTOR('',#44701,1000.);
#10876=VECTOR('',#44706,1000.);
#10877=VECTOR('',#44707,1000.);
#10878=VECTOR('',#44712,1000.);
#10879=VECTOR('',#44713,1000.);
#10880=VECTOR('',#44718,1000.);
#10881=VECTOR('',#44719,1000.);
#10882=VECTOR('',#44724,1000.);
#10883=VECTOR('',#44725,1000.);
#10884=VECTOR('',#44730,1000.);
#10885=VECTOR('',#44731,1000.);
#10886=VECTOR('',#44736,1000.);
#10887=VECTOR('',#44737,1000.);
#10888=VECTOR('',#44742,1000.);
#10889=VECTOR('',#44743,1000.);
#10890=VECTOR('',#44748,1000.);
#10891=VECTOR('',#44749,1000.);
#10892=VECTOR('',#44754,1000.);
#10893=VECTOR('',#44755,1000.);
#10894=VECTOR('',#44760,1000.);
#10895=VECTOR('',#44761,1000.);
#10896=VECTOR('',#44766,1000.);
#10897=VECTOR('',#44767,1000.);
#10898=VECTOR('',#44772,1000.);
#10899=VECTOR('',#44773,1000.);
#10900=VECTOR('',#44778,1000.);
#10901=VECTOR('',#44779,1000.);
#10902=VECTOR('',#44784,1000.);
#10903=VECTOR('',#44785,1000.);
#10904=VECTOR('',#44790,1000.);
#10905=VECTOR('',#44791,1000.);
#10906=VECTOR('',#44796,1000.);
#10907=VECTOR('',#44797,1000.);
#10908=VECTOR('',#44802,1000.);
#10909=VECTOR('',#44803,1000.);
#10910=VECTOR('',#44808,1000.);
#10911=VECTOR('',#44809,1000.);
#10912=VECTOR('',#44814,1000.);
#10913=VECTOR('',#44815,1000.);
#10914=VECTOR('',#44820,1000.);
#10915=VECTOR('',#44821,1000.);
#10916=VECTOR('',#44826,1000.);
#10917=VECTOR('',#44827,1000.);
#10918=VECTOR('',#44832,1000.);
#10919=VECTOR('',#44835,1000.);
#10920=VECTOR('',#44838,1000.);
#10921=VECTOR('',#44841,1000.);
#10922=VECTOR('',#44844,1000.);
#10923=VECTOR('',#44847,1000.);
#10924=VECTOR('',#44850,1000.);
#10925=VECTOR('',#44853,1000.);
#10926=VECTOR('',#44856,1000.);
#10927=VECTOR('',#44859,1000.);
#10928=VECTOR('',#44862,1000.);
#10929=VECTOR('',#44865,1000.);
#10930=VECTOR('',#44868,1000.);
#10931=VECTOR('',#44871,1000.);
#10932=VECTOR('',#44874,1000.);
#10933=VECTOR('',#44877,1000.);
#10934=VECTOR('',#44880,1000.);
#10935=VECTOR('',#44883,1000.);
#10936=VECTOR('',#44886,1000.);
#10937=VECTOR('',#44889,1000.);
#10938=VECTOR('',#44892,1000.);
#10939=VECTOR('',#44895,1000.);
#10940=VECTOR('',#44898,1000.);
#10941=VECTOR('',#44901,1000.);
#10942=VECTOR('',#44904,1000.);
#10943=VECTOR('',#44907,1000.);
#10944=VECTOR('',#44910,1000.);
#10945=VECTOR('',#44913,1000.);
#10946=VECTOR('',#44916,1000.);
#10947=VECTOR('',#44917,1000.);
#10948=VECTOR('',#45408,1000.);
#10949=VECTOR('',#45409,1000.);
#10950=VECTOR('',#45422,1000.);
#10951=VECTOR('',#45423,1000.);
#10952=VECTOR('',#45424,1000.);
#10953=VECTOR('',#45425,1000.);
#10954=VECTOR('',#45426,1000.);
#10955=VECTOR('',#45427,1000.);
#10956=VECTOR('',#45430,1000.);
#10957=VECTOR('',#45431,1000.);
#10958=VECTOR('',#45434,1000.);
#10959=VECTOR('',#45437,1000.);
#10960=VECTOR('',#45440,1000.);
#10961=VECTOR('',#45443,1000.);
#10962=VECTOR('',#45446,10.);
#10963=VECTOR('',#45451,1000.);
#10964=VECTOR('',#45454,1000.);
#10965=VECTOR('',#45459,1000.);
#10966=VECTOR('',#45462,1000.);
#10967=VECTOR('',#45467,1000.);
#10968=VECTOR('',#45470,1000.);
#10969=VECTOR('',#45475,1000.);
#10970=VECTOR('',#45478,1000.);
#10971=VECTOR('',#45483,1000.);
#10972=VECTOR('',#45486,1000.);
#10973=VECTOR('',#45491,1000.);
#10974=VECTOR('',#45494,1000.);
#10975=VECTOR('',#45499,1000.);
#10976=VECTOR('',#45502,1000.);
#10977=VECTOR('',#45543,1000.);
#10978=VECTOR('',#45546,1000.);
#10979=VECTOR('',#45551,1000.);
#10980=VECTOR('',#45554,1000.);
#10981=VECTOR('',#45559,1000.);
#10982=VECTOR('',#45562,1000.);
#10983=VECTOR('',#45567,1000.);
#10984=VECTOR('',#45570,1000.);
#10985=VECTOR('',#45575,1000.);
#10986=VECTOR('',#45578,1000.);
#10987=VECTOR('',#45583,1000.);
#10988=VECTOR('',#45586,1000.);
#10989=VECTOR('',#45591,1000.);
#10990=VECTOR('',#45594,1000.);
#10991=VECTOR('',#45599,1000.);
#10992=VECTOR('',#45602,1000.);
#10993=VECTOR('',#45607,1000.);
#10994=VECTOR('',#45610,1000.);
#10995=VECTOR('',#45615,1000.);
#10996=VECTOR('',#45618,1000.);
#10997=VECTOR('',#45623,1000.);
#10998=VECTOR('',#45626,1000.);
#10999=VECTOR('',#45631,1000.);
#11000=VECTOR('',#45634,1000.);
#11001=VECTOR('',#45639,1000.);
#11002=VECTOR('',#45642,1000.);
#11003=VECTOR('',#45647,1000.);
#11004=VECTOR('',#45650,1000.);
#11005=VECTOR('',#45655,1000.);
#11006=VECTOR('',#45658,1000.);
#11007=VECTOR('',#45663,1000.);
#11008=VECTOR('',#45666,1000.);
#11009=VECTOR('',#45671,1000.);
#11010=VECTOR('',#45674,1000.);
#11011=VECTOR('',#45679,1000.);
#11012=VECTOR('',#45682,1000.);
#11013=VECTOR('',#45687,1000.);
#11014=VECTOR('',#45690,1000.);
#11015=VECTOR('',#45695,1000.);
#11016=VECTOR('',#45698,1000.);
#11017=VECTOR('',#45703,1000.);
#11018=VECTOR('',#45706,1000.);
#11019=VECTOR('',#45711,1000.);
#11020=VECTOR('',#45714,1000.);
#11021=VECTOR('',#45719,1000.);
#11022=VECTOR('',#45722,1000.);
#11023=VECTOR('',#45727,1000.);
#11024=VECTOR('',#45730,1000.);
#11025=VECTOR('',#45735,1000.);
#11026=VECTOR('',#45738,1000.);
#11027=VECTOR('',#45743,1000.);
#11028=VECTOR('',#45746,1000.);
#11029=VECTOR('',#45751,1000.);
#11030=VECTOR('',#45754,1000.);
#11031=VECTOR('',#45759,1000.);
#11032=VECTOR('',#45762,1000.);
#11033=VECTOR('',#45767,1000.);
#11034=VECTOR('',#45770,1000.);
#11035=VECTOR('',#45775,1000.);
#11036=VECTOR('',#45778,1000.);
#11037=VECTOR('',#45783,1000.);
#11038=VECTOR('',#45786,1000.);
#11039=VECTOR('',#45791,1000.);
#11040=VECTOR('',#45794,1000.);
#11041=VECTOR('',#45799,1000.);
#11042=VECTOR('',#45802,1000.);
#11043=VECTOR('',#45807,1000.);
#11044=VECTOR('',#45810,1000.);
#11045=VECTOR('',#45815,1000.);
#11046=VECTOR('',#45818,1000.);
#11047=VECTOR('',#45823,1000.);
#11048=VECTOR('',#45826,1000.);
#11049=VECTOR('',#45831,1000.);
#11050=VECTOR('',#45834,1000.);
#11051=VECTOR('',#45839,1000.);
#11052=VECTOR('',#45842,1000.);
#11053=VECTOR('',#45847,1000.);
#11054=VECTOR('',#45850,1000.);
#11055=VECTOR('',#45855,1000.);
#11056=VECTOR('',#45858,1000.);
#11057=VECTOR('',#45863,1000.);
#11058=VECTOR('',#45866,1000.);
#11059=VECTOR('',#45871,1000.);
#11060=VECTOR('',#45874,1000.);
#11061=VECTOR('',#45879,1000.);
#11062=VECTOR('',#45882,1000.);
#11063=VECTOR('',#45887,1000.);
#11064=VECTOR('',#45890,1000.);
#11065=VECTOR('',#45895,1000.);
#11066=VECTOR('',#45898,1000.);
#11067=VECTOR('',#45903,1000.);
#11068=VECTOR('',#45906,1000.);
#11069=VECTOR('',#45911,1000.);
#11070=VECTOR('',#45914,1000.);
#11071=VECTOR('',#45919,1000.);
#11072=VECTOR('',#45922,1000.);
#11073=VECTOR('',#45927,1000.);
#11074=VECTOR('',#45930,1000.);
#11075=VECTOR('',#45935,1000.);
#11076=VECTOR('',#45938,1000.);
#11077=VECTOR('',#45943,1000.);
#11078=VECTOR('',#45946,1000.);
#11079=VECTOR('',#45951,1000.);
#11080=VECTOR('',#45954,1000.);
#11081=VECTOR('',#45959,1000.);
#11082=VECTOR('',#45962,1000.);
#11083=VECTOR('',#45967,1000.);
#11084=VECTOR('',#45970,1000.);
#11085=VECTOR('',#45975,1000.);
#11086=VECTOR('',#45978,1000.);
#11087=VECTOR('',#45983,1000.);
#11088=VECTOR('',#45986,1000.);
#11089=VECTOR('',#45991,1000.);
#11090=VECTOR('',#45994,1000.);
#11091=VECTOR('',#45999,1000.);
#11092=VECTOR('',#46002,1000.);
#13374=VERTEX_POINT('',#65622);
#13375=VERTEX_POINT('',#65623);
#13376=VERTEX_POINT('',#65625);
#13377=VERTEX_POINT('',#65662);
#13378=VERTEX_POINT('',#65665);
#13379=VERTEX_POINT('',#65702);
#13380=VERTEX_POINT('',#65703);
#13381=VERTEX_POINT('',#65778);
#13382=VERTEX_POINT('',#65779);
#13383=VERTEX_POINT('',#65856);
#13384=VERTEX_POINT('',#65857);
#13385=VERTEX_POINT('',#65932);
#13386=VERTEX_POINT('',#65933);
#13387=VERTEX_POINT('',#66008);
#13388=VERTEX_POINT('',#66009);
#13389=VERTEX_POINT('',#66084);
#13390=VERTEX_POINT('',#66085);
#13391=VERTEX_POINT('',#66160);
#13392=VERTEX_POINT('',#66161);
#13393=VERTEX_POINT('',#66238);
#13394=VERTEX_POINT('',#66239);
#13395=VERTEX_POINT('',#66316);
#13396=VERTEX_POINT('',#66317);
#13397=VERTEX_POINT('',#66392);
#13398=VERTEX_POINT('',#66393);
#13399=VERTEX_POINT('',#66468);
#13400=VERTEX_POINT('',#66469);
#13401=VERTEX_POINT('',#66544);
#13402=VERTEX_POINT('',#66545);
#13403=VERTEX_POINT('',#66620);
#13404=VERTEX_POINT('',#66621);
#13405=VERTEX_POINT('',#66698);
#13406=VERTEX_POINT('',#66699);
#13407=VERTEX_POINT('',#66774);
#13408=VERTEX_POINT('',#66775);
#13409=VERTEX_POINT('',#66852);
#13410=VERTEX_POINT('',#66853);
#13411=VERTEX_POINT('',#66928);
#13412=VERTEX_POINT('',#66929);
#13413=VERTEX_POINT('',#67004);
#13414=VERTEX_POINT('',#67005);
#13415=VERTEX_POINT('',#67080);
#13416=VERTEX_POINT('',#67081);
#13417=VERTEX_POINT('',#67156);
#13418=VERTEX_POINT('',#67157);
#13419=VERTEX_POINT('',#67234);
#13420=VERTEX_POINT('',#67235);
#13421=VERTEX_POINT('',#67312);
#13422=VERTEX_POINT('',#67313);
#13423=VERTEX_POINT('',#67388);
#13424=VERTEX_POINT('',#67389);
#13425=VERTEX_POINT('',#67464);
#13426=VERTEX_POINT('',#67465);
#13427=VERTEX_POINT('',#67540);
#13428=VERTEX_POINT('',#67541);
#13429=VERTEX_POINT('',#67616);
#13430=VERTEX_POINT('',#67617);
#13431=VERTEX_POINT('',#67694);
#13432=VERTEX_POINT('',#67695);
#13433=VERTEX_POINT('',#67770);
#13434=VERTEX_POINT('',#67771);
#13435=VERTEX_POINT('',#67773);
#13436=VERTEX_POINT('',#67796);
#13437=VERTEX_POINT('',#67798);
#13438=VERTEX_POINT('',#67809);
#13439=VERTEX_POINT('',#67810);
#13440=VERTEX_POINT('',#67885);
#13441=VERTEX_POINT('',#67886);
#13442=VERTEX_POINT('',#67961);
#13443=VERTEX_POINT('',#67962);
#13444=VERTEX_POINT('',#68039);
#13445=VERTEX_POINT('',#68040);
#13446=VERTEX_POINT('',#68115);
#13447=VERTEX_POINT('',#68116);
#13448=VERTEX_POINT('',#68193);
#13449=VERTEX_POINT('',#68194);
#13450=VERTEX_POINT('',#68269);
#13451=VERTEX_POINT('',#68270);
#13452=VERTEX_POINT('',#68345);
#13453=VERTEX_POINT('',#68346);
#13454=VERTEX_POINT('',#68421);
#13455=VERTEX_POINT('',#68422);
#13456=VERTEX_POINT('',#68497);
#13457=VERTEX_POINT('',#68498);
#13458=VERTEX_POINT('',#68575);
#13459=VERTEX_POINT('',#68576);
#13460=VERTEX_POINT('',#68651);
#13461=VERTEX_POINT('',#68652);
#13462=VERTEX_POINT('',#68729);
#13463=VERTEX_POINT('',#68730);
#13464=VERTEX_POINT('',#68805);
#13465=VERTEX_POINT('',#68806);
#13466=VERTEX_POINT('',#68881);
#13467=VERTEX_POINT('',#68882);
#13468=VERTEX_POINT('',#68957);
#13469=VERTEX_POINT('',#68958);
#13470=VERTEX_POINT('',#69033);
#13471=VERTEX_POINT('',#69034);
#13472=VERTEX_POINT('',#69109);
#13473=VERTEX_POINT('',#69110);
#13474=VERTEX_POINT('',#69187);
#13475=VERTEX_POINT('',#69188);
#13476=VERTEX_POINT('',#69263);
#13477=VERTEX_POINT('',#69264);
#13478=VERTEX_POINT('',#69341);
#13479=VERTEX_POINT('',#69342);
#13480=VERTEX_POINT('',#69417);
#13481=VERTEX_POINT('',#69418);
#13482=VERTEX_POINT('',#69493);
#13483=VERTEX_POINT('',#69494);
#13484=VERTEX_POINT('',#69569);
#13485=VERTEX_POINT('',#69570);
#13486=VERTEX_POINT('',#69645);
#13487=VERTEX_POINT('',#69646);
#13488=VERTEX_POINT('',#69723);
#13489=VERTEX_POINT('',#69724);
#13490=VERTEX_POINT('',#69799);
#13491=VERTEX_POINT('',#69800);
#13492=VERTEX_POINT('',#69877);
#13493=VERTEX_POINT('',#69878);
#13494=VERTEX_POINT('',#69953);
#13495=VERTEX_POINT('',#69954);
#13496=VERTEX_POINT('',#70029);
#13497=VERTEX_POINT('',#70041);
#13498=VERTEX_POINT('',#70054);
#13499=VERTEX_POINT('',#70146);
#13500=VERTEX_POINT('',#70147);
#13501=VERTEX_POINT('',#70149);
#13502=VERTEX_POINT('',#70151);
#13503=VERTEX_POINT('',#70155);
#13504=VERTEX_POINT('',#70156);
#13505=VERTEX_POINT('',#70158);
#13506=VERTEX_POINT('',#70160);
#13507=VERTEX_POINT('',#70164);
#13508=VERTEX_POINT('',#70165);
#13509=VERTEX_POINT('',#70167);
#13510=VERTEX_POINT('',#70169);
#13511=VERTEX_POINT('',#70173);
#13512=VERTEX_POINT('',#70174);
#13513=VERTEX_POINT('',#70176);
#13514=VERTEX_POINT('',#70178);
#13515=VERTEX_POINT('',#70182);
#13516=VERTEX_POINT('',#70183);
#13517=VERTEX_POINT('',#70185);
#13518=VERTEX_POINT('',#70187);
#13519=VERTEX_POINT('',#70191);
#13520=VERTEX_POINT('',#70192);
#13521=VERTEX_POINT('',#70194);
#13522=VERTEX_POINT('',#70196);
#13523=VERTEX_POINT('',#70200);
#13524=VERTEX_POINT('',#70201);
#13525=VERTEX_POINT('',#70203);
#13526=VERTEX_POINT('',#70205);
#13527=VERTEX_POINT('',#70209);
#13528=VERTEX_POINT('',#70210);
#13529=VERTEX_POINT('',#70212);
#13530=VERTEX_POINT('',#70214);
#13531=VERTEX_POINT('',#70218);
#13532=VERTEX_POINT('',#70219);
#13533=VERTEX_POINT('',#70221);
#13534=VERTEX_POINT('',#70223);
#13535=VERTEX_POINT('',#70227);
#13536=VERTEX_POINT('',#70228);
#13537=VERTEX_POINT('',#70230);
#13538=VERTEX_POINT('',#70232);
#13539=VERTEX_POINT('',#70236);
#13540=VERTEX_POINT('',#70237);
#13541=VERTEX_POINT('',#70239);
#13542=VERTEX_POINT('',#70241);
#13543=VERTEX_POINT('',#70245);
#13544=VERTEX_POINT('',#70246);
#13545=VERTEX_POINT('',#70248);
#13546=VERTEX_POINT('',#70250);
#13547=VERTEX_POINT('',#70254);
#13548=VERTEX_POINT('',#70255);
#13549=VERTEX_POINT('',#70257);
#13550=VERTEX_POINT('',#70259);
#13551=VERTEX_POINT('',#70263);
#13552=VERTEX_POINT('',#70264);
#13553=VERTEX_POINT('',#70266);
#13554=VERTEX_POINT('',#70268);
#13555=VERTEX_POINT('',#70272);
#13556=VERTEX_POINT('',#70273);
#13557=VERTEX_POINT('',#70275);
#13558=VERTEX_POINT('',#70277);
#13559=VERTEX_POINT('',#70281);
#13560=VERTEX_POINT('',#70282);
#13561=VERTEX_POINT('',#70286);
#13562=VERTEX_POINT('',#70290);
#13563=VERTEX_POINT('',#70294);
#13564=VERTEX_POINT('',#70298);
#13565=VERTEX_POINT('',#70302);
#13566=VERTEX_POINT('',#70309);
#13567=VERTEX_POINT('',#70313);
#13568=VERTEX_POINT('',#70315);
#13569=VERTEX_POINT('',#70319);
#13570=VERTEX_POINT('',#70320);
#13571=VERTEX_POINT('',#70329);
#13572=VERTEX_POINT('',#70333);
#13573=VERTEX_POINT('',#70335);
#13574=VERTEX_POINT('',#70339);
#13575=VERTEX_POINT('',#70341);
#13576=VERTEX_POINT('',#70345);
#13577=VERTEX_POINT('',#70347);
#13578=VERTEX_POINT('',#70351);
#13579=VERTEX_POINT('',#70353);
#13580=VERTEX_POINT('',#70357);
#13581=VERTEX_POINT('',#70359);
#13582=VERTEX_POINT('',#70363);
#13583=VERTEX_POINT('',#70365);
#13584=VERTEX_POINT('',#70369);
#13585=VERTEX_POINT('',#70371);
#13586=VERTEX_POINT('',#70375);
#13587=VERTEX_POINT('',#70377);
#13588=VERTEX_POINT('',#70381);
#13589=VERTEX_POINT('',#70383);
#13590=VERTEX_POINT('',#70387);
#13591=VERTEX_POINT('',#70389);
#13592=VERTEX_POINT('',#70393);
#13593=VERTEX_POINT('',#70395);
#13594=VERTEX_POINT('',#70399);
#13595=VERTEX_POINT('',#70401);
#13596=VERTEX_POINT('',#70405);
#13597=VERTEX_POINT('',#70407);
#13598=VERTEX_POINT('',#70411);
#13599=VERTEX_POINT('',#70413);
#13600=VERTEX_POINT('',#70417);
#13601=VERTEX_POINT('',#70419);
#13602=VERTEX_POINT('',#70423);
#13603=VERTEX_POINT('',#70425);
#13604=VERTEX_POINT('',#70429);
#13605=VERTEX_POINT('',#70431);
#13606=VERTEX_POINT('',#70435);
#13607=VERTEX_POINT('',#70437);
#13608=VERTEX_POINT('',#70441);
#13609=VERTEX_POINT('',#70443);
#13610=VERTEX_POINT('',#70447);
#13611=VERTEX_POINT('',#70449);
#13612=VERTEX_POINT('',#70453);
#13613=VERTEX_POINT('',#70455);
#13614=VERTEX_POINT('',#70459);
#13615=VERTEX_POINT('',#70461);
#13616=VERTEX_POINT('',#70465);
#13617=VERTEX_POINT('',#70467);
#13618=VERTEX_POINT('',#70471);
#13619=VERTEX_POINT('',#70473);
#13620=VERTEX_POINT('',#70477);
#13621=VERTEX_POINT('',#70479);
#13622=VERTEX_POINT('',#70483);
#13623=VERTEX_POINT('',#70485);
#13624=VERTEX_POINT('',#70489);
#13625=VERTEX_POINT('',#70491);
#13626=VERTEX_POINT('',#70495);
#13627=VERTEX_POINT('',#70497);
#13628=VERTEX_POINT('',#70501);
#13629=VERTEX_POINT('',#70503);
#13630=VERTEX_POINT('',#70507);
#13631=VERTEX_POINT('',#70509);
#13632=VERTEX_POINT('',#70513);
#13633=VERTEX_POINT('',#70515);
#13634=VERTEX_POINT('',#70519);
#13635=VERTEX_POINT('',#70521);
#13636=VERTEX_POINT('',#70525);
#13637=VERTEX_POINT('',#70527);
#13638=VERTEX_POINT('',#70531);
#13639=VERTEX_POINT('',#70533);
#13640=VERTEX_POINT('',#70537);
#13641=VERTEX_POINT('',#70539);
#13642=VERTEX_POINT('',#70543);
#13643=VERTEX_POINT('',#70545);
#13644=VERTEX_POINT('',#70549);
#13645=VERTEX_POINT('',#70551);
#13646=VERTEX_POINT('',#70555);
#13647=VERTEX_POINT('',#70557);
#13648=VERTEX_POINT('',#70561);
#13649=VERTEX_POINT('',#70563);
#13650=VERTEX_POINT('',#70567);
#13651=VERTEX_POINT('',#70569);
#13652=VERTEX_POINT('',#70573);
#13653=VERTEX_POINT('',#70575);
#13654=VERTEX_POINT('',#70579);
#13655=VERTEX_POINT('',#70581);
#13656=VERTEX_POINT('',#70585);
#13657=VERTEX_POINT('',#70587);
#13658=VERTEX_POINT('',#70591);
#13659=VERTEX_POINT('',#70593);
#13660=VERTEX_POINT('',#70597);
#13661=VERTEX_POINT('',#70599);
#13662=VERTEX_POINT('',#70603);
#13663=VERTEX_POINT('',#70605);
#13664=VERTEX_POINT('',#70609);
#13665=VERTEX_POINT('',#70611);
#13666=VERTEX_POINT('',#70615);
#13667=VERTEX_POINT('',#70617);
#13668=VERTEX_POINT('',#70621);
#13669=VERTEX_POINT('',#70623);
#13670=VERTEX_POINT('',#70627);
#13671=VERTEX_POINT('',#70629);
#13672=VERTEX_POINT('',#70633);
#13673=VERTEX_POINT('',#70635);
#13674=VERTEX_POINT('',#70639);
#13675=VERTEX_POINT('',#70641);
#13676=VERTEX_POINT('',#70645);
#13677=VERTEX_POINT('',#70647);
#13678=VERTEX_POINT('',#70651);
#13679=VERTEX_POINT('',#70653);
#13680=VERTEX_POINT('',#70657);
#13681=VERTEX_POINT('',#70659);
#13682=VERTEX_POINT('',#70663);
#13683=VERTEX_POINT('',#70665);
#13684=VERTEX_POINT('',#70669);
#13685=VERTEX_POINT('',#70671);
#13686=VERTEX_POINT('',#70675);
#13687=VERTEX_POINT('',#70677);
#13688=VERTEX_POINT('',#70681);
#13689=VERTEX_POINT('',#70683);
#13690=VERTEX_POINT('',#70687);
#13691=VERTEX_POINT('',#70689);
#13692=VERTEX_POINT('',#70693);
#13693=VERTEX_POINT('',#70695);
#13694=VERTEX_POINT('',#70699);
#13695=VERTEX_POINT('',#70701);
#13696=VERTEX_POINT('',#70705);
#13697=VERTEX_POINT('',#70707);
#13698=VERTEX_POINT('',#70711);
#13699=VERTEX_POINT('',#70713);
#13700=VERTEX_POINT('',#70717);
#13701=VERTEX_POINT('',#70719);
#13702=VERTEX_POINT('',#70723);
#13703=VERTEX_POINT('',#70725);
#13704=VERTEX_POINT('',#70729);
#13705=VERTEX_POINT('',#70731);
#13706=VERTEX_POINT('',#70735);
#13707=VERTEX_POINT('',#70737);
#13708=VERTEX_POINT('',#70741);
#13709=VERTEX_POINT('',#70743);
#13710=VERTEX_POINT('',#70747);
#13711=VERTEX_POINT('',#70749);
#13712=VERTEX_POINT('',#70753);
#13713=VERTEX_POINT('',#70755);
#13714=VERTEX_POINT('',#70759);
#13715=VERTEX_POINT('',#70761);
#13716=VERTEX_POINT('',#70765);
#13717=VERTEX_POINT('',#70767);
#13718=VERTEX_POINT('',#70771);
#13719=VERTEX_POINT('',#70773);
#13720=VERTEX_POINT('',#70777);
#13721=VERTEX_POINT('',#70779);
#13722=VERTEX_POINT('',#70783);
#13723=VERTEX_POINT('',#70785);
#13724=VERTEX_POINT('',#70789);
#13725=VERTEX_POINT('',#70791);
#13726=VERTEX_POINT('',#70795);
#13727=VERTEX_POINT('',#70797);
#13728=VERTEX_POINT('',#70801);
#13729=VERTEX_POINT('',#70803);
#13730=VERTEX_POINT('',#70807);
#13731=VERTEX_POINT('',#70809);
#13732=VERTEX_POINT('',#70813);
#13733=VERTEX_POINT('',#70815);
#13734=VERTEX_POINT('',#70819);
#13735=VERTEX_POINT('',#70821);
#13736=VERTEX_POINT('',#70825);
#13737=VERTEX_POINT('',#70827);
#13738=VERTEX_POINT('',#70831);
#13739=VERTEX_POINT('',#70833);
#13740=VERTEX_POINT('',#70837);
#13741=VERTEX_POINT('',#70839);
#13742=VERTEX_POINT('',#70843);
#13743=VERTEX_POINT('',#70845);
#13744=VERTEX_POINT('',#70849);
#13745=VERTEX_POINT('',#70851);
#13746=VERTEX_POINT('',#70855);
#13747=VERTEX_POINT('',#70857);
#13748=VERTEX_POINT('',#70861);
#13749=VERTEX_POINT('',#70863);
#13750=VERTEX_POINT('',#70867);
#13751=VERTEX_POINT('',#70869);
#13752=VERTEX_POINT('',#70873);
#13753=VERTEX_POINT('',#70878);
#13754=VERTEX_POINT('',#70882);
#13755=VERTEX_POINT('',#70887);
#13756=VERTEX_POINT('',#70891);
#13757=VERTEX_POINT('',#70896);
#13758=VERTEX_POINT('',#70900);
#13759=VERTEX_POINT('',#70905);
#13760=VERTEX_POINT('',#70909);
#13761=VERTEX_POINT('',#70914);
#13762=VERTEX_POINT('',#70918);
#13763=VERTEX_POINT('',#70923);
#13764=VERTEX_POINT('',#70927);
#13765=VERTEX_POINT('',#70932);
#13766=VERTEX_POINT('',#70936);
#13767=VERTEX_POINT('',#70941);
#13768=VERTEX_POINT('',#70945);
#13769=VERTEX_POINT('',#70950);
#13770=VERTEX_POINT('',#70954);
#13771=VERTEX_POINT('',#70959);
#13772=VERTEX_POINT('',#70963);
#13773=VERTEX_POINT('',#70968);
#13774=VERTEX_POINT('',#70972);
#13775=VERTEX_POINT('',#70977);
#13776=VERTEX_POINT('',#70981);
#13777=VERTEX_POINT('',#70986);
#13778=VERTEX_POINT('',#70990);
#13779=VERTEX_POINT('',#70995);
#13780=VERTEX_POINT('',#70999);
#13781=VERTEX_POINT('',#71004);
#13782=VERTEX_POINT('',#71008);
#13783=VERTEX_POINT('',#71010);
#13784=VERTEX_POINT('',#71014);
#13785=VERTEX_POINT('',#71016);
#13786=VERTEX_POINT('',#71020);
#13787=VERTEX_POINT('',#71022);
#13788=VERTEX_POINT('',#71026);
#13789=VERTEX_POINT('',#71028);
#13790=VERTEX_POINT('',#71032);
#13791=VERTEX_POINT('',#71034);
#13792=VERTEX_POINT('',#71038);
#13793=VERTEX_POINT('',#71040);
#13794=VERTEX_POINT('',#71044);
#13795=VERTEX_POINT('',#71046);
#13796=VERTEX_POINT('',#71050);
#13797=VERTEX_POINT('',#71052);
#13798=VERTEX_POINT('',#71056);
#13799=VERTEX_POINT('',#71058);
#13800=VERTEX_POINT('',#71062);
#13801=VERTEX_POINT('',#71064);
#13802=VERTEX_POINT('',#71068);
#13803=VERTEX_POINT('',#71070);
#13804=VERTEX_POINT('',#71074);
#13805=VERTEX_POINT('',#71076);
#13806=VERTEX_POINT('',#71080);
#13807=VERTEX_POINT('',#71082);
#13808=VERTEX_POINT('',#71086);
#13809=VERTEX_POINT('',#71088);
#13810=VERTEX_POINT('',#71092);
#13811=VERTEX_POINT('',#71094);
#13812=VERTEX_POINT('',#71098);
#13813=VERTEX_POINT('',#71100);
#13814=VERTEX_POINT('',#71104);
#13815=VERTEX_POINT('',#71106);
#13816=VERTEX_POINT('',#71110);
#13817=VERTEX_POINT('',#71112);
#13818=VERTEX_POINT('',#71116);
#13819=VERTEX_POINT('',#71118);
#13820=VERTEX_POINT('',#71122);
#13821=VERTEX_POINT('',#71124);
#13822=VERTEX_POINT('',#71128);
#13823=VERTEX_POINT('',#71130);
#13824=VERTEX_POINT('',#71134);
#13825=VERTEX_POINT('',#71136);
#13826=VERTEX_POINT('',#71140);
#13827=VERTEX_POINT('',#71142);
#13828=VERTEX_POINT('',#71146);
#13829=VERTEX_POINT('',#71148);
#13830=VERTEX_POINT('',#71152);
#13831=VERTEX_POINT('',#71154);
#13832=VERTEX_POINT('',#71158);
#13833=VERTEX_POINT('',#71160);
#13834=VERTEX_POINT('',#71164);
#13835=VERTEX_POINT('',#71166);
#13836=VERTEX_POINT('',#71170);
#13837=VERTEX_POINT('',#71172);
#13838=VERTEX_POINT('',#71176);
#13839=VERTEX_POINT('',#71178);
#13840=VERTEX_POINT('',#71182);
#13841=VERTEX_POINT('',#71184);
#13842=VERTEX_POINT('',#71188);
#13843=VERTEX_POINT('',#71190);
#13844=VERTEX_POINT('',#71194);
#13845=VERTEX_POINT('',#71196);
#13846=VERTEX_POINT('',#71200);
#13847=VERTEX_POINT('',#71202);
#13848=VERTEX_POINT('',#71206);
#13849=VERTEX_POINT('',#71208);
#13850=VERTEX_POINT('',#71212);
#13851=VERTEX_POINT('',#71214);
#13852=VERTEX_POINT('',#71218);
#13853=VERTEX_POINT('',#71220);
#13854=VERTEX_POINT('',#71224);
#13855=VERTEX_POINT('',#71226);
#13856=VERTEX_POINT('',#71230);
#13857=VERTEX_POINT('',#71232);
#13858=VERTEX_POINT('',#71236);
#13859=VERTEX_POINT('',#71238);
#13860=VERTEX_POINT('',#71252);
#13861=VERTEX_POINT('',#71253);
#13862=VERTEX_POINT('',#71262);
#13863=VERTEX_POINT('',#71266);
#13864=VERTEX_POINT('',#71268);
#13865=VERTEX_POINT('',#71272);
#13866=VERTEX_POINT('',#71274);
#13867=VERTEX_POINT('',#71278);
#13868=VERTEX_POINT('',#71280);
#13869=VERTEX_POINT('',#71284);
#13870=VERTEX_POINT('',#71286);
#13871=VERTEX_POINT('',#71290);
#13872=VERTEX_POINT('',#71292);
#13873=VERTEX_POINT('',#71296);
#13874=VERTEX_POINT('',#71298);
#13875=VERTEX_POINT('',#71302);
#13876=VERTEX_POINT('',#71304);
#13877=VERTEX_POINT('',#71308);
#13878=VERTEX_POINT('',#71310);
#13879=VERTEX_POINT('',#71314);
#13880=VERTEX_POINT('',#71316);
#13881=VERTEX_POINT('',#71320);
#13882=VERTEX_POINT('',#71322);
#13883=VERTEX_POINT('',#71326);
#13884=VERTEX_POINT('',#71328);
#13885=VERTEX_POINT('',#71332);
#13886=VERTEX_POINT('',#71334);
#13887=VERTEX_POINT('',#71338);
#13888=VERTEX_POINT('',#71340);
#13889=VERTEX_POINT('',#71344);
#13890=VERTEX_POINT('',#71346);
#13891=VERTEX_POINT('',#71350);
#13892=VERTEX_POINT('',#71352);
#13893=VERTEX_POINT('',#71356);
#13894=VERTEX_POINT('',#71358);
#13895=VERTEX_POINT('',#71362);
#13896=VERTEX_POINT('',#71364);
#13897=VERTEX_POINT('',#71368);
#13898=VERTEX_POINT('',#71370);
#13899=VERTEX_POINT('',#71374);
#13900=VERTEX_POINT('',#71376);
#13901=VERTEX_POINT('',#71380);
#13902=VERTEX_POINT('',#71382);
#13903=VERTEX_POINT('',#71386);
#13904=VERTEX_POINT('',#71388);
#13905=VERTEX_POINT('',#71392);
#13906=VERTEX_POINT('',#71394);
#13907=VERTEX_POINT('',#71398);
#13908=VERTEX_POINT('',#71400);
#13909=VERTEX_POINT('',#71404);
#13910=VERTEX_POINT('',#71406);
#13911=VERTEX_POINT('',#71410);
#13912=VERTEX_POINT('',#71412);
#13913=VERTEX_POINT('',#71416);
#13914=VERTEX_POINT('',#71418);
#13915=VERTEX_POINT('',#71422);
#13916=VERTEX_POINT('',#71424);
#13917=VERTEX_POINT('',#71428);
#13918=VERTEX_POINT('',#71430);
#13919=VERTEX_POINT('',#71434);
#13920=VERTEX_POINT('',#71436);
#13921=VERTEX_POINT('',#71440);
#13922=VERTEX_POINT('',#71442);
#13923=VERTEX_POINT('',#71446);
#13924=VERTEX_POINT('',#71448);
#13925=VERTEX_POINT('',#71452);
#13926=VERTEX_POINT('',#71454);
#13927=VERTEX_POINT('',#71458);
#13928=VERTEX_POINT('',#71460);
#13929=VERTEX_POINT('',#71464);
#13930=VERTEX_POINT('',#71466);
#13931=VERTEX_POINT('',#71470);
#13932=VERTEX_POINT('',#71472);
#13933=VERTEX_POINT('',#71476);
#13934=VERTEX_POINT('',#71478);
#13935=VERTEX_POINT('',#71482);
#13936=VERTEX_POINT('',#71484);
#13937=VERTEX_POINT('',#71488);
#13938=VERTEX_POINT('',#71490);
#13939=VERTEX_POINT('',#71494);
#13940=VERTEX_POINT('',#71496);
#13941=VERTEX_POINT('',#71500);
#13942=VERTEX_POINT('',#71502);
#13943=VERTEX_POINT('',#71506);
#13944=VERTEX_POINT('',#71508);
#13945=VERTEX_POINT('',#71512);
#13946=VERTEX_POINT('',#71514);
#13947=VERTEX_POINT('',#71518);
#13948=VERTEX_POINT('',#71520);
#13949=VERTEX_POINT('',#71524);
#13950=VERTEX_POINT('',#71526);
#13951=VERTEX_POINT('',#71530);
#13952=VERTEX_POINT('',#71532);
#13953=VERTEX_POINT('',#71536);
#13954=VERTEX_POINT('',#71538);
#13955=VERTEX_POINT('',#71542);
#13956=VERTEX_POINT('',#71544);
#13957=VERTEX_POINT('',#71548);
#13958=VERTEX_POINT('',#71550);
#13959=VERTEX_POINT('',#71554);
#13960=VERTEX_POINT('',#71556);
#13961=VERTEX_POINT('',#71560);
#13962=VERTEX_POINT('',#71562);
#13963=VERTEX_POINT('',#71566);
#13964=VERTEX_POINT('',#71568);
#13965=VERTEX_POINT('',#71572);
#13966=VERTEX_POINT('',#71574);
#13967=VERTEX_POINT('',#71578);
#13968=VERTEX_POINT('',#71580);
#13969=VERTEX_POINT('',#71584);
#13970=VERTEX_POINT('',#71586);
#13971=VERTEX_POINT('',#71590);
#13972=VERTEX_POINT('',#71592);
#13973=VERTEX_POINT('',#71596);
#13974=VERTEX_POINT('',#71598);
#13975=VERTEX_POINT('',#71602);
#13976=VERTEX_POINT('',#71604);
#13977=VERTEX_POINT('',#71608);
#13978=VERTEX_POINT('',#71610);
#13979=VERTEX_POINT('',#71614);
#13980=VERTEX_POINT('',#71616);
#13981=VERTEX_POINT('',#71620);
#13982=VERTEX_POINT('',#71622);
#13983=VERTEX_POINT('',#71626);
#13984=VERTEX_POINT('',#71628);
#13985=VERTEX_POINT('',#71632);
#13986=VERTEX_POINT('',#71634);
#13987=VERTEX_POINT('',#71638);
#13988=VERTEX_POINT('',#71640);
#13989=VERTEX_POINT('',#71644);
#13990=VERTEX_POINT('',#71646);
#13991=VERTEX_POINT('',#71650);
#13992=VERTEX_POINT('',#71652);
#13993=VERTEX_POINT('',#71656);
#13994=VERTEX_POINT('',#71658);
#13995=VERTEX_POINT('',#71662);
#13996=VERTEX_POINT('',#71664);
#13997=VERTEX_POINT('',#71668);
#13998=VERTEX_POINT('',#71670);
#13999=VERTEX_POINT('',#71674);
#14000=VERTEX_POINT('',#71676);
#14001=VERTEX_POINT('',#71680);
#14002=VERTEX_POINT('',#71682);
#14003=VERTEX_POINT('',#71686);
#14004=VERTEX_POINT('',#71688);
#14005=VERTEX_POINT('',#71692);
#14006=VERTEX_POINT('',#71694);
#14007=VERTEX_POINT('',#71698);
#14008=VERTEX_POINT('',#71700);
#14009=VERTEX_POINT('',#71704);
#14010=VERTEX_POINT('',#71706);
#14011=VERTEX_POINT('',#71710);
#14012=VERTEX_POINT('',#71712);
#14013=VERTEX_POINT('',#71716);
#14014=VERTEX_POINT('',#71718);
#14015=VERTEX_POINT('',#71722);
#14016=VERTEX_POINT('',#71724);
#14017=VERTEX_POINT('',#71728);
#14018=VERTEX_POINT('',#71730);
#14019=VERTEX_POINT('',#71734);
#14020=VERTEX_POINT('',#71736);
#14021=VERTEX_POINT('',#71740);
#14022=VERTEX_POINT('',#71742);
#14023=VERTEX_POINT('',#71746);
#14024=VERTEX_POINT('',#71748);
#14025=VERTEX_POINT('',#71752);
#14026=VERTEX_POINT('',#71754);
#14027=VERTEX_POINT('',#71758);
#14028=VERTEX_POINT('',#71760);
#14029=VERTEX_POINT('',#71764);
#14030=VERTEX_POINT('',#71766);
#14031=VERTEX_POINT('',#71770);
#14032=VERTEX_POINT('',#71772);
#14033=VERTEX_POINT('',#71776);
#14034=VERTEX_POINT('',#71778);
#14035=VERTEX_POINT('',#71782);
#14036=VERTEX_POINT('',#71784);
#14037=VERTEX_POINT('',#71788);
#14038=VERTEX_POINT('',#71790);
#14039=VERTEX_POINT('',#71794);
#14040=VERTEX_POINT('',#71796);
#14041=VERTEX_POINT('',#71800);
#14042=VERTEX_POINT('',#71802);
#14043=VERTEX_POINT('',#71806);
#14044=VERTEX_POINT('',#71808);
#14045=VERTEX_POINT('',#71812);
#14046=VERTEX_POINT('',#71814);
#14047=VERTEX_POINT('',#71818);
#14048=VERTEX_POINT('',#71820);
#14049=VERTEX_POINT('',#71824);
#14050=VERTEX_POINT('',#71826);
#14051=VERTEX_POINT('',#71830);
#14052=VERTEX_POINT('',#71832);
#14053=VERTEX_POINT('',#71836);
#14054=VERTEX_POINT('',#71838);
#14055=VERTEX_POINT('',#71842);
#14056=VERTEX_POINT('',#71844);
#14057=VERTEX_POINT('',#71848);
#14058=VERTEX_POINT('',#71850);
#14059=VERTEX_POINT('',#71854);
#14060=VERTEX_POINT('',#71856);
#14061=VERTEX_POINT('',#71860);
#14062=VERTEX_POINT('',#71862);
#14063=VERTEX_POINT('',#71866);
#14064=VERTEX_POINT('',#71868);
#14065=VERTEX_POINT('',#71872);
#14066=VERTEX_POINT('',#71874);
#14067=VERTEX_POINT('',#71878);
#14068=VERTEX_POINT('',#71880);
#14069=VERTEX_POINT('',#71884);
#14070=VERTEX_POINT('',#71886);
#14071=VERTEX_POINT('',#71890);
#14072=VERTEX_POINT('',#71892);
#14073=VERTEX_POINT('',#71896);
#14074=VERTEX_POINT('',#71898);
#14075=VERTEX_POINT('',#71902);
#14076=VERTEX_POINT('',#71904);
#14077=VERTEX_POINT('',#71908);
#14078=VERTEX_POINT('',#71910);
#14079=VERTEX_POINT('',#71914);
#14080=VERTEX_POINT('',#71916);
#14081=VERTEX_POINT('',#71920);
#14082=VERTEX_POINT('',#71922);
#14083=VERTEX_POINT('',#71926);
#14084=VERTEX_POINT('',#71928);
#14085=VERTEX_POINT('',#71932);
#14086=VERTEX_POINT('',#71934);
#14087=VERTEX_POINT('',#71938);
#14088=VERTEX_POINT('',#71940);
#14089=VERTEX_POINT('',#71944);
#14090=VERTEX_POINT('',#71946);
#14091=VERTEX_POINT('',#71950);
#14092=VERTEX_POINT('',#71952);
#14093=VERTEX_POINT('',#71956);
#14094=VERTEX_POINT('',#71958);
#14095=VERTEX_POINT('',#71962);
#14096=VERTEX_POINT('',#71964);
#14097=VERTEX_POINT('',#71968);
#14098=VERTEX_POINT('',#71970);
#14099=VERTEX_POINT('',#71974);
#14100=VERTEX_POINT('',#71979);
#14101=VERTEX_POINT('',#71983);
#14102=VERTEX_POINT('',#71988);
#14103=VERTEX_POINT('',#71992);
#14104=VERTEX_POINT('',#71997);
#14105=VERTEX_POINT('',#72001);
#14106=VERTEX_POINT('',#72006);
#14107=VERTEX_POINT('',#72010);
#14108=VERTEX_POINT('',#72015);
#14109=VERTEX_POINT('',#72019);
#14110=VERTEX_POINT('',#72024);
#14111=VERTEX_POINT('',#72028);
#14112=VERTEX_POINT('',#72033);
#14113=VERTEX_POINT('',#72037);
#14114=VERTEX_POINT('',#72042);
#14115=VERTEX_POINT('',#72046);
#14116=VERTEX_POINT('',#72051);
#14117=VERTEX_POINT('',#72055);
#14118=VERTEX_POINT('',#72060);
#14119=VERTEX_POINT('',#72064);
#14120=VERTEX_POINT('',#72069);
#14121=VERTEX_POINT('',#72073);
#14122=VERTEX_POINT('',#72078);
#14123=VERTEX_POINT('',#72082);
#14124=VERTEX_POINT('',#72087);
#14125=VERTEX_POINT('',#72091);
#14126=VERTEX_POINT('',#72096);
#14127=VERTEX_POINT('',#72100);
#14128=VERTEX_POINT('',#72105);
#14129=VERTEX_POINT('',#72109);
#14130=VERTEX_POINT('',#72111);
#14131=VERTEX_POINT('',#72115);
#14132=VERTEX_POINT('',#72117);
#14133=VERTEX_POINT('',#72121);
#14134=VERTEX_POINT('',#72123);
#14135=VERTEX_POINT('',#72127);
#14136=VERTEX_POINT('',#72129);
#14137=VERTEX_POINT('',#72133);
#14138=VERTEX_POINT('',#72135);
#14139=VERTEX_POINT('',#72139);
#14140=VERTEX_POINT('',#72141);
#14141=VERTEX_POINT('',#72145);
#14142=VERTEX_POINT('',#72147);
#14143=VERTEX_POINT('',#72151);
#14144=VERTEX_POINT('',#72153);
#14145=VERTEX_POINT('',#72157);
#14146=VERTEX_POINT('',#72159);
#14147=VERTEX_POINT('',#72163);
#14148=VERTEX_POINT('',#72165);
#14149=VERTEX_POINT('',#72169);
#14150=VERTEX_POINT('',#72171);
#14151=VERTEX_POINT('',#72183);
#14152=VERTEX_POINT('',#72185);
#14153=VERTEX_POINT('',#72189);
#14154=VERTEX_POINT('',#72193);
#14155=VERTEX_POINT('',#72197);
#14156=VERTEX_POINT('',#72201);
#14157=VERTEX_POINT('',#72205);
#14158=VERTEX_POINT('',#72207);
#14159=VERTEX_POINT('',#72211);
#14160=VERTEX_POINT('',#72213);
#14161=VERTEX_POINT('',#72217);
#14162=VERTEX_POINT('',#72219);
#14163=VERTEX_POINT('',#72223);
#14164=VERTEX_POINT('',#72225);
#14165=VERTEX_POINT('',#72229);
#14166=VERTEX_POINT('',#72231);
#14167=VERTEX_POINT('',#72235);
#14168=VERTEX_POINT('',#72237);
#14169=VERTEX_POINT('',#72241);
#14170=VERTEX_POINT('',#72243);
#14171=VERTEX_POINT('',#72247);
#14172=VERTEX_POINT('',#72249);
#14173=VERTEX_POINT('',#72253);
#14174=VERTEX_POINT('',#72255);
#14175=VERTEX_POINT('',#72259);
#14176=VERTEX_POINT('',#72261);
#14177=VERTEX_POINT('',#72265);
#14178=VERTEX_POINT('',#72267);
#14179=VERTEX_POINT('',#72271);
#14180=VERTEX_POINT('',#72273);
#14181=VERTEX_POINT('',#72277);
#14182=VERTEX_POINT('',#72279);
#14183=VERTEX_POINT('',#72283);
#14184=VERTEX_POINT('',#72285);
#14185=VERTEX_POINT('',#72289);
#14186=VERTEX_POINT('',#72291);
#14187=VERTEX_POINT('',#72295);
#14188=VERTEX_POINT('',#72297);
#14189=VERTEX_POINT('',#72301);
#14190=VERTEX_POINT('',#72303);
#14191=VERTEX_POINT('',#72307);
#14192=VERTEX_POINT('',#72309);
#14193=VERTEX_POINT('',#72313);
#14194=VERTEX_POINT('',#72315);
#14195=VERTEX_POINT('',#72319);
#14196=VERTEX_POINT('',#72321);
#14197=VERTEX_POINT('',#72325);
#14198=VERTEX_POINT('',#72327);
#14199=VERTEX_POINT('',#72331);
#14200=VERTEX_POINT('',#72333);
#14201=VERTEX_POINT('',#72337);
#14202=VERTEX_POINT('',#72339);
#14203=VERTEX_POINT('',#72343);
#14204=VERTEX_POINT('',#72345);
#14205=VERTEX_POINT('',#72349);
#14206=VERTEX_POINT('',#72351);
#14207=VERTEX_POINT('',#72355);
#14208=VERTEX_POINT('',#72357);
#14209=VERTEX_POINT('',#72361);
#14210=VERTEX_POINT('',#72363);
#14211=VERTEX_POINT('',#72367);
#14212=VERTEX_POINT('',#72369);
#14213=VERTEX_POINT('',#72373);
#14214=VERTEX_POINT('',#72375);
#14215=VERTEX_POINT('',#72379);
#14216=VERTEX_POINT('',#72381);
#14217=VERTEX_POINT('',#72385);
#14218=VERTEX_POINT('',#72387);
#14219=VERTEX_POINT('',#72391);
#14220=VERTEX_POINT('',#72393);
#14221=VERTEX_POINT('',#72397);
#14222=VERTEX_POINT('',#72399);
#14223=VERTEX_POINT('',#72403);
#14224=VERTEX_POINT('',#72405);
#14225=VERTEX_POINT('',#72409);
#14226=VERTEX_POINT('',#72411);
#14227=VERTEX_POINT('',#72415);
#14228=VERTEX_POINT('',#72417);
#14229=VERTEX_POINT('',#72421);
#14230=VERTEX_POINT('',#72423);
#14231=VERTEX_POINT('',#72427);
#14232=VERTEX_POINT('',#72429);
#14233=VERTEX_POINT('',#72433);
#14234=VERTEX_POINT('',#72435);
#14235=VERTEX_POINT('',#72439);
#14236=VERTEX_POINT('',#72441);
#14237=VERTEX_POINT('',#72445);
#14238=VERTEX_POINT('',#72447);
#14239=VERTEX_POINT('',#72451);
#14240=VERTEX_POINT('',#72453);
#14241=VERTEX_POINT('',#72457);
#14242=VERTEX_POINT('',#72459);
#14243=VERTEX_POINT('',#72463);
#14244=VERTEX_POINT('',#72465);
#14245=VERTEX_POINT('',#72469);
#14246=VERTEX_POINT('',#72471);
#14247=VERTEX_POINT('',#72475);
#14248=VERTEX_POINT('',#72477);
#14249=VERTEX_POINT('',#72481);
#14250=VERTEX_POINT('',#72483);
#14251=VERTEX_POINT('',#72487);
#14252=VERTEX_POINT('',#72489);
#14253=VERTEX_POINT('',#72493);
#14254=VERTEX_POINT('',#72495);
#14255=VERTEX_POINT('',#72499);
#14256=VERTEX_POINT('',#72501);
#14257=VERTEX_POINT('',#72505);
#14258=VERTEX_POINT('',#72507);
#14259=VERTEX_POINT('',#72511);
#14260=VERTEX_POINT('',#72513);
#14261=VERTEX_POINT('',#72517);
#14262=VERTEX_POINT('',#72519);
#14263=VERTEX_POINT('',#72523);
#14264=VERTEX_POINT('',#72525);
#14265=VERTEX_POINT('',#72529);
#14266=VERTEX_POINT('',#72531);
#14267=VERTEX_POINT('',#72535);
#14268=VERTEX_POINT('',#72537);
#14269=VERTEX_POINT('',#72541);
#14270=VERTEX_POINT('',#72543);
#14271=VERTEX_POINT('',#72547);
#14272=VERTEX_POINT('',#72549);
#14273=VERTEX_POINT('',#72553);
#14274=VERTEX_POINT('',#72555);
#14275=VERTEX_POINT('',#72559);
#14276=VERTEX_POINT('',#72561);
#14277=VERTEX_POINT('',#72565);
#14278=VERTEX_POINT('',#72567);
#14279=VERTEX_POINT('',#72571);
#14280=VERTEX_POINT('',#72573);
#14281=VERTEX_POINT('',#72577);
#14282=VERTEX_POINT('',#72579);
#14283=VERTEX_POINT('',#72583);
#14284=VERTEX_POINT('',#72585);
#14285=VERTEX_POINT('',#72589);
#14286=VERTEX_POINT('',#72591);
#14287=VERTEX_POINT('',#72595);
#14288=VERTEX_POINT('',#72597);
#14289=VERTEX_POINT('',#72601);
#14290=VERTEX_POINT('',#72603);
#14291=VERTEX_POINT('',#72607);
#14292=VERTEX_POINT('',#72609);
#14293=VERTEX_POINT('',#72613);
#14294=VERTEX_POINT('',#72615);
#14295=VERTEX_POINT('',#72619);
#14296=VERTEX_POINT('',#72621);
#14297=VERTEX_POINT('',#72625);
#14298=VERTEX_POINT('',#72627);
#14299=VERTEX_POINT('',#72631);
#14300=VERTEX_POINT('',#72633);
#14301=VERTEX_POINT('',#72637);
#14302=VERTEX_POINT('',#72639);
#14303=VERTEX_POINT('',#72643);
#14304=VERTEX_POINT('',#72645);
#14305=VERTEX_POINT('',#72649);
#14306=VERTEX_POINT('',#72651);
#14307=VERTEX_POINT('',#72655);
#14308=VERTEX_POINT('',#72657);
#14309=VERTEX_POINT('',#72661);
#14310=VERTEX_POINT('',#72663);
#14311=VERTEX_POINT('',#72667);
#14312=VERTEX_POINT('',#72669);
#14313=VERTEX_POINT('',#72673);
#14314=VERTEX_POINT('',#72675);
#14315=VERTEX_POINT('',#72679);
#14316=VERTEX_POINT('',#72681);
#14317=VERTEX_POINT('',#72685);
#14318=VERTEX_POINT('',#72687);
#14319=VERTEX_POINT('',#72691);
#14320=VERTEX_POINT('',#72693);
#14321=VERTEX_POINT('',#72697);
#14322=VERTEX_POINT('',#72699);
#14323=VERTEX_POINT('',#72703);
#14324=VERTEX_POINT('',#72705);
#14325=VERTEX_POINT('',#72709);
#14326=VERTEX_POINT('',#72711);
#14327=VERTEX_POINT('',#72715);
#14328=VERTEX_POINT('',#72717);
#14329=VERTEX_POINT('',#72721);
#14330=VERTEX_POINT('',#72723);
#14331=VERTEX_POINT('',#72727);
#14332=VERTEX_POINT('',#72729);
#14333=VERTEX_POINT('',#72733);
#14334=VERTEX_POINT('',#72735);
#14335=VERTEX_POINT('',#72739);
#14336=VERTEX_POINT('',#72741);
#14337=VERTEX_POINT('',#72745);
#14338=VERTEX_POINT('',#72747);
#14339=VERTEX_POINT('',#72751);
#14340=VERTEX_POINT('',#72753);
#14341=VERTEX_POINT('',#72757);
#14342=VERTEX_POINT('',#72759);
#14343=VERTEX_POINT('',#72763);
#14344=VERTEX_POINT('',#72765);
#14345=VERTEX_POINT('',#72769);
#14346=VERTEX_POINT('',#72771);
#14347=VERTEX_POINT('',#72775);
#14348=VERTEX_POINT('',#72777);
#14349=VERTEX_POINT('',#72781);
#14350=VERTEX_POINT('',#72783);
#14351=VERTEX_POINT('',#72787);
#14352=VERTEX_POINT('',#72789);
#14353=VERTEX_POINT('',#72793);
#14354=VERTEX_POINT('',#72795);
#14355=VERTEX_POINT('',#72799);
#14356=VERTEX_POINT('',#72801);
#14357=VERTEX_POINT('',#72805);
#14358=VERTEX_POINT('',#72807);
#14359=VERTEX_POINT('',#72811);
#14360=VERTEX_POINT('',#72813);
#14361=VERTEX_POINT('',#72817);
#14362=VERTEX_POINT('',#72819);
#14363=VERTEX_POINT('',#72823);
#14364=VERTEX_POINT('',#72825);
#14365=VERTEX_POINT('',#72829);
#14366=VERTEX_POINT('',#72831);
#14367=VERTEX_POINT('',#72835);
#14368=VERTEX_POINT('',#72837);
#14369=VERTEX_POINT('',#72841);
#14370=VERTEX_POINT('',#72843);
#14371=VERTEX_POINT('',#72847);
#14372=VERTEX_POINT('',#72849);
#14373=VERTEX_POINT('',#72853);
#14374=VERTEX_POINT('',#72855);
#14375=VERTEX_POINT('',#72859);
#14376=VERTEX_POINT('',#72861);
#14377=VERTEX_POINT('',#72865);
#14378=VERTEX_POINT('',#72867);
#14379=VERTEX_POINT('',#72871);
#14380=VERTEX_POINT('',#72873);
#14381=VERTEX_POINT('',#72877);
#14382=VERTEX_POINT('',#72879);
#14383=VERTEX_POINT('',#72883);
#14384=VERTEX_POINT('',#72885);
#14385=VERTEX_POINT('',#72889);
#14386=VERTEX_POINT('',#72891);
#14387=VERTEX_POINT('',#72895);
#14388=VERTEX_POINT('',#72897);
#14389=VERTEX_POINT('',#72901);
#14390=VERTEX_POINT('',#72903);
#14391=VERTEX_POINT('',#72907);
#14392=VERTEX_POINT('',#72909);
#14393=VERTEX_POINT('',#72913);
#14394=VERTEX_POINT('',#72915);
#14395=VERTEX_POINT('',#72919);
#14396=VERTEX_POINT('',#72921);
#14397=VERTEX_POINT('',#72925);
#14398=VERTEX_POINT('',#72927);
#14399=VERTEX_POINT('',#72931);
#14400=VERTEX_POINT('',#72933);
#14401=VERTEX_POINT('',#72937);
#14402=VERTEX_POINT('',#72939);
#14403=VERTEX_POINT('',#72943);
#14404=VERTEX_POINT('',#72945);
#14405=VERTEX_POINT('',#72949);
#14406=VERTEX_POINT('',#72951);
#14407=VERTEX_POINT('',#72955);
#14408=VERTEX_POINT('',#72957);
#14409=VERTEX_POINT('',#72961);
#14410=VERTEX_POINT('',#72963);
#14411=VERTEX_POINT('',#72967);
#14412=VERTEX_POINT('',#72969);
#14413=VERTEX_POINT('',#72973);
#14414=VERTEX_POINT('',#72975);
#14415=VERTEX_POINT('',#72979);
#14416=VERTEX_POINT('',#72981);
#14417=VERTEX_POINT('',#72985);
#14418=VERTEX_POINT('',#72987);
#14419=VERTEX_POINT('',#72991);
#14420=VERTEX_POINT('',#72993);
#14421=VERTEX_POINT('',#72997);
#14422=VERTEX_POINT('',#72999);
#14423=VERTEX_POINT('',#73003);
#14424=VERTEX_POINT('',#73005);
#14425=VERTEX_POINT('',#73009);
#14426=VERTEX_POINT('',#73011);
#14427=VERTEX_POINT('',#73015);
#14428=VERTEX_POINT('',#73017);
#14429=VERTEX_POINT('',#73021);
#14430=VERTEX_POINT('',#73023);
#14431=VERTEX_POINT('',#73027);
#14432=VERTEX_POINT('',#73029);
#14433=VERTEX_POINT('',#73033);
#14434=VERTEX_POINT('',#73035);
#14435=VERTEX_POINT('',#73039);
#14436=VERTEX_POINT('',#73041);
#14437=VERTEX_POINT('',#73045);
#14438=VERTEX_POINT('',#73047);
#14439=VERTEX_POINT('',#73051);
#14440=VERTEX_POINT('',#73053);
#14441=VERTEX_POINT('',#73057);
#14442=VERTEX_POINT('',#73059);
#14443=VERTEX_POINT('',#73063);
#14444=VERTEX_POINT('',#73065);
#14445=VERTEX_POINT('',#73069);
#14446=VERTEX_POINT('',#73071);
#14447=VERTEX_POINT('',#73075);
#14448=VERTEX_POINT('',#73077);
#14449=VERTEX_POINT('',#73081);
#14450=VERTEX_POINT('',#73083);
#14451=VERTEX_POINT('',#73087);
#14452=VERTEX_POINT('',#73089);
#14453=VERTEX_POINT('',#73093);
#14454=VERTEX_POINT('',#73095);
#14455=VERTEX_POINT('',#73099);
#14456=VERTEX_POINT('',#73101);
#14457=VERTEX_POINT('',#73105);
#14458=VERTEX_POINT('',#73107);
#14459=VERTEX_POINT('',#73111);
#14460=VERTEX_POINT('',#73113);
#14461=VERTEX_POINT('',#73117);
#14462=VERTEX_POINT('',#73119);
#14463=VERTEX_POINT('',#73123);
#14464=VERTEX_POINT('',#73125);
#14465=VERTEX_POINT('',#73129);
#14466=VERTEX_POINT('',#73131);
#14467=VERTEX_POINT('',#73135);
#14468=VERTEX_POINT('',#73137);
#14469=VERTEX_POINT('',#73141);
#14470=VERTEX_POINT('',#73143);
#14471=VERTEX_POINT('',#73147);
#14472=VERTEX_POINT('',#73149);
#14473=VERTEX_POINT('',#73392);
#14474=VERTEX_POINT('',#73394);
#14475=VERTEX_POINT('',#73398);
#14476=VERTEX_POINT('',#73400);
#14477=VERTEX_POINT('',#73408);
#14478=VERTEX_POINT('',#73409);
#14479=VERTEX_POINT('',#73411);
#14480=VERTEX_POINT('',#73413);
#14481=VERTEX_POINT('',#73415);
#14482=VERTEX_POINT('',#73417);
#17909=EDGE_CURVE('',#13374,#13375,#9450,.T.);
#17910=EDGE_CURVE('',#13376,#13374,#3226,.F.);
#17911=EDGE_CURVE('',#13376,#13377,#9451,.T.);
#17912=EDGE_CURVE('',#13377,#13377,#4115,.T.);
#17913=EDGE_CURVE('',#13378,#13376,#4116,.T.);
#17914=EDGE_CURVE('',#13375,#13378,#3227,.F.);
#17915=EDGE_CURVE('',#13379,#13380,#9452,.T.);
#17916=EDGE_CURVE('',#13374,#13379,#3228,.F.);
#17917=EDGE_CURVE('',#13380,#13375,#3229,.F.);
#17918=EDGE_CURVE('',#13381,#13382,#9453,.T.);
#17919=EDGE_CURVE('',#13379,#13381,#3230,.F.);
#17920=EDGE_CURVE('',#13382,#13380,#3231,.F.);
#17921=EDGE_CURVE('',#13383,#13384,#9454,.T.);
#17922=EDGE_CURVE('',#13381,#13383,#3232,.F.);
#17923=EDGE_CURVE('',#13384,#13382,#3233,.F.);
#17924=EDGE_CURVE('',#13385,#13386,#9455,.T.);
#17925=EDGE_CURVE('',#13383,#13385,#3234,.F.);
#17926=EDGE_CURVE('',#13386,#13384,#3235,.F.);
#17927=EDGE_CURVE('',#13387,#13388,#9456,.T.);
#17928=EDGE_CURVE('',#13385,#13387,#3236,.F.);
#17929=EDGE_CURVE('',#13388,#13386,#3237,.F.);
#17930=EDGE_CURVE('',#13389,#13390,#9457,.T.);
#17931=EDGE_CURVE('',#13387,#13389,#3238,.F.);
#17932=EDGE_CURVE('',#13390,#13388,#3239,.F.);
#17933=EDGE_CURVE('',#13391,#13392,#9458,.T.);
#17934=EDGE_CURVE('',#13389,#13391,#3240,.F.);
#17935=EDGE_CURVE('',#13392,#13390,#3241,.F.);
#17936=EDGE_CURVE('',#13393,#13394,#9459,.T.);
#17937=EDGE_CURVE('',#13391,#13393,#3242,.F.);
#17938=EDGE_CURVE('',#13394,#13392,#3243,.F.);
#17939=EDGE_CURVE('',#13395,#13396,#9460,.T.);
#17940=EDGE_CURVE('',#13393,#13395,#3244,.F.);
#17941=EDGE_CURVE('',#13396,#13394,#3245,.F.);
#17942=EDGE_CURVE('',#13397,#13398,#9461,.T.);
#17943=EDGE_CURVE('',#13395,#13397,#3246,.F.);
#17944=EDGE_CURVE('',#13398,#13396,#3247,.F.);
#17945=EDGE_CURVE('',#13399,#13400,#9462,.T.);
#17946=EDGE_CURVE('',#13397,#13399,#3248,.F.);
#17947=EDGE_CURVE('',#13400,#13398,#3249,.F.);
#17948=EDGE_CURVE('',#13401,#13402,#9463,.T.);
#17949=EDGE_CURVE('',#13399,#13401,#3250,.F.);
#17950=EDGE_CURVE('',#13402,#13400,#3251,.F.);
#17951=EDGE_CURVE('',#13403,#13404,#9464,.T.);
#17952=EDGE_CURVE('',#13401,#13403,#3252,.F.);
#17953=EDGE_CURVE('',#13404,#13402,#3253,.F.);
#17954=EDGE_CURVE('',#13405,#13406,#9465,.T.);
#17955=EDGE_CURVE('',#13403,#13405,#3254,.F.);
#17956=EDGE_CURVE('',#13406,#13404,#3255,.F.);
#17957=EDGE_CURVE('',#13407,#13408,#9466,.T.);
#17958=EDGE_CURVE('',#13405,#13407,#3256,.F.);
#17959=EDGE_CURVE('',#13408,#13406,#3257,.F.);
#17960=EDGE_CURVE('',#13409,#13410,#9467,.T.);
#17961=EDGE_CURVE('',#13407,#13409,#3258,.F.);
#17962=EDGE_CURVE('',#13410,#13408,#3259,.F.);
#17963=EDGE_CURVE('',#13411,#13412,#9468,.T.);
#17964=EDGE_CURVE('',#13409,#13411,#3260,.F.);
#17965=EDGE_CURVE('',#13412,#13410,#3261,.F.);
#17966=EDGE_CURVE('',#13413,#13414,#9469,.T.);
#17967=EDGE_CURVE('',#13411,#13413,#3262,.F.);
#17968=EDGE_CURVE('',#13414,#13412,#3263,.F.);
#17969=EDGE_CURVE('',#13415,#13416,#9470,.T.);
#17970=EDGE_CURVE('',#13413,#13415,#3264,.F.);
#17971=EDGE_CURVE('',#13416,#13414,#3265,.F.);
#17972=EDGE_CURVE('',#13417,#13418,#9471,.T.);
#17973=EDGE_CURVE('',#13415,#13417,#3266,.F.);
#17974=EDGE_CURVE('',#13418,#13416,#3267,.F.);
#17975=EDGE_CURVE('',#13419,#13420,#9472,.T.);
#17976=EDGE_CURVE('',#13417,#13419,#3268,.F.);
#17977=EDGE_CURVE('',#13420,#13418,#3269,.F.);
#17978=EDGE_CURVE('',#13421,#13422,#9473,.T.);
#17979=EDGE_CURVE('',#13419,#13421,#3270,.F.);
#17980=EDGE_CURVE('',#13422,#13420,#3271,.F.);
#17981=EDGE_CURVE('',#13423,#13424,#9474,.T.);
#17982=EDGE_CURVE('',#13421,#13423,#3272,.F.);
#17983=EDGE_CURVE('',#13424,#13422,#3273,.F.);
#17984=EDGE_CURVE('',#13425,#13426,#9475,.T.);
#17985=EDGE_CURVE('',#13423,#13425,#3274,.F.);
#17986=EDGE_CURVE('',#13426,#13424,#3275,.F.);
#17987=EDGE_CURVE('',#13427,#13428,#9476,.T.);
#17988=EDGE_CURVE('',#13425,#13427,#3276,.F.);
#17989=EDGE_CURVE('',#13428,#13426,#3277,.F.);
#17990=EDGE_CURVE('',#13429,#13430,#9477,.T.);
#17991=EDGE_CURVE('',#13427,#13429,#3278,.F.);
#17992=EDGE_CURVE('',#13430,#13428,#3279,.F.);
#17993=EDGE_CURVE('',#13431,#13432,#9478,.T.);
#17994=EDGE_CURVE('',#13429,#13431,#3280,.F.);
#17995=EDGE_CURVE('',#13432,#13430,#3281,.F.);
#17996=EDGE_CURVE('',#13433,#13434,#9479,.T.);
#17997=EDGE_CURVE('',#13433,#13435,#3282,.F.);
#17998=EDGE_CURVE('',#13434,#13435,#4117,.T.);
#17999=EDGE_CURVE('',#13436,#13435,#9480,.T.);
#18000=EDGE_CURVE('',#13437,#13436,#3283,.F.);
#18001=EDGE_CURVE('',#13435,#13437,#4118,.T.);
#18002=EDGE_CURVE('',#13438,#13439,#9481,.T.);
#18003=EDGE_CURVE('',#13436,#13438,#3284,.F.);
#18004=EDGE_CURVE('',#13435,#13439,#3285,.T.);
#18005=EDGE_CURVE('',#13440,#13441,#9482,.T.);
#18006=EDGE_CURVE('',#13438,#13440,#3286,.F.);
#18007=EDGE_CURVE('',#13439,#13441,#3287,.T.);
#18008=EDGE_CURVE('',#13442,#13443,#9483,.T.);
#18009=EDGE_CURVE('',#13440,#13442,#3288,.F.);
#18010=EDGE_CURVE('',#13441,#13443,#3289,.T.);
#18011=EDGE_CURVE('',#13444,#13445,#9484,.T.);
#18012=EDGE_CURVE('',#13442,#13444,#3290,.F.);
#18013=EDGE_CURVE('',#13443,#13445,#3291,.T.);
#18014=EDGE_CURVE('',#13446,#13447,#9485,.T.);
#18015=EDGE_CURVE('',#13444,#13446,#3292,.F.);
#18016=EDGE_CURVE('',#13445,#13447,#3293,.T.);
#18017=EDGE_CURVE('',#13448,#13449,#9486,.T.);
#18018=EDGE_CURVE('',#13446,#13448,#3294,.F.);
#18019=EDGE_CURVE('',#13447,#13449,#3295,.T.);
#18020=EDGE_CURVE('',#13450,#13451,#9487,.T.);
#18021=EDGE_CURVE('',#13448,#13450,#3296,.F.);
#18022=EDGE_CURVE('',#13449,#13451,#3297,.T.);
#18023=EDGE_CURVE('',#13452,#13453,#9488,.T.);
#18024=EDGE_CURVE('',#13450,#13452,#3298,.F.);
#18025=EDGE_CURVE('',#13451,#13453,#3299,.T.);
#18026=EDGE_CURVE('',#13454,#13455,#9489,.T.);
#18027=EDGE_CURVE('',#13452,#13454,#3300,.F.);
#18028=EDGE_CURVE('',#13453,#13455,#3301,.T.);
#18029=EDGE_CURVE('',#13456,#13457,#9490,.T.);
#18030=EDGE_CURVE('',#13454,#13456,#3302,.F.);
#18031=EDGE_CURVE('',#13455,#13457,#3303,.T.);
#18032=EDGE_CURVE('',#13458,#13459,#9491,.T.);
#18033=EDGE_CURVE('',#13456,#13458,#3304,.F.);
#18034=EDGE_CURVE('',#13457,#13459,#3305,.T.);
#18035=EDGE_CURVE('',#13460,#13461,#9492,.T.);
#18036=EDGE_CURVE('',#13458,#13460,#3306,.F.);
#18037=EDGE_CURVE('',#13459,#13461,#3307,.T.);
#18038=EDGE_CURVE('',#13462,#13463,#9493,.T.);
#18039=EDGE_CURVE('',#13460,#13462,#3308,.F.);
#18040=EDGE_CURVE('',#13461,#13463,#3309,.T.);
#18041=EDGE_CURVE('',#13464,#13465,#9494,.T.);
#18042=EDGE_CURVE('',#13462,#13464,#3310,.F.);
#18043=EDGE_CURVE('',#13463,#13465,#3311,.T.);
#18044=EDGE_CURVE('',#13466,#13467,#9495,.T.);
#18045=EDGE_CURVE('',#13464,#13466,#3312,.F.);
#18046=EDGE_CURVE('',#13465,#13467,#3313,.T.);
#18047=EDGE_CURVE('',#13468,#13469,#9496,.T.);
#18048=EDGE_CURVE('',#13466,#13468,#3314,.F.);
#18049=EDGE_CURVE('',#13467,#13469,#3315,.T.);
#18050=EDGE_CURVE('',#13470,#13471,#9497,.T.);
#18051=EDGE_CURVE('',#13468,#13470,#3316,.F.);
#18052=EDGE_CURVE('',#13469,#13471,#3317,.T.);
#18053=EDGE_CURVE('',#13472,#13473,#9498,.T.);
#18054=EDGE_CURVE('',#13470,#13472,#3318,.F.);
#18055=EDGE_CURVE('',#13471,#13473,#3319,.T.);
#18056=EDGE_CURVE('',#13474,#13475,#9499,.T.);
#18057=EDGE_CURVE('',#13472,#13474,#3320,.F.);
#18058=EDGE_CURVE('',#13473,#13475,#3321,.T.);
#18059=EDGE_CURVE('',#13476,#13477,#9500,.T.);
#18060=EDGE_CURVE('',#13474,#13476,#3322,.F.);
#18061=EDGE_CURVE('',#13475,#13477,#3323,.T.);
#18062=EDGE_CURVE('',#13478,#13479,#9501,.T.);
#18063=EDGE_CURVE('',#13476,#13478,#3324,.F.);
#18064=EDGE_CURVE('',#13477,#13479,#3325,.T.);
#18065=EDGE_CURVE('',#13480,#13481,#9502,.T.);
#18066=EDGE_CURVE('',#13478,#13480,#3326,.F.);
#18067=EDGE_CURVE('',#13479,#13481,#3327,.T.);
#18068=EDGE_CURVE('',#13482,#13483,#9503,.T.);
#18069=EDGE_CURVE('',#13480,#13482,#3328,.F.);
#18070=EDGE_CURVE('',#13481,#13483,#3329,.T.);
#18071=EDGE_CURVE('',#13484,#13485,#9504,.T.);
#18072=EDGE_CURVE('',#13482,#13484,#3330,.F.);
#18073=EDGE_CURVE('',#13483,#13485,#3331,.T.);
#18074=EDGE_CURVE('',#13486,#13487,#9505,.T.);
#18075=EDGE_CURVE('',#13484,#13486,#3332,.F.);
#18076=EDGE_CURVE('',#13485,#13487,#3333,.T.);
#18077=EDGE_CURVE('',#13488,#13489,#9506,.T.);
#18078=EDGE_CURVE('',#13486,#13488,#3334,.F.);
#18079=EDGE_CURVE('',#13487,#13489,#3335,.T.);
#18080=EDGE_CURVE('',#13490,#13491,#9507,.T.);
#18081=EDGE_CURVE('',#13488,#13490,#3336,.F.);
#18082=EDGE_CURVE('',#13489,#13491,#3337,.T.);
#18083=EDGE_CURVE('',#13492,#13493,#9508,.T.);
#18084=EDGE_CURVE('',#13490,#13492,#3338,.F.);
#18085=EDGE_CURVE('',#13491,#13493,#3339,.T.);
#18086=EDGE_CURVE('',#13494,#13495,#9509,.T.);
#18087=EDGE_CURVE('',#13492,#13494,#3340,.F.);
#18088=EDGE_CURVE('',#13493,#13495,#3341,.T.);
#18089=EDGE_CURVE('',#13495,#13496,#3342,.T.);
#18090=EDGE_CURVE('',#13494,#13496,#4119,.T.);
#18091=EDGE_CURVE('',#13437,#13434,#4120,.T.);
#18092=EDGE_CURVE('',#13437,#13497,#3343,.T.);
#18093=EDGE_CURVE('',#13497,#13498,#4121,.T.);
#18094=EDGE_CURVE('',#13498,#13433,#3344,.F.);
#18095=EDGE_CURVE('',#13498,#13432,#3345,.F.);
#18096=EDGE_CURVE('',#13431,#13497,#3346,.F.);
#18097=EDGE_CURVE('',#13499,#13500,#2478,.T.);
#18098=EDGE_CURVE('',#13500,#13501,#9510,.T.);
#18099=EDGE_CURVE('',#13501,#13502,#2479,.T.);
#18100=EDGE_CURVE('',#13499,#13502,#9511,.T.);
#18101=EDGE_CURVE('',#13503,#13504,#2480,.T.);
#18102=EDGE_CURVE('',#13504,#13505,#9512,.T.);
#18103=EDGE_CURVE('',#13505,#13506,#2481,.T.);
#18104=EDGE_CURVE('',#13503,#13506,#9513,.T.);
#18105=EDGE_CURVE('',#13507,#13508,#2482,.T.);
#18106=EDGE_CURVE('',#13508,#13509,#9514,.T.);
#18107=EDGE_CURVE('',#13509,#13510,#2483,.T.);
#18108=EDGE_CURVE('',#13507,#13510,#9515,.T.);
#18109=EDGE_CURVE('',#13511,#13512,#2484,.T.);
#18110=EDGE_CURVE('',#13512,#13513,#9516,.T.);
#18111=EDGE_CURVE('',#13513,#13514,#2485,.T.);
#18112=EDGE_CURVE('',#13511,#13514,#9517,.T.);
#18113=EDGE_CURVE('',#13515,#13516,#2486,.T.);
#18114=EDGE_CURVE('',#13516,#13517,#9518,.T.);
#18115=EDGE_CURVE('',#13517,#13518,#2487,.T.);
#18116=EDGE_CURVE('',#13515,#13518,#9519,.T.);
#18117=EDGE_CURVE('',#13519,#13520,#2488,.T.);
#18118=EDGE_CURVE('',#13520,#13521,#9520,.T.);
#18119=EDGE_CURVE('',#13521,#13522,#2489,.T.);
#18120=EDGE_CURVE('',#13519,#13522,#9521,.T.);
#18121=EDGE_CURVE('',#13523,#13524,#2490,.T.);
#18122=EDGE_CURVE('',#13524,#13525,#9522,.T.);
#18123=EDGE_CURVE('',#13525,#13526,#2491,.T.);
#18124=EDGE_CURVE('',#13523,#13526,#9523,.T.);
#18125=EDGE_CURVE('',#13527,#13528,#2492,.T.);
#18126=EDGE_CURVE('',#13528,#13529,#9524,.T.);
#18127=EDGE_CURVE('',#13529,#13530,#2493,.T.);
#18128=EDGE_CURVE('',#13527,#13530,#9525,.T.);
#18129=EDGE_CURVE('',#13531,#13532,#2494,.T.);
#18130=EDGE_CURVE('',#13532,#13533,#9526,.T.);
#18131=EDGE_CURVE('',#13533,#13534,#2495,.T.);
#18132=EDGE_CURVE('',#13531,#13534,#9527,.T.);
#18133=EDGE_CURVE('',#13535,#13536,#2496,.T.);
#18134=EDGE_CURVE('',#13536,#13537,#9528,.T.);
#18135=EDGE_CURVE('',#13537,#13538,#2497,.T.);
#18136=EDGE_CURVE('',#13535,#13538,#9529,.T.);
#18137=EDGE_CURVE('',#13539,#13540,#2498,.T.);
#18138=EDGE_CURVE('',#13540,#13541,#9530,.T.);
#18139=EDGE_CURVE('',#13541,#13542,#2499,.T.);
#18140=EDGE_CURVE('',#13539,#13542,#9531,.T.);
#18141=EDGE_CURVE('',#13543,#13544,#2500,.T.);
#18142=EDGE_CURVE('',#13544,#13545,#9532,.T.);
#18143=EDGE_CURVE('',#13545,#13546,#2501,.T.);
#18144=EDGE_CURVE('',#13543,#13546,#9533,.T.);
#18145=EDGE_CURVE('',#13547,#13548,#2502,.T.);
#18146=EDGE_CURVE('',#13548,#13549,#9534,.T.);
#18147=EDGE_CURVE('',#13549,#13550,#2503,.T.);
#18148=EDGE_CURVE('',#13547,#13550,#9535,.T.);
#18149=EDGE_CURVE('',#13551,#13552,#2504,.T.);
#18150=EDGE_CURVE('',#13552,#13553,#9536,.T.);
#18151=EDGE_CURVE('',#13553,#13554,#2505,.T.);
#18152=EDGE_CURVE('',#13551,#13554,#9537,.T.);
#18153=EDGE_CURVE('',#13555,#13556,#2506,.T.);
#18154=EDGE_CURVE('',#13556,#13557,#9538,.T.);
#18155=EDGE_CURVE('',#13557,#13558,#2507,.T.);
#18156=EDGE_CURVE('',#13555,#13558,#9539,.T.);
#18157=EDGE_CURVE('',#13559,#13560,#1195,.T.);
#18158=EDGE_CURVE('',#13561,#13559,#1196,.T.);
#18159=EDGE_CURVE('',#13562,#13561,#1197,.T.);
#18160=EDGE_CURVE('',#13563,#13562,#1198,.T.);
#18161=EDGE_CURVE('',#13564,#13563,#1199,.T.);
#18162=EDGE_CURVE('',#13565,#13564,#1200,.T.);
#18163=EDGE_CURVE('',#13560,#13565,#1201,.T.);
#18164=EDGE_CURVE('',#13560,#13566,#9540,.T.);
#18165=EDGE_CURVE('',#13566,#13566,#4122,.T.);
#18166=EDGE_CURVE('',#13567,#13567,#4123,.T.);
#18167=EDGE_CURVE('',#13567,#13568,#4124,.T.);
#18168=EDGE_CURVE('',#13568,#13568,#4125,.T.);
#18169=EDGE_CURVE('',#13569,#13570,#3347,.T.);
#18170=EDGE_CURVE('',#13571,#13569,#1202,.T.);
#18171=EDGE_CURVE('',#13572,#13571,#4126,.T.);
#18172=EDGE_CURVE('',#13573,#13572,#1203,.T.);
#18173=EDGE_CURVE('',#13574,#13573,#2508,.T.);
#18174=EDGE_CURVE('',#13575,#13574,#1204,.T.);
#18175=EDGE_CURVE('',#13576,#13575,#4127,.T.);
#18176=EDGE_CURVE('',#13577,#13576,#1205,.T.);
#18177=EDGE_CURVE('',#13578,#13577,#2509,.T.);
#18178=EDGE_CURVE('',#13579,#13578,#1206,.T.);
#18179=EDGE_CURVE('',#13580,#13579,#4128,.T.);
#18180=EDGE_CURVE('',#13581,#13580,#1207,.T.);
#18181=EDGE_CURVE('',#13582,#13581,#2510,.T.);
#18182=EDGE_CURVE('',#13583,#13582,#1208,.T.);
#18183=EDGE_CURVE('',#13584,#13583,#4129,.T.);
#18184=EDGE_CURVE('',#13585,#13584,#1209,.T.);
#18185=EDGE_CURVE('',#13586,#13585,#2511,.T.);
#18186=EDGE_CURVE('',#13587,#13586,#1210,.T.);
#18187=EDGE_CURVE('',#13588,#13587,#4130,.T.);
#18188=EDGE_CURVE('',#13589,#13588,#1211,.T.);
#18189=EDGE_CURVE('',#13590,#13589,#2512,.T.);
#18190=EDGE_CURVE('',#13591,#13590,#1212,.T.);
#18191=EDGE_CURVE('',#13592,#13591,#4131,.T.);
#18192=EDGE_CURVE('',#13593,#13592,#1213,.T.);
#18193=EDGE_CURVE('',#13594,#13593,#2513,.T.);
#18194=EDGE_CURVE('',#13595,#13594,#1214,.T.);
#18195=EDGE_CURVE('',#13596,#13595,#4132,.T.);
#18196=EDGE_CURVE('',#13597,#13596,#1215,.T.);
#18197=EDGE_CURVE('',#13598,#13597,#2514,.T.);
#18198=EDGE_CURVE('',#13599,#13598,#1216,.T.);
#18199=EDGE_CURVE('',#13600,#13599,#4133,.T.);
#18200=EDGE_CURVE('',#13601,#13600,#1217,.T.);
#18201=EDGE_CURVE('',#13602,#13601,#2515,.T.);
#18202=EDGE_CURVE('',#13603,#13602,#1218,.T.);
#18203=EDGE_CURVE('',#13604,#13603,#4134,.T.);
#18204=EDGE_CURVE('',#13605,#13604,#1219,.T.);
#18205=EDGE_CURVE('',#13606,#13605,#2516,.T.);
#18206=EDGE_CURVE('',#13607,#13606,#1220,.T.);
#18207=EDGE_CURVE('',#13608,#13607,#4135,.T.);
#18208=EDGE_CURVE('',#13609,#13608,#1221,.T.);
#18209=EDGE_CURVE('',#13610,#13609,#2517,.T.);
#18210=EDGE_CURVE('',#13611,#13610,#1222,.T.);
#18211=EDGE_CURVE('',#13612,#13611,#4136,.T.);
#18212=EDGE_CURVE('',#13613,#13612,#1223,.T.);
#18213=EDGE_CURVE('',#13614,#13613,#2518,.T.);
#18214=EDGE_CURVE('',#13615,#13614,#1224,.T.);
#18215=EDGE_CURVE('',#13616,#13615,#4137,.T.);
#18216=EDGE_CURVE('',#13617,#13616,#1225,.T.);
#18217=EDGE_CURVE('',#13618,#13617,#2519,.T.);
#18218=EDGE_CURVE('',#13619,#13618,#1226,.T.);
#18219=EDGE_CURVE('',#13620,#13619,#4138,.T.);
#18220=EDGE_CURVE('',#13621,#13620,#1227,.T.);
#18221=EDGE_CURVE('',#13622,#13621,#2520,.T.);
#18222=EDGE_CURVE('',#13623,#13622,#1228,.T.);
#18223=EDGE_CURVE('',#13624,#13623,#4139,.T.);
#18224=EDGE_CURVE('',#13625,#13624,#1229,.T.);
#18225=EDGE_CURVE('',#13626,#13625,#2521,.T.);
#18226=EDGE_CURVE('',#13627,#13626,#1230,.T.);
#18227=EDGE_CURVE('',#13628,#13627,#4140,.T.);
#18228=EDGE_CURVE('',#13629,#13628,#1231,.T.);
#18229=EDGE_CURVE('',#13630,#13629,#2522,.T.);
#18230=EDGE_CURVE('',#13631,#13630,#1232,.T.);
#18231=EDGE_CURVE('',#13632,#13631,#4141,.T.);
#18232=EDGE_CURVE('',#13633,#13632,#1233,.T.);
#18233=EDGE_CURVE('',#13634,#13633,#2523,.T.);
#18234=EDGE_CURVE('',#13635,#13634,#1234,.T.);
#18235=EDGE_CURVE('',#13636,#13635,#4142,.T.);
#18236=EDGE_CURVE('',#13637,#13636,#1235,.T.);
#18237=EDGE_CURVE('',#13638,#13637,#2524,.T.);
#18238=EDGE_CURVE('',#13639,#13638,#1236,.T.);
#18239=EDGE_CURVE('',#13640,#13639,#4143,.T.);
#18240=EDGE_CURVE('',#13641,#13640,#1237,.T.);
#18241=EDGE_CURVE('',#13642,#13641,#2525,.T.);
#18242=EDGE_CURVE('',#13643,#13642,#1238,.T.);
#18243=EDGE_CURVE('',#13644,#13643,#4144,.T.);
#18244=EDGE_CURVE('',#13645,#13644,#1239,.T.);
#18245=EDGE_CURVE('',#13646,#13645,#2526,.T.);
#18246=EDGE_CURVE('',#13647,#13646,#1240,.T.);
#18247=EDGE_CURVE('',#13648,#13647,#4145,.T.);
#18248=EDGE_CURVE('',#13649,#13648,#1241,.T.);
#18249=EDGE_CURVE('',#13650,#13649,#2527,.T.);
#18250=EDGE_CURVE('',#13651,#13650,#1242,.T.);
#18251=EDGE_CURVE('',#13652,#13651,#4146,.T.);
#18252=EDGE_CURVE('',#13653,#13652,#1243,.T.);
#18253=EDGE_CURVE('',#13654,#13653,#2528,.T.);
#18254=EDGE_CURVE('',#13655,#13654,#1244,.T.);
#18255=EDGE_CURVE('',#13656,#13655,#4147,.T.);
#18256=EDGE_CURVE('',#13657,#13656,#1245,.T.);
#18257=EDGE_CURVE('',#13658,#13657,#2529,.T.);
#18258=EDGE_CURVE('',#13659,#13658,#1246,.T.);
#18259=EDGE_CURVE('',#13660,#13659,#4148,.T.);
#18260=EDGE_CURVE('',#13661,#13660,#1247,.T.);
#18261=EDGE_CURVE('',#13662,#13661,#2530,.T.);
#18262=EDGE_CURVE('',#13663,#13662,#1248,.T.);
#18263=EDGE_CURVE('',#13664,#13663,#4149,.T.);
#18264=EDGE_CURVE('',#13665,#13664,#1249,.T.);
#18265=EDGE_CURVE('',#13666,#13665,#2531,.T.);
#18266=EDGE_CURVE('',#13667,#13666,#1250,.T.);
#18267=EDGE_CURVE('',#13668,#13667,#4150,.T.);
#18268=EDGE_CURVE('',#13669,#13668,#1251,.T.);
#18269=EDGE_CURVE('',#13670,#13669,#2532,.T.);
#18270=EDGE_CURVE('',#13671,#13670,#1252,.T.);
#18271=EDGE_CURVE('',#13672,#13671,#4151,.T.);
#18272=EDGE_CURVE('',#13673,#13672,#1253,.T.);
#18273=EDGE_CURVE('',#13674,#13673,#2533,.T.);
#18274=EDGE_CURVE('',#13675,#13674,#1254,.T.);
#18275=EDGE_CURVE('',#13676,#13675,#4152,.T.);
#18276=EDGE_CURVE('',#13677,#13676,#1255,.T.);
#18277=EDGE_CURVE('',#13678,#13677,#2534,.T.);
#18278=EDGE_CURVE('',#13679,#13678,#1256,.T.);
#18279=EDGE_CURVE('',#13680,#13679,#4153,.T.);
#18280=EDGE_CURVE('',#13681,#13680,#1257,.T.);
#18281=EDGE_CURVE('',#13682,#13681,#2535,.T.);
#18282=EDGE_CURVE('',#13683,#13682,#1258,.T.);
#18283=EDGE_CURVE('',#13684,#13683,#4154,.T.);
#18284=EDGE_CURVE('',#13685,#13684,#1259,.T.);
#18285=EDGE_CURVE('',#13686,#13685,#2536,.T.);
#18286=EDGE_CURVE('',#13687,#13686,#1260,.T.);
#18287=EDGE_CURVE('',#13688,#13687,#4155,.T.);
#18288=EDGE_CURVE('',#13689,#13688,#1261,.T.);
#18289=EDGE_CURVE('',#13690,#13689,#2537,.T.);
#18290=EDGE_CURVE('',#13691,#13690,#1262,.T.);
#18291=EDGE_CURVE('',#13692,#13691,#4156,.T.);
#18292=EDGE_CURVE('',#13693,#13692,#1263,.T.);
#18293=EDGE_CURVE('',#13694,#13693,#2538,.T.);
#18294=EDGE_CURVE('',#13695,#13694,#1264,.T.);
#18295=EDGE_CURVE('',#13696,#13695,#4157,.T.);
#18296=EDGE_CURVE('',#13697,#13696,#1265,.T.);
#18297=EDGE_CURVE('',#13698,#13697,#2539,.T.);
#18298=EDGE_CURVE('',#13699,#13698,#1266,.T.);
#18299=EDGE_CURVE('',#13700,#13699,#4158,.T.);
#18300=EDGE_CURVE('',#13701,#13700,#1267,.T.);
#18301=EDGE_CURVE('',#13702,#13701,#2540,.T.);
#18302=EDGE_CURVE('',#13703,#13702,#1268,.T.);
#18303=EDGE_CURVE('',#13704,#13703,#4159,.T.);
#18304=EDGE_CURVE('',#13705,#13704,#1269,.T.);
#18305=EDGE_CURVE('',#13706,#13705,#2541,.T.);
#18306=EDGE_CURVE('',#13707,#13706,#1270,.T.);
#18307=EDGE_CURVE('',#13708,#13707,#4160,.T.);
#18308=EDGE_CURVE('',#13709,#13708,#1271,.T.);
#18309=EDGE_CURVE('',#13710,#13709,#2542,.T.);
#18310=EDGE_CURVE('',#13711,#13710,#1272,.T.);
#18311=EDGE_CURVE('',#13712,#13711,#4161,.T.);
#18312=EDGE_CURVE('',#13713,#13712,#1273,.T.);
#18313=EDGE_CURVE('',#13714,#13713,#2543,.T.);
#18314=EDGE_CURVE('',#13715,#13714,#1274,.T.);
#18315=EDGE_CURVE('',#13716,#13715,#4162,.T.);
#18316=EDGE_CURVE('',#13717,#13716,#1275,.T.);
#18317=EDGE_CURVE('',#13718,#13717,#2544,.T.);
#18318=EDGE_CURVE('',#13719,#13718,#1276,.T.);
#18319=EDGE_CURVE('',#13720,#13719,#4163,.T.);
#18320=EDGE_CURVE('',#13721,#13720,#1277,.T.);
#18321=EDGE_CURVE('',#13722,#13721,#2545,.T.);
#18322=EDGE_CURVE('',#13723,#13722,#1278,.T.);
#18323=EDGE_CURVE('',#13724,#13723,#4164,.T.);
#18324=EDGE_CURVE('',#13725,#13724,#1279,.T.);
#18325=EDGE_CURVE('',#13726,#13725,#2546,.T.);
#18326=EDGE_CURVE('',#13727,#13726,#1280,.T.);
#18327=EDGE_CURVE('',#13728,#13727,#4165,.T.);
#18328=EDGE_CURVE('',#13729,#13728,#1281,.T.);
#18329=EDGE_CURVE('',#13730,#13729,#2547,.T.);
#18330=EDGE_CURVE('',#13731,#13730,#1282,.T.);
#18331=EDGE_CURVE('',#13732,#13731,#4166,.T.);
#18332=EDGE_CURVE('',#13733,#13732,#1283,.T.);
#18333=EDGE_CURVE('',#13734,#13733,#2548,.T.);
#18334=EDGE_CURVE('',#13735,#13734,#1284,.T.);
#18335=EDGE_CURVE('',#13736,#13735,#4167,.T.);
#18336=EDGE_CURVE('',#13737,#13736,#1285,.T.);
#18337=EDGE_CURVE('',#13738,#13737,#2549,.T.);
#18338=EDGE_CURVE('',#13739,#13738,#1286,.T.);
#18339=EDGE_CURVE('',#13740,#13739,#4168,.T.);
#18340=EDGE_CURVE('',#13741,#13740,#1287,.T.);
#18341=EDGE_CURVE('',#13742,#13741,#2550,.T.);
#18342=EDGE_CURVE('',#13743,#13742,#1288,.T.);
#18343=EDGE_CURVE('',#13744,#13743,#4169,.T.);
#18344=EDGE_CURVE('',#13745,#13744,#1289,.T.);
#18345=EDGE_CURVE('',#13746,#13745,#2551,.T.);
#18346=EDGE_CURVE('',#13747,#13746,#1290,.T.);
#18347=EDGE_CURVE('',#13748,#13747,#4170,.T.);
#18348=EDGE_CURVE('',#13749,#13748,#1291,.T.);
#18349=EDGE_CURVE('',#13750,#13749,#2552,.T.);
#18350=EDGE_CURVE('',#13751,#13750,#1292,.T.);
#18351=EDGE_CURVE('',#13752,#13751,#4171,.T.);
#18352=EDGE_CURVE('',#13558,#13752,#1293,.T.);
#18353=EDGE_CURVE('',#13753,#13557,#1294,.T.);
#18354=EDGE_CURVE('',#13754,#13753,#4172,.T.);
#18355=EDGE_CURVE('',#13554,#13754,#1295,.T.);
#18356=EDGE_CURVE('',#13755,#13553,#1296,.T.);
#18357=EDGE_CURVE('',#13756,#13755,#4173,.T.);
#18358=EDGE_CURVE('',#13550,#13756,#1297,.T.);
#18359=EDGE_CURVE('',#13757,#13549,#1298,.T.);
#18360=EDGE_CURVE('',#13758,#13757,#4174,.T.);
#18361=EDGE_CURVE('',#13546,#13758,#1299,.T.);
#18362=EDGE_CURVE('',#13759,#13545,#1300,.T.);
#18363=EDGE_CURVE('',#13760,#13759,#4175,.T.);
#18364=EDGE_CURVE('',#13542,#13760,#1301,.T.);
#18365=EDGE_CURVE('',#13761,#13541,#1302,.T.);
#18366=EDGE_CURVE('',#13762,#13761,#4176,.T.);
#18367=EDGE_CURVE('',#13538,#13762,#1303,.T.);
#18368=EDGE_CURVE('',#13763,#13537,#1304,.T.);
#18369=EDGE_CURVE('',#13764,#13763,#4177,.T.);
#18370=EDGE_CURVE('',#13534,#13764,#1305,.T.);
#18371=EDGE_CURVE('',#13765,#13533,#1306,.T.);
#18372=EDGE_CURVE('',#13766,#13765,#4178,.T.);
#18373=EDGE_CURVE('',#13530,#13766,#1307,.T.);
#18374=EDGE_CURVE('',#13767,#13529,#1308,.T.);
#18375=EDGE_CURVE('',#13768,#13767,#4179,.T.);
#18376=EDGE_CURVE('',#13526,#13768,#1309,.T.);
#18377=EDGE_CURVE('',#13769,#13525,#1310,.T.);
#18378=EDGE_CURVE('',#13770,#13769,#4180,.T.);
#18379=EDGE_CURVE('',#13502,#13770,#1311,.T.);
#18380=EDGE_CURVE('',#13771,#13501,#1312,.T.);
#18381=EDGE_CURVE('',#13772,#13771,#4181,.T.);
#18382=EDGE_CURVE('',#13506,#13772,#1313,.T.);
#18383=EDGE_CURVE('',#13773,#13505,#1314,.T.);
#18384=EDGE_CURVE('',#13774,#13773,#4182,.T.);
#18385=EDGE_CURVE('',#13510,#13774,#1315,.T.);
#18386=EDGE_CURVE('',#13775,#13509,#1316,.T.);
#18387=EDGE_CURVE('',#13776,#13775,#4183,.T.);
#18388=EDGE_CURVE('',#13514,#13776,#1317,.T.);
#18389=EDGE_CURVE('',#13777,#13513,#1318,.T.);
#18390=EDGE_CURVE('',#13778,#13777,#4184,.T.);
#18391=EDGE_CURVE('',#13518,#13778,#1319,.T.);
#18392=EDGE_CURVE('',#13779,#13517,#1320,.T.);
#18393=EDGE_CURVE('',#13780,#13779,#4185,.T.);
#18394=EDGE_CURVE('',#13522,#13780,#1321,.T.);
#18395=EDGE_CURVE('',#13781,#13521,#1322,.T.);
#18396=EDGE_CURVE('',#13782,#13781,#4186,.T.);
#18397=EDGE_CURVE('',#13783,#13782,#1323,.T.);
#18398=EDGE_CURVE('',#13784,#13783,#2553,.T.);
#18399=EDGE_CURVE('',#13785,#13784,#1324,.T.);
#18400=EDGE_CURVE('',#13786,#13785,#4187,.T.);
#18401=EDGE_CURVE('',#13787,#13786,#1325,.T.);
#18402=EDGE_CURVE('',#13788,#13787,#2554,.T.);
#18403=EDGE_CURVE('',#13789,#13788,#1326,.T.);
#18404=EDGE_CURVE('',#13790,#13789,#4188,.T.);
#18405=EDGE_CURVE('',#13791,#13790,#1327,.T.);
#18406=EDGE_CURVE('',#13792,#13791,#2555,.T.);
#18407=EDGE_CURVE('',#13793,#13792,#1328,.T.);
#18408=EDGE_CURVE('',#13794,#13793,#4189,.T.);
#18409=EDGE_CURVE('',#13795,#13794,#1329,.T.);
#18410=EDGE_CURVE('',#13796,#13795,#2556,.T.);
#18411=EDGE_CURVE('',#13797,#13796,#1330,.T.);
#18412=EDGE_CURVE('',#13798,#13797,#4190,.T.);
#18413=EDGE_CURVE('',#13799,#13798,#1331,.T.);
#18414=EDGE_CURVE('',#13800,#13799,#2557,.T.);
#18415=EDGE_CURVE('',#13801,#13800,#1332,.T.);
#18416=EDGE_CURVE('',#13802,#13801,#4191,.T.);
#18417=EDGE_CURVE('',#13803,#13802,#1333,.T.);
#18418=EDGE_CURVE('',#13804,#13803,#2558,.T.);
#18419=EDGE_CURVE('',#13805,#13804,#1334,.T.);
#18420=EDGE_CURVE('',#13806,#13805,#4192,.T.);
#18421=EDGE_CURVE('',#13807,#13806,#1335,.T.);
#18422=EDGE_CURVE('',#13808,#13807,#2559,.T.);
#18423=EDGE_CURVE('',#13809,#13808,#1336,.T.);
#18424=EDGE_CURVE('',#13810,#13809,#4193,.T.);
#18425=EDGE_CURVE('',#13811,#13810,#1337,.T.);
#18426=EDGE_CURVE('',#13812,#13811,#2560,.T.);
#18427=EDGE_CURVE('',#13813,#13812,#1338,.T.);
#18428=EDGE_CURVE('',#13814,#13813,#4194,.T.);
#18429=EDGE_CURVE('',#13815,#13814,#1339,.T.);
#18430=EDGE_CURVE('',#13816,#13815,#2561,.T.);
#18431=EDGE_CURVE('',#13817,#13816,#1340,.T.);
#18432=EDGE_CURVE('',#13818,#13817,#4195,.T.);
#18433=EDGE_CURVE('',#13819,#13818,#1341,.T.);
#18434=EDGE_CURVE('',#13820,#13819,#2562,.T.);
#18435=EDGE_CURVE('',#13821,#13820,#1342,.T.);
#18436=EDGE_CURVE('',#13822,#13821,#4196,.T.);
#18437=EDGE_CURVE('',#13823,#13822,#1343,.T.);
#18438=EDGE_CURVE('',#13824,#13823,#2563,.T.);
#18439=EDGE_CURVE('',#13825,#13824,#1344,.T.);
#18440=EDGE_CURVE('',#13826,#13825,#4197,.T.);
#18441=EDGE_CURVE('',#13827,#13826,#1345,.T.);
#18442=EDGE_CURVE('',#13828,#13827,#2564,.T.);
#18443=EDGE_CURVE('',#13829,#13828,#1346,.T.);
#18444=EDGE_CURVE('',#13830,#13829,#4198,.T.);
#18445=EDGE_CURVE('',#13831,#13830,#1347,.T.);
#18446=EDGE_CURVE('',#13832,#13831,#2565,.T.);
#18447=EDGE_CURVE('',#13833,#13832,#1348,.T.);
#18448=EDGE_CURVE('',#13834,#13833,#4199,.T.);
#18449=EDGE_CURVE('',#13835,#13834,#1349,.T.);
#18450=EDGE_CURVE('',#13836,#13835,#2566,.T.);
#18451=EDGE_CURVE('',#13837,#13836,#1350,.T.);
#18452=EDGE_CURVE('',#13838,#13837,#4200,.T.);
#18453=EDGE_CURVE('',#13839,#13838,#1351,.T.);
#18454=EDGE_CURVE('',#13840,#13839,#2567,.T.);
#18455=EDGE_CURVE('',#13841,#13840,#1352,.T.);
#18456=EDGE_CURVE('',#13842,#13841,#4201,.T.);
#18457=EDGE_CURVE('',#13843,#13842,#1353,.T.);
#18458=EDGE_CURVE('',#13844,#13843,#2568,.T.);
#18459=EDGE_CURVE('',#13845,#13844,#1354,.T.);
#18460=EDGE_CURVE('',#13846,#13845,#4202,.T.);
#18461=EDGE_CURVE('',#13847,#13846,#1355,.T.);
#18462=EDGE_CURVE('',#13848,#13847,#2569,.T.);
#18463=EDGE_CURVE('',#13849,#13848,#1356,.T.);
#18464=EDGE_CURVE('',#13850,#13849,#4203,.T.);
#18465=EDGE_CURVE('',#13851,#13850,#1357,.T.);
#18466=EDGE_CURVE('',#13852,#13851,#2570,.T.);
#18467=EDGE_CURVE('',#13853,#13852,#1358,.T.);
#18468=EDGE_CURVE('',#13854,#13853,#4204,.T.);
#18469=EDGE_CURVE('',#13855,#13854,#1359,.T.);
#18470=EDGE_CURVE('',#13856,#13855,#2571,.T.);
#18471=EDGE_CURVE('',#13857,#13856,#1360,.T.);
#18472=EDGE_CURVE('',#13858,#13857,#4205,.T.);
#18473=EDGE_CURVE('',#13859,#13858,#1361,.T.);
#18474=EDGE_CURVE('',#13570,#13859,#3348,.T.);
#18475=EDGE_CURVE('',#13570,#13567,#9541,.T.);
#18476=EDGE_CURVE('',#13860,#13861,#3349,.T.);
#18477=EDGE_CURVE('',#13862,#13860,#1362,.T.);
#18478=EDGE_CURVE('',#13862,#13863,#4206,.T.);
#18479=EDGE_CURVE('',#13864,#13863,#1363,.T.);
#18480=EDGE_CURVE('',#13865,#13864,#2572,.T.);
#18481=EDGE_CURVE('',#13866,#13865,#1364,.T.);
#18482=EDGE_CURVE('',#13866,#13867,#4207,.T.);
#18483=EDGE_CURVE('',#13868,#13867,#1365,.T.);
#18484=EDGE_CURVE('',#13869,#13868,#2573,.T.);
#18485=EDGE_CURVE('',#13870,#13869,#1366,.T.);
#18486=EDGE_CURVE('',#13870,#13871,#4208,.T.);
#18487=EDGE_CURVE('',#13872,#13871,#1367,.T.);
#18488=EDGE_CURVE('',#13873,#13872,#2574,.T.);
#18489=EDGE_CURVE('',#13874,#13873,#1368,.T.);
#18490=EDGE_CURVE('',#13874,#13875,#4209,.T.);
#18491=EDGE_CURVE('',#13876,#13875,#1369,.T.);
#18492=EDGE_CURVE('',#13877,#13876,#2575,.T.);
#18493=EDGE_CURVE('',#13878,#13877,#1370,.T.);
#18494=EDGE_CURVE('',#13878,#13879,#4210,.T.);
#18495=EDGE_CURVE('',#13880,#13879,#1371,.T.);
#18496=EDGE_CURVE('',#13881,#13880,#2576,.T.);
#18497=EDGE_CURVE('',#13882,#13881,#1372,.T.);
#18498=EDGE_CURVE('',#13882,#13883,#4211,.T.);
#18499=EDGE_CURVE('',#13884,#13883,#1373,.T.);
#18500=EDGE_CURVE('',#13885,#13884,#2577,.T.);
#18501=EDGE_CURVE('',#13886,#13885,#1374,.T.);
#18502=EDGE_CURVE('',#13886,#13887,#4212,.T.);
#18503=EDGE_CURVE('',#13888,#13887,#1375,.T.);
#18504=EDGE_CURVE('',#13889,#13888,#2578,.T.);
#18505=EDGE_CURVE('',#13890,#13889,#1376,.T.);
#18506=EDGE_CURVE('',#13890,#13891,#4213,.T.);
#18507=EDGE_CURVE('',#13892,#13891,#1377,.T.);
#18508=EDGE_CURVE('',#13893,#13892,#2579,.T.);
#18509=EDGE_CURVE('',#13894,#13893,#1378,.T.);
#18510=EDGE_CURVE('',#13894,#13895,#4214,.T.);
#18511=EDGE_CURVE('',#13896,#13895,#1379,.T.);
#18512=EDGE_CURVE('',#13897,#13896,#2580,.T.);
#18513=EDGE_CURVE('',#13898,#13897,#1380,.T.);
#18514=EDGE_CURVE('',#13898,#13899,#4215,.T.);
#18515=EDGE_CURVE('',#13900,#13899,#1381,.T.);
#18516=EDGE_CURVE('',#13901,#13900,#2581,.T.);
#18517=EDGE_CURVE('',#13902,#13901,#1382,.T.);
#18518=EDGE_CURVE('',#13902,#13903,#4216,.T.);
#18519=EDGE_CURVE('',#13904,#13903,#1383,.T.);
#18520=EDGE_CURVE('',#13905,#13904,#2582,.T.);
#18521=EDGE_CURVE('',#13906,#13905,#1384,.T.);
#18522=EDGE_CURVE('',#13906,#13907,#4217,.T.);
#18523=EDGE_CURVE('',#13908,#13907,#1385,.T.);
#18524=EDGE_CURVE('',#13909,#13908,#2583,.T.);
#18525=EDGE_CURVE('',#13910,#13909,#1386,.T.);
#18526=EDGE_CURVE('',#13910,#13911,#4218,.T.);
#18527=EDGE_CURVE('',#13912,#13911,#1387,.T.);
#18528=EDGE_CURVE('',#13913,#13912,#2584,.T.);
#18529=EDGE_CURVE('',#13914,#13913,#1388,.T.);
#18530=EDGE_CURVE('',#13914,#13915,#4219,.T.);
#18531=EDGE_CURVE('',#13916,#13915,#1389,.T.);
#18532=EDGE_CURVE('',#13917,#13916,#2585,.T.);
#18533=EDGE_CURVE('',#13918,#13917,#1390,.T.);
#18534=EDGE_CURVE('',#13918,#13919,#4220,.T.);
#18535=EDGE_CURVE('',#13920,#13919,#1391,.T.);
#18536=EDGE_CURVE('',#13921,#13920,#2586,.T.);
#18537=EDGE_CURVE('',#13922,#13921,#1392,.T.);
#18538=EDGE_CURVE('',#13922,#13923,#4221,.T.);
#18539=EDGE_CURVE('',#13924,#13923,#1393,.T.);
#18540=EDGE_CURVE('',#13925,#13924,#2587,.T.);
#18541=EDGE_CURVE('',#13926,#13925,#1394,.T.);
#18542=EDGE_CURVE('',#13926,#13927,#4222,.T.);
#18543=EDGE_CURVE('',#13928,#13927,#1395,.T.);
#18544=EDGE_CURVE('',#13929,#13928,#2588,.T.);
#18545=EDGE_CURVE('',#13930,#13929,#1396,.T.);
#18546=EDGE_CURVE('',#13930,#13931,#4223,.T.);
#18547=EDGE_CURVE('',#13932,#13931,#1397,.T.);
#18548=EDGE_CURVE('',#13933,#13932,#2589,.T.);
#18549=EDGE_CURVE('',#13934,#13933,#1398,.T.);
#18550=EDGE_CURVE('',#13934,#13935,#4224,.T.);
#18551=EDGE_CURVE('',#13936,#13935,#1399,.T.);
#18552=EDGE_CURVE('',#13937,#13936,#2590,.T.);
#18553=EDGE_CURVE('',#13938,#13937,#1400,.T.);
#18554=EDGE_CURVE('',#13938,#13939,#4225,.T.);
#18555=EDGE_CURVE('',#13940,#13939,#1401,.T.);
#18556=EDGE_CURVE('',#13941,#13940,#2591,.T.);
#18557=EDGE_CURVE('',#13942,#13941,#1402,.T.);
#18558=EDGE_CURVE('',#13942,#13943,#4226,.T.);
#18559=EDGE_CURVE('',#13944,#13943,#1403,.T.);
#18560=EDGE_CURVE('',#13945,#13944,#2592,.T.);
#18561=EDGE_CURVE('',#13946,#13945,#1404,.T.);
#18562=EDGE_CURVE('',#13946,#13947,#4227,.T.);
#18563=EDGE_CURVE('',#13948,#13947,#1405,.T.);
#18564=EDGE_CURVE('',#13949,#13948,#2593,.T.);
#18565=EDGE_CURVE('',#13950,#13949,#1406,.T.);
#18566=EDGE_CURVE('',#13950,#13951,#4228,.T.);
#18567=EDGE_CURVE('',#13952,#13951,#1407,.T.);
#18568=EDGE_CURVE('',#13953,#13952,#2594,.T.);
#18569=EDGE_CURVE('',#13954,#13953,#1408,.T.);
#18570=EDGE_CURVE('',#13954,#13955,#4229,.T.);
#18571=EDGE_CURVE('',#13956,#13955,#1409,.T.);
#18572=EDGE_CURVE('',#13957,#13956,#2595,.T.);
#18573=EDGE_CURVE('',#13958,#13957,#1410,.T.);
#18574=EDGE_CURVE('',#13958,#13959,#4230,.T.);
#18575=EDGE_CURVE('',#13960,#13959,#1411,.T.);
#18576=EDGE_CURVE('',#13961,#13960,#2596,.T.);
#18577=EDGE_CURVE('',#13962,#13961,#1412,.T.);
#18578=EDGE_CURVE('',#13962,#13963,#4231,.T.);
#18579=EDGE_CURVE('',#13964,#13963,#1413,.T.);
#18580=EDGE_CURVE('',#13965,#13964,#2597,.T.);
#18581=EDGE_CURVE('',#13966,#13965,#1414,.T.);
#18582=EDGE_CURVE('',#13966,#13967,#4232,.T.);
#18583=EDGE_CURVE('',#13968,#13967,#1415,.T.);
#18584=EDGE_CURVE('',#13969,#13968,#2598,.T.);
#18585=EDGE_CURVE('',#13970,#13969,#1416,.T.);
#18586=EDGE_CURVE('',#13970,#13971,#4233,.T.);
#18587=EDGE_CURVE('',#13972,#13971,#1417,.T.);
#18588=EDGE_CURVE('',#13973,#13972,#2599,.T.);
#18589=EDGE_CURVE('',#13974,#13973,#1418,.T.);
#18590=EDGE_CURVE('',#13974,#13975,#4234,.T.);
#18591=EDGE_CURVE('',#13976,#13975,#1419,.T.);
#18592=EDGE_CURVE('',#13977,#13976,#2600,.T.);
#18593=EDGE_CURVE('',#13978,#13977,#1420,.T.);
#18594=EDGE_CURVE('',#13978,#13979,#4235,.T.);
#18595=EDGE_CURVE('',#13980,#13979,#1421,.T.);
#18596=EDGE_CURVE('',#13981,#13980,#2601,.T.);
#18597=EDGE_CURVE('',#13982,#13981,#1422,.T.);
#18598=EDGE_CURVE('',#13982,#13983,#4236,.T.);
#18599=EDGE_CURVE('',#13984,#13983,#1423,.T.);
#18600=EDGE_CURVE('',#13985,#13984,#2602,.T.);
#18601=EDGE_CURVE('',#13986,#13985,#1424,.T.);
#18602=EDGE_CURVE('',#13986,#13987,#4237,.T.);
#18603=EDGE_CURVE('',#13988,#13987,#1425,.T.);
#18604=EDGE_CURVE('',#13989,#13988,#2603,.T.);
#18605=EDGE_CURVE('',#13990,#13989,#1426,.T.);
#18606=EDGE_CURVE('',#13990,#13991,#4238,.T.);
#18607=EDGE_CURVE('',#13992,#13991,#1427,.T.);
#18608=EDGE_CURVE('',#13993,#13992,#2604,.T.);
#18609=EDGE_CURVE('',#13994,#13993,#1428,.T.);
#18610=EDGE_CURVE('',#13994,#13995,#4239,.T.);
#18611=EDGE_CURVE('',#13996,#13995,#1429,.T.);
#18612=EDGE_CURVE('',#13997,#13996,#2605,.T.);
#18613=EDGE_CURVE('',#13998,#13997,#1430,.T.);
#18614=EDGE_CURVE('',#13998,#13999,#4240,.T.);
#18615=EDGE_CURVE('',#14000,#13999,#1431,.T.);
#18616=EDGE_CURVE('',#14001,#14000,#2606,.T.);
#18617=EDGE_CURVE('',#14002,#14001,#1432,.T.);
#18618=EDGE_CURVE('',#14002,#14003,#4241,.T.);
#18619=EDGE_CURVE('',#14004,#14003,#1433,.T.);
#18620=EDGE_CURVE('',#14005,#14004,#2607,.T.);
#18621=EDGE_CURVE('',#14006,#14005,#1434,.T.);
#18622=EDGE_CURVE('',#14006,#14007,#4242,.T.);
#18623=EDGE_CURVE('',#14008,#14007,#1435,.T.);
#18624=EDGE_CURVE('',#14009,#14008,#2608,.T.);
#18625=EDGE_CURVE('',#14010,#14009,#1436,.T.);
#18626=EDGE_CURVE('',#14010,#14011,#4243,.T.);
#18627=EDGE_CURVE('',#14012,#14011,#1437,.T.);
#18628=EDGE_CURVE('',#14013,#14012,#2609,.T.);
#18629=EDGE_CURVE('',#14014,#14013,#1438,.T.);
#18630=EDGE_CURVE('',#14014,#14015,#4244,.T.);
#18631=EDGE_CURVE('',#14016,#14015,#1439,.T.);
#18632=EDGE_CURVE('',#14017,#14016,#2610,.T.);
#18633=EDGE_CURVE('',#14018,#14017,#1440,.T.);
#18634=EDGE_CURVE('',#14018,#14019,#4245,.T.);
#18635=EDGE_CURVE('',#14020,#14019,#1441,.T.);
#18636=EDGE_CURVE('',#14021,#14020,#2611,.T.);
#18637=EDGE_CURVE('',#14022,#14021,#1442,.T.);
#18638=EDGE_CURVE('',#14022,#14023,#4246,.T.);
#18639=EDGE_CURVE('',#14024,#14023,#1443,.T.);
#18640=EDGE_CURVE('',#14025,#14024,#2612,.T.);
#18641=EDGE_CURVE('',#14026,#14025,#1444,.T.);
#18642=EDGE_CURVE('',#14026,#14027,#4247,.T.);
#18643=EDGE_CURVE('',#14028,#14027,#1445,.T.);
#18644=EDGE_CURVE('',#14029,#14028,#2613,.T.);
#18645=EDGE_CURVE('',#14030,#14029,#1446,.T.);
#18646=EDGE_CURVE('',#14030,#14031,#4248,.T.);
#18647=EDGE_CURVE('',#14032,#14031,#1447,.T.);
#18648=EDGE_CURVE('',#14033,#14032,#2614,.T.);
#18649=EDGE_CURVE('',#14034,#14033,#1448,.T.);
#18650=EDGE_CURVE('',#14034,#14035,#4249,.T.);
#18651=EDGE_CURVE('',#14036,#14035,#1449,.T.);
#18652=EDGE_CURVE('',#14037,#14036,#2615,.T.);
#18653=EDGE_CURVE('',#14038,#14037,#1450,.T.);
#18654=EDGE_CURVE('',#14038,#14039,#4250,.T.);
#18655=EDGE_CURVE('',#14040,#14039,#1451,.T.);
#18656=EDGE_CURVE('',#14041,#14040,#2616,.T.);
#18657=EDGE_CURVE('',#14042,#14041,#1452,.T.);
#18658=EDGE_CURVE('',#14042,#14043,#4251,.T.);
#18659=EDGE_CURVE('',#14044,#14043,#1453,.T.);
#18660=EDGE_CURVE('',#14045,#14044,#2617,.T.);
#18661=EDGE_CURVE('',#14046,#14045,#1454,.T.);
#18662=EDGE_CURVE('',#14046,#14047,#4252,.T.);
#18663=EDGE_CURVE('',#14048,#14047,#1455,.T.);
#18664=EDGE_CURVE('',#14049,#14048,#2618,.T.);
#18665=EDGE_CURVE('',#14050,#14049,#1456,.T.);
#18666=EDGE_CURVE('',#14050,#14051,#4253,.T.);
#18667=EDGE_CURVE('',#14052,#14051,#1457,.T.);
#18668=EDGE_CURVE('',#14053,#14052,#2619,.T.);
#18669=EDGE_CURVE('',#14054,#14053,#1458,.T.);
#18670=EDGE_CURVE('',#14054,#14055,#4254,.T.);
#18671=EDGE_CURVE('',#14056,#14055,#1459,.T.);
#18672=EDGE_CURVE('',#14057,#14056,#2620,.T.);
#18673=EDGE_CURVE('',#14058,#14057,#1460,.T.);
#18674=EDGE_CURVE('',#14058,#14059,#4255,.T.);
#18675=EDGE_CURVE('',#14060,#14059,#1461,.T.);
#18676=EDGE_CURVE('',#14061,#14060,#2621,.T.);
#18677=EDGE_CURVE('',#14062,#14061,#1462,.T.);
#18678=EDGE_CURVE('',#14062,#14063,#4256,.T.);
#18679=EDGE_CURVE('',#14064,#14063,#1463,.T.);
#18680=EDGE_CURVE('',#14065,#14064,#2622,.T.);
#18681=EDGE_CURVE('',#14066,#14065,#1464,.T.);
#18682=EDGE_CURVE('',#14066,#14067,#4257,.T.);
#18683=EDGE_CURVE('',#14068,#14067,#1465,.T.);
#18684=EDGE_CURVE('',#14069,#14068,#2623,.T.);
#18685=EDGE_CURVE('',#14070,#14069,#1466,.T.);
#18686=EDGE_CURVE('',#14070,#14071,#4258,.T.);
#18687=EDGE_CURVE('',#14072,#14071,#1467,.T.);
#18688=EDGE_CURVE('',#14073,#14072,#2624,.T.);
#18689=EDGE_CURVE('',#14074,#14073,#1468,.T.);
#18690=EDGE_CURVE('',#14074,#14075,#4259,.T.);
#18691=EDGE_CURVE('',#14076,#14075,#1469,.T.);
#18692=EDGE_CURVE('',#14077,#14076,#2625,.T.);
#18693=EDGE_CURVE('',#14078,#14077,#1470,.T.);
#18694=EDGE_CURVE('',#14078,#14079,#4260,.T.);
#18695=EDGE_CURVE('',#14080,#14079,#1471,.T.);
#18696=EDGE_CURVE('',#14081,#14080,#2626,.T.);
#18697=EDGE_CURVE('',#14082,#14081,#1472,.T.);
#18698=EDGE_CURVE('',#14082,#14083,#4261,.T.);
#18699=EDGE_CURVE('',#14084,#14083,#1473,.T.);
#18700=EDGE_CURVE('',#14085,#14084,#2627,.T.);
#18701=EDGE_CURVE('',#14086,#14085,#1474,.T.);
#18702=EDGE_CURVE('',#14086,#14087,#4262,.T.);
#18703=EDGE_CURVE('',#14088,#14087,#1475,.T.);
#18704=EDGE_CURVE('',#14089,#14088,#2628,.T.);
#18705=EDGE_CURVE('',#14090,#14089,#1476,.T.);
#18706=EDGE_CURVE('',#14090,#14091,#4263,.T.);
#18707=EDGE_CURVE('',#14092,#14091,#1477,.T.);
#18708=EDGE_CURVE('',#14093,#14092,#2629,.T.);
#18709=EDGE_CURVE('',#14094,#14093,#1478,.T.);
#18710=EDGE_CURVE('',#14094,#14095,#4264,.T.);
#18711=EDGE_CURVE('',#14096,#14095,#1479,.T.);
#18712=EDGE_CURVE('',#14097,#14096,#2630,.T.);
#18713=EDGE_CURVE('',#14098,#14097,#1480,.T.);
#18714=EDGE_CURVE('',#14098,#14099,#4265,.T.);
#18715=EDGE_CURVE('',#13520,#14099,#1481,.T.);
#18716=EDGE_CURVE('',#14100,#13519,#1482,.T.);
#18717=EDGE_CURVE('',#14100,#14101,#4266,.T.);
#18718=EDGE_CURVE('',#13516,#14101,#1483,.T.);
#18719=EDGE_CURVE('',#14102,#13515,#1484,.T.);
#18720=EDGE_CURVE('',#14102,#14103,#4267,.T.);
#18721=EDGE_CURVE('',#13512,#14103,#1485,.T.);
#18722=EDGE_CURVE('',#14104,#13511,#1486,.T.);
#18723=EDGE_CURVE('',#14104,#14105,#4268,.T.);
#18724=EDGE_CURVE('',#13508,#14105,#1487,.T.);
#18725=EDGE_CURVE('',#14106,#13507,#1488,.T.);
#18726=EDGE_CURVE('',#14106,#14107,#4269,.T.);
#18727=EDGE_CURVE('',#13504,#14107,#1489,.T.);
#18728=EDGE_CURVE('',#14108,#13503,#1490,.T.);
#18729=EDGE_CURVE('',#14108,#14109,#4270,.T.);
#18730=EDGE_CURVE('',#13500,#14109,#1491,.T.);
#18731=EDGE_CURVE('',#14110,#13499,#1492,.T.);
#18732=EDGE_CURVE('',#14110,#14111,#4271,.T.);
#18733=EDGE_CURVE('',#13524,#14111,#1493,.T.);
#18734=EDGE_CURVE('',#14112,#13523,#1494,.T.);
#18735=EDGE_CURVE('',#14112,#14113,#4272,.T.);
#18736=EDGE_CURVE('',#13528,#14113,#1495,.T.);
#18737=EDGE_CURVE('',#14114,#13527,#1496,.T.);
#18738=EDGE_CURVE('',#14114,#14115,#4273,.T.);
#18739=EDGE_CURVE('',#13532,#14115,#1497,.T.);
#18740=EDGE_CURVE('',#14116,#13531,#1498,.T.);
#18741=EDGE_CURVE('',#14116,#14117,#4274,.T.);
#18742=EDGE_CURVE('',#13536,#14117,#1499,.T.);
#18743=EDGE_CURVE('',#14118,#13535,#1500,.T.);
#18744=EDGE_CURVE('',#14118,#14119,#4275,.T.);
#18745=EDGE_CURVE('',#13540,#14119,#1501,.T.);
#18746=EDGE_CURVE('',#14120,#13539,#1502,.T.);
#18747=EDGE_CURVE('',#14120,#14121,#4276,.T.);
#18748=EDGE_CURVE('',#13544,#14121,#1503,.T.);
#18749=EDGE_CURVE('',#14122,#13543,#1504,.T.);
#18750=EDGE_CURVE('',#14122,#14123,#4277,.T.);
#18751=EDGE_CURVE('',#13548,#14123,#1505,.T.);
#18752=EDGE_CURVE('',#14124,#13547,#1506,.T.);
#18753=EDGE_CURVE('',#14124,#14125,#4278,.T.);
#18754=EDGE_CURVE('',#13552,#14125,#1507,.T.);
#18755=EDGE_CURVE('',#14126,#13551,#1508,.T.);
#18756=EDGE_CURVE('',#14126,#14127,#4279,.T.);
#18757=EDGE_CURVE('',#13556,#14127,#1509,.T.);
#18758=EDGE_CURVE('',#14128,#13555,#1510,.T.);
#18759=EDGE_CURVE('',#14128,#14129,#4280,.T.);
#18760=EDGE_CURVE('',#14130,#14129,#1511,.T.);
#18761=EDGE_CURVE('',#14131,#14130,#2631,.T.);
#18762=EDGE_CURVE('',#14132,#14131,#1512,.T.);
#18763=EDGE_CURVE('',#14132,#14133,#4281,.T.);
#18764=EDGE_CURVE('',#14134,#14133,#1513,.T.);
#18765=EDGE_CURVE('',#14135,#14134,#2632,.T.);
#18766=EDGE_CURVE('',#14136,#14135,#1514,.T.);
#18767=EDGE_CURVE('',#14136,#14137,#4282,.T.);
#18768=EDGE_CURVE('',#14138,#14137,#1515,.T.);
#18769=EDGE_CURVE('',#14139,#14138,#2633,.T.);
#18770=EDGE_CURVE('',#14140,#14139,#1516,.T.);
#18771=EDGE_CURVE('',#14140,#14141,#4283,.T.);
#18772=EDGE_CURVE('',#14142,#14141,#1517,.T.);
#18773=EDGE_CURVE('',#14143,#14142,#2634,.T.);
#18774=EDGE_CURVE('',#14144,#14143,#1518,.T.);
#18775=EDGE_CURVE('',#14144,#14145,#4284,.T.);
#18776=EDGE_CURVE('',#14146,#14145,#1519,.T.);
#18777=EDGE_CURVE('',#14147,#14146,#2635,.T.);
#18778=EDGE_CURVE('',#14148,#14147,#1520,.T.);
#18779=EDGE_CURVE('',#14148,#14149,#4285,.T.);
#18780=EDGE_CURVE('',#14150,#14149,#1521,.T.);
#18781=EDGE_CURVE('',#13861,#14150,#3350,.T.);
#18782=EDGE_CURVE('',#13861,#14151,#9542,.T.);
#18783=EDGE_CURVE('',#14152,#14151,#4286,.T.);
#18784=EDGE_CURVE('',#14151,#14152,#4287,.T.);
#18785=EDGE_CURVE('',#14153,#14153,#4288,.T.);
#18786=EDGE_CURVE('',#14153,#14152,#4289,.T.);
#18787=EDGE_CURVE('',#14154,#14154,#4290,.T.);
#18788=EDGE_CURVE('',#14154,#14153,#9543,.T.);
#18789=EDGE_CURVE('',#14155,#14155,#4291,.T.);
#18790=EDGE_CURVE('',#14155,#14154,#4292,.T.);
#18791=EDGE_CURVE('',#13377,#14156,#4293,.T.);
#18792=EDGE_CURVE('',#14156,#14156,#4294,.T.);
#18793=EDGE_CURVE('',#14157,#14110,#2636,.T.);
#18794=EDGE_CURVE('',#14157,#14158,#4295,.T.);
#18795=EDGE_CURVE('',#14111,#14158,#2637,.T.);
#18796=EDGE_CURVE('',#14109,#14159,#2638,.T.);
#18797=EDGE_CURVE('',#14160,#14108,#2639,.T.);
#18798=EDGE_CURVE('',#14160,#14159,#4296,.T.);
#18799=EDGE_CURVE('',#14107,#14161,#2640,.T.);
#18800=EDGE_CURVE('',#14162,#14106,#2641,.T.);
#18801=EDGE_CURVE('',#14162,#14161,#4297,.T.);
#18802=EDGE_CURVE('',#14105,#14163,#2642,.T.);
#18803=EDGE_CURVE('',#14164,#14104,#2643,.T.);
#18804=EDGE_CURVE('',#14164,#14163,#4298,.T.);
#18805=EDGE_CURVE('',#14103,#14165,#2644,.T.);
#18806=EDGE_CURVE('',#14166,#14102,#2645,.T.);
#18807=EDGE_CURVE('',#14166,#14165,#4299,.T.);
#18808=EDGE_CURVE('',#14101,#14167,#2646,.T.);
#18809=EDGE_CURVE('',#14168,#14100,#2647,.T.);
#18810=EDGE_CURVE('',#14168,#14167,#4300,.T.);
#18811=EDGE_CURVE('',#14099,#14169,#2648,.T.);
#18812=EDGE_CURVE('',#14170,#14098,#2649,.T.);
#18813=EDGE_CURVE('',#14170,#14169,#4301,.T.);
#18814=EDGE_CURVE('',#14095,#14171,#2650,.T.);
#18815=EDGE_CURVE('',#14172,#14094,#2651,.T.);
#18816=EDGE_CURVE('',#14172,#14171,#4302,.T.);
#18817=EDGE_CURVE('',#14091,#14173,#2652,.T.);
#18818=EDGE_CURVE('',#14174,#14090,#2653,.T.);
#18819=EDGE_CURVE('',#14174,#14173,#4303,.T.);
#18820=EDGE_CURVE('',#14087,#14175,#2654,.T.);
#18821=EDGE_CURVE('',#14176,#14086,#2655,.T.);
#18822=EDGE_CURVE('',#14176,#14175,#4304,.T.);
#18823=EDGE_CURVE('',#14083,#14177,#2656,.T.);
#18824=EDGE_CURVE('',#14178,#14082,#2657,.T.);
#18825=EDGE_CURVE('',#14178,#14177,#4305,.T.);
#18826=EDGE_CURVE('',#14079,#14179,#2658,.T.);
#18827=EDGE_CURVE('',#14180,#14078,#2659,.T.);
#18828=EDGE_CURVE('',#14180,#14179,#4306,.T.);
#18829=EDGE_CURVE('',#14075,#14181,#2660,.T.);
#18830=EDGE_CURVE('',#14182,#14074,#2661,.T.);
#18831=EDGE_CURVE('',#14182,#14181,#4307,.T.);
#18832=EDGE_CURVE('',#14071,#14183,#2662,.T.);
#18833=EDGE_CURVE('',#14184,#14070,#2663,.T.);
#18834=EDGE_CURVE('',#14184,#14183,#4308,.T.);
#18835=EDGE_CURVE('',#14067,#14185,#2664,.T.);
#18836=EDGE_CURVE('',#14186,#14066,#2665,.T.);
#18837=EDGE_CURVE('',#14186,#14185,#4309,.T.);
#18838=EDGE_CURVE('',#14063,#14187,#2666,.T.);
#18839=EDGE_CURVE('',#14188,#14062,#2667,.T.);
#18840=EDGE_CURVE('',#14188,#14187,#4310,.T.);
#18841=EDGE_CURVE('',#14059,#14189,#2668,.T.);
#18842=EDGE_CURVE('',#14190,#14058,#2669,.T.);
#18843=EDGE_CURVE('',#14190,#14189,#4311,.T.);
#18844=EDGE_CURVE('',#14055,#14191,#2670,.T.);
#18845=EDGE_CURVE('',#14192,#14054,#2671,.T.);
#18846=EDGE_CURVE('',#14192,#14191,#4312,.T.);
#18847=EDGE_CURVE('',#14051,#14193,#2672,.T.);
#18848=EDGE_CURVE('',#14194,#14050,#2673,.T.);
#18849=EDGE_CURVE('',#14194,#14193,#4313,.T.);
#18850=EDGE_CURVE('',#14047,#14195,#2674,.T.);
#18851=EDGE_CURVE('',#14196,#14046,#2675,.T.);
#18852=EDGE_CURVE('',#14196,#14195,#4314,.T.);
#18853=EDGE_CURVE('',#14043,#14197,#2676,.T.);
#18854=EDGE_CURVE('',#14198,#14042,#2677,.T.);
#18855=EDGE_CURVE('',#14198,#14197,#4315,.T.);
#18856=EDGE_CURVE('',#14039,#14199,#2678,.T.);
#18857=EDGE_CURVE('',#14200,#14038,#2679,.T.);
#18858=EDGE_CURVE('',#14200,#14199,#4316,.T.);
#18859=EDGE_CURVE('',#14035,#14201,#2680,.T.);
#18860=EDGE_CURVE('',#14202,#14034,#2681,.T.);
#18861=EDGE_CURVE('',#14202,#14201,#4317,.T.);
#18862=EDGE_CURVE('',#14031,#14203,#2682,.T.);
#18863=EDGE_CURVE('',#14204,#14030,#2683,.T.);
#18864=EDGE_CURVE('',#14204,#14203,#4318,.T.);
#18865=EDGE_CURVE('',#14027,#14205,#2684,.T.);
#18866=EDGE_CURVE('',#14206,#14026,#2685,.T.);
#18867=EDGE_CURVE('',#14206,#14205,#4319,.T.);
#18868=EDGE_CURVE('',#14023,#14207,#2686,.T.);
#18869=EDGE_CURVE('',#14208,#14022,#2687,.T.);
#18870=EDGE_CURVE('',#14208,#14207,#4320,.T.);
#18871=EDGE_CURVE('',#14019,#14209,#2688,.T.);
#18872=EDGE_CURVE('',#14210,#14018,#2689,.T.);
#18873=EDGE_CURVE('',#14210,#14209,#4321,.T.);
#18874=EDGE_CURVE('',#14015,#14211,#2690,.T.);
#18875=EDGE_CURVE('',#14212,#14014,#2691,.T.);
#18876=EDGE_CURVE('',#14212,#14211,#4322,.T.);
#18877=EDGE_CURVE('',#14011,#14213,#2692,.T.);
#18878=EDGE_CURVE('',#14214,#14010,#2693,.T.);
#18879=EDGE_CURVE('',#14214,#14213,#4323,.T.);
#18880=EDGE_CURVE('',#14007,#14215,#2694,.T.);
#18881=EDGE_CURVE('',#14216,#14006,#2695,.T.);
#18882=EDGE_CURVE('',#14216,#14215,#4324,.T.);
#18883=EDGE_CURVE('',#14003,#14217,#2696,.T.);
#18884=EDGE_CURVE('',#14218,#14002,#2697,.T.);
#18885=EDGE_CURVE('',#14218,#14217,#4325,.T.);
#18886=EDGE_CURVE('',#13999,#14219,#2698,.T.);
#18887=EDGE_CURVE('',#14220,#13998,#2699,.T.);
#18888=EDGE_CURVE('',#14220,#14219,#4326,.T.);
#18889=EDGE_CURVE('',#13995,#14221,#2700,.T.);
#18890=EDGE_CURVE('',#14222,#13994,#2701,.T.);
#18891=EDGE_CURVE('',#14222,#14221,#4327,.T.);
#18892=EDGE_CURVE('',#13991,#14223,#2702,.T.);
#18893=EDGE_CURVE('',#14224,#13990,#2703,.T.);
#18894=EDGE_CURVE('',#14224,#14223,#4328,.T.);
#18895=EDGE_CURVE('',#13987,#14225,#2704,.T.);
#18896=EDGE_CURVE('',#14226,#13986,#2705,.T.);
#18897=EDGE_CURVE('',#14226,#14225,#4329,.T.);
#18898=EDGE_CURVE('',#13983,#14227,#2706,.T.);
#18899=EDGE_CURVE('',#14228,#13982,#2707,.T.);
#18900=EDGE_CURVE('',#14228,#14227,#4330,.T.);
#18901=EDGE_CURVE('',#13979,#14229,#2708,.T.);
#18902=EDGE_CURVE('',#14230,#13978,#2709,.T.);
#18903=EDGE_CURVE('',#14230,#14229,#4331,.T.);
#18904=EDGE_CURVE('',#13975,#14231,#2710,.T.);
#18905=EDGE_CURVE('',#14232,#13974,#2711,.T.);
#18906=EDGE_CURVE('',#14232,#14231,#4332,.T.);
#18907=EDGE_CURVE('',#13971,#14233,#2712,.T.);
#18908=EDGE_CURVE('',#14234,#13970,#2713,.T.);
#18909=EDGE_CURVE('',#14234,#14233,#4333,.T.);
#18910=EDGE_CURVE('',#13967,#14235,#2714,.T.);
#18911=EDGE_CURVE('',#14236,#13966,#2715,.T.);
#18912=EDGE_CURVE('',#14236,#14235,#4334,.T.);
#18913=EDGE_CURVE('',#13963,#14237,#2716,.T.);
#18914=EDGE_CURVE('',#14238,#13962,#2717,.T.);
#18915=EDGE_CURVE('',#14238,#14237,#4335,.T.);
#18916=EDGE_CURVE('',#13959,#14239,#2718,.T.);
#18917=EDGE_CURVE('',#14240,#13958,#2719,.T.);
#18918=EDGE_CURVE('',#14240,#14239,#4336,.T.);
#18919=EDGE_CURVE('',#13955,#14241,#2720,.T.);
#18920=EDGE_CURVE('',#14242,#13954,#2721,.T.);
#18921=EDGE_CURVE('',#14242,#14241,#4337,.T.);
#18922=EDGE_CURVE('',#13951,#14243,#2722,.T.);
#18923=EDGE_CURVE('',#14244,#13950,#2723,.T.);
#18924=EDGE_CURVE('',#14244,#14243,#4338,.T.);
#18925=EDGE_CURVE('',#13947,#14245,#2724,.T.);
#18926=EDGE_CURVE('',#14246,#13946,#2725,.T.);
#18927=EDGE_CURVE('',#14246,#14245,#4339,.T.);
#18928=EDGE_CURVE('',#13943,#14247,#2726,.T.);
#18929=EDGE_CURVE('',#14248,#13942,#2727,.T.);
#18930=EDGE_CURVE('',#14248,#14247,#4340,.T.);
#18931=EDGE_CURVE('',#13939,#14249,#2728,.T.);
#18932=EDGE_CURVE('',#14250,#13938,#2729,.T.);
#18933=EDGE_CURVE('',#14250,#14249,#4341,.T.);
#18934=EDGE_CURVE('',#13935,#14251,#2730,.T.);
#18935=EDGE_CURVE('',#14252,#13934,#2731,.T.);
#18936=EDGE_CURVE('',#14252,#14251,#4342,.T.);
#18937=EDGE_CURVE('',#13931,#14253,#2732,.T.);
#18938=EDGE_CURVE('',#14254,#13930,#2733,.T.);
#18939=EDGE_CURVE('',#14254,#14253,#4343,.T.);
#18940=EDGE_CURVE('',#13927,#14255,#2734,.T.);
#18941=EDGE_CURVE('',#14256,#13926,#2735,.T.);
#18942=EDGE_CURVE('',#14256,#14255,#4344,.T.);
#18943=EDGE_CURVE('',#13923,#14257,#2736,.T.);
#18944=EDGE_CURVE('',#14258,#13922,#2737,.T.);
#18945=EDGE_CURVE('',#14258,#14257,#4345,.T.);
#18946=EDGE_CURVE('',#13919,#14259,#2738,.T.);
#18947=EDGE_CURVE('',#14260,#13918,#2739,.T.);
#18948=EDGE_CURVE('',#14260,#14259,#4346,.T.);
#18949=EDGE_CURVE('',#13915,#14261,#2740,.T.);
#18950=EDGE_CURVE('',#14262,#13914,#2741,.T.);
#18951=EDGE_CURVE('',#14262,#14261,#4347,.T.);
#18952=EDGE_CURVE('',#13911,#14263,#2742,.T.);
#18953=EDGE_CURVE('',#14264,#13910,#2743,.T.);
#18954=EDGE_CURVE('',#14264,#14263,#4348,.T.);
#18955=EDGE_CURVE('',#13907,#14265,#2744,.T.);
#18956=EDGE_CURVE('',#14266,#13906,#2745,.T.);
#18957=EDGE_CURVE('',#14266,#14265,#4349,.T.);
#18958=EDGE_CURVE('',#13903,#14267,#2746,.T.);
#18959=EDGE_CURVE('',#14268,#13902,#2747,.T.);
#18960=EDGE_CURVE('',#14268,#14267,#4350,.T.);
#18961=EDGE_CURVE('',#13899,#14269,#2748,.T.);
#18962=EDGE_CURVE('',#14270,#13898,#2749,.T.);
#18963=EDGE_CURVE('',#14270,#14269,#4351,.T.);
#18964=EDGE_CURVE('',#13895,#14271,#2750,.T.);
#18965=EDGE_CURVE('',#14272,#13894,#2751,.T.);
#18966=EDGE_CURVE('',#14272,#14271,#4352,.T.);
#18967=EDGE_CURVE('',#13891,#14273,#2752,.T.);
#18968=EDGE_CURVE('',#14274,#13890,#2753,.T.);
#18969=EDGE_CURVE('',#14274,#14273,#4353,.T.);
#18970=EDGE_CURVE('',#13887,#14275,#2754,.T.);
#18971=EDGE_CURVE('',#14276,#13886,#2755,.T.);
#18972=EDGE_CURVE('',#14276,#14275,#4354,.T.);
#18973=EDGE_CURVE('',#13883,#14277,#2756,.T.);
#18974=EDGE_CURVE('',#14278,#13882,#2757,.T.);
#18975=EDGE_CURVE('',#14278,#14277,#4355,.T.);
#18976=EDGE_CURVE('',#13879,#14279,#2758,.T.);
#18977=EDGE_CURVE('',#14280,#13878,#2759,.T.);
#18978=EDGE_CURVE('',#14280,#14279,#4356,.T.);
#18979=EDGE_CURVE('',#13875,#14281,#2760,.T.);
#18980=EDGE_CURVE('',#14282,#13874,#2761,.T.);
#18981=EDGE_CURVE('',#14282,#14281,#4357,.T.);
#18982=EDGE_CURVE('',#13871,#14283,#2762,.T.);
#18983=EDGE_CURVE('',#14284,#13870,#2763,.T.);
#18984=EDGE_CURVE('',#14284,#14283,#4358,.T.);
#18985=EDGE_CURVE('',#14285,#14112,#2764,.T.);
#18986=EDGE_CURVE('',#14285,#14286,#4359,.T.);
#18987=EDGE_CURVE('',#14113,#14286,#2765,.T.);
#18988=EDGE_CURVE('',#14287,#14114,#2766,.T.);
#18989=EDGE_CURVE('',#14287,#14288,#4360,.T.);
#18990=EDGE_CURVE('',#14115,#14288,#2767,.T.);
#18991=EDGE_CURVE('',#14289,#14116,#2768,.T.);
#18992=EDGE_CURVE('',#14289,#14290,#4361,.T.);
#18993=EDGE_CURVE('',#14117,#14290,#2769,.T.);
#18994=EDGE_CURVE('',#14291,#14118,#2770,.T.);
#18995=EDGE_CURVE('',#14291,#14292,#4362,.T.);
#18996=EDGE_CURVE('',#14119,#14292,#2771,.T.);
#18997=EDGE_CURVE('',#14293,#14120,#2772,.T.);
#18998=EDGE_CURVE('',#14293,#14294,#4363,.T.);
#18999=EDGE_CURVE('',#14121,#14294,#2773,.T.);
#19000=EDGE_CURVE('',#14295,#14122,#2774,.T.);
#19001=EDGE_CURVE('',#14295,#14296,#4364,.T.);
#19002=EDGE_CURVE('',#14123,#14296,#2775,.T.);
#19003=EDGE_CURVE('',#14297,#14124,#2776,.T.);
#19004=EDGE_CURVE('',#14297,#14298,#4365,.T.);
#19005=EDGE_CURVE('',#14125,#14298,#2777,.T.);
#19006=EDGE_CURVE('',#14299,#14126,#2778,.T.);
#19007=EDGE_CURVE('',#14299,#14300,#4366,.T.);
#19008=EDGE_CURVE('',#14127,#14300,#2779,.T.);
#19009=EDGE_CURVE('',#14301,#14128,#2780,.T.);
#19010=EDGE_CURVE('',#14301,#14302,#4367,.T.);
#19011=EDGE_CURVE('',#14129,#14302,#2781,.T.);
#19012=EDGE_CURVE('',#14303,#14132,#2782,.T.);
#19013=EDGE_CURVE('',#14303,#14304,#4368,.T.);
#19014=EDGE_CURVE('',#14133,#14304,#2783,.T.);
#19015=EDGE_CURVE('',#14305,#14136,#2784,.T.);
#19016=EDGE_CURVE('',#14305,#14306,#4369,.T.);
#19017=EDGE_CURVE('',#14137,#14306,#2785,.T.);
#19018=EDGE_CURVE('',#14307,#14140,#2786,.T.);
#19019=EDGE_CURVE('',#14307,#14308,#4370,.T.);
#19020=EDGE_CURVE('',#14141,#14308,#2787,.T.);
#19021=EDGE_CURVE('',#14309,#14144,#2788,.T.);
#19022=EDGE_CURVE('',#14309,#14310,#4371,.T.);
#19023=EDGE_CURVE('',#14145,#14310,#2789,.T.);
#19024=EDGE_CURVE('',#14311,#14148,#2790,.T.);
#19025=EDGE_CURVE('',#14311,#14312,#4372,.T.);
#19026=EDGE_CURVE('',#14149,#14312,#2791,.T.);
#19027=EDGE_CURVE('',#13867,#14313,#2792,.T.);
#19028=EDGE_CURVE('',#14314,#13866,#2793,.T.);
#19029=EDGE_CURVE('',#14314,#14313,#4373,.T.);
#19030=EDGE_CURVE('',#14315,#14157,#9544,.T.);
#19031=EDGE_CURVE('',#14315,#14316,#4374,.T.);
#19032=EDGE_CURVE('',#14158,#14316,#9545,.T.);
#19033=EDGE_CURVE('',#14159,#14317,#9546,.T.);
#19034=EDGE_CURVE('',#14318,#14160,#9547,.T.);
#19035=EDGE_CURVE('',#14318,#14317,#4375,.T.);
#19036=EDGE_CURVE('',#14161,#14319,#9548,.T.);
#19037=EDGE_CURVE('',#14320,#14162,#9549,.T.);
#19038=EDGE_CURVE('',#14320,#14319,#4376,.T.);
#19039=EDGE_CURVE('',#14163,#14321,#9550,.T.);
#19040=EDGE_CURVE('',#14322,#14164,#9551,.T.);
#19041=EDGE_CURVE('',#14322,#14321,#4377,.T.);
#19042=EDGE_CURVE('',#14165,#14323,#9552,.T.);
#19043=EDGE_CURVE('',#14324,#14166,#9553,.T.);
#19044=EDGE_CURVE('',#14324,#14323,#4378,.T.);
#19045=EDGE_CURVE('',#14167,#14325,#9554,.T.);
#19046=EDGE_CURVE('',#14326,#14168,#9555,.T.);
#19047=EDGE_CURVE('',#14326,#14325,#4379,.T.);
#19048=EDGE_CURVE('',#14169,#14327,#9556,.T.);
#19049=EDGE_CURVE('',#14328,#14170,#9557,.T.);
#19050=EDGE_CURVE('',#14328,#14327,#4380,.T.);
#19051=EDGE_CURVE('',#14171,#14329,#9558,.T.);
#19052=EDGE_CURVE('',#14330,#14172,#9559,.T.);
#19053=EDGE_CURVE('',#14330,#14329,#4381,.T.);
#19054=EDGE_CURVE('',#14173,#14331,#9560,.T.);
#19055=EDGE_CURVE('',#14332,#14174,#9561,.T.);
#19056=EDGE_CURVE('',#14332,#14331,#4382,.T.);
#19057=EDGE_CURVE('',#14175,#14333,#9562,.T.);
#19058=EDGE_CURVE('',#14334,#14176,#9563,.T.);
#19059=EDGE_CURVE('',#14334,#14333,#4383,.T.);
#19060=EDGE_CURVE('',#14177,#14335,#9564,.T.);
#19061=EDGE_CURVE('',#14336,#14178,#9565,.T.);
#19062=EDGE_CURVE('',#14336,#14335,#4384,.T.);
#19063=EDGE_CURVE('',#14179,#14337,#9566,.T.);
#19064=EDGE_CURVE('',#14338,#14180,#9567,.T.);
#19065=EDGE_CURVE('',#14338,#14337,#4385,.T.);
#19066=EDGE_CURVE('',#14181,#14339,#9568,.T.);
#19067=EDGE_CURVE('',#14340,#14182,#9569,.T.);
#19068=EDGE_CURVE('',#14340,#14339,#4386,.T.);
#19069=EDGE_CURVE('',#14183,#14341,#9570,.T.);
#19070=EDGE_CURVE('',#14342,#14184,#9571,.T.);
#19071=EDGE_CURVE('',#14342,#14341,#4387,.T.);
#19072=EDGE_CURVE('',#14185,#14343,#9572,.T.);
#19073=EDGE_CURVE('',#14344,#14186,#9573,.T.);
#19074=EDGE_CURVE('',#14344,#14343,#4388,.T.);
#19075=EDGE_CURVE('',#14187,#14345,#9574,.T.);
#19076=EDGE_CURVE('',#14346,#14188,#9575,.T.);
#19077=EDGE_CURVE('',#14346,#14345,#4389,.T.);
#19078=EDGE_CURVE('',#14189,#14347,#9576,.T.);
#19079=EDGE_CURVE('',#14348,#14190,#9577,.T.);
#19080=EDGE_CURVE('',#14348,#14347,#4390,.T.);
#19081=EDGE_CURVE('',#14191,#14349,#9578,.T.);
#19082=EDGE_CURVE('',#14350,#14192,#9579,.T.);
#19083=EDGE_CURVE('',#14350,#14349,#4391,.T.);
#19084=EDGE_CURVE('',#14193,#14351,#9580,.T.);
#19085=EDGE_CURVE('',#14352,#14194,#9581,.T.);
#19086=EDGE_CURVE('',#14352,#14351,#4392,.T.);
#19087=EDGE_CURVE('',#14195,#14353,#9582,.T.);
#19088=EDGE_CURVE('',#14354,#14196,#9583,.T.);
#19089=EDGE_CURVE('',#14354,#14353,#4393,.T.);
#19090=EDGE_CURVE('',#14197,#14355,#9584,.T.);
#19091=EDGE_CURVE('',#14356,#14198,#9585,.T.);
#19092=EDGE_CURVE('',#14356,#14355,#4394,.T.);
#19093=EDGE_CURVE('',#14199,#14357,#9586,.T.);
#19094=EDGE_CURVE('',#14358,#14200,#9587,.T.);
#19095=EDGE_CURVE('',#14358,#14357,#4395,.T.);
#19096=EDGE_CURVE('',#14201,#14359,#9588,.T.);
#19097=EDGE_CURVE('',#14360,#14202,#9589,.T.);
#19098=EDGE_CURVE('',#14360,#14359,#4396,.T.);
#19099=EDGE_CURVE('',#14203,#14361,#9590,.T.);
#19100=EDGE_CURVE('',#14362,#14204,#9591,.T.);
#19101=EDGE_CURVE('',#14362,#14361,#4397,.T.);
#19102=EDGE_CURVE('',#14205,#14363,#9592,.T.);
#19103=EDGE_CURVE('',#14364,#14206,#9593,.T.);
#19104=EDGE_CURVE('',#14364,#14363,#4398,.T.);
#19105=EDGE_CURVE('',#14207,#14365,#9594,.T.);
#19106=EDGE_CURVE('',#14366,#14208,#9595,.T.);
#19107=EDGE_CURVE('',#14366,#14365,#4399,.T.);
#19108=EDGE_CURVE('',#14209,#14367,#9596,.T.);
#19109=EDGE_CURVE('',#14368,#14210,#9597,.T.);
#19110=EDGE_CURVE('',#14368,#14367,#4400,.T.);
#19111=EDGE_CURVE('',#14211,#14369,#9598,.T.);
#19112=EDGE_CURVE('',#14370,#14212,#9599,.T.);
#19113=EDGE_CURVE('',#14370,#14369,#4401,.T.);
#19114=EDGE_CURVE('',#14213,#14371,#9600,.T.);
#19115=EDGE_CURVE('',#14372,#14214,#9601,.T.);
#19116=EDGE_CURVE('',#14372,#14371,#4402,.T.);
#19117=EDGE_CURVE('',#14215,#14373,#9602,.T.);
#19118=EDGE_CURVE('',#14374,#14216,#9603,.T.);
#19119=EDGE_CURVE('',#14374,#14373,#4403,.T.);
#19120=EDGE_CURVE('',#14217,#14375,#9604,.T.);
#19121=EDGE_CURVE('',#14376,#14218,#9605,.T.);
#19122=EDGE_CURVE('',#14376,#14375,#4404,.T.);
#19123=EDGE_CURVE('',#14219,#14377,#9606,.T.);
#19124=EDGE_CURVE('',#14378,#14220,#9607,.T.);
#19125=EDGE_CURVE('',#14378,#14377,#4405,.T.);
#19126=EDGE_CURVE('',#14221,#14379,#9608,.T.);
#19127=EDGE_CURVE('',#14380,#14222,#9609,.T.);
#19128=EDGE_CURVE('',#14380,#14379,#4406,.T.);
#19129=EDGE_CURVE('',#14223,#14381,#9610,.T.);
#19130=EDGE_CURVE('',#14382,#14224,#9611,.T.);
#19131=EDGE_CURVE('',#14382,#14381,#4407,.T.);
#19132=EDGE_CURVE('',#14225,#14383,#9612,.T.);
#19133=EDGE_CURVE('',#14384,#14226,#9613,.T.);
#19134=EDGE_CURVE('',#14384,#14383,#4408,.T.);
#19135=EDGE_CURVE('',#14227,#14385,#9614,.T.);
#19136=EDGE_CURVE('',#14386,#14228,#9615,.T.);
#19137=EDGE_CURVE('',#14386,#14385,#4409,.T.);
#19138=EDGE_CURVE('',#14229,#14387,#9616,.T.);
#19139=EDGE_CURVE('',#14388,#14230,#9617,.T.);
#19140=EDGE_CURVE('',#14388,#14387,#4410,.T.);
#19141=EDGE_CURVE('',#14231,#14389,#9618,.T.);
#19142=EDGE_CURVE('',#14390,#14232,#9619,.T.);
#19143=EDGE_CURVE('',#14390,#14389,#4411,.T.);
#19144=EDGE_CURVE('',#14233,#14391,#9620,.T.);
#19145=EDGE_CURVE('',#14392,#14234,#9621,.T.);
#19146=EDGE_CURVE('',#14392,#14391,#4412,.T.);
#19147=EDGE_CURVE('',#14235,#14393,#9622,.T.);
#19148=EDGE_CURVE('',#14394,#14236,#9623,.T.);
#19149=EDGE_CURVE('',#14394,#14393,#4413,.T.);
#19150=EDGE_CURVE('',#14237,#14395,#9624,.T.);
#19151=EDGE_CURVE('',#14396,#14238,#9625,.T.);
#19152=EDGE_CURVE('',#14396,#14395,#4414,.T.);
#19153=EDGE_CURVE('',#14239,#14397,#9626,.T.);
#19154=EDGE_CURVE('',#14398,#14240,#9627,.T.);
#19155=EDGE_CURVE('',#14398,#14397,#4415,.T.);
#19156=EDGE_CURVE('',#14241,#14399,#9628,.T.);
#19157=EDGE_CURVE('',#14400,#14242,#9629,.T.);
#19158=EDGE_CURVE('',#14400,#14399,#4416,.T.);
#19159=EDGE_CURVE('',#14243,#14401,#9630,.T.);
#19160=EDGE_CURVE('',#14402,#14244,#9631,.T.);
#19161=EDGE_CURVE('',#14402,#14401,#4417,.T.);
#19162=EDGE_CURVE('',#14245,#14403,#9632,.T.);
#19163=EDGE_CURVE('',#14404,#14246,#9633,.T.);
#19164=EDGE_CURVE('',#14404,#14403,#4418,.T.);
#19165=EDGE_CURVE('',#14247,#14405,#9634,.T.);
#19166=EDGE_CURVE('',#14406,#14248,#9635,.T.);
#19167=EDGE_CURVE('',#14406,#14405,#4419,.T.);
#19168=EDGE_CURVE('',#14249,#14407,#9636,.T.);
#19169=EDGE_CURVE('',#14408,#14250,#9637,.T.);
#19170=EDGE_CURVE('',#14408,#14407,#4420,.T.);
#19171=EDGE_CURVE('',#14251,#14409,#9638,.T.);
#19172=EDGE_CURVE('',#14410,#14252,#9639,.T.);
#19173=EDGE_CURVE('',#14410,#14409,#4421,.T.);
#19174=EDGE_CURVE('',#14253,#14411,#9640,.T.);
#19175=EDGE_CURVE('',#14412,#14254,#9641,.T.);
#19176=EDGE_CURVE('',#14412,#14411,#4422,.T.);
#19177=EDGE_CURVE('',#14255,#14413,#9642,.T.);
#19178=EDGE_CURVE('',#14414,#14256,#9643,.T.);
#19179=EDGE_CURVE('',#14414,#14413,#4423,.T.);
#19180=EDGE_CURVE('',#14257,#14415,#9644,.T.);
#19181=EDGE_CURVE('',#14416,#14258,#9645,.T.);
#19182=EDGE_CURVE('',#14416,#14415,#4424,.T.);
#19183=EDGE_CURVE('',#14259,#14417,#9646,.T.);
#19184=EDGE_CURVE('',#14418,#14260,#9647,.T.);
#19185=EDGE_CURVE('',#14418,#14417,#4425,.T.);
#19186=EDGE_CURVE('',#14261,#14419,#9648,.T.);
#19187=EDGE_CURVE('',#14420,#14262,#9649,.T.);
#19188=EDGE_CURVE('',#14420,#14419,#4426,.T.);
#19189=EDGE_CURVE('',#14263,#14421,#9650,.T.);
#19190=EDGE_CURVE('',#14422,#14264,#9651,.T.);
#19191=EDGE_CURVE('',#14422,#14421,#4427,.T.);
#19192=EDGE_CURVE('',#14265,#14423,#9652,.T.);
#19193=EDGE_CURVE('',#14424,#14266,#9653,.T.);
#19194=EDGE_CURVE('',#14424,#14423,#4428,.T.);
#19195=EDGE_CURVE('',#14267,#14425,#9654,.T.);
#19196=EDGE_CURVE('',#14426,#14268,#9655,.T.);
#19197=EDGE_CURVE('',#14426,#14425,#4429,.T.);
#19198=EDGE_CURVE('',#14269,#14427,#9656,.T.);
#19199=EDGE_CURVE('',#14428,#14270,#9657,.T.);
#19200=EDGE_CURVE('',#14428,#14427,#4430,.T.);
#19201=EDGE_CURVE('',#14271,#14429,#9658,.T.);
#19202=EDGE_CURVE('',#14430,#14272,#9659,.T.);
#19203=EDGE_CURVE('',#14430,#14429,#4431,.T.);
#19204=EDGE_CURVE('',#14273,#14431,#9660,.T.);
#19205=EDGE_CURVE('',#14432,#14274,#9661,.T.);
#19206=EDGE_CURVE('',#14432,#14431,#4432,.T.);
#19207=EDGE_CURVE('',#14275,#14433,#9662,.T.);
#19208=EDGE_CURVE('',#14434,#14276,#9663,.T.);
#19209=EDGE_CURVE('',#14434,#14433,#4433,.T.);
#19210=EDGE_CURVE('',#14277,#14435,#9664,.T.);
#19211=EDGE_CURVE('',#14436,#14278,#9665,.T.);
#19212=EDGE_CURVE('',#14436,#14435,#4434,.T.);
#19213=EDGE_CURVE('',#14279,#14437,#9666,.T.);
#19214=EDGE_CURVE('',#14438,#14280,#9667,.T.);
#19215=EDGE_CURVE('',#14438,#14437,#4435,.T.);
#19216=EDGE_CURVE('',#14281,#14439,#9668,.T.);
#19217=EDGE_CURVE('',#14440,#14282,#9669,.T.);
#19218=EDGE_CURVE('',#14440,#14439,#4436,.T.);
#19219=EDGE_CURVE('',#14283,#14441,#9670,.T.);
#19220=EDGE_CURVE('',#14442,#14284,#9671,.T.);
#19221=EDGE_CURVE('',#14442,#14441,#4437,.T.);
#19222=EDGE_CURVE('',#14443,#14285,#9672,.T.);
#19223=EDGE_CURVE('',#14443,#14444,#4438,.T.);
#19224=EDGE_CURVE('',#14286,#14444,#9673,.T.);
#19225=EDGE_CURVE('',#14445,#14287,#9674,.T.);
#19226=EDGE_CURVE('',#14445,#14446,#4439,.T.);
#19227=EDGE_CURVE('',#14288,#14446,#9675,.T.);
#19228=EDGE_CURVE('',#14447,#14289,#9676,.T.);
#19229=EDGE_CURVE('',#14447,#14448,#4440,.T.);
#19230=EDGE_CURVE('',#14290,#14448,#9677,.T.);
#19231=EDGE_CURVE('',#14449,#14291,#9678,.T.);
#19232=EDGE_CURVE('',#14449,#14450,#4441,.T.);
#19233=EDGE_CURVE('',#14292,#14450,#9679,.T.);
#19234=EDGE_CURVE('',#14451,#14293,#9680,.T.);
#19235=EDGE_CURVE('',#14451,#14452,#4442,.T.);
#19236=EDGE_CURVE('',#14294,#14452,#9681,.T.);
#19237=EDGE_CURVE('',#14453,#14295,#9682,.T.);
#19238=EDGE_CURVE('',#14453,#14454,#4443,.T.);
#19239=EDGE_CURVE('',#14296,#14454,#9683,.T.);
#19240=EDGE_CURVE('',#14455,#14297,#9684,.T.);
#19241=EDGE_CURVE('',#14455,#14456,#4444,.T.);
#19242=EDGE_CURVE('',#14298,#14456,#9685,.T.);
#19243=EDGE_CURVE('',#14457,#14299,#9686,.T.);
#19244=EDGE_CURVE('',#14457,#14458,#4445,.T.);
#19245=EDGE_CURVE('',#14300,#14458,#9687,.T.);
#19246=EDGE_CURVE('',#14459,#14301,#9688,.T.);
#19247=EDGE_CURVE('',#14459,#14460,#4446,.T.);
#19248=EDGE_CURVE('',#14302,#14460,#9689,.T.);
#19249=EDGE_CURVE('',#14461,#14303,#9690,.T.);
#19250=EDGE_CURVE('',#14461,#14462,#4447,.T.);
#19251=EDGE_CURVE('',#14304,#14462,#9691,.T.);
#19252=EDGE_CURVE('',#14463,#14305,#9692,.T.);
#19253=EDGE_CURVE('',#14463,#14464,#4448,.T.);
#19254=EDGE_CURVE('',#14306,#14464,#9693,.T.);
#19255=EDGE_CURVE('',#14465,#14307,#9694,.T.);
#19256=EDGE_CURVE('',#14465,#14466,#4449,.T.);
#19257=EDGE_CURVE('',#14308,#14466,#9695,.T.);
#19258=EDGE_CURVE('',#14467,#14309,#9696,.T.);
#19259=EDGE_CURVE('',#14467,#14468,#4450,.T.);
#19260=EDGE_CURVE('',#14310,#14468,#9697,.T.);
#19261=EDGE_CURVE('',#14469,#14311,#9698,.T.);
#19262=EDGE_CURVE('',#14469,#14470,#4451,.T.);
#19263=EDGE_CURVE('',#14312,#14470,#9699,.T.);
#19264=EDGE_CURVE('',#14313,#14471,#9700,.T.);
#19265=EDGE_CURVE('',#14472,#14314,#9701,.T.);
#19266=EDGE_CURVE('',#14472,#14471,#4452,.T.);
#19267=EDGE_CURVE('',#13770,#14315,#2794,.T.);
#19268=EDGE_CURVE('',#14316,#13769,#2795,.T.);
#19269=EDGE_CURVE('',#14317,#13771,#2796,.T.);
#19270=EDGE_CURVE('',#13772,#14318,#2797,.T.);
#19271=EDGE_CURVE('',#14319,#13773,#2798,.T.);
#19272=EDGE_CURVE('',#13774,#14320,#2799,.T.);
#19273=EDGE_CURVE('',#14321,#13775,#2800,.T.);
#19274=EDGE_CURVE('',#13776,#14322,#2801,.T.);
#19275=EDGE_CURVE('',#14323,#13777,#2802,.T.);
#19276=EDGE_CURVE('',#13778,#14324,#2803,.T.);
#19277=EDGE_CURVE('',#14325,#13779,#2804,.T.);
#19278=EDGE_CURVE('',#13780,#14326,#2805,.T.);
#19279=EDGE_CURVE('',#14327,#13781,#2806,.T.);
#19280=EDGE_CURVE('',#13782,#14328,#2807,.T.);
#19281=EDGE_CURVE('',#14329,#13785,#2808,.T.);
#19282=EDGE_CURVE('',#13786,#14330,#2809,.T.);
#19283=EDGE_CURVE('',#14331,#13789,#2810,.T.);
#19284=EDGE_CURVE('',#13790,#14332,#2811,.T.);
#19285=EDGE_CURVE('',#14333,#13793,#2812,.T.);
#19286=EDGE_CURVE('',#13794,#14334,#2813,.T.);
#19287=EDGE_CURVE('',#14335,#13797,#2814,.T.);
#19288=EDGE_CURVE('',#13798,#14336,#2815,.T.);
#19289=EDGE_CURVE('',#14337,#13801,#2816,.T.);
#19290=EDGE_CURVE('',#13802,#14338,#2817,.T.);
#19291=EDGE_CURVE('',#14339,#13805,#2818,.T.);
#19292=EDGE_CURVE('',#13806,#14340,#2819,.T.);
#19293=EDGE_CURVE('',#14341,#13809,#2820,.T.);
#19294=EDGE_CURVE('',#13810,#14342,#2821,.T.);
#19295=EDGE_CURVE('',#14343,#13813,#2822,.T.);
#19296=EDGE_CURVE('',#13814,#14344,#2823,.T.);
#19297=EDGE_CURVE('',#14345,#13817,#2824,.T.);
#19298=EDGE_CURVE('',#13818,#14346,#2825,.T.);
#19299=EDGE_CURVE('',#14347,#13821,#2826,.T.);
#19300=EDGE_CURVE('',#13822,#14348,#2827,.T.);
#19301=EDGE_CURVE('',#14349,#13825,#2828,.T.);
#19302=EDGE_CURVE('',#13826,#14350,#2829,.T.);
#19303=EDGE_CURVE('',#14351,#13829,#2830,.T.);
#19304=EDGE_CURVE('',#13830,#14352,#2831,.T.);
#19305=EDGE_CURVE('',#14353,#13833,#2832,.T.);
#19306=EDGE_CURVE('',#13834,#14354,#2833,.T.);
#19307=EDGE_CURVE('',#14355,#13837,#2834,.T.);
#19308=EDGE_CURVE('',#13838,#14356,#2835,.T.);
#19309=EDGE_CURVE('',#14357,#13841,#2836,.T.);
#19310=EDGE_CURVE('',#13842,#14358,#2837,.T.);
#19311=EDGE_CURVE('',#14359,#13845,#2838,.T.);
#19312=EDGE_CURVE('',#13846,#14360,#2839,.T.);
#19313=EDGE_CURVE('',#14361,#13849,#2840,.T.);
#19314=EDGE_CURVE('',#13850,#14362,#2841,.T.);
#19315=EDGE_CURVE('',#14363,#13853,#2842,.T.);
#19316=EDGE_CURVE('',#13854,#14364,#2843,.T.);
#19317=EDGE_CURVE('',#14365,#13857,#2844,.T.);
#19318=EDGE_CURVE('',#13858,#14366,#2845,.T.);
#19319=EDGE_CURVE('',#14367,#13571,#2846,.T.);
#19320=EDGE_CURVE('',#13572,#14368,#2847,.T.);
#19321=EDGE_CURVE('',#14369,#13575,#2848,.T.);
#19322=EDGE_CURVE('',#13576,#14370,#2849,.T.);
#19323=EDGE_CURVE('',#14371,#13579,#2850,.T.);
#19324=EDGE_CURVE('',#13580,#14372,#2851,.T.);
#19325=EDGE_CURVE('',#14373,#13583,#2852,.T.);
#19326=EDGE_CURVE('',#13584,#14374,#2853,.T.);
#19327=EDGE_CURVE('',#14375,#13587,#2854,.T.);
#19328=EDGE_CURVE('',#13588,#14376,#2855,.T.);
#19329=EDGE_CURVE('',#14377,#13591,#2856,.T.);
#19330=EDGE_CURVE('',#13592,#14378,#2857,.T.);
#19331=EDGE_CURVE('',#14379,#13595,#2858,.T.);
#19332=EDGE_CURVE('',#13596,#14380,#2859,.T.);
#19333=EDGE_CURVE('',#14381,#13599,#2860,.T.);
#19334=EDGE_CURVE('',#13600,#14382,#2861,.T.);
#19335=EDGE_CURVE('',#14383,#13603,#2862,.T.);
#19336=EDGE_CURVE('',#13604,#14384,#2863,.T.);
#19337=EDGE_CURVE('',#14385,#13607,#2864,.T.);
#19338=EDGE_CURVE('',#13608,#14386,#2865,.T.);
#19339=EDGE_CURVE('',#14387,#13611,#2866,.T.);
#19340=EDGE_CURVE('',#13612,#14388,#2867,.T.);
#19341=EDGE_CURVE('',#14389,#13615,#2868,.T.);
#19342=EDGE_CURVE('',#13616,#14390,#2869,.T.);
#19343=EDGE_CURVE('',#14391,#13619,#2870,.T.);
#19344=EDGE_CURVE('',#13620,#14392,#2871,.T.);
#19345=EDGE_CURVE('',#14393,#13623,#2872,.T.);
#19346=EDGE_CURVE('',#13624,#14394,#2873,.T.);
#19347=EDGE_CURVE('',#14395,#13627,#2874,.T.);
#19348=EDGE_CURVE('',#13628,#14396,#2875,.T.);
#19349=EDGE_CURVE('',#14397,#13631,#2876,.T.);
#19350=EDGE_CURVE('',#13632,#14398,#2877,.T.);
#19351=EDGE_CURVE('',#14399,#13635,#2878,.T.);
#19352=EDGE_CURVE('',#13636,#14400,#2879,.T.);
#19353=EDGE_CURVE('',#14401,#13639,#2880,.T.);
#19354=EDGE_CURVE('',#13640,#14402,#2881,.T.);
#19355=EDGE_CURVE('',#14403,#13643,#2882,.T.);
#19356=EDGE_CURVE('',#13644,#14404,#2883,.T.);
#19357=EDGE_CURVE('',#14405,#13647,#2884,.T.);
#19358=EDGE_CURVE('',#13648,#14406,#2885,.T.);
#19359=EDGE_CURVE('',#14407,#13651,#2886,.T.);
#19360=EDGE_CURVE('',#13652,#14408,#2887,.T.);
#19361=EDGE_CURVE('',#14409,#13655,#2888,.T.);
#19362=EDGE_CURVE('',#13656,#14410,#2889,.T.);
#19363=EDGE_CURVE('',#14411,#13659,#2890,.T.);
#19364=EDGE_CURVE('',#13660,#14412,#2891,.T.);
#19365=EDGE_CURVE('',#14413,#13663,#2892,.T.);
#19366=EDGE_CURVE('',#13664,#14414,#2893,.T.);
#19367=EDGE_CURVE('',#14415,#13667,#2894,.T.);
#19368=EDGE_CURVE('',#13668,#14416,#2895,.T.);
#19369=EDGE_CURVE('',#14417,#13671,#2896,.T.);
#19370=EDGE_CURVE('',#13672,#14418,#2897,.T.);
#19371=EDGE_CURVE('',#14419,#13675,#2898,.T.);
#19372=EDGE_CURVE('',#13676,#14420,#2899,.T.);
#19373=EDGE_CURVE('',#14421,#13679,#2900,.T.);
#19374=EDGE_CURVE('',#13680,#14422,#2901,.T.);
#19375=EDGE_CURVE('',#14423,#13683,#2902,.T.);
#19376=EDGE_CURVE('',#13684,#14424,#2903,.T.);
#19377=EDGE_CURVE('',#14425,#13687,#2904,.T.);
#19378=EDGE_CURVE('',#13688,#14426,#2905,.T.);
#19379=EDGE_CURVE('',#14427,#13691,#2906,.T.);
#19380=EDGE_CURVE('',#13692,#14428,#2907,.T.);
#19381=EDGE_CURVE('',#14429,#13695,#2908,.T.);
#19382=EDGE_CURVE('',#13696,#14430,#2909,.T.);
#19383=EDGE_CURVE('',#14431,#13699,#2910,.T.);
#19384=EDGE_CURVE('',#13700,#14432,#2911,.T.);
#19385=EDGE_CURVE('',#14433,#13703,#2912,.T.);
#19386=EDGE_CURVE('',#13704,#14434,#2913,.T.);
#19387=EDGE_CURVE('',#14435,#13707,#2914,.T.);
#19388=EDGE_CURVE('',#13708,#14436,#2915,.T.);
#19389=EDGE_CURVE('',#14437,#13711,#2916,.T.);
#19390=EDGE_CURVE('',#13712,#14438,#2917,.T.);
#19391=EDGE_CURVE('',#14439,#13715,#2918,.T.);
#19392=EDGE_CURVE('',#13716,#14440,#2919,.T.);
#19393=EDGE_CURVE('',#14441,#13719,#2920,.T.);
#19394=EDGE_CURVE('',#13720,#14442,#2921,.T.);
#19395=EDGE_CURVE('',#13768,#14443,#2922,.T.);
#19396=EDGE_CURVE('',#14444,#13767,#2923,.T.);
#19397=EDGE_CURVE('',#13766,#14445,#2924,.T.);
#19398=EDGE_CURVE('',#14446,#13765,#2925,.T.);
#19399=EDGE_CURVE('',#13764,#14447,#2926,.T.);
#19400=EDGE_CURVE('',#14448,#13763,#2927,.T.);
#19401=EDGE_CURVE('',#13762,#14449,#2928,.T.);
#19402=EDGE_CURVE('',#14450,#13761,#2929,.T.);
#19403=EDGE_CURVE('',#13760,#14451,#2930,.T.);
#19404=EDGE_CURVE('',#14452,#13759,#2931,.T.);
#19405=EDGE_CURVE('',#13758,#14453,#2932,.T.);
#19406=EDGE_CURVE('',#14454,#13757,#2933,.T.);
#19407=EDGE_CURVE('',#13756,#14455,#2934,.T.);
#19408=EDGE_CURVE('',#14456,#13755,#2935,.T.);
#19409=EDGE_CURVE('',#13754,#14457,#2936,.T.);
#19410=EDGE_CURVE('',#14458,#13753,#2937,.T.);
#19411=EDGE_CURVE('',#13752,#14459,#2938,.T.);
#19412=EDGE_CURVE('',#14460,#13751,#2939,.T.);
#19413=EDGE_CURVE('',#13748,#14461,#2940,.T.);
#19414=EDGE_CURVE('',#14462,#13747,#2941,.T.);
#19415=EDGE_CURVE('',#13744,#14463,#2942,.T.);
#19416=EDGE_CURVE('',#14464,#13743,#2943,.T.);
#19417=EDGE_CURVE('',#13740,#14465,#2944,.T.);
#19418=EDGE_CURVE('',#14466,#13739,#2945,.T.);
#19419=EDGE_CURVE('',#13736,#14467,#2946,.T.);
#19420=EDGE_CURVE('',#14468,#13735,#2947,.T.);
#19421=EDGE_CURVE('',#13732,#14469,#2948,.T.);
#19422=EDGE_CURVE('',#14470,#13731,#2949,.T.);
#19423=EDGE_CURVE('',#14471,#13723,#2950,.T.);
#19424=EDGE_CURVE('',#13724,#14472,#2951,.T.);
#19425=EDGE_CURVE('',#13863,#14473,#2952,.T.);
#19426=EDGE_CURVE('',#14474,#13862,#2953,.T.);
#19427=EDGE_CURVE('',#14474,#14473,#4453,.T.);
#19428=EDGE_CURVE('',#14473,#14475,#9702,.T.);
#19429=EDGE_CURVE('',#14476,#14474,#9703,.T.);
#19430=EDGE_CURVE('',#14476,#14475,#4454,.T.);
#19431=EDGE_CURVE('',#14475,#13727,#2954,.T.);
#19432=EDGE_CURVE('',#13728,#14476,#2955,.T.);
#19433=EDGE_CURVE('',#14477,#14478,#9704,.T.);
#19434=EDGE_CURVE('',#14478,#14479,#9705,.T.);
#19435=EDGE_CURVE('',#14479,#14480,#9706,.T.);
#19436=EDGE_CURVE('',#14480,#14481,#9707,.T.);
#19437=EDGE_CURVE('',#14481,#14482,#9708,.T.);
#19438=EDGE_CURVE('',#14482,#14477,#9709,.T.);
#19439=EDGE_CURVE('',#14478,#13563,#9710,.T.);
#19440=EDGE_CURVE('',#14479,#13562,#9711,.T.);
#19441=EDGE_CURVE('',#14480,#13561,#9712,.T.);
#19442=EDGE_CURVE('',#14481,#13559,#9713,.T.);
#19443=EDGE_CURVE('',#14482,#13565,#9714,.T.);
#19444=EDGE_CURVE('',#14477,#13564,#9715,.T.);
#19445=EDGE_CURVE('',#13496,#13378,#3351,.T.);
#19446=EDGE_CURVE('',#13376,#13494,#9716,.T.);
#19447=EDGE_CURVE('',#13860,#13729,#9717,.T.);
#19448=EDGE_CURVE('',#14150,#13730,#9718,.T.);
#19449=EDGE_CURVE('',#13865,#13725,#9719,.T.);
#19450=EDGE_CURVE('',#13864,#13726,#9720,.T.);
#19451=EDGE_CURVE('',#14147,#13733,#9721,.T.);
#19452=EDGE_CURVE('',#14146,#13734,#9722,.T.);
#19453=EDGE_CURVE('',#14143,#13737,#9723,.T.);
#19454=EDGE_CURVE('',#14142,#13738,#9724,.T.);
#19455=EDGE_CURVE('',#14139,#13741,#9725,.T.);
#19456=EDGE_CURVE('',#14138,#13742,#9726,.T.);
#19457=EDGE_CURVE('',#14135,#13745,#9727,.T.);
#19458=EDGE_CURVE('',#14134,#13746,#9728,.T.);
#19459=EDGE_CURVE('',#14131,#13749,#9729,.T.);
#19460=EDGE_CURVE('',#14130,#13750,#9730,.T.);
#19461=EDGE_CURVE('',#13869,#13721,#9731,.T.);
#19462=EDGE_CURVE('',#13868,#13722,#9732,.T.);
#19463=EDGE_CURVE('',#13873,#13717,#9733,.T.);
#19464=EDGE_CURVE('',#13872,#13718,#9734,.T.);
#19465=EDGE_CURVE('',#13877,#13713,#9735,.T.);
#19466=EDGE_CURVE('',#13876,#13714,#9736,.T.);
#19467=EDGE_CURVE('',#13881,#13709,#9737,.T.);
#19468=EDGE_CURVE('',#13880,#13710,#9738,.T.);
#19469=EDGE_CURVE('',#13885,#13705,#9739,.T.);
#19470=EDGE_CURVE('',#13884,#13706,#9740,.T.);
#19471=EDGE_CURVE('',#13889,#13701,#9741,.T.);
#19472=EDGE_CURVE('',#13888,#13702,#9742,.T.);
#19473=EDGE_CURVE('',#13893,#13697,#9743,.T.);
#19474=EDGE_CURVE('',#13892,#13698,#9744,.T.);
#19475=EDGE_CURVE('',#13897,#13693,#9745,.T.);
#19476=EDGE_CURVE('',#13896,#13694,#9746,.T.);
#19477=EDGE_CURVE('',#13901,#13689,#9747,.T.);
#19478=EDGE_CURVE('',#13900,#13690,#9748,.T.);
#19479=EDGE_CURVE('',#13905,#13685,#9749,.T.);
#19480=EDGE_CURVE('',#13904,#13686,#9750,.T.);
#19481=EDGE_CURVE('',#13909,#13681,#9751,.T.);
#19482=EDGE_CURVE('',#13908,#13682,#9752,.T.);
#19483=EDGE_CURVE('',#13913,#13677,#9753,.T.);
#19484=EDGE_CURVE('',#13912,#13678,#9754,.T.);
#19485=EDGE_CURVE('',#13917,#13673,#9755,.T.);
#19486=EDGE_CURVE('',#13916,#13674,#9756,.T.);
#19487=EDGE_CURVE('',#13921,#13669,#9757,.T.);
#19488=EDGE_CURVE('',#13920,#13670,#9758,.T.);
#19489=EDGE_CURVE('',#13925,#13665,#9759,.T.);
#19490=EDGE_CURVE('',#13924,#13666,#9760,.T.);
#19491=EDGE_CURVE('',#13929,#13661,#9761,.T.);
#19492=EDGE_CURVE('',#13928,#13662,#9762,.T.);
#19493=EDGE_CURVE('',#13933,#13657,#9763,.T.);
#19494=EDGE_CURVE('',#13932,#13658,#9764,.T.);
#19495=EDGE_CURVE('',#13937,#13653,#9765,.T.);
#19496=EDGE_CURVE('',#13936,#13654,#9766,.T.);
#19497=EDGE_CURVE('',#13941,#13649,#9767,.T.);
#19498=EDGE_CURVE('',#13940,#13650,#9768,.T.);
#19499=EDGE_CURVE('',#13945,#13645,#9769,.T.);
#19500=EDGE_CURVE('',#13944,#13646,#9770,.T.);
#19501=EDGE_CURVE('',#13949,#13641,#9771,.T.);
#19502=EDGE_CURVE('',#13948,#13642,#9772,.T.);
#19503=EDGE_CURVE('',#13953,#13637,#9773,.T.);
#19504=EDGE_CURVE('',#13952,#13638,#9774,.T.);
#19505=EDGE_CURVE('',#13957,#13633,#9775,.T.);
#19506=EDGE_CURVE('',#13956,#13634,#9776,.T.);
#19507=EDGE_CURVE('',#13961,#13629,#9777,.T.);
#19508=EDGE_CURVE('',#13960,#13630,#9778,.T.);
#19509=EDGE_CURVE('',#13965,#13625,#9779,.T.);
#19510=EDGE_CURVE('',#13964,#13626,#9780,.T.);
#19511=EDGE_CURVE('',#13969,#13621,#9781,.T.);
#19512=EDGE_CURVE('',#13968,#13622,#9782,.T.);
#19513=EDGE_CURVE('',#13973,#13617,#9783,.T.);
#19514=EDGE_CURVE('',#13972,#13618,#9784,.T.);
#19515=EDGE_CURVE('',#13977,#13613,#9785,.T.);
#19516=EDGE_CURVE('',#13976,#13614,#9786,.T.);
#19517=EDGE_CURVE('',#13981,#13609,#9787,.T.);
#19518=EDGE_CURVE('',#13980,#13610,#9788,.T.);
#19519=EDGE_CURVE('',#13985,#13605,#9789,.T.);
#19520=EDGE_CURVE('',#13984,#13606,#9790,.T.);
#19521=EDGE_CURVE('',#13989,#13601,#9791,.T.);
#19522=EDGE_CURVE('',#13988,#13602,#9792,.T.);
#19523=EDGE_CURVE('',#13993,#13597,#9793,.T.);
#19524=EDGE_CURVE('',#13992,#13598,#9794,.T.);
#19525=EDGE_CURVE('',#13997,#13593,#9795,.T.);
#19526=EDGE_CURVE('',#13996,#13594,#9796,.T.);
#19527=EDGE_CURVE('',#14001,#13589,#9797,.T.);
#19528=EDGE_CURVE('',#14000,#13590,#9798,.T.);
#19529=EDGE_CURVE('',#14005,#13585,#9799,.T.);
#19530=EDGE_CURVE('',#14004,#13586,#9800,.T.);
#19531=EDGE_CURVE('',#14009,#13581,#9801,.T.);
#19532=EDGE_CURVE('',#14008,#13582,#9802,.T.);
#19533=EDGE_CURVE('',#14013,#13577,#9803,.T.);
#19534=EDGE_CURVE('',#14012,#13578,#9804,.T.);
#19535=EDGE_CURVE('',#14017,#13573,#9805,.T.);
#19536=EDGE_CURVE('',#14016,#13574,#9806,.T.);
#19537=EDGE_CURVE('',#14021,#13859,#9807,.T.);
#19538=EDGE_CURVE('',#14020,#13569,#9808,.T.);
#19539=EDGE_CURVE('',#14025,#13855,#9809,.T.);
#19540=EDGE_CURVE('',#14024,#13856,#9810,.T.);
#19541=EDGE_CURVE('',#14029,#13851,#9811,.T.);
#19542=EDGE_CURVE('',#14028,#13852,#9812,.T.);
#19543=EDGE_CURVE('',#14033,#13847,#9813,.T.);
#19544=EDGE_CURVE('',#14032,#13848,#9814,.T.);
#19545=EDGE_CURVE('',#14037,#13843,#9815,.T.);
#19546=EDGE_CURVE('',#14036,#13844,#9816,.T.);
#19547=EDGE_CURVE('',#14041,#13839,#9817,.T.);
#19548=EDGE_CURVE('',#14040,#13840,#9818,.T.);
#19549=EDGE_CURVE('',#14045,#13835,#9819,.T.);
#19550=EDGE_CURVE('',#14044,#13836,#9820,.T.);
#19551=EDGE_CURVE('',#14049,#13831,#9821,.T.);
#19552=EDGE_CURVE('',#14048,#13832,#9822,.T.);
#19553=EDGE_CURVE('',#14053,#13827,#9823,.T.);
#19554=EDGE_CURVE('',#14052,#13828,#9824,.T.);
#19555=EDGE_CURVE('',#14057,#13823,#9825,.T.);
#19556=EDGE_CURVE('',#14056,#13824,#9826,.T.);
#19557=EDGE_CURVE('',#14061,#13819,#9827,.T.);
#19558=EDGE_CURVE('',#14060,#13820,#9828,.T.);
#19559=EDGE_CURVE('',#14065,#13815,#9829,.T.);
#19560=EDGE_CURVE('',#14064,#13816,#9830,.T.);
#19561=EDGE_CURVE('',#14069,#13811,#9831,.T.);
#19562=EDGE_CURVE('',#14068,#13812,#9832,.T.);
#19563=EDGE_CURVE('',#14073,#13807,#9833,.T.);
#19564=EDGE_CURVE('',#14072,#13808,#9834,.T.);
#19565=EDGE_CURVE('',#14077,#13803,#9835,.T.);
#19566=EDGE_CURVE('',#14076,#13804,#9836,.T.);
#19567=EDGE_CURVE('',#14081,#13799,#9837,.T.);
#19568=EDGE_CURVE('',#14080,#13800,#9838,.T.);
#19569=EDGE_CURVE('',#14085,#13795,#9839,.T.);
#19570=EDGE_CURVE('',#14084,#13796,#9840,.T.);
#19571=EDGE_CURVE('',#14089,#13791,#9841,.T.);
#19572=EDGE_CURVE('',#14088,#13792,#9842,.T.);
#19573=EDGE_CURVE('',#14093,#13787,#9843,.T.);
#19574=EDGE_CURVE('',#14092,#13788,#9844,.T.);
#19575=EDGE_CURVE('',#14097,#13783,#9845,.T.);
#19576=EDGE_CURVE('',#14096,#13784,#9846,.T.);
#26429=ORIENTED_EDGE('',*,*,#17909,.F.);
#26430=ORIENTED_EDGE('',*,*,#17910,.F.);
#26431=ORIENTED_EDGE('',*,*,#17911,.T.);
#26432=ORIENTED_EDGE('',*,*,#17912,.T.);
#26433=ORIENTED_EDGE('',*,*,#17911,.F.);
#26434=ORIENTED_EDGE('',*,*,#17913,.F.);
#26435=ORIENTED_EDGE('',*,*,#17914,.F.);
#26436=ORIENTED_EDGE('',*,*,#17915,.F.);
#26437=ORIENTED_EDGE('',*,*,#17916,.F.);
#26438=ORIENTED_EDGE('',*,*,#17909,.T.);
#26439=ORIENTED_EDGE('',*,*,#17917,.F.);
#26440=ORIENTED_EDGE('',*,*,#17918,.F.);
#26441=ORIENTED_EDGE('',*,*,#17919,.F.);
#26442=ORIENTED_EDGE('',*,*,#17915,.T.);
#26443=ORIENTED_EDGE('',*,*,#17920,.F.);
#26444=ORIENTED_EDGE('',*,*,#17921,.F.);
#26445=ORIENTED_EDGE('',*,*,#17922,.F.);
#26446=ORIENTED_EDGE('',*,*,#17918,.T.);
#26447=ORIENTED_EDGE('',*,*,#17923,.F.);
#26448=ORIENTED_EDGE('',*,*,#17924,.F.);
#26449=ORIENTED_EDGE('',*,*,#17925,.F.);
#26450=ORIENTED_EDGE('',*,*,#17921,.T.);
#26451=ORIENTED_EDGE('',*,*,#17926,.F.);
#26452=ORIENTED_EDGE('',*,*,#17927,.F.);
#26453=ORIENTED_EDGE('',*,*,#17928,.F.);
#26454=ORIENTED_EDGE('',*,*,#17924,.T.);
#26455=ORIENTED_EDGE('',*,*,#17929,.F.);
#26456=ORIENTED_EDGE('',*,*,#17930,.F.);
#26457=ORIENTED_EDGE('',*,*,#17931,.F.);
#26458=ORIENTED_EDGE('',*,*,#17927,.T.);
#26459=ORIENTED_EDGE('',*,*,#17932,.F.);
#26460=ORIENTED_EDGE('',*,*,#17933,.F.);
#26461=ORIENTED_EDGE('',*,*,#17934,.F.);
#26462=ORIENTED_EDGE('',*,*,#17930,.T.);
#26463=ORIENTED_EDGE('',*,*,#17935,.F.);
#26464=ORIENTED_EDGE('',*,*,#17936,.F.);
#26465=ORIENTED_EDGE('',*,*,#17937,.F.);
#26466=ORIENTED_EDGE('',*,*,#17933,.T.);
#26467=ORIENTED_EDGE('',*,*,#17938,.F.);
#26468=ORIENTED_EDGE('',*,*,#17939,.F.);
#26469=ORIENTED_EDGE('',*,*,#17940,.F.);
#26470=ORIENTED_EDGE('',*,*,#17936,.T.);
#26471=ORIENTED_EDGE('',*,*,#17941,.F.);
#26472=ORIENTED_EDGE('',*,*,#17942,.F.);
#26473=ORIENTED_EDGE('',*,*,#17943,.F.);
#26474=ORIENTED_EDGE('',*,*,#17939,.T.);
#26475=ORIENTED_EDGE('',*,*,#17944,.F.);
#26476=ORIENTED_EDGE('',*,*,#17945,.F.);
#26477=ORIENTED_EDGE('',*,*,#17946,.F.);
#26478=ORIENTED_EDGE('',*,*,#17942,.T.);
#26479=ORIENTED_EDGE('',*,*,#17947,.F.);
#26480=ORIENTED_EDGE('',*,*,#17948,.F.);
#26481=ORIENTED_EDGE('',*,*,#17949,.F.);
#26482=ORIENTED_EDGE('',*,*,#17945,.T.);
#26483=ORIENTED_EDGE('',*,*,#17950,.F.);
#26484=ORIENTED_EDGE('',*,*,#17951,.F.);
#26485=ORIENTED_EDGE('',*,*,#17952,.F.);
#26486=ORIENTED_EDGE('',*,*,#17948,.T.);
#26487=ORIENTED_EDGE('',*,*,#17953,.F.);
#26488=ORIENTED_EDGE('',*,*,#17954,.F.);
#26489=ORIENTED_EDGE('',*,*,#17955,.F.);
#26490=ORIENTED_EDGE('',*,*,#17951,.T.);
#26491=ORIENTED_EDGE('',*,*,#17956,.F.);
#26492=ORIENTED_EDGE('',*,*,#17957,.F.);
#26493=ORIENTED_EDGE('',*,*,#17958,.F.);
#26494=ORIENTED_EDGE('',*,*,#17954,.T.);
#26495=ORIENTED_EDGE('',*,*,#17959,.F.);
#26496=ORIENTED_EDGE('',*,*,#17960,.F.);
#26497=ORIENTED_EDGE('',*,*,#17961,.F.);
#26498=ORIENTED_EDGE('',*,*,#17957,.T.);
#26499=ORIENTED_EDGE('',*,*,#17962,.F.);
#26500=ORIENTED_EDGE('',*,*,#17963,.F.);
#26501=ORIENTED_EDGE('',*,*,#17964,.F.);
#26502=ORIENTED_EDGE('',*,*,#17960,.T.);
#26503=ORIENTED_EDGE('',*,*,#17965,.F.);
#26504=ORIENTED_EDGE('',*,*,#17966,.F.);
#26505=ORIENTED_EDGE('',*,*,#17967,.F.);
#26506=ORIENTED_EDGE('',*,*,#17963,.T.);
#26507=ORIENTED_EDGE('',*,*,#17968,.F.);
#26508=ORIENTED_EDGE('',*,*,#17969,.F.);
#26509=ORIENTED_EDGE('',*,*,#17970,.F.);
#26510=ORIENTED_EDGE('',*,*,#17966,.T.);
#26511=ORIENTED_EDGE('',*,*,#17971,.F.);
#26512=ORIENTED_EDGE('',*,*,#17972,.F.);
#26513=ORIENTED_EDGE('',*,*,#17973,.F.);
#26514=ORIENTED_EDGE('',*,*,#17969,.T.);
#26515=ORIENTED_EDGE('',*,*,#17974,.F.);
#26516=ORIENTED_EDGE('',*,*,#17975,.F.);
#26517=ORIENTED_EDGE('',*,*,#17976,.F.);
#26518=ORIENTED_EDGE('',*,*,#17972,.T.);
#26519=ORIENTED_EDGE('',*,*,#17977,.F.);
#26520=ORIENTED_EDGE('',*,*,#17978,.F.);
#26521=ORIENTED_EDGE('',*,*,#17979,.F.);
#26522=ORIENTED_EDGE('',*,*,#17975,.T.);
#26523=ORIENTED_EDGE('',*,*,#17980,.F.);
#26524=ORIENTED_EDGE('',*,*,#17981,.F.);
#26525=ORIENTED_EDGE('',*,*,#17982,.F.);
#26526=ORIENTED_EDGE('',*,*,#17978,.T.);
#26527=ORIENTED_EDGE('',*,*,#17983,.F.);
#26528=ORIENTED_EDGE('',*,*,#17984,.F.);
#26529=ORIENTED_EDGE('',*,*,#17985,.F.);
#26530=ORIENTED_EDGE('',*,*,#17981,.T.);
#26531=ORIENTED_EDGE('',*,*,#17986,.F.);
#26532=ORIENTED_EDGE('',*,*,#17987,.F.);
#26533=ORIENTED_EDGE('',*,*,#17988,.F.);
#26534=ORIENTED_EDGE('',*,*,#17984,.T.);
#26535=ORIENTED_EDGE('',*,*,#17989,.F.);
#26536=ORIENTED_EDGE('',*,*,#17990,.F.);
#26537=ORIENTED_EDGE('',*,*,#17991,.F.);
#26538=ORIENTED_EDGE('',*,*,#17987,.T.);
#26539=ORIENTED_EDGE('',*,*,#17992,.F.);
#26540=ORIENTED_EDGE('',*,*,#17993,.F.);
#26541=ORIENTED_EDGE('',*,*,#17994,.F.);
#26542=ORIENTED_EDGE('',*,*,#17990,.T.);
#26543=ORIENTED_EDGE('',*,*,#17995,.F.);
#26544=ORIENTED_EDGE('',*,*,#17996,.F.);
#26545=ORIENTED_EDGE('',*,*,#17997,.T.);
#26546=ORIENTED_EDGE('',*,*,#17998,.F.);
#26547=ORIENTED_EDGE('',*,*,#17999,.F.);
#26548=ORIENTED_EDGE('',*,*,#18000,.F.);
#26549=ORIENTED_EDGE('',*,*,#18001,.F.);
#26550=ORIENTED_EDGE('',*,*,#18002,.F.);
#26551=ORIENTED_EDGE('',*,*,#18003,.F.);
#26552=ORIENTED_EDGE('',*,*,#17999,.T.);
#26553=ORIENTED_EDGE('',*,*,#18004,.T.);
#26554=ORIENTED_EDGE('',*,*,#18005,.F.);
#26555=ORIENTED_EDGE('',*,*,#18006,.F.);
#26556=ORIENTED_EDGE('',*,*,#18002,.T.);
#26557=ORIENTED_EDGE('',*,*,#18007,.T.);
#26558=ORIENTED_EDGE('',*,*,#18008,.F.);
#26559=ORIENTED_EDGE('',*,*,#18009,.F.);
#26560=ORIENTED_EDGE('',*,*,#18005,.T.);
#26561=ORIENTED_EDGE('',*,*,#18010,.T.);
#26562=ORIENTED_EDGE('',*,*,#18011,.F.);
#26563=ORIENTED_EDGE('',*,*,#18012,.F.);
#26564=ORIENTED_EDGE('',*,*,#18008,.T.);
#26565=ORIENTED_EDGE('',*,*,#18013,.T.);
#26566=ORIENTED_EDGE('',*,*,#18014,.F.);
#26567=ORIENTED_EDGE('',*,*,#18015,.F.);
#26568=ORIENTED_EDGE('',*,*,#18011,.T.);
#26569=ORIENTED_EDGE('',*,*,#18016,.T.);
#26570=ORIENTED_EDGE('',*,*,#18017,.F.);
#26571=ORIENTED_EDGE('',*,*,#18018,.F.);
#26572=ORIENTED_EDGE('',*,*,#18014,.T.);
#26573=ORIENTED_EDGE('',*,*,#18019,.T.);
#26574=ORIENTED_EDGE('',*,*,#18020,.F.);
#26575=ORIENTED_EDGE('',*,*,#18021,.F.);
#26576=ORIENTED_EDGE('',*,*,#18017,.T.);
#26577=ORIENTED_EDGE('',*,*,#18022,.T.);
#26578=ORIENTED_EDGE('',*,*,#18023,.F.);
#26579=ORIENTED_EDGE('',*,*,#18024,.F.);
#26580=ORIENTED_EDGE('',*,*,#18020,.T.);
#26581=ORIENTED_EDGE('',*,*,#18025,.T.);
#26582=ORIENTED_EDGE('',*,*,#18026,.F.);
#26583=ORIENTED_EDGE('',*,*,#18027,.F.);
#26584=ORIENTED_EDGE('',*,*,#18023,.T.);
#26585=ORIENTED_EDGE('',*,*,#18028,.T.);
#26586=ORIENTED_EDGE('',*,*,#18029,.F.);
#26587=ORIENTED_EDGE('',*,*,#18030,.F.);
#26588=ORIENTED_EDGE('',*,*,#18026,.T.);
#26589=ORIENTED_EDGE('',*,*,#18031,.T.);
#26590=ORIENTED_EDGE('',*,*,#18032,.F.);
#26591=ORIENTED_EDGE('',*,*,#18033,.F.);
#26592=ORIENTED_EDGE('',*,*,#18029,.T.);
#26593=ORIENTED_EDGE('',*,*,#18034,.T.);
#26594=ORIENTED_EDGE('',*,*,#18035,.F.);
#26595=ORIENTED_EDGE('',*,*,#18036,.F.);
#26596=ORIENTED_EDGE('',*,*,#18032,.T.);
#26597=ORIENTED_EDGE('',*,*,#18037,.T.);
#26598=ORIENTED_EDGE('',*,*,#18038,.F.);
#26599=ORIENTED_EDGE('',*,*,#18039,.F.);
#26600=ORIENTED_EDGE('',*,*,#18035,.T.);
#26601=ORIENTED_EDGE('',*,*,#18040,.T.);
#26602=ORIENTED_EDGE('',*,*,#18041,.F.);
#26603=ORIENTED_EDGE('',*,*,#18042,.F.);
#26604=ORIENTED_EDGE('',*,*,#18038,.T.);
#26605=ORIENTED_EDGE('',*,*,#18043,.T.);
#26606=ORIENTED_EDGE('',*,*,#18044,.F.);
#26607=ORIENTED_EDGE('',*,*,#18045,.F.);
#26608=ORIENTED_EDGE('',*,*,#18041,.T.);
#26609=ORIENTED_EDGE('',*,*,#18046,.T.);
#26610=ORIENTED_EDGE('',*,*,#18047,.F.);
#26611=ORIENTED_EDGE('',*,*,#18048,.F.);
#26612=ORIENTED_EDGE('',*,*,#18044,.T.);
#26613=ORIENTED_EDGE('',*,*,#18049,.T.);
#26614=ORIENTED_EDGE('',*,*,#18050,.F.);
#26615=ORIENTED_EDGE('',*,*,#18051,.F.);
#26616=ORIENTED_EDGE('',*,*,#18047,.T.);
#26617=ORIENTED_EDGE('',*,*,#18052,.T.);
#26618=ORIENTED_EDGE('',*,*,#18053,.F.);
#26619=ORIENTED_EDGE('',*,*,#18054,.F.);
#26620=ORIENTED_EDGE('',*,*,#18050,.T.);
#26621=ORIENTED_EDGE('',*,*,#18055,.T.);
#26622=ORIENTED_EDGE('',*,*,#18056,.F.);
#26623=ORIENTED_EDGE('',*,*,#18057,.F.);
#26624=ORIENTED_EDGE('',*,*,#18053,.T.);
#26625=ORIENTED_EDGE('',*,*,#18058,.T.);
#26626=ORIENTED_EDGE('',*,*,#18059,.F.);
#26627=ORIENTED_EDGE('',*,*,#18060,.F.);
#26628=ORIENTED_EDGE('',*,*,#18056,.T.);
#26629=ORIENTED_EDGE('',*,*,#18061,.T.);
#26630=ORIENTED_EDGE('',*,*,#18062,.F.);
#26631=ORIENTED_EDGE('',*,*,#18063,.F.);
#26632=ORIENTED_EDGE('',*,*,#18059,.T.);
#26633=ORIENTED_EDGE('',*,*,#18064,.T.);
#26634=ORIENTED_EDGE('',*,*,#18065,.F.);
#26635=ORIENTED_EDGE('',*,*,#18066,.F.);
#26636=ORIENTED_EDGE('',*,*,#18062,.T.);
#26637=ORIENTED_EDGE('',*,*,#18067,.T.);
#26638=ORIENTED_EDGE('',*,*,#18068,.F.);
#26639=ORIENTED_EDGE('',*,*,#18069,.F.);
#26640=ORIENTED_EDGE('',*,*,#18065,.T.);
#26641=ORIENTED_EDGE('',*,*,#18070,.T.);
#26642=ORIENTED_EDGE('',*,*,#18071,.F.);
#26643=ORIENTED_EDGE('',*,*,#18072,.F.);
#26644=ORIENTED_EDGE('',*,*,#18068,.T.);
#26645=ORIENTED_EDGE('',*,*,#18073,.T.);
#26646=ORIENTED_EDGE('',*,*,#18074,.F.);
#26647=ORIENTED_EDGE('',*,*,#18075,.F.);
#26648=ORIENTED_EDGE('',*,*,#18071,.T.);
#26649=ORIENTED_EDGE('',*,*,#18076,.T.);
#26650=ORIENTED_EDGE('',*,*,#18077,.F.);
#26651=ORIENTED_EDGE('',*,*,#18078,.F.);
#26652=ORIENTED_EDGE('',*,*,#18074,.T.);
#26653=ORIENTED_EDGE('',*,*,#18079,.T.);
#26654=ORIENTED_EDGE('',*,*,#18080,.F.);
#26655=ORIENTED_EDGE('',*,*,#18081,.F.);
#26656=ORIENTED_EDGE('',*,*,#18077,.T.);
#26657=ORIENTED_EDGE('',*,*,#18082,.T.);
#26658=ORIENTED_EDGE('',*,*,#18083,.F.);
#26659=ORIENTED_EDGE('',*,*,#18084,.F.);
#26660=ORIENTED_EDGE('',*,*,#18080,.T.);
#26661=ORIENTED_EDGE('',*,*,#18085,.T.);
#26662=ORIENTED_EDGE('',*,*,#18086,.F.);
#26663=ORIENTED_EDGE('',*,*,#18087,.F.);
#26664=ORIENTED_EDGE('',*,*,#18083,.T.);
#26665=ORIENTED_EDGE('',*,*,#18088,.T.);
#26666=ORIENTED_EDGE('',*,*,#18086,.T.);
#26667=ORIENTED_EDGE('',*,*,#18089,.T.);
#26668=ORIENTED_EDGE('',*,*,#18090,.F.);
#26669=ORIENTED_EDGE('',*,*,#17996,.T.);
#26670=ORIENTED_EDGE('',*,*,#18091,.F.);
#26671=ORIENTED_EDGE('',*,*,#18092,.T.);
#26672=ORIENTED_EDGE('',*,*,#18093,.T.);
#26673=ORIENTED_EDGE('',*,*,#18094,.T.);
#26674=ORIENTED_EDGE('',*,*,#17993,.T.);
#26675=ORIENTED_EDGE('',*,*,#18095,.F.);
#26676=ORIENTED_EDGE('',*,*,#18093,.F.);
#26677=ORIENTED_EDGE('',*,*,#18096,.F.);
#26678=ORIENTED_EDGE('',*,*,#18097,.T.);
#26679=ORIENTED_EDGE('',*,*,#18098,.T.);
#26680=ORIENTED_EDGE('',*,*,#18099,.T.);
#26681=ORIENTED_EDGE('',*,*,#18100,.F.);
#26682=ORIENTED_EDGE('',*,*,#18101,.T.);
#26683=ORIENTED_EDGE('',*,*,#18102,.T.);
#26684=ORIENTED_EDGE('',*,*,#18103,.T.);
#26685=ORIENTED_EDGE('',*,*,#18104,.F.);
#26686=ORIENTED_EDGE('',*,*,#18105,.T.);
#26687=ORIENTED_EDGE('',*,*,#18106,.T.);
#26688=ORIENTED_EDGE('',*,*,#18107,.T.);
#26689=ORIENTED_EDGE('',*,*,#18108,.F.);
#26690=ORIENTED_EDGE('',*,*,#18109,.T.);
#26691=ORIENTED_EDGE('',*,*,#18110,.T.);
#26692=ORIENTED_EDGE('',*,*,#18111,.T.);
#26693=ORIENTED_EDGE('',*,*,#18112,.F.);
#26694=ORIENTED_EDGE('',*,*,#18113,.T.);
#26695=ORIENTED_EDGE('',*,*,#18114,.T.);
#26696=ORIENTED_EDGE('',*,*,#18115,.T.);
#26697=ORIENTED_EDGE('',*,*,#18116,.F.);
#26698=ORIENTED_EDGE('',*,*,#18117,.T.);
#26699=ORIENTED_EDGE('',*,*,#18118,.T.);
#26700=ORIENTED_EDGE('',*,*,#18119,.T.);
#26701=ORIENTED_EDGE('',*,*,#18120,.F.);
#26702=ORIENTED_EDGE('',*,*,#18121,.T.);
#26703=ORIENTED_EDGE('',*,*,#18122,.T.);
#26704=ORIENTED_EDGE('',*,*,#18123,.T.);
#26705=ORIENTED_EDGE('',*,*,#18124,.F.);
#26706=ORIENTED_EDGE('',*,*,#18125,.T.);
#26707=ORIENTED_EDGE('',*,*,#18126,.T.);
#26708=ORIENTED_EDGE('',*,*,#18127,.T.);
#26709=ORIENTED_EDGE('',*,*,#18128,.F.);
#26710=ORIENTED_EDGE('',*,*,#18129,.T.);
#26711=ORIENTED_EDGE('',*,*,#18130,.T.);
#26712=ORIENTED_EDGE('',*,*,#18131,.T.);
#26713=ORIENTED_EDGE('',*,*,#18132,.F.);
#26714=ORIENTED_EDGE('',*,*,#18133,.T.);
#26715=ORIENTED_EDGE('',*,*,#18134,.T.);
#26716=ORIENTED_EDGE('',*,*,#18135,.T.);
#26717=ORIENTED_EDGE('',*,*,#18136,.F.);
#26718=ORIENTED_EDGE('',*,*,#18137,.T.);
#26719=ORIENTED_EDGE('',*,*,#18138,.T.);
#26720=ORIENTED_EDGE('',*,*,#18139,.T.);
#26721=ORIENTED_EDGE('',*,*,#18140,.F.);
#26722=ORIENTED_EDGE('',*,*,#18141,.T.);
#26723=ORIENTED_EDGE('',*,*,#18142,.T.);
#26724=ORIENTED_EDGE('',*,*,#18143,.T.);
#26725=ORIENTED_EDGE('',*,*,#18144,.F.);
#26726=ORIENTED_EDGE('',*,*,#18145,.T.);
#26727=ORIENTED_EDGE('',*,*,#18146,.T.);
#26728=ORIENTED_EDGE('',*,*,#18147,.T.);
#26729=ORIENTED_EDGE('',*,*,#18148,.F.);
#26730=ORIENTED_EDGE('',*,*,#18149,.T.);
#26731=ORIENTED_EDGE('',*,*,#18150,.T.);
#26732=ORIENTED_EDGE('',*,*,#18151,.T.);
#26733=ORIENTED_EDGE('',*,*,#18152,.F.);
#26734=ORIENTED_EDGE('',*,*,#18153,.T.);
#26735=ORIENTED_EDGE('',*,*,#18154,.T.);
#26736=ORIENTED_EDGE('',*,*,#18155,.T.);
#26737=ORIENTED_EDGE('',*,*,#18156,.F.);
#26738=ORIENTED_EDGE('',*,*,#18157,.F.);
#26739=ORIENTED_EDGE('',*,*,#18158,.F.);
#26740=ORIENTED_EDGE('',*,*,#18159,.F.);
#26741=ORIENTED_EDGE('',*,*,#18160,.F.);
#26742=ORIENTED_EDGE('',*,*,#18161,.F.);
#26743=ORIENTED_EDGE('',*,*,#18162,.F.);
#26744=ORIENTED_EDGE('',*,*,#18163,.F.);
#26745=ORIENTED_EDGE('',*,*,#18164,.T.);
#26746=ORIENTED_EDGE('',*,*,#18165,.T.);
#26747=ORIENTED_EDGE('',*,*,#18164,.F.);
#26748=ORIENTED_EDGE('',*,*,#18166,.F.);
#26749=ORIENTED_EDGE('',*,*,#18167,.T.);
#26750=ORIENTED_EDGE('',*,*,#18168,.T.);
#26751=ORIENTED_EDGE('',*,*,#18167,.F.);
#26752=ORIENTED_EDGE('',*,*,#18169,.F.);
#26753=ORIENTED_EDGE('',*,*,#18170,.F.);
#26754=ORIENTED_EDGE('',*,*,#18171,.F.);
#26755=ORIENTED_EDGE('',*,*,#18172,.F.);
#26756=ORIENTED_EDGE('',*,*,#18173,.F.);
#26757=ORIENTED_EDGE('',*,*,#18174,.F.);
#26758=ORIENTED_EDGE('',*,*,#18175,.F.);
#26759=ORIENTED_EDGE('',*,*,#18176,.F.);
#26760=ORIENTED_EDGE('',*,*,#18177,.F.);
#26761=ORIENTED_EDGE('',*,*,#18178,.F.);
#26762=ORIENTED_EDGE('',*,*,#18179,.F.);
#26763=ORIENTED_EDGE('',*,*,#18180,.F.);
#26764=ORIENTED_EDGE('',*,*,#18181,.F.);
#26765=ORIENTED_EDGE('',*,*,#18182,.F.);
#26766=ORIENTED_EDGE('',*,*,#18183,.F.);
#26767=ORIENTED_EDGE('',*,*,#18184,.F.);
#26768=ORIENTED_EDGE('',*,*,#18185,.F.);
#26769=ORIENTED_EDGE('',*,*,#18186,.F.);
#26770=ORIENTED_EDGE('',*,*,#18187,.F.);
#26771=ORIENTED_EDGE('',*,*,#18188,.F.);
#26772=ORIENTED_EDGE('',*,*,#18189,.F.);
#26773=ORIENTED_EDGE('',*,*,#18190,.F.);
#26774=ORIENTED_EDGE('',*,*,#18191,.F.);
#26775=ORIENTED_EDGE('',*,*,#18192,.F.);
#26776=ORIENTED_EDGE('',*,*,#18193,.F.);
#26777=ORIENTED_EDGE('',*,*,#18194,.F.);
#26778=ORIENTED_EDGE('',*,*,#18195,.F.);
#26779=ORIENTED_EDGE('',*,*,#18196,.F.);
#26780=ORIENTED_EDGE('',*,*,#18197,.F.);
#26781=ORIENTED_EDGE('',*,*,#18198,.F.);
#26782=ORIENTED_EDGE('',*,*,#18199,.F.);
#26783=ORIENTED_EDGE('',*,*,#18200,.F.);
#26784=ORIENTED_EDGE('',*,*,#18201,.F.);
#26785=ORIENTED_EDGE('',*,*,#18202,.F.);
#26786=ORIENTED_EDGE('',*,*,#18203,.F.);
#26787=ORIENTED_EDGE('',*,*,#18204,.F.);
#26788=ORIENTED_EDGE('',*,*,#18205,.F.);
#26789=ORIENTED_EDGE('',*,*,#18206,.F.);
#26790=ORIENTED_EDGE('',*,*,#18207,.F.);
#26791=ORIENTED_EDGE('',*,*,#18208,.F.);
#26792=ORIENTED_EDGE('',*,*,#18209,.F.);
#26793=ORIENTED_EDGE('',*,*,#18210,.F.);
#26794=ORIENTED_EDGE('',*,*,#18211,.F.);
#26795=ORIENTED_EDGE('',*,*,#18212,.F.);
#26796=ORIENTED_EDGE('',*,*,#18213,.F.);
#26797=ORIENTED_EDGE('',*,*,#18214,.F.);
#26798=ORIENTED_EDGE('',*,*,#18215,.F.);
#26799=ORIENTED_EDGE('',*,*,#18216,.F.);
#26800=ORIENTED_EDGE('',*,*,#18217,.F.);
#26801=ORIENTED_EDGE('',*,*,#18218,.F.);
#26802=ORIENTED_EDGE('',*,*,#18219,.F.);
#26803=ORIENTED_EDGE('',*,*,#18220,.F.);
#26804=ORIENTED_EDGE('',*,*,#18221,.F.);
#26805=ORIENTED_EDGE('',*,*,#18222,.F.);
#26806=ORIENTED_EDGE('',*,*,#18223,.F.);
#26807=ORIENTED_EDGE('',*,*,#18224,.F.);
#26808=ORIENTED_EDGE('',*,*,#18225,.F.);
#26809=ORIENTED_EDGE('',*,*,#18226,.F.);
#26810=ORIENTED_EDGE('',*,*,#18227,.F.);
#26811=ORIENTED_EDGE('',*,*,#18228,.F.);
#26812=ORIENTED_EDGE('',*,*,#18229,.F.);
#26813=ORIENTED_EDGE('',*,*,#18230,.F.);
#26814=ORIENTED_EDGE('',*,*,#18231,.F.);
#26815=ORIENTED_EDGE('',*,*,#18232,.F.);
#26816=ORIENTED_EDGE('',*,*,#18233,.F.);
#26817=ORIENTED_EDGE('',*,*,#18234,.F.);
#26818=ORIENTED_EDGE('',*,*,#18235,.F.);
#26819=ORIENTED_EDGE('',*,*,#18236,.F.);
#26820=ORIENTED_EDGE('',*,*,#18237,.F.);
#26821=ORIENTED_EDGE('',*,*,#18238,.F.);
#26822=ORIENTED_EDGE('',*,*,#18239,.F.);
#26823=ORIENTED_EDGE('',*,*,#18240,.F.);
#26824=ORIENTED_EDGE('',*,*,#18241,.F.);
#26825=ORIENTED_EDGE('',*,*,#18242,.F.);
#26826=ORIENTED_EDGE('',*,*,#18243,.F.);
#26827=ORIENTED_EDGE('',*,*,#18244,.F.);
#26828=ORIENTED_EDGE('',*,*,#18245,.F.);
#26829=ORIENTED_EDGE('',*,*,#18246,.F.);
#26830=ORIENTED_EDGE('',*,*,#18247,.F.);
#26831=ORIENTED_EDGE('',*,*,#18248,.F.);
#26832=ORIENTED_EDGE('',*,*,#18249,.F.);
#26833=ORIENTED_EDGE('',*,*,#18250,.F.);
#26834=ORIENTED_EDGE('',*,*,#18251,.F.);
#26835=ORIENTED_EDGE('',*,*,#18252,.F.);
#26836=ORIENTED_EDGE('',*,*,#18253,.F.);
#26837=ORIENTED_EDGE('',*,*,#18254,.F.);
#26838=ORIENTED_EDGE('',*,*,#18255,.F.);
#26839=ORIENTED_EDGE('',*,*,#18256,.F.);
#26840=ORIENTED_EDGE('',*,*,#18257,.F.);
#26841=ORIENTED_EDGE('',*,*,#18258,.F.);
#26842=ORIENTED_EDGE('',*,*,#18259,.F.);
#26843=ORIENTED_EDGE('',*,*,#18260,.F.);
#26844=ORIENTED_EDGE('',*,*,#18261,.F.);
#26845=ORIENTED_EDGE('',*,*,#18262,.F.);
#26846=ORIENTED_EDGE('',*,*,#18263,.F.);
#26847=ORIENTED_EDGE('',*,*,#18264,.F.);
#26848=ORIENTED_EDGE('',*,*,#18265,.F.);
#26849=ORIENTED_EDGE('',*,*,#18266,.F.);
#26850=ORIENTED_EDGE('',*,*,#18267,.F.);
#26851=ORIENTED_EDGE('',*,*,#18268,.F.);
#26852=ORIENTED_EDGE('',*,*,#18269,.F.);
#26853=ORIENTED_EDGE('',*,*,#18270,.F.);
#26854=ORIENTED_EDGE('',*,*,#18271,.F.);
#26855=ORIENTED_EDGE('',*,*,#18272,.F.);
#26856=ORIENTED_EDGE('',*,*,#18273,.F.);
#26857=ORIENTED_EDGE('',*,*,#18274,.F.);
#26858=ORIENTED_EDGE('',*,*,#18275,.F.);
#26859=ORIENTED_EDGE('',*,*,#18276,.F.);
#26860=ORIENTED_EDGE('',*,*,#18277,.F.);
#26861=ORIENTED_EDGE('',*,*,#18278,.F.);
#26862=ORIENTED_EDGE('',*,*,#18279,.F.);
#26863=ORIENTED_EDGE('',*,*,#18280,.F.);
#26864=ORIENTED_EDGE('',*,*,#18281,.F.);
#26865=ORIENTED_EDGE('',*,*,#18282,.F.);
#26866=ORIENTED_EDGE('',*,*,#18283,.F.);
#26867=ORIENTED_EDGE('',*,*,#18284,.F.);
#26868=ORIENTED_EDGE('',*,*,#18285,.F.);
#26869=ORIENTED_EDGE('',*,*,#18286,.F.);
#26870=ORIENTED_EDGE('',*,*,#18287,.F.);
#26871=ORIENTED_EDGE('',*,*,#18288,.F.);
#26872=ORIENTED_EDGE('',*,*,#18289,.F.);
#26873=ORIENTED_EDGE('',*,*,#18290,.F.);
#26874=ORIENTED_EDGE('',*,*,#18291,.F.);
#26875=ORIENTED_EDGE('',*,*,#18292,.F.);
#26876=ORIENTED_EDGE('',*,*,#18293,.F.);
#26877=ORIENTED_EDGE('',*,*,#18294,.F.);
#26878=ORIENTED_EDGE('',*,*,#18295,.F.);
#26879=ORIENTED_EDGE('',*,*,#18296,.F.);
#26880=ORIENTED_EDGE('',*,*,#18297,.F.);
#26881=ORIENTED_EDGE('',*,*,#18298,.F.);
#26882=ORIENTED_EDGE('',*,*,#18299,.F.);
#26883=ORIENTED_EDGE('',*,*,#18300,.F.);
#26884=ORIENTED_EDGE('',*,*,#18301,.F.);
#26885=ORIENTED_EDGE('',*,*,#18302,.F.);
#26886=ORIENTED_EDGE('',*,*,#18303,.F.);
#26887=ORIENTED_EDGE('',*,*,#18304,.F.);
#26888=ORIENTED_EDGE('',*,*,#18305,.F.);
#26889=ORIENTED_EDGE('',*,*,#18306,.F.);
#26890=ORIENTED_EDGE('',*,*,#18307,.F.);
#26891=ORIENTED_EDGE('',*,*,#18308,.F.);
#26892=ORIENTED_EDGE('',*,*,#18309,.F.);
#26893=ORIENTED_EDGE('',*,*,#18310,.F.);
#26894=ORIENTED_EDGE('',*,*,#18311,.F.);
#26895=ORIENTED_EDGE('',*,*,#18312,.F.);
#26896=ORIENTED_EDGE('',*,*,#18313,.F.);
#26897=ORIENTED_EDGE('',*,*,#18314,.F.);
#26898=ORIENTED_EDGE('',*,*,#18315,.F.);
#26899=ORIENTED_EDGE('',*,*,#18316,.F.);
#26900=ORIENTED_EDGE('',*,*,#18317,.F.);
#26901=ORIENTED_EDGE('',*,*,#18318,.F.);
#26902=ORIENTED_EDGE('',*,*,#18319,.F.);
#26903=ORIENTED_EDGE('',*,*,#18320,.F.);
#26904=ORIENTED_EDGE('',*,*,#18321,.F.);
#26905=ORIENTED_EDGE('',*,*,#18322,.F.);
#26906=ORIENTED_EDGE('',*,*,#18323,.F.);
#26907=ORIENTED_EDGE('',*,*,#18324,.F.);
#26908=ORIENTED_EDGE('',*,*,#18325,.F.);
#26909=ORIENTED_EDGE('',*,*,#18326,.F.);
#26910=ORIENTED_EDGE('',*,*,#18327,.F.);
#26911=ORIENTED_EDGE('',*,*,#18328,.F.);
#26912=ORIENTED_EDGE('',*,*,#18329,.F.);
#26913=ORIENTED_EDGE('',*,*,#18330,.F.);
#26914=ORIENTED_EDGE('',*,*,#18331,.F.);
#26915=ORIENTED_EDGE('',*,*,#18332,.F.);
#26916=ORIENTED_EDGE('',*,*,#18333,.F.);
#26917=ORIENTED_EDGE('',*,*,#18334,.F.);
#26918=ORIENTED_EDGE('',*,*,#18335,.F.);
#26919=ORIENTED_EDGE('',*,*,#18336,.F.);
#26920=ORIENTED_EDGE('',*,*,#18337,.F.);
#26921=ORIENTED_EDGE('',*,*,#18338,.F.);
#26922=ORIENTED_EDGE('',*,*,#18339,.F.);
#26923=ORIENTED_EDGE('',*,*,#18340,.F.);
#26924=ORIENTED_EDGE('',*,*,#18341,.F.);
#26925=ORIENTED_EDGE('',*,*,#18342,.F.);
#26926=ORIENTED_EDGE('',*,*,#18343,.F.);
#26927=ORIENTED_EDGE('',*,*,#18344,.F.);
#26928=ORIENTED_EDGE('',*,*,#18345,.F.);
#26929=ORIENTED_EDGE('',*,*,#18346,.F.);
#26930=ORIENTED_EDGE('',*,*,#18347,.F.);
#26931=ORIENTED_EDGE('',*,*,#18348,.F.);
#26932=ORIENTED_EDGE('',*,*,#18349,.F.);
#26933=ORIENTED_EDGE('',*,*,#18350,.F.);
#26934=ORIENTED_EDGE('',*,*,#18351,.F.);
#26935=ORIENTED_EDGE('',*,*,#18352,.F.);
#26936=ORIENTED_EDGE('',*,*,#18155,.F.);
#26937=ORIENTED_EDGE('',*,*,#18353,.F.);
#26938=ORIENTED_EDGE('',*,*,#18354,.F.);
#26939=ORIENTED_EDGE('',*,*,#18355,.F.);
#26940=ORIENTED_EDGE('',*,*,#18151,.F.);
#26941=ORIENTED_EDGE('',*,*,#18356,.F.);
#26942=ORIENTED_EDGE('',*,*,#18357,.F.);
#26943=ORIENTED_EDGE('',*,*,#18358,.F.);
#26944=ORIENTED_EDGE('',*,*,#18147,.F.);
#26945=ORIENTED_EDGE('',*,*,#18359,.F.);
#26946=ORIENTED_EDGE('',*,*,#18360,.F.);
#26947=ORIENTED_EDGE('',*,*,#18361,.F.);
#26948=ORIENTED_EDGE('',*,*,#18143,.F.);
#26949=ORIENTED_EDGE('',*,*,#18362,.F.);
#26950=ORIENTED_EDGE('',*,*,#18363,.F.);
#26951=ORIENTED_EDGE('',*,*,#18364,.F.);
#26952=ORIENTED_EDGE('',*,*,#18139,.F.);
#26953=ORIENTED_EDGE('',*,*,#18365,.F.);
#26954=ORIENTED_EDGE('',*,*,#18366,.F.);
#26955=ORIENTED_EDGE('',*,*,#18367,.F.);
#26956=ORIENTED_EDGE('',*,*,#18135,.F.);
#26957=ORIENTED_EDGE('',*,*,#18368,.F.);
#26958=ORIENTED_EDGE('',*,*,#18369,.F.);
#26959=ORIENTED_EDGE('',*,*,#18370,.F.);
#26960=ORIENTED_EDGE('',*,*,#18131,.F.);
#26961=ORIENTED_EDGE('',*,*,#18371,.F.);
#26962=ORIENTED_EDGE('',*,*,#18372,.F.);
#26963=ORIENTED_EDGE('',*,*,#18373,.F.);
#26964=ORIENTED_EDGE('',*,*,#18127,.F.);
#26965=ORIENTED_EDGE('',*,*,#18374,.F.);
#26966=ORIENTED_EDGE('',*,*,#18375,.F.);
#26967=ORIENTED_EDGE('',*,*,#18376,.F.);
#26968=ORIENTED_EDGE('',*,*,#18123,.F.);
#26969=ORIENTED_EDGE('',*,*,#18377,.F.);
#26970=ORIENTED_EDGE('',*,*,#18378,.F.);
#26971=ORIENTED_EDGE('',*,*,#18379,.F.);
#26972=ORIENTED_EDGE('',*,*,#18099,.F.);
#26973=ORIENTED_EDGE('',*,*,#18380,.F.);
#26974=ORIENTED_EDGE('',*,*,#18381,.F.);
#26975=ORIENTED_EDGE('',*,*,#18382,.F.);
#26976=ORIENTED_EDGE('',*,*,#18103,.F.);
#26977=ORIENTED_EDGE('',*,*,#18383,.F.);
#26978=ORIENTED_EDGE('',*,*,#18384,.F.);
#26979=ORIENTED_EDGE('',*,*,#18385,.F.);
#26980=ORIENTED_EDGE('',*,*,#18107,.F.);
#26981=ORIENTED_EDGE('',*,*,#18386,.F.);
#26982=ORIENTED_EDGE('',*,*,#18387,.F.);
#26983=ORIENTED_EDGE('',*,*,#18388,.F.);
#26984=ORIENTED_EDGE('',*,*,#18111,.F.);
#26985=ORIENTED_EDGE('',*,*,#18389,.F.);
#26986=ORIENTED_EDGE('',*,*,#18390,.F.);
#26987=ORIENTED_EDGE('',*,*,#18391,.F.);
#26988=ORIENTED_EDGE('',*,*,#18115,.F.);
#26989=ORIENTED_EDGE('',*,*,#18392,.F.);
#26990=ORIENTED_EDGE('',*,*,#18393,.F.);
#26991=ORIENTED_EDGE('',*,*,#18394,.F.);
#26992=ORIENTED_EDGE('',*,*,#18119,.F.);
#26993=ORIENTED_EDGE('',*,*,#18395,.F.);
#26994=ORIENTED_EDGE('',*,*,#18396,.F.);
#26995=ORIENTED_EDGE('',*,*,#18397,.F.);
#26996=ORIENTED_EDGE('',*,*,#18398,.F.);
#26997=ORIENTED_EDGE('',*,*,#18399,.F.);
#26998=ORIENTED_EDGE('',*,*,#18400,.F.);
#26999=ORIENTED_EDGE('',*,*,#18401,.F.);
#27000=ORIENTED_EDGE('',*,*,#18402,.F.);
#27001=ORIENTED_EDGE('',*,*,#18403,.F.);
#27002=ORIENTED_EDGE('',*,*,#18404,.F.);
#27003=ORIENTED_EDGE('',*,*,#18405,.F.);
#27004=ORIENTED_EDGE('',*,*,#18406,.F.);
#27005=ORIENTED_EDGE('',*,*,#18407,.F.);
#27006=ORIENTED_EDGE('',*,*,#18408,.F.);
#27007=ORIENTED_EDGE('',*,*,#18409,.F.);
#27008=ORIENTED_EDGE('',*,*,#18410,.F.);
#27009=ORIENTED_EDGE('',*,*,#18411,.F.);
#27010=ORIENTED_EDGE('',*,*,#18412,.F.);
#27011=ORIENTED_EDGE('',*,*,#18413,.F.);
#27012=ORIENTED_EDGE('',*,*,#18414,.F.);
#27013=ORIENTED_EDGE('',*,*,#18415,.F.);
#27014=ORIENTED_EDGE('',*,*,#18416,.F.);
#27015=ORIENTED_EDGE('',*,*,#18417,.F.);
#27016=ORIENTED_EDGE('',*,*,#18418,.F.);
#27017=ORIENTED_EDGE('',*,*,#18419,.F.);
#27018=ORIENTED_EDGE('',*,*,#18420,.F.);
#27019=ORIENTED_EDGE('',*,*,#18421,.F.);
#27020=ORIENTED_EDGE('',*,*,#18422,.F.);
#27021=ORIENTED_EDGE('',*,*,#18423,.F.);
#27022=ORIENTED_EDGE('',*,*,#18424,.F.);
#27023=ORIENTED_EDGE('',*,*,#18425,.F.);
#27024=ORIENTED_EDGE('',*,*,#18426,.F.);
#27025=ORIENTED_EDGE('',*,*,#18427,.F.);
#27026=ORIENTED_EDGE('',*,*,#18428,.F.);
#27027=ORIENTED_EDGE('',*,*,#18429,.F.);
#27028=ORIENTED_EDGE('',*,*,#18430,.F.);
#27029=ORIENTED_EDGE('',*,*,#18431,.F.);
#27030=ORIENTED_EDGE('',*,*,#18432,.F.);
#27031=ORIENTED_EDGE('',*,*,#18433,.F.);
#27032=ORIENTED_EDGE('',*,*,#18434,.F.);
#27033=ORIENTED_EDGE('',*,*,#18435,.F.);
#27034=ORIENTED_EDGE('',*,*,#18436,.F.);
#27035=ORIENTED_EDGE('',*,*,#18437,.F.);
#27036=ORIENTED_EDGE('',*,*,#18438,.F.);
#27037=ORIENTED_EDGE('',*,*,#18439,.F.);
#27038=ORIENTED_EDGE('',*,*,#18440,.F.);
#27039=ORIENTED_EDGE('',*,*,#18441,.F.);
#27040=ORIENTED_EDGE('',*,*,#18442,.F.);
#27041=ORIENTED_EDGE('',*,*,#18443,.F.);
#27042=ORIENTED_EDGE('',*,*,#18444,.F.);
#27043=ORIENTED_EDGE('',*,*,#18445,.F.);
#27044=ORIENTED_EDGE('',*,*,#18446,.F.);
#27045=ORIENTED_EDGE('',*,*,#18447,.F.);
#27046=ORIENTED_EDGE('',*,*,#18448,.F.);
#27047=ORIENTED_EDGE('',*,*,#18449,.F.);
#27048=ORIENTED_EDGE('',*,*,#18450,.F.);
#27049=ORIENTED_EDGE('',*,*,#18451,.F.);
#27050=ORIENTED_EDGE('',*,*,#18452,.F.);
#27051=ORIENTED_EDGE('',*,*,#18453,.F.);
#27052=ORIENTED_EDGE('',*,*,#18454,.F.);
#27053=ORIENTED_EDGE('',*,*,#18455,.F.);
#27054=ORIENTED_EDGE('',*,*,#18456,.F.);
#27055=ORIENTED_EDGE('',*,*,#18457,.F.);
#27056=ORIENTED_EDGE('',*,*,#18458,.F.);
#27057=ORIENTED_EDGE('',*,*,#18459,.F.);
#27058=ORIENTED_EDGE('',*,*,#18460,.F.);
#27059=ORIENTED_EDGE('',*,*,#18461,.F.);
#27060=ORIENTED_EDGE('',*,*,#18462,.F.);
#27061=ORIENTED_EDGE('',*,*,#18463,.F.);
#27062=ORIENTED_EDGE('',*,*,#18464,.F.);
#27063=ORIENTED_EDGE('',*,*,#18465,.F.);
#27064=ORIENTED_EDGE('',*,*,#18466,.F.);
#27065=ORIENTED_EDGE('',*,*,#18467,.F.);
#27066=ORIENTED_EDGE('',*,*,#18468,.F.);
#27067=ORIENTED_EDGE('',*,*,#18469,.F.);
#27068=ORIENTED_EDGE('',*,*,#18470,.F.);
#27069=ORIENTED_EDGE('',*,*,#18471,.F.);
#27070=ORIENTED_EDGE('',*,*,#18472,.F.);
#27071=ORIENTED_EDGE('',*,*,#18473,.F.);
#27072=ORIENTED_EDGE('',*,*,#18474,.F.);
#27073=ORIENTED_EDGE('',*,*,#18475,.T.);
#27074=ORIENTED_EDGE('',*,*,#18166,.T.);
#27075=ORIENTED_EDGE('',*,*,#18475,.F.);
#27076=ORIENTED_EDGE('',*,*,#18476,.F.);
#27077=ORIENTED_EDGE('',*,*,#18477,.F.);
#27078=ORIENTED_EDGE('',*,*,#18478,.T.);
#27079=ORIENTED_EDGE('',*,*,#18479,.F.);
#27080=ORIENTED_EDGE('',*,*,#18480,.F.);
#27081=ORIENTED_EDGE('',*,*,#18481,.F.);
#27082=ORIENTED_EDGE('',*,*,#18482,.T.);
#27083=ORIENTED_EDGE('',*,*,#18483,.F.);
#27084=ORIENTED_EDGE('',*,*,#18484,.F.);
#27085=ORIENTED_EDGE('',*,*,#18485,.F.);
#27086=ORIENTED_EDGE('',*,*,#18486,.T.);
#27087=ORIENTED_EDGE('',*,*,#18487,.F.);
#27088=ORIENTED_EDGE('',*,*,#18488,.F.);
#27089=ORIENTED_EDGE('',*,*,#18489,.F.);
#27090=ORIENTED_EDGE('',*,*,#18490,.T.);
#27091=ORIENTED_EDGE('',*,*,#18491,.F.);
#27092=ORIENTED_EDGE('',*,*,#18492,.F.);
#27093=ORIENTED_EDGE('',*,*,#18493,.F.);
#27094=ORIENTED_EDGE('',*,*,#18494,.T.);
#27095=ORIENTED_EDGE('',*,*,#18495,.F.);
#27096=ORIENTED_EDGE('',*,*,#18496,.F.);
#27097=ORIENTED_EDGE('',*,*,#18497,.F.);
#27098=ORIENTED_EDGE('',*,*,#18498,.T.);
#27099=ORIENTED_EDGE('',*,*,#18499,.F.);
#27100=ORIENTED_EDGE('',*,*,#18500,.F.);
#27101=ORIENTED_EDGE('',*,*,#18501,.F.);
#27102=ORIENTED_EDGE('',*,*,#18502,.T.);
#27103=ORIENTED_EDGE('',*,*,#18503,.F.);
#27104=ORIENTED_EDGE('',*,*,#18504,.F.);
#27105=ORIENTED_EDGE('',*,*,#18505,.F.);
#27106=ORIENTED_EDGE('',*,*,#18506,.T.);
#27107=ORIENTED_EDGE('',*,*,#18507,.F.);
#27108=ORIENTED_EDGE('',*,*,#18508,.F.);
#27109=ORIENTED_EDGE('',*,*,#18509,.F.);
#27110=ORIENTED_EDGE('',*,*,#18510,.T.);
#27111=ORIENTED_EDGE('',*,*,#18511,.F.);
#27112=ORIENTED_EDGE('',*,*,#18512,.F.);
#27113=ORIENTED_EDGE('',*,*,#18513,.F.);
#27114=ORIENTED_EDGE('',*,*,#18514,.T.);
#27115=ORIENTED_EDGE('',*,*,#18515,.F.);
#27116=ORIENTED_EDGE('',*,*,#18516,.F.);
#27117=ORIENTED_EDGE('',*,*,#18517,.F.);
#27118=ORIENTED_EDGE('',*,*,#18518,.T.);
#27119=ORIENTED_EDGE('',*,*,#18519,.F.);
#27120=ORIENTED_EDGE('',*,*,#18520,.F.);
#27121=ORIENTED_EDGE('',*,*,#18521,.F.);
#27122=ORIENTED_EDGE('',*,*,#18522,.T.);
#27123=ORIENTED_EDGE('',*,*,#18523,.F.);
#27124=ORIENTED_EDGE('',*,*,#18524,.F.);
#27125=ORIENTED_EDGE('',*,*,#18525,.F.);
#27126=ORIENTED_EDGE('',*,*,#18526,.T.);
#27127=ORIENTED_EDGE('',*,*,#18527,.F.);
#27128=ORIENTED_EDGE('',*,*,#18528,.F.);
#27129=ORIENTED_EDGE('',*,*,#18529,.F.);
#27130=ORIENTED_EDGE('',*,*,#18530,.T.);
#27131=ORIENTED_EDGE('',*,*,#18531,.F.);
#27132=ORIENTED_EDGE('',*,*,#18532,.F.);
#27133=ORIENTED_EDGE('',*,*,#18533,.F.);
#27134=ORIENTED_EDGE('',*,*,#18534,.T.);
#27135=ORIENTED_EDGE('',*,*,#18535,.F.);
#27136=ORIENTED_EDGE('',*,*,#18536,.F.);
#27137=ORIENTED_EDGE('',*,*,#18537,.F.);
#27138=ORIENTED_EDGE('',*,*,#18538,.T.);
#27139=ORIENTED_EDGE('',*,*,#18539,.F.);
#27140=ORIENTED_EDGE('',*,*,#18540,.F.);
#27141=ORIENTED_EDGE('',*,*,#18541,.F.);
#27142=ORIENTED_EDGE('',*,*,#18542,.T.);
#27143=ORIENTED_EDGE('',*,*,#18543,.F.);
#27144=ORIENTED_EDGE('',*,*,#18544,.F.);
#27145=ORIENTED_EDGE('',*,*,#18545,.F.);
#27146=ORIENTED_EDGE('',*,*,#18546,.T.);
#27147=ORIENTED_EDGE('',*,*,#18547,.F.);
#27148=ORIENTED_EDGE('',*,*,#18548,.F.);
#27149=ORIENTED_EDGE('',*,*,#18549,.F.);
#27150=ORIENTED_EDGE('',*,*,#18550,.T.);
#27151=ORIENTED_EDGE('',*,*,#18551,.F.);
#27152=ORIENTED_EDGE('',*,*,#18552,.F.);
#27153=ORIENTED_EDGE('',*,*,#18553,.F.);
#27154=ORIENTED_EDGE('',*,*,#18554,.T.);
#27155=ORIENTED_EDGE('',*,*,#18555,.F.);
#27156=ORIENTED_EDGE('',*,*,#18556,.F.);
#27157=ORIENTED_EDGE('',*,*,#18557,.F.);
#27158=ORIENTED_EDGE('',*,*,#18558,.T.);
#27159=ORIENTED_EDGE('',*,*,#18559,.F.);
#27160=ORIENTED_EDGE('',*,*,#18560,.F.);
#27161=ORIENTED_EDGE('',*,*,#18561,.F.);
#27162=ORIENTED_EDGE('',*,*,#18562,.T.);
#27163=ORIENTED_EDGE('',*,*,#18563,.F.);
#27164=ORIENTED_EDGE('',*,*,#18564,.F.);
#27165=ORIENTED_EDGE('',*,*,#18565,.F.);
#27166=ORIENTED_EDGE('',*,*,#18566,.T.);
#27167=ORIENTED_EDGE('',*,*,#18567,.F.);
#27168=ORIENTED_EDGE('',*,*,#18568,.F.);
#27169=ORIENTED_EDGE('',*,*,#18569,.F.);
#27170=ORIENTED_EDGE('',*,*,#18570,.T.);
#27171=ORIENTED_EDGE('',*,*,#18571,.F.);
#27172=ORIENTED_EDGE('',*,*,#18572,.F.);
#27173=ORIENTED_EDGE('',*,*,#18573,.F.);
#27174=ORIENTED_EDGE('',*,*,#18574,.T.);
#27175=ORIENTED_EDGE('',*,*,#18575,.F.);
#27176=ORIENTED_EDGE('',*,*,#18576,.F.);
#27177=ORIENTED_EDGE('',*,*,#18577,.F.);
#27178=ORIENTED_EDGE('',*,*,#18578,.T.);
#27179=ORIENTED_EDGE('',*,*,#18579,.F.);
#27180=ORIENTED_EDGE('',*,*,#18580,.F.);
#27181=ORIENTED_EDGE('',*,*,#18581,.F.);
#27182=ORIENTED_EDGE('',*,*,#18582,.T.);
#27183=ORIENTED_EDGE('',*,*,#18583,.F.);
#27184=ORIENTED_EDGE('',*,*,#18584,.F.);
#27185=ORIENTED_EDGE('',*,*,#18585,.F.);
#27186=ORIENTED_EDGE('',*,*,#18586,.T.);
#27187=ORIENTED_EDGE('',*,*,#18587,.F.);
#27188=ORIENTED_EDGE('',*,*,#18588,.F.);
#27189=ORIENTED_EDGE('',*,*,#18589,.F.);
#27190=ORIENTED_EDGE('',*,*,#18590,.T.);
#27191=ORIENTED_EDGE('',*,*,#18591,.F.);
#27192=ORIENTED_EDGE('',*,*,#18592,.F.);
#27193=ORIENTED_EDGE('',*,*,#18593,.F.);
#27194=ORIENTED_EDGE('',*,*,#18594,.T.);
#27195=ORIENTED_EDGE('',*,*,#18595,.F.);
#27196=ORIENTED_EDGE('',*,*,#18596,.F.);
#27197=ORIENTED_EDGE('',*,*,#18597,.F.);
#27198=ORIENTED_EDGE('',*,*,#18598,.T.);
#27199=ORIENTED_EDGE('',*,*,#18599,.F.);
#27200=ORIENTED_EDGE('',*,*,#18600,.F.);
#27201=ORIENTED_EDGE('',*,*,#18601,.F.);
#27202=ORIENTED_EDGE('',*,*,#18602,.T.);
#27203=ORIENTED_EDGE('',*,*,#18603,.F.);
#27204=ORIENTED_EDGE('',*,*,#18604,.F.);
#27205=ORIENTED_EDGE('',*,*,#18605,.F.);
#27206=ORIENTED_EDGE('',*,*,#18606,.T.);
#27207=ORIENTED_EDGE('',*,*,#18607,.F.);
#27208=ORIENTED_EDGE('',*,*,#18608,.F.);
#27209=ORIENTED_EDGE('',*,*,#18609,.F.);
#27210=ORIENTED_EDGE('',*,*,#18610,.T.);
#27211=ORIENTED_EDGE('',*,*,#18611,.F.);
#27212=ORIENTED_EDGE('',*,*,#18612,.F.);
#27213=ORIENTED_EDGE('',*,*,#18613,.F.);
#27214=ORIENTED_EDGE('',*,*,#18614,.T.);
#27215=ORIENTED_EDGE('',*,*,#18615,.F.);
#27216=ORIENTED_EDGE('',*,*,#18616,.F.);
#27217=ORIENTED_EDGE('',*,*,#18617,.F.);
#27218=ORIENTED_EDGE('',*,*,#18618,.T.);
#27219=ORIENTED_EDGE('',*,*,#18619,.F.);
#27220=ORIENTED_EDGE('',*,*,#18620,.F.);
#27221=ORIENTED_EDGE('',*,*,#18621,.F.);
#27222=ORIENTED_EDGE('',*,*,#18622,.T.);
#27223=ORIENTED_EDGE('',*,*,#18623,.F.);
#27224=ORIENTED_EDGE('',*,*,#18624,.F.);
#27225=ORIENTED_EDGE('',*,*,#18625,.F.);
#27226=ORIENTED_EDGE('',*,*,#18626,.T.);
#27227=ORIENTED_EDGE('',*,*,#18627,.F.);
#27228=ORIENTED_EDGE('',*,*,#18628,.F.);
#27229=ORIENTED_EDGE('',*,*,#18629,.F.);
#27230=ORIENTED_EDGE('',*,*,#18630,.T.);
#27231=ORIENTED_EDGE('',*,*,#18631,.F.);
#27232=ORIENTED_EDGE('',*,*,#18632,.F.);
#27233=ORIENTED_EDGE('',*,*,#18633,.F.);
#27234=ORIENTED_EDGE('',*,*,#18634,.T.);
#27235=ORIENTED_EDGE('',*,*,#18635,.F.);
#27236=ORIENTED_EDGE('',*,*,#18636,.F.);
#27237=ORIENTED_EDGE('',*,*,#18637,.F.);
#27238=ORIENTED_EDGE('',*,*,#18638,.T.);
#27239=ORIENTED_EDGE('',*,*,#18639,.F.);
#27240=ORIENTED_EDGE('',*,*,#18640,.F.);
#27241=ORIENTED_EDGE('',*,*,#18641,.F.);
#27242=ORIENTED_EDGE('',*,*,#18642,.T.);
#27243=ORIENTED_EDGE('',*,*,#18643,.F.);
#27244=ORIENTED_EDGE('',*,*,#18644,.F.);
#27245=ORIENTED_EDGE('',*,*,#18645,.F.);
#27246=ORIENTED_EDGE('',*,*,#18646,.T.);
#27247=ORIENTED_EDGE('',*,*,#18647,.F.);
#27248=ORIENTED_EDGE('',*,*,#18648,.F.);
#27249=ORIENTED_EDGE('',*,*,#18649,.F.);
#27250=ORIENTED_EDGE('',*,*,#18650,.T.);
#27251=ORIENTED_EDGE('',*,*,#18651,.F.);
#27252=ORIENTED_EDGE('',*,*,#18652,.F.);
#27253=ORIENTED_EDGE('',*,*,#18653,.F.);
#27254=ORIENTED_EDGE('',*,*,#18654,.T.);
#27255=ORIENTED_EDGE('',*,*,#18655,.F.);
#27256=ORIENTED_EDGE('',*,*,#18656,.F.);
#27257=ORIENTED_EDGE('',*,*,#18657,.F.);
#27258=ORIENTED_EDGE('',*,*,#18658,.T.);
#27259=ORIENTED_EDGE('',*,*,#18659,.F.);
#27260=ORIENTED_EDGE('',*,*,#18660,.F.);
#27261=ORIENTED_EDGE('',*,*,#18661,.F.);
#27262=ORIENTED_EDGE('',*,*,#18662,.T.);
#27263=ORIENTED_EDGE('',*,*,#18663,.F.);
#27264=ORIENTED_EDGE('',*,*,#18664,.F.);
#27265=ORIENTED_EDGE('',*,*,#18665,.F.);
#27266=ORIENTED_EDGE('',*,*,#18666,.T.);
#27267=ORIENTED_EDGE('',*,*,#18667,.F.);
#27268=ORIENTED_EDGE('',*,*,#18668,.F.);
#27269=ORIENTED_EDGE('',*,*,#18669,.F.);
#27270=ORIENTED_EDGE('',*,*,#18670,.T.);
#27271=ORIENTED_EDGE('',*,*,#18671,.F.);
#27272=ORIENTED_EDGE('',*,*,#18672,.F.);
#27273=ORIENTED_EDGE('',*,*,#18673,.F.);
#27274=ORIENTED_EDGE('',*,*,#18674,.T.);
#27275=ORIENTED_EDGE('',*,*,#18675,.F.);
#27276=ORIENTED_EDGE('',*,*,#18676,.F.);
#27277=ORIENTED_EDGE('',*,*,#18677,.F.);
#27278=ORIENTED_EDGE('',*,*,#18678,.T.);
#27279=ORIENTED_EDGE('',*,*,#18679,.F.);
#27280=ORIENTED_EDGE('',*,*,#18680,.F.);
#27281=ORIENTED_EDGE('',*,*,#18681,.F.);
#27282=ORIENTED_EDGE('',*,*,#18682,.T.);
#27283=ORIENTED_EDGE('',*,*,#18683,.F.);
#27284=ORIENTED_EDGE('',*,*,#18684,.F.);
#27285=ORIENTED_EDGE('',*,*,#18685,.F.);
#27286=ORIENTED_EDGE('',*,*,#18686,.T.);
#27287=ORIENTED_EDGE('',*,*,#18687,.F.);
#27288=ORIENTED_EDGE('',*,*,#18688,.F.);
#27289=ORIENTED_EDGE('',*,*,#18689,.F.);
#27290=ORIENTED_EDGE('',*,*,#18690,.T.);
#27291=ORIENTED_EDGE('',*,*,#18691,.F.);
#27292=ORIENTED_EDGE('',*,*,#18692,.F.);
#27293=ORIENTED_EDGE('',*,*,#18693,.F.);
#27294=ORIENTED_EDGE('',*,*,#18694,.T.);
#27295=ORIENTED_EDGE('',*,*,#18695,.F.);
#27296=ORIENTED_EDGE('',*,*,#18696,.F.);
#27297=ORIENTED_EDGE('',*,*,#18697,.F.);
#27298=ORIENTED_EDGE('',*,*,#18698,.T.);
#27299=ORIENTED_EDGE('',*,*,#18699,.F.);
#27300=ORIENTED_EDGE('',*,*,#18700,.F.);
#27301=ORIENTED_EDGE('',*,*,#18701,.F.);
#27302=ORIENTED_EDGE('',*,*,#18702,.T.);
#27303=ORIENTED_EDGE('',*,*,#18703,.F.);
#27304=ORIENTED_EDGE('',*,*,#18704,.F.);
#27305=ORIENTED_EDGE('',*,*,#18705,.F.);
#27306=ORIENTED_EDGE('',*,*,#18706,.T.);
#27307=ORIENTED_EDGE('',*,*,#18707,.F.);
#27308=ORIENTED_EDGE('',*,*,#18708,.F.);
#27309=ORIENTED_EDGE('',*,*,#18709,.F.);
#27310=ORIENTED_EDGE('',*,*,#18710,.T.);
#27311=ORIENTED_EDGE('',*,*,#18711,.F.);
#27312=ORIENTED_EDGE('',*,*,#18712,.F.);
#27313=ORIENTED_EDGE('',*,*,#18713,.F.);
#27314=ORIENTED_EDGE('',*,*,#18714,.T.);
#27315=ORIENTED_EDGE('',*,*,#18715,.F.);
#27316=ORIENTED_EDGE('',*,*,#18117,.F.);
#27317=ORIENTED_EDGE('',*,*,#18716,.F.);
#27318=ORIENTED_EDGE('',*,*,#18717,.T.);
#27319=ORIENTED_EDGE('',*,*,#18718,.F.);
#27320=ORIENTED_EDGE('',*,*,#18113,.F.);
#27321=ORIENTED_EDGE('',*,*,#18719,.F.);
#27322=ORIENTED_EDGE('',*,*,#18720,.T.);
#27323=ORIENTED_EDGE('',*,*,#18721,.F.);
#27324=ORIENTED_EDGE('',*,*,#18109,.F.);
#27325=ORIENTED_EDGE('',*,*,#18722,.F.);
#27326=ORIENTED_EDGE('',*,*,#18723,.T.);
#27327=ORIENTED_EDGE('',*,*,#18724,.F.);
#27328=ORIENTED_EDGE('',*,*,#18105,.F.);
#27329=ORIENTED_EDGE('',*,*,#18725,.F.);
#27330=ORIENTED_EDGE('',*,*,#18726,.T.);
#27331=ORIENTED_EDGE('',*,*,#18727,.F.);
#27332=ORIENTED_EDGE('',*,*,#18101,.F.);
#27333=ORIENTED_EDGE('',*,*,#18728,.F.);
#27334=ORIENTED_EDGE('',*,*,#18729,.T.);
#27335=ORIENTED_EDGE('',*,*,#18730,.F.);
#27336=ORIENTED_EDGE('',*,*,#18097,.F.);
#27337=ORIENTED_EDGE('',*,*,#18731,.F.);
#27338=ORIENTED_EDGE('',*,*,#18732,.T.);
#27339=ORIENTED_EDGE('',*,*,#18733,.F.);
#27340=ORIENTED_EDGE('',*,*,#18121,.F.);
#27341=ORIENTED_EDGE('',*,*,#18734,.F.);
#27342=ORIENTED_EDGE('',*,*,#18735,.T.);
#27343=ORIENTED_EDGE('',*,*,#18736,.F.);
#27344=ORIENTED_EDGE('',*,*,#18125,.F.);
#27345=ORIENTED_EDGE('',*,*,#18737,.F.);
#27346=ORIENTED_EDGE('',*,*,#18738,.T.);
#27347=ORIENTED_EDGE('',*,*,#18739,.F.);
#27348=ORIENTED_EDGE('',*,*,#18129,.F.);
#27349=ORIENTED_EDGE('',*,*,#18740,.F.);
#27350=ORIENTED_EDGE('',*,*,#18741,.T.);
#27351=ORIENTED_EDGE('',*,*,#18742,.F.);
#27352=ORIENTED_EDGE('',*,*,#18133,.F.);
#27353=ORIENTED_EDGE('',*,*,#18743,.F.);
#27354=ORIENTED_EDGE('',*,*,#18744,.T.);
#27355=ORIENTED_EDGE('',*,*,#18745,.F.);
#27356=ORIENTED_EDGE('',*,*,#18137,.F.);
#27357=ORIENTED_EDGE('',*,*,#18746,.F.);
#27358=ORIENTED_EDGE('',*,*,#18747,.T.);
#27359=ORIENTED_EDGE('',*,*,#18748,.F.);
#27360=ORIENTED_EDGE('',*,*,#18141,.F.);
#27361=ORIENTED_EDGE('',*,*,#18749,.F.);
#27362=ORIENTED_EDGE('',*,*,#18750,.T.);
#27363=ORIENTED_EDGE('',*,*,#18751,.F.);
#27364=ORIENTED_EDGE('',*,*,#18145,.F.);
#27365=ORIENTED_EDGE('',*,*,#18752,.F.);
#27366=ORIENTED_EDGE('',*,*,#18753,.T.);
#27367=ORIENTED_EDGE('',*,*,#18754,.F.);
#27368=ORIENTED_EDGE('',*,*,#18149,.F.);
#27369=ORIENTED_EDGE('',*,*,#18755,.F.);
#27370=ORIENTED_EDGE('',*,*,#18756,.T.);
#27371=ORIENTED_EDGE('',*,*,#18757,.F.);
#27372=ORIENTED_EDGE('',*,*,#18153,.F.);
#27373=ORIENTED_EDGE('',*,*,#18758,.F.);
#27374=ORIENTED_EDGE('',*,*,#18759,.T.);
#27375=ORIENTED_EDGE('',*,*,#18760,.F.);
#27376=ORIENTED_EDGE('',*,*,#18761,.F.);
#27377=ORIENTED_EDGE('',*,*,#18762,.F.);
#27378=ORIENTED_EDGE('',*,*,#18763,.T.);
#27379=ORIENTED_EDGE('',*,*,#18764,.F.);
#27380=ORIENTED_EDGE('',*,*,#18765,.F.);
#27381=ORIENTED_EDGE('',*,*,#18766,.F.);
#27382=ORIENTED_EDGE('',*,*,#18767,.T.);
#27383=ORIENTED_EDGE('',*,*,#18768,.F.);
#27384=ORIENTED_EDGE('',*,*,#18769,.F.);
#27385=ORIENTED_EDGE('',*,*,#18770,.F.);
#27386=ORIENTED_EDGE('',*,*,#18771,.T.);
#27387=ORIENTED_EDGE('',*,*,#18772,.F.);
#27388=ORIENTED_EDGE('',*,*,#18773,.F.);
#27389=ORIENTED_EDGE('',*,*,#18774,.F.);
#27390=ORIENTED_EDGE('',*,*,#18775,.T.);
#27391=ORIENTED_EDGE('',*,*,#18776,.F.);
#27392=ORIENTED_EDGE('',*,*,#18777,.F.);
#27393=ORIENTED_EDGE('',*,*,#18778,.F.);
#27394=ORIENTED_EDGE('',*,*,#18779,.T.);
#27395=ORIENTED_EDGE('',*,*,#18780,.F.);
#27396=ORIENTED_EDGE('',*,*,#18781,.F.);
#27397=ORIENTED_EDGE('',*,*,#18782,.T.);
#27398=ORIENTED_EDGE('',*,*,#18783,.F.);
#27399=ORIENTED_EDGE('',*,*,#18784,.F.);
#27400=ORIENTED_EDGE('',*,*,#18782,.F.);
#27401=ORIENTED_EDGE('',*,*,#18785,.F.);
#27402=ORIENTED_EDGE('',*,*,#18786,.T.);
#27403=ORIENTED_EDGE('',*,*,#18783,.T.);
#27404=ORIENTED_EDGE('',*,*,#18784,.T.);
#27405=ORIENTED_EDGE('',*,*,#18786,.F.);
#27406=ORIENTED_EDGE('',*,*,#18787,.F.);
#27407=ORIENTED_EDGE('',*,*,#18788,.T.);
#27408=ORIENTED_EDGE('',*,*,#18785,.T.);
#27409=ORIENTED_EDGE('',*,*,#18788,.F.);
#27410=ORIENTED_EDGE('',*,*,#18789,.F.);
#27411=ORIENTED_EDGE('',*,*,#18790,.T.);
#27412=ORIENTED_EDGE('',*,*,#18787,.T.);
#27413=ORIENTED_EDGE('',*,*,#18790,.F.);
#27414=ORIENTED_EDGE('',*,*,#17912,.F.);
#27415=ORIENTED_EDGE('',*,*,#18791,.T.);
#27416=ORIENTED_EDGE('',*,*,#18792,.T.);
#27417=ORIENTED_EDGE('',*,*,#18791,.F.);
#27418=ORIENTED_EDGE('',*,*,#18793,.F.);
#27419=ORIENTED_EDGE('',*,*,#18794,.T.);
#27420=ORIENTED_EDGE('',*,*,#18795,.F.);
#27421=ORIENTED_EDGE('',*,*,#18732,.F.);
#27422=ORIENTED_EDGE('',*,*,#18796,.F.);
#27423=ORIENTED_EDGE('',*,*,#18729,.F.);
#27424=ORIENTED_EDGE('',*,*,#18797,.F.);
#27425=ORIENTED_EDGE('',*,*,#18798,.T.);
#27426=ORIENTED_EDGE('',*,*,#18799,.F.);
#27427=ORIENTED_EDGE('',*,*,#18726,.F.);
#27428=ORIENTED_EDGE('',*,*,#18800,.F.);
#27429=ORIENTED_EDGE('',*,*,#18801,.T.);
#27430=ORIENTED_EDGE('',*,*,#18802,.F.);
#27431=ORIENTED_EDGE('',*,*,#18723,.F.);
#27432=ORIENTED_EDGE('',*,*,#18803,.F.);
#27433=ORIENTED_EDGE('',*,*,#18804,.T.);
#27434=ORIENTED_EDGE('',*,*,#18805,.F.);
#27435=ORIENTED_EDGE('',*,*,#18720,.F.);
#27436=ORIENTED_EDGE('',*,*,#18806,.F.);
#27437=ORIENTED_EDGE('',*,*,#18807,.T.);
#27438=ORIENTED_EDGE('',*,*,#18808,.F.);
#27439=ORIENTED_EDGE('',*,*,#18717,.F.);
#27440=ORIENTED_EDGE('',*,*,#18809,.F.);
#27441=ORIENTED_EDGE('',*,*,#18810,.T.);
#27442=ORIENTED_EDGE('',*,*,#18811,.F.);
#27443=ORIENTED_EDGE('',*,*,#18714,.F.);
#27444=ORIENTED_EDGE('',*,*,#18812,.F.);
#27445=ORIENTED_EDGE('',*,*,#18813,.T.);
#27446=ORIENTED_EDGE('',*,*,#18814,.F.);
#27447=ORIENTED_EDGE('',*,*,#18710,.F.);
#27448=ORIENTED_EDGE('',*,*,#18815,.F.);
#27449=ORIENTED_EDGE('',*,*,#18816,.T.);
#27450=ORIENTED_EDGE('',*,*,#18817,.F.);
#27451=ORIENTED_EDGE('',*,*,#18706,.F.);
#27452=ORIENTED_EDGE('',*,*,#18818,.F.);
#27453=ORIENTED_EDGE('',*,*,#18819,.T.);
#27454=ORIENTED_EDGE('',*,*,#18820,.F.);
#27455=ORIENTED_EDGE('',*,*,#18702,.F.);
#27456=ORIENTED_EDGE('',*,*,#18821,.F.);
#27457=ORIENTED_EDGE('',*,*,#18822,.T.);
#27458=ORIENTED_EDGE('',*,*,#18823,.F.);
#27459=ORIENTED_EDGE('',*,*,#18698,.F.);
#27460=ORIENTED_EDGE('',*,*,#18824,.F.);
#27461=ORIENTED_EDGE('',*,*,#18825,.T.);
#27462=ORIENTED_EDGE('',*,*,#18826,.F.);
#27463=ORIENTED_EDGE('',*,*,#18694,.F.);
#27464=ORIENTED_EDGE('',*,*,#18827,.F.);
#27465=ORIENTED_EDGE('',*,*,#18828,.T.);
#27466=ORIENTED_EDGE('',*,*,#18829,.F.);
#27467=ORIENTED_EDGE('',*,*,#18690,.F.);
#27468=ORIENTED_EDGE('',*,*,#18830,.F.);
#27469=ORIENTED_EDGE('',*,*,#18831,.T.);
#27470=ORIENTED_EDGE('',*,*,#18832,.F.);
#27471=ORIENTED_EDGE('',*,*,#18686,.F.);
#27472=ORIENTED_EDGE('',*,*,#18833,.F.);
#27473=ORIENTED_EDGE('',*,*,#18834,.T.);
#27474=ORIENTED_EDGE('',*,*,#18835,.F.);
#27475=ORIENTED_EDGE('',*,*,#18682,.F.);
#27476=ORIENTED_EDGE('',*,*,#18836,.F.);
#27477=ORIENTED_EDGE('',*,*,#18837,.T.);
#27478=ORIENTED_EDGE('',*,*,#18838,.F.);
#27479=ORIENTED_EDGE('',*,*,#18678,.F.);
#27480=ORIENTED_EDGE('',*,*,#18839,.F.);
#27481=ORIENTED_EDGE('',*,*,#18840,.T.);
#27482=ORIENTED_EDGE('',*,*,#18841,.F.);
#27483=ORIENTED_EDGE('',*,*,#18674,.F.);
#27484=ORIENTED_EDGE('',*,*,#18842,.F.);
#27485=ORIENTED_EDGE('',*,*,#18843,.T.);
#27486=ORIENTED_EDGE('',*,*,#18844,.F.);
#27487=ORIENTED_EDGE('',*,*,#18670,.F.);
#27488=ORIENTED_EDGE('',*,*,#18845,.F.);
#27489=ORIENTED_EDGE('',*,*,#18846,.T.);
#27490=ORIENTED_EDGE('',*,*,#18847,.F.);
#27491=ORIENTED_EDGE('',*,*,#18666,.F.);
#27492=ORIENTED_EDGE('',*,*,#18848,.F.);
#27493=ORIENTED_EDGE('',*,*,#18849,.T.);
#27494=ORIENTED_EDGE('',*,*,#18850,.F.);
#27495=ORIENTED_EDGE('',*,*,#18662,.F.);
#27496=ORIENTED_EDGE('',*,*,#18851,.F.);
#27497=ORIENTED_EDGE('',*,*,#18852,.T.);
#27498=ORIENTED_EDGE('',*,*,#18853,.F.);
#27499=ORIENTED_EDGE('',*,*,#18658,.F.);
#27500=ORIENTED_EDGE('',*,*,#18854,.F.);
#27501=ORIENTED_EDGE('',*,*,#18855,.T.);
#27502=ORIENTED_EDGE('',*,*,#18856,.F.);
#27503=ORIENTED_EDGE('',*,*,#18654,.F.);
#27504=ORIENTED_EDGE('',*,*,#18857,.F.);
#27505=ORIENTED_EDGE('',*,*,#18858,.T.);
#27506=ORIENTED_EDGE('',*,*,#18859,.F.);
#27507=ORIENTED_EDGE('',*,*,#18650,.F.);
#27508=ORIENTED_EDGE('',*,*,#18860,.F.);
#27509=ORIENTED_EDGE('',*,*,#18861,.T.);
#27510=ORIENTED_EDGE('',*,*,#18862,.F.);
#27511=ORIENTED_EDGE('',*,*,#18646,.F.);
#27512=ORIENTED_EDGE('',*,*,#18863,.F.);
#27513=ORIENTED_EDGE('',*,*,#18864,.T.);
#27514=ORIENTED_EDGE('',*,*,#18865,.F.);
#27515=ORIENTED_EDGE('',*,*,#18642,.F.);
#27516=ORIENTED_EDGE('',*,*,#18866,.F.);
#27517=ORIENTED_EDGE('',*,*,#18867,.T.);
#27518=ORIENTED_EDGE('',*,*,#18868,.F.);
#27519=ORIENTED_EDGE('',*,*,#18638,.F.);
#27520=ORIENTED_EDGE('',*,*,#18869,.F.);
#27521=ORIENTED_EDGE('',*,*,#18870,.T.);
#27522=ORIENTED_EDGE('',*,*,#18871,.F.);
#27523=ORIENTED_EDGE('',*,*,#18634,.F.);
#27524=ORIENTED_EDGE('',*,*,#18872,.F.);
#27525=ORIENTED_EDGE('',*,*,#18873,.T.);
#27526=ORIENTED_EDGE('',*,*,#18874,.F.);
#27527=ORIENTED_EDGE('',*,*,#18630,.F.);
#27528=ORIENTED_EDGE('',*,*,#18875,.F.);
#27529=ORIENTED_EDGE('',*,*,#18876,.T.);
#27530=ORIENTED_EDGE('',*,*,#18877,.F.);
#27531=ORIENTED_EDGE('',*,*,#18626,.F.);
#27532=ORIENTED_EDGE('',*,*,#18878,.F.);
#27533=ORIENTED_EDGE('',*,*,#18879,.T.);
#27534=ORIENTED_EDGE('',*,*,#18880,.F.);
#27535=ORIENTED_EDGE('',*,*,#18622,.F.);
#27536=ORIENTED_EDGE('',*,*,#18881,.F.);
#27537=ORIENTED_EDGE('',*,*,#18882,.T.);
#27538=ORIENTED_EDGE('',*,*,#18883,.F.);
#27539=ORIENTED_EDGE('',*,*,#18618,.F.);
#27540=ORIENTED_EDGE('',*,*,#18884,.F.);
#27541=ORIENTED_EDGE('',*,*,#18885,.T.);
#27542=ORIENTED_EDGE('',*,*,#18886,.F.);
#27543=ORIENTED_EDGE('',*,*,#18614,.F.);
#27544=ORIENTED_EDGE('',*,*,#18887,.F.);
#27545=ORIENTED_EDGE('',*,*,#18888,.T.);
#27546=ORIENTED_EDGE('',*,*,#18889,.F.);
#27547=ORIENTED_EDGE('',*,*,#18610,.F.);
#27548=ORIENTED_EDGE('',*,*,#18890,.F.);
#27549=ORIENTED_EDGE('',*,*,#18891,.T.);
#27550=ORIENTED_EDGE('',*,*,#18892,.F.);
#27551=ORIENTED_EDGE('',*,*,#18606,.F.);
#27552=ORIENTED_EDGE('',*,*,#18893,.F.);
#27553=ORIENTED_EDGE('',*,*,#18894,.T.);
#27554=ORIENTED_EDGE('',*,*,#18895,.F.);
#27555=ORIENTED_EDGE('',*,*,#18602,.F.);
#27556=ORIENTED_EDGE('',*,*,#18896,.F.);
#27557=ORIENTED_EDGE('',*,*,#18897,.T.);
#27558=ORIENTED_EDGE('',*,*,#18898,.F.);
#27559=ORIENTED_EDGE('',*,*,#18598,.F.);
#27560=ORIENTED_EDGE('',*,*,#18899,.F.);
#27561=ORIENTED_EDGE('',*,*,#18900,.T.);
#27562=ORIENTED_EDGE('',*,*,#18901,.F.);
#27563=ORIENTED_EDGE('',*,*,#18594,.F.);
#27564=ORIENTED_EDGE('',*,*,#18902,.F.);
#27565=ORIENTED_EDGE('',*,*,#18903,.T.);
#27566=ORIENTED_EDGE('',*,*,#18904,.F.);
#27567=ORIENTED_EDGE('',*,*,#18590,.F.);
#27568=ORIENTED_EDGE('',*,*,#18905,.F.);
#27569=ORIENTED_EDGE('',*,*,#18906,.T.);
#27570=ORIENTED_EDGE('',*,*,#18907,.F.);
#27571=ORIENTED_EDGE('',*,*,#18586,.F.);
#27572=ORIENTED_EDGE('',*,*,#18908,.F.);
#27573=ORIENTED_EDGE('',*,*,#18909,.T.);
#27574=ORIENTED_EDGE('',*,*,#18910,.F.);
#27575=ORIENTED_EDGE('',*,*,#18582,.F.);
#27576=ORIENTED_EDGE('',*,*,#18911,.F.);
#27577=ORIENTED_EDGE('',*,*,#18912,.T.);
#27578=ORIENTED_EDGE('',*,*,#18913,.F.);
#27579=ORIENTED_EDGE('',*,*,#18578,.F.);
#27580=ORIENTED_EDGE('',*,*,#18914,.F.);
#27581=ORIENTED_EDGE('',*,*,#18915,.T.);
#27582=ORIENTED_EDGE('',*,*,#18916,.F.);
#27583=ORIENTED_EDGE('',*,*,#18574,.F.);
#27584=ORIENTED_EDGE('',*,*,#18917,.F.);
#27585=ORIENTED_EDGE('',*,*,#18918,.T.);
#27586=ORIENTED_EDGE('',*,*,#18919,.F.);
#27587=ORIENTED_EDGE('',*,*,#18570,.F.);
#27588=ORIENTED_EDGE('',*,*,#18920,.F.);
#27589=ORIENTED_EDGE('',*,*,#18921,.T.);
#27590=ORIENTED_EDGE('',*,*,#18922,.F.);
#27591=ORIENTED_EDGE('',*,*,#18566,.F.);
#27592=ORIENTED_EDGE('',*,*,#18923,.F.);
#27593=ORIENTED_EDGE('',*,*,#18924,.T.);
#27594=ORIENTED_EDGE('',*,*,#18925,.F.);
#27595=ORIENTED_EDGE('',*,*,#18562,.F.);
#27596=ORIENTED_EDGE('',*,*,#18926,.F.);
#27597=ORIENTED_EDGE('',*,*,#18927,.T.);
#27598=ORIENTED_EDGE('',*,*,#18928,.F.);
#27599=ORIENTED_EDGE('',*,*,#18558,.F.);
#27600=ORIENTED_EDGE('',*,*,#18929,.F.);
#27601=ORIENTED_EDGE('',*,*,#18930,.T.);
#27602=ORIENTED_EDGE('',*,*,#18931,.F.);
#27603=ORIENTED_EDGE('',*,*,#18554,.F.);
#27604=ORIENTED_EDGE('',*,*,#18932,.F.);
#27605=ORIENTED_EDGE('',*,*,#18933,.T.);
#27606=ORIENTED_EDGE('',*,*,#18934,.F.);
#27607=ORIENTED_EDGE('',*,*,#18550,.F.);
#27608=ORIENTED_EDGE('',*,*,#18935,.F.);
#27609=ORIENTED_EDGE('',*,*,#18936,.T.);
#27610=ORIENTED_EDGE('',*,*,#18937,.F.);
#27611=ORIENTED_EDGE('',*,*,#18546,.F.);
#27612=ORIENTED_EDGE('',*,*,#18938,.F.);
#27613=ORIENTED_EDGE('',*,*,#18939,.T.);
#27614=ORIENTED_EDGE('',*,*,#18940,.F.);
#27615=ORIENTED_EDGE('',*,*,#18542,.F.);
#27616=ORIENTED_EDGE('',*,*,#18941,.F.);
#27617=ORIENTED_EDGE('',*,*,#18942,.T.);
#27618=ORIENTED_EDGE('',*,*,#18943,.F.);
#27619=ORIENTED_EDGE('',*,*,#18538,.F.);
#27620=ORIENTED_EDGE('',*,*,#18944,.F.);
#27621=ORIENTED_EDGE('',*,*,#18945,.T.);
#27622=ORIENTED_EDGE('',*,*,#18946,.F.);
#27623=ORIENTED_EDGE('',*,*,#18534,.F.);
#27624=ORIENTED_EDGE('',*,*,#18947,.F.);
#27625=ORIENTED_EDGE('',*,*,#18948,.T.);
#27626=ORIENTED_EDGE('',*,*,#18949,.F.);
#27627=ORIENTED_EDGE('',*,*,#18530,.F.);
#27628=ORIENTED_EDGE('',*,*,#18950,.F.);
#27629=ORIENTED_EDGE('',*,*,#18951,.T.);
#27630=ORIENTED_EDGE('',*,*,#18952,.F.);
#27631=ORIENTED_EDGE('',*,*,#18526,.F.);
#27632=ORIENTED_EDGE('',*,*,#18953,.F.);
#27633=ORIENTED_EDGE('',*,*,#18954,.T.);
#27634=ORIENTED_EDGE('',*,*,#18955,.F.);
#27635=ORIENTED_EDGE('',*,*,#18522,.F.);
#27636=ORIENTED_EDGE('',*,*,#18956,.F.);
#27637=ORIENTED_EDGE('',*,*,#18957,.T.);
#27638=ORIENTED_EDGE('',*,*,#18958,.F.);
#27639=ORIENTED_EDGE('',*,*,#18518,.F.);
#27640=ORIENTED_EDGE('',*,*,#18959,.F.);
#27641=ORIENTED_EDGE('',*,*,#18960,.T.);
#27642=ORIENTED_EDGE('',*,*,#18961,.F.);
#27643=ORIENTED_EDGE('',*,*,#18514,.F.);
#27644=ORIENTED_EDGE('',*,*,#18962,.F.);
#27645=ORIENTED_EDGE('',*,*,#18963,.T.);
#27646=ORIENTED_EDGE('',*,*,#18964,.F.);
#27647=ORIENTED_EDGE('',*,*,#18510,.F.);
#27648=ORIENTED_EDGE('',*,*,#18965,.F.);
#27649=ORIENTED_EDGE('',*,*,#18966,.T.);
#27650=ORIENTED_EDGE('',*,*,#18967,.F.);
#27651=ORIENTED_EDGE('',*,*,#18506,.F.);
#27652=ORIENTED_EDGE('',*,*,#18968,.F.);
#27653=ORIENTED_EDGE('',*,*,#18969,.T.);
#27654=ORIENTED_EDGE('',*,*,#18970,.F.);
#27655=ORIENTED_EDGE('',*,*,#18502,.F.);
#27656=ORIENTED_EDGE('',*,*,#18971,.F.);
#27657=ORIENTED_EDGE('',*,*,#18972,.T.);
#27658=ORIENTED_EDGE('',*,*,#18973,.F.);
#27659=ORIENTED_EDGE('',*,*,#18498,.F.);
#27660=ORIENTED_EDGE('',*,*,#18974,.F.);
#27661=ORIENTED_EDGE('',*,*,#18975,.T.);
#27662=ORIENTED_EDGE('',*,*,#18976,.F.);
#27663=ORIENTED_EDGE('',*,*,#18494,.F.);
#27664=ORIENTED_EDGE('',*,*,#18977,.F.);
#27665=ORIENTED_EDGE('',*,*,#18978,.T.);
#27666=ORIENTED_EDGE('',*,*,#18979,.F.);
#27667=ORIENTED_EDGE('',*,*,#18490,.F.);
#27668=ORIENTED_EDGE('',*,*,#18980,.F.);
#27669=ORIENTED_EDGE('',*,*,#18981,.T.);
#27670=ORIENTED_EDGE('',*,*,#18982,.F.);
#27671=ORIENTED_EDGE('',*,*,#18486,.F.);
#27672=ORIENTED_EDGE('',*,*,#18983,.F.);
#27673=ORIENTED_EDGE('',*,*,#18984,.T.);
#27674=ORIENTED_EDGE('',*,*,#18985,.F.);
#27675=ORIENTED_EDGE('',*,*,#18986,.T.);
#27676=ORIENTED_EDGE('',*,*,#18987,.F.);
#27677=ORIENTED_EDGE('',*,*,#18735,.F.);
#27678=ORIENTED_EDGE('',*,*,#18988,.F.);
#27679=ORIENTED_EDGE('',*,*,#18989,.T.);
#27680=ORIENTED_EDGE('',*,*,#18990,.F.);
#27681=ORIENTED_EDGE('',*,*,#18738,.F.);
#27682=ORIENTED_EDGE('',*,*,#18991,.F.);
#27683=ORIENTED_EDGE('',*,*,#18992,.T.);
#27684=ORIENTED_EDGE('',*,*,#18993,.F.);
#27685=ORIENTED_EDGE('',*,*,#18741,.F.);
#27686=ORIENTED_EDGE('',*,*,#18994,.F.);
#27687=ORIENTED_EDGE('',*,*,#18995,.T.);
#27688=ORIENTED_EDGE('',*,*,#18996,.F.);
#27689=ORIENTED_EDGE('',*,*,#18744,.F.);
#27690=ORIENTED_EDGE('',*,*,#18997,.F.);
#27691=ORIENTED_EDGE('',*,*,#18998,.T.);
#27692=ORIENTED_EDGE('',*,*,#18999,.F.);
#27693=ORIENTED_EDGE('',*,*,#18747,.F.);
#27694=ORIENTED_EDGE('',*,*,#19000,.F.);
#27695=ORIENTED_EDGE('',*,*,#19001,.T.);
#27696=ORIENTED_EDGE('',*,*,#19002,.F.);
#27697=ORIENTED_EDGE('',*,*,#18750,.F.);
#27698=ORIENTED_EDGE('',*,*,#19003,.F.);
#27699=ORIENTED_EDGE('',*,*,#19004,.T.);
#27700=ORIENTED_EDGE('',*,*,#19005,.F.);
#27701=ORIENTED_EDGE('',*,*,#18753,.F.);
#27702=ORIENTED_EDGE('',*,*,#19006,.F.);
#27703=ORIENTED_EDGE('',*,*,#19007,.T.);
#27704=ORIENTED_EDGE('',*,*,#19008,.F.);
#27705=ORIENTED_EDGE('',*,*,#18756,.F.);
#27706=ORIENTED_EDGE('',*,*,#19009,.F.);
#27707=ORIENTED_EDGE('',*,*,#19010,.T.);
#27708=ORIENTED_EDGE('',*,*,#19011,.F.);
#27709=ORIENTED_EDGE('',*,*,#18759,.F.);
#27710=ORIENTED_EDGE('',*,*,#19012,.F.);
#27711=ORIENTED_EDGE('',*,*,#19013,.T.);
#27712=ORIENTED_EDGE('',*,*,#19014,.F.);
#27713=ORIENTED_EDGE('',*,*,#18763,.F.);
#27714=ORIENTED_EDGE('',*,*,#19015,.F.);
#27715=ORIENTED_EDGE('',*,*,#19016,.T.);
#27716=ORIENTED_EDGE('',*,*,#19017,.F.);
#27717=ORIENTED_EDGE('',*,*,#18767,.F.);
#27718=ORIENTED_EDGE('',*,*,#19018,.F.);
#27719=ORIENTED_EDGE('',*,*,#19019,.T.);
#27720=ORIENTED_EDGE('',*,*,#19020,.F.);
#27721=ORIENTED_EDGE('',*,*,#18771,.F.);
#27722=ORIENTED_EDGE('',*,*,#19021,.F.);
#27723=ORIENTED_EDGE('',*,*,#19022,.T.);
#27724=ORIENTED_EDGE('',*,*,#19023,.F.);
#27725=ORIENTED_EDGE('',*,*,#18775,.F.);
#27726=ORIENTED_EDGE('',*,*,#19024,.F.);
#27727=ORIENTED_EDGE('',*,*,#19025,.T.);
#27728=ORIENTED_EDGE('',*,*,#19026,.F.);
#27729=ORIENTED_EDGE('',*,*,#18779,.F.);
#27730=ORIENTED_EDGE('',*,*,#19027,.F.);
#27731=ORIENTED_EDGE('',*,*,#18482,.F.);
#27732=ORIENTED_EDGE('',*,*,#19028,.F.);
#27733=ORIENTED_EDGE('',*,*,#19029,.T.);
#27734=ORIENTED_EDGE('',*,*,#19030,.F.);
#27735=ORIENTED_EDGE('',*,*,#19031,.T.);
#27736=ORIENTED_EDGE('',*,*,#19032,.F.);
#27737=ORIENTED_EDGE('',*,*,#18794,.F.);
#27738=ORIENTED_EDGE('',*,*,#19033,.F.);
#27739=ORIENTED_EDGE('',*,*,#18798,.F.);
#27740=ORIENTED_EDGE('',*,*,#19034,.F.);
#27741=ORIENTED_EDGE('',*,*,#19035,.T.);
#27742=ORIENTED_EDGE('',*,*,#19036,.F.);
#27743=ORIENTED_EDGE('',*,*,#18801,.F.);
#27744=ORIENTED_EDGE('',*,*,#19037,.F.);
#27745=ORIENTED_EDGE('',*,*,#19038,.T.);
#27746=ORIENTED_EDGE('',*,*,#19039,.F.);
#27747=ORIENTED_EDGE('',*,*,#18804,.F.);
#27748=ORIENTED_EDGE('',*,*,#19040,.F.);
#27749=ORIENTED_EDGE('',*,*,#19041,.T.);
#27750=ORIENTED_EDGE('',*,*,#19042,.F.);
#27751=ORIENTED_EDGE('',*,*,#18807,.F.);
#27752=ORIENTED_EDGE('',*,*,#19043,.F.);
#27753=ORIENTED_EDGE('',*,*,#19044,.T.);
#27754=ORIENTED_EDGE('',*,*,#19045,.F.);
#27755=ORIENTED_EDGE('',*,*,#18810,.F.);
#27756=ORIENTED_EDGE('',*,*,#19046,.F.);
#27757=ORIENTED_EDGE('',*,*,#19047,.T.);
#27758=ORIENTED_EDGE('',*,*,#19048,.F.);
#27759=ORIENTED_EDGE('',*,*,#18813,.F.);
#27760=ORIENTED_EDGE('',*,*,#19049,.F.);
#27761=ORIENTED_EDGE('',*,*,#19050,.T.);
#27762=ORIENTED_EDGE('',*,*,#19051,.F.);
#27763=ORIENTED_EDGE('',*,*,#18816,.F.);
#27764=ORIENTED_EDGE('',*,*,#19052,.F.);
#27765=ORIENTED_EDGE('',*,*,#19053,.T.);
#27766=ORIENTED_EDGE('',*,*,#19054,.F.);
#27767=ORIENTED_EDGE('',*,*,#18819,.F.);
#27768=ORIENTED_EDGE('',*,*,#19055,.F.);
#27769=ORIENTED_EDGE('',*,*,#19056,.T.);
#27770=ORIENTED_EDGE('',*,*,#19057,.F.);
#27771=ORIENTED_EDGE('',*,*,#18822,.F.);
#27772=ORIENTED_EDGE('',*,*,#19058,.F.);
#27773=ORIENTED_EDGE('',*,*,#19059,.T.);
#27774=ORIENTED_EDGE('',*,*,#19060,.F.);
#27775=ORIENTED_EDGE('',*,*,#18825,.F.);
#27776=ORIENTED_EDGE('',*,*,#19061,.F.);
#27777=ORIENTED_EDGE('',*,*,#19062,.T.);
#27778=ORIENTED_EDGE('',*,*,#19063,.F.);
#27779=ORIENTED_EDGE('',*,*,#18828,.F.);
#27780=ORIENTED_EDGE('',*,*,#19064,.F.);
#27781=ORIENTED_EDGE('',*,*,#19065,.T.);
#27782=ORIENTED_EDGE('',*,*,#19066,.F.);
#27783=ORIENTED_EDGE('',*,*,#18831,.F.);
#27784=ORIENTED_EDGE('',*,*,#19067,.F.);
#27785=ORIENTED_EDGE('',*,*,#19068,.T.);
#27786=ORIENTED_EDGE('',*,*,#19069,.F.);
#27787=ORIENTED_EDGE('',*,*,#18834,.F.);
#27788=ORIENTED_EDGE('',*,*,#19070,.F.);
#27789=ORIENTED_EDGE('',*,*,#19071,.T.);
#27790=ORIENTED_EDGE('',*,*,#19072,.F.);
#27791=ORIENTED_EDGE('',*,*,#18837,.F.);
#27792=ORIENTED_EDGE('',*,*,#19073,.F.);
#27793=ORIENTED_EDGE('',*,*,#19074,.T.);
#27794=ORIENTED_EDGE('',*,*,#19075,.F.);
#27795=ORIENTED_EDGE('',*,*,#18840,.F.);
#27796=ORIENTED_EDGE('',*,*,#19076,.F.);
#27797=ORIENTED_EDGE('',*,*,#19077,.T.);
#27798=ORIENTED_EDGE('',*,*,#19078,.F.);
#27799=ORIENTED_EDGE('',*,*,#18843,.F.);
#27800=ORIENTED_EDGE('',*,*,#19079,.F.);
#27801=ORIENTED_EDGE('',*,*,#19080,.T.);
#27802=ORIENTED_EDGE('',*,*,#19081,.F.);
#27803=ORIENTED_EDGE('',*,*,#18846,.F.);
#27804=ORIENTED_EDGE('',*,*,#19082,.F.);
#27805=ORIENTED_EDGE('',*,*,#19083,.T.);
#27806=ORIENTED_EDGE('',*,*,#19084,.F.);
#27807=ORIENTED_EDGE('',*,*,#18849,.F.);
#27808=ORIENTED_EDGE('',*,*,#19085,.F.);
#27809=ORIENTED_EDGE('',*,*,#19086,.T.);
#27810=ORIENTED_EDGE('',*,*,#19087,.F.);
#27811=ORIENTED_EDGE('',*,*,#18852,.F.);
#27812=ORIENTED_EDGE('',*,*,#19088,.F.);
#27813=ORIENTED_EDGE('',*,*,#19089,.T.);
#27814=ORIENTED_EDGE('',*,*,#19090,.F.);
#27815=ORIENTED_EDGE('',*,*,#18855,.F.);
#27816=ORIENTED_EDGE('',*,*,#19091,.F.);
#27817=ORIENTED_EDGE('',*,*,#19092,.T.);
#27818=ORIENTED_EDGE('',*,*,#19093,.F.);
#27819=ORIENTED_EDGE('',*,*,#18858,.F.);
#27820=ORIENTED_EDGE('',*,*,#19094,.F.);
#27821=ORIENTED_EDGE('',*,*,#19095,.T.);
#27822=ORIENTED_EDGE('',*,*,#19096,.F.);
#27823=ORIENTED_EDGE('',*,*,#18861,.F.);
#27824=ORIENTED_EDGE('',*,*,#19097,.F.);
#27825=ORIENTED_EDGE('',*,*,#19098,.T.);
#27826=ORIENTED_EDGE('',*,*,#19099,.F.);
#27827=ORIENTED_EDGE('',*,*,#18864,.F.);
#27828=ORIENTED_EDGE('',*,*,#19100,.F.);
#27829=ORIENTED_EDGE('',*,*,#19101,.T.);
#27830=ORIENTED_EDGE('',*,*,#19102,.F.);
#27831=ORIENTED_EDGE('',*,*,#18867,.F.);
#27832=ORIENTED_EDGE('',*,*,#19103,.F.);
#27833=ORIENTED_EDGE('',*,*,#19104,.T.);
#27834=ORIENTED_EDGE('',*,*,#19105,.F.);
#27835=ORIENTED_EDGE('',*,*,#18870,.F.);
#27836=ORIENTED_EDGE('',*,*,#19106,.F.);
#27837=ORIENTED_EDGE('',*,*,#19107,.T.);
#27838=ORIENTED_EDGE('',*,*,#19108,.F.);
#27839=ORIENTED_EDGE('',*,*,#18873,.F.);
#27840=ORIENTED_EDGE('',*,*,#19109,.F.);
#27841=ORIENTED_EDGE('',*,*,#19110,.T.);
#27842=ORIENTED_EDGE('',*,*,#19111,.F.);
#27843=ORIENTED_EDGE('',*,*,#18876,.F.);
#27844=ORIENTED_EDGE('',*,*,#19112,.F.);
#27845=ORIENTED_EDGE('',*,*,#19113,.T.);
#27846=ORIENTED_EDGE('',*,*,#19114,.F.);
#27847=ORIENTED_EDGE('',*,*,#18879,.F.);
#27848=ORIENTED_EDGE('',*,*,#19115,.F.);
#27849=ORIENTED_EDGE('',*,*,#19116,.T.);
#27850=ORIENTED_EDGE('',*,*,#19117,.F.);
#27851=ORIENTED_EDGE('',*,*,#18882,.F.);
#27852=ORIENTED_EDGE('',*,*,#19118,.F.);
#27853=ORIENTED_EDGE('',*,*,#19119,.T.);
#27854=ORIENTED_EDGE('',*,*,#19120,.F.);
#27855=ORIENTED_EDGE('',*,*,#18885,.F.);
#27856=ORIENTED_EDGE('',*,*,#19121,.F.);
#27857=ORIENTED_EDGE('',*,*,#19122,.T.);
#27858=ORIENTED_EDGE('',*,*,#19123,.F.);
#27859=ORIENTED_EDGE('',*,*,#18888,.F.);
#27860=ORIENTED_EDGE('',*,*,#19124,.F.);
#27861=ORIENTED_EDGE('',*,*,#19125,.T.);
#27862=ORIENTED_EDGE('',*,*,#19126,.F.);
#27863=ORIENTED_EDGE('',*,*,#18891,.F.);
#27864=ORIENTED_EDGE('',*,*,#19127,.F.);
#27865=ORIENTED_EDGE('',*,*,#19128,.T.);
#27866=ORIENTED_EDGE('',*,*,#19129,.F.);
#27867=ORIENTED_EDGE('',*,*,#18894,.F.);
#27868=ORIENTED_EDGE('',*,*,#19130,.F.);
#27869=ORIENTED_EDGE('',*,*,#19131,.T.);
#27870=ORIENTED_EDGE('',*,*,#19132,.F.);
#27871=ORIENTED_EDGE('',*,*,#18897,.F.);
#27872=ORIENTED_EDGE('',*,*,#19133,.F.);
#27873=ORIENTED_EDGE('',*,*,#19134,.T.);
#27874=ORIENTED_EDGE('',*,*,#19135,.F.);
#27875=ORIENTED_EDGE('',*,*,#18900,.F.);
#27876=ORIENTED_EDGE('',*,*,#19136,.F.);
#27877=ORIENTED_EDGE('',*,*,#19137,.T.);
#27878=ORIENTED_EDGE('',*,*,#19138,.F.);
#27879=ORIENTED_EDGE('',*,*,#18903,.F.);
#27880=ORIENTED_EDGE('',*,*,#19139,.F.);
#27881=ORIENTED_EDGE('',*,*,#19140,.T.);
#27882=ORIENTED_EDGE('',*,*,#19141,.F.);
#27883=ORIENTED_EDGE('',*,*,#18906,.F.);
#27884=ORIENTED_EDGE('',*,*,#19142,.F.);
#27885=ORIENTED_EDGE('',*,*,#19143,.T.);
#27886=ORIENTED_EDGE('',*,*,#19144,.F.);
#27887=ORIENTED_EDGE('',*,*,#18909,.F.);
#27888=ORIENTED_EDGE('',*,*,#19145,.F.);
#27889=ORIENTED_EDGE('',*,*,#19146,.T.);
#27890=ORIENTED_EDGE('',*,*,#19147,.F.);
#27891=ORIENTED_EDGE('',*,*,#18912,.F.);
#27892=ORIENTED_EDGE('',*,*,#19148,.F.);
#27893=ORIENTED_EDGE('',*,*,#19149,.T.);
#27894=ORIENTED_EDGE('',*,*,#19150,.F.);
#27895=ORIENTED_EDGE('',*,*,#18915,.F.);
#27896=ORIENTED_EDGE('',*,*,#19151,.F.);
#27897=ORIENTED_EDGE('',*,*,#19152,.T.);
#27898=ORIENTED_EDGE('',*,*,#19153,.F.);
#27899=ORIENTED_EDGE('',*,*,#18918,.F.);
#27900=ORIENTED_EDGE('',*,*,#19154,.F.);
#27901=ORIENTED_EDGE('',*,*,#19155,.T.);
#27902=ORIENTED_EDGE('',*,*,#19156,.F.);
#27903=ORIENTED_EDGE('',*,*,#18921,.F.);
#27904=ORIENTED_EDGE('',*,*,#19157,.F.);
#27905=ORIENTED_EDGE('',*,*,#19158,.T.);
#27906=ORIENTED_EDGE('',*,*,#19159,.F.);
#27907=ORIENTED_EDGE('',*,*,#18924,.F.);
#27908=ORIENTED_EDGE('',*,*,#19160,.F.);
#27909=ORIENTED_EDGE('',*,*,#19161,.T.);
#27910=ORIENTED_EDGE('',*,*,#19162,.F.);
#27911=ORIENTED_EDGE('',*,*,#18927,.F.);
#27912=ORIENTED_EDGE('',*,*,#19163,.F.);
#27913=ORIENTED_EDGE('',*,*,#19164,.T.);
#27914=ORIENTED_EDGE('',*,*,#19165,.F.);
#27915=ORIENTED_EDGE('',*,*,#18930,.F.);
#27916=ORIENTED_EDGE('',*,*,#19166,.F.);
#27917=ORIENTED_EDGE('',*,*,#19167,.T.);
#27918=ORIENTED_EDGE('',*,*,#19168,.F.);
#27919=ORIENTED_EDGE('',*,*,#18933,.F.);
#27920=ORIENTED_EDGE('',*,*,#19169,.F.);
#27921=ORIENTED_EDGE('',*,*,#19170,.T.);
#27922=ORIENTED_EDGE('',*,*,#19171,.F.);
#27923=ORIENTED_EDGE('',*,*,#18936,.F.);
#27924=ORIENTED_EDGE('',*,*,#19172,.F.);
#27925=ORIENTED_EDGE('',*,*,#19173,.T.);
#27926=ORIENTED_EDGE('',*,*,#19174,.F.);
#27927=ORIENTED_EDGE('',*,*,#18939,.F.);
#27928=ORIENTED_EDGE('',*,*,#19175,.F.);
#27929=ORIENTED_EDGE('',*,*,#19176,.T.);
#27930=ORIENTED_EDGE('',*,*,#19177,.F.);
#27931=ORIENTED_EDGE('',*,*,#18942,.F.);
#27932=ORIENTED_EDGE('',*,*,#19178,.F.);
#27933=ORIENTED_EDGE('',*,*,#19179,.T.);
#27934=ORIENTED_EDGE('',*,*,#19180,.F.);
#27935=ORIENTED_EDGE('',*,*,#18945,.F.);
#27936=ORIENTED_EDGE('',*,*,#19181,.F.);
#27937=ORIENTED_EDGE('',*,*,#19182,.T.);
#27938=ORIENTED_EDGE('',*,*,#19183,.F.);
#27939=ORIENTED_EDGE('',*,*,#18948,.F.);
#27940=ORIENTED_EDGE('',*,*,#19184,.F.);
#27941=ORIENTED_EDGE('',*,*,#19185,.T.);
#27942=ORIENTED_EDGE('',*,*,#19186,.F.);
#27943=ORIENTED_EDGE('',*,*,#18951,.F.);
#27944=ORIENTED_EDGE('',*,*,#19187,.F.);
#27945=ORIENTED_EDGE('',*,*,#19188,.T.);
#27946=ORIENTED_EDGE('',*,*,#19189,.F.);
#27947=ORIENTED_EDGE('',*,*,#18954,.F.);
#27948=ORIENTED_EDGE('',*,*,#19190,.F.);
#27949=ORIENTED_EDGE('',*,*,#19191,.T.);
#27950=ORIENTED_EDGE('',*,*,#19192,.F.);
#27951=ORIENTED_EDGE('',*,*,#18957,.F.);
#27952=ORIENTED_EDGE('',*,*,#19193,.F.);
#27953=ORIENTED_EDGE('',*,*,#19194,.T.);
#27954=ORIENTED_EDGE('',*,*,#19195,.F.);
#27955=ORIENTED_EDGE('',*,*,#18960,.F.);
#27956=ORIENTED_EDGE('',*,*,#19196,.F.);
#27957=ORIENTED_EDGE('',*,*,#19197,.T.);
#27958=ORIENTED_EDGE('',*,*,#19198,.F.);
#27959=ORIENTED_EDGE('',*,*,#18963,.F.);
#27960=ORIENTED_EDGE('',*,*,#19199,.F.);
#27961=ORIENTED_EDGE('',*,*,#19200,.T.);
#27962=ORIENTED_EDGE('',*,*,#19201,.F.);
#27963=ORIENTED_EDGE('',*,*,#18966,.F.);
#27964=ORIENTED_EDGE('',*,*,#19202,.F.);
#27965=ORIENTED_EDGE('',*,*,#19203,.T.);
#27966=ORIENTED_EDGE('',*,*,#19204,.F.);
#27967=ORIENTED_EDGE('',*,*,#18969,.F.);
#27968=ORIENTED_EDGE('',*,*,#19205,.F.);
#27969=ORIENTED_EDGE('',*,*,#19206,.T.);
#27970=ORIENTED_EDGE('',*,*,#19207,.F.);
#27971=ORIENTED_EDGE('',*,*,#18972,.F.);
#27972=ORIENTED_EDGE('',*,*,#19208,.F.);
#27973=ORIENTED_EDGE('',*,*,#19209,.T.);
#27974=ORIENTED_EDGE('',*,*,#19210,.F.);
#27975=ORIENTED_EDGE('',*,*,#18975,.F.);
#27976=ORIENTED_EDGE('',*,*,#19211,.F.);
#27977=ORIENTED_EDGE('',*,*,#19212,.T.);
#27978=ORIENTED_EDGE('',*,*,#19213,.F.);
#27979=ORIENTED_EDGE('',*,*,#18978,.F.);
#27980=ORIENTED_EDGE('',*,*,#19214,.F.);
#27981=ORIENTED_EDGE('',*,*,#19215,.T.);
#27982=ORIENTED_EDGE('',*,*,#19216,.F.);
#27983=ORIENTED_EDGE('',*,*,#18981,.F.);
#27984=ORIENTED_EDGE('',*,*,#19217,.F.);
#27985=ORIENTED_EDGE('',*,*,#19218,.T.);
#27986=ORIENTED_EDGE('',*,*,#19219,.F.);
#27987=ORIENTED_EDGE('',*,*,#18984,.F.);
#27988=ORIENTED_EDGE('',*,*,#19220,.F.);
#27989=ORIENTED_EDGE('',*,*,#19221,.T.);
#27990=ORIENTED_EDGE('',*,*,#19222,.F.);
#27991=ORIENTED_EDGE('',*,*,#19223,.T.);
#27992=ORIENTED_EDGE('',*,*,#19224,.F.);
#27993=ORIENTED_EDGE('',*,*,#18986,.F.);
#27994=ORIENTED_EDGE('',*,*,#19225,.F.);
#27995=ORIENTED_EDGE('',*,*,#19226,.T.);
#27996=ORIENTED_EDGE('',*,*,#19227,.F.);
#27997=ORIENTED_EDGE('',*,*,#18989,.F.);
#27998=ORIENTED_EDGE('',*,*,#19228,.F.);
#27999=ORIENTED_EDGE('',*,*,#19229,.T.);
#28000=ORIENTED_EDGE('',*,*,#19230,.F.);
#28001=ORIENTED_EDGE('',*,*,#18992,.F.);
#28002=ORIENTED_EDGE('',*,*,#19231,.F.);
#28003=ORIENTED_EDGE('',*,*,#19232,.T.);
#28004=ORIENTED_EDGE('',*,*,#19233,.F.);
#28005=ORIENTED_EDGE('',*,*,#18995,.F.);
#28006=ORIENTED_EDGE('',*,*,#19234,.F.);
#28007=ORIENTED_EDGE('',*,*,#19235,.T.);
#28008=ORIENTED_EDGE('',*,*,#19236,.F.);
#28009=ORIENTED_EDGE('',*,*,#18998,.F.);
#28010=ORIENTED_EDGE('',*,*,#19237,.F.);
#28011=ORIENTED_EDGE('',*,*,#19238,.T.);
#28012=ORIENTED_EDGE('',*,*,#19239,.F.);
#28013=ORIENTED_EDGE('',*,*,#19001,.F.);
#28014=ORIENTED_EDGE('',*,*,#19240,.F.);
#28015=ORIENTED_EDGE('',*,*,#19241,.T.);
#28016=ORIENTED_EDGE('',*,*,#19242,.F.);
#28017=ORIENTED_EDGE('',*,*,#19004,.F.);
#28018=ORIENTED_EDGE('',*,*,#19243,.F.);
#28019=ORIENTED_EDGE('',*,*,#19244,.T.);
#28020=ORIENTED_EDGE('',*,*,#19245,.F.);
#28021=ORIENTED_EDGE('',*,*,#19007,.F.);
#28022=ORIENTED_EDGE('',*,*,#19246,.F.);
#28023=ORIENTED_EDGE('',*,*,#19247,.T.);
#28024=ORIENTED_EDGE('',*,*,#19248,.F.);
#28025=ORIENTED_EDGE('',*,*,#19010,.F.);
#28026=ORIENTED_EDGE('',*,*,#19249,.F.);
#28027=ORIENTED_EDGE('',*,*,#19250,.T.);
#28028=ORIENTED_EDGE('',*,*,#19251,.F.);
#28029=ORIENTED_EDGE('',*,*,#19013,.F.);
#28030=ORIENTED_EDGE('',*,*,#19252,.F.);
#28031=ORIENTED_EDGE('',*,*,#19253,.T.);
#28032=ORIENTED_EDGE('',*,*,#19254,.F.);
#28033=ORIENTED_EDGE('',*,*,#19016,.F.);
#28034=ORIENTED_EDGE('',*,*,#19255,.F.);
#28035=ORIENTED_EDGE('',*,*,#19256,.T.);
#28036=ORIENTED_EDGE('',*,*,#19257,.F.);
#28037=ORIENTED_EDGE('',*,*,#19019,.F.);
#28038=ORIENTED_EDGE('',*,*,#19258,.F.);
#28039=ORIENTED_EDGE('',*,*,#19259,.T.);
#28040=ORIENTED_EDGE('',*,*,#19260,.F.);
#28041=ORIENTED_EDGE('',*,*,#19022,.F.);
#28042=ORIENTED_EDGE('',*,*,#19261,.F.);
#28043=ORIENTED_EDGE('',*,*,#19262,.T.);
#28044=ORIENTED_EDGE('',*,*,#19263,.F.);
#28045=ORIENTED_EDGE('',*,*,#19025,.F.);
#28046=ORIENTED_EDGE('',*,*,#19264,.F.);
#28047=ORIENTED_EDGE('',*,*,#19029,.F.);
#28048=ORIENTED_EDGE('',*,*,#19265,.F.);
#28049=ORIENTED_EDGE('',*,*,#19266,.T.);
#28050=ORIENTED_EDGE('',*,*,#19267,.F.);
#28051=ORIENTED_EDGE('',*,*,#18378,.T.);
#28052=ORIENTED_EDGE('',*,*,#19268,.F.);
#28053=ORIENTED_EDGE('',*,*,#19031,.F.);
#28054=ORIENTED_EDGE('',*,*,#19269,.F.);
#28055=ORIENTED_EDGE('',*,*,#19035,.F.);
#28056=ORIENTED_EDGE('',*,*,#19270,.F.);
#28057=ORIENTED_EDGE('',*,*,#18381,.T.);
#28058=ORIENTED_EDGE('',*,*,#19271,.F.);
#28059=ORIENTED_EDGE('',*,*,#19038,.F.);
#28060=ORIENTED_EDGE('',*,*,#19272,.F.);
#28061=ORIENTED_EDGE('',*,*,#18384,.T.);
#28062=ORIENTED_EDGE('',*,*,#19273,.F.);
#28063=ORIENTED_EDGE('',*,*,#19041,.F.);
#28064=ORIENTED_EDGE('',*,*,#19274,.F.);
#28065=ORIENTED_EDGE('',*,*,#18387,.T.);
#28066=ORIENTED_EDGE('',*,*,#19275,.F.);
#28067=ORIENTED_EDGE('',*,*,#19044,.F.);
#28068=ORIENTED_EDGE('',*,*,#19276,.F.);
#28069=ORIENTED_EDGE('',*,*,#18390,.T.);
#28070=ORIENTED_EDGE('',*,*,#19277,.F.);
#28071=ORIENTED_EDGE('',*,*,#19047,.F.);
#28072=ORIENTED_EDGE('',*,*,#19278,.F.);
#28073=ORIENTED_EDGE('',*,*,#18393,.T.);
#28074=ORIENTED_EDGE('',*,*,#19279,.F.);
#28075=ORIENTED_EDGE('',*,*,#19050,.F.);
#28076=ORIENTED_EDGE('',*,*,#19280,.F.);
#28077=ORIENTED_EDGE('',*,*,#18396,.T.);
#28078=ORIENTED_EDGE('',*,*,#19281,.F.);
#28079=ORIENTED_EDGE('',*,*,#19053,.F.);
#28080=ORIENTED_EDGE('',*,*,#19282,.F.);
#28081=ORIENTED_EDGE('',*,*,#18400,.T.);
#28082=ORIENTED_EDGE('',*,*,#19283,.F.);
#28083=ORIENTED_EDGE('',*,*,#19056,.F.);
#28084=ORIENTED_EDGE('',*,*,#19284,.F.);
#28085=ORIENTED_EDGE('',*,*,#18404,.T.);
#28086=ORIENTED_EDGE('',*,*,#19285,.F.);
#28087=ORIENTED_EDGE('',*,*,#19059,.F.);
#28088=ORIENTED_EDGE('',*,*,#19286,.F.);
#28089=ORIENTED_EDGE('',*,*,#18408,.T.);
#28090=ORIENTED_EDGE('',*,*,#19287,.F.);
#28091=ORIENTED_EDGE('',*,*,#19062,.F.);
#28092=ORIENTED_EDGE('',*,*,#19288,.F.);
#28093=ORIENTED_EDGE('',*,*,#18412,.T.);
#28094=ORIENTED_EDGE('',*,*,#19289,.F.);
#28095=ORIENTED_EDGE('',*,*,#19065,.F.);
#28096=ORIENTED_EDGE('',*,*,#19290,.F.);
#28097=ORIENTED_EDGE('',*,*,#18416,.T.);
#28098=ORIENTED_EDGE('',*,*,#19291,.F.);
#28099=ORIENTED_EDGE('',*,*,#19068,.F.);
#28100=ORIENTED_EDGE('',*,*,#19292,.F.);
#28101=ORIENTED_EDGE('',*,*,#18420,.T.);
#28102=ORIENTED_EDGE('',*,*,#19293,.F.);
#28103=ORIENTED_EDGE('',*,*,#19071,.F.);
#28104=ORIENTED_EDGE('',*,*,#19294,.F.);
#28105=ORIENTED_EDGE('',*,*,#18424,.T.);
#28106=ORIENTED_EDGE('',*,*,#19295,.F.);
#28107=ORIENTED_EDGE('',*,*,#19074,.F.);
#28108=ORIENTED_EDGE('',*,*,#19296,.F.);
#28109=ORIENTED_EDGE('',*,*,#18428,.T.);
#28110=ORIENTED_EDGE('',*,*,#19297,.F.);
#28111=ORIENTED_EDGE('',*,*,#19077,.F.);
#28112=ORIENTED_EDGE('',*,*,#19298,.F.);
#28113=ORIENTED_EDGE('',*,*,#18432,.T.);
#28114=ORIENTED_EDGE('',*,*,#19299,.F.);
#28115=ORIENTED_EDGE('',*,*,#19080,.F.);
#28116=ORIENTED_EDGE('',*,*,#19300,.F.);
#28117=ORIENTED_EDGE('',*,*,#18436,.T.);
#28118=ORIENTED_EDGE('',*,*,#19301,.F.);
#28119=ORIENTED_EDGE('',*,*,#19083,.F.);
#28120=ORIENTED_EDGE('',*,*,#19302,.F.);
#28121=ORIENTED_EDGE('',*,*,#18440,.T.);
#28122=ORIENTED_EDGE('',*,*,#19303,.F.);
#28123=ORIENTED_EDGE('',*,*,#19086,.F.);
#28124=ORIENTED_EDGE('',*,*,#19304,.F.);
#28125=ORIENTED_EDGE('',*,*,#18444,.T.);
#28126=ORIENTED_EDGE('',*,*,#19305,.F.);
#28127=ORIENTED_EDGE('',*,*,#19089,.F.);
#28128=ORIENTED_EDGE('',*,*,#19306,.F.);
#28129=ORIENTED_EDGE('',*,*,#18448,.T.);
#28130=ORIENTED_EDGE('',*,*,#19307,.F.);
#28131=ORIENTED_EDGE('',*,*,#19092,.F.);
#28132=ORIENTED_EDGE('',*,*,#19308,.F.);
#28133=ORIENTED_EDGE('',*,*,#18452,.T.);
#28134=ORIENTED_EDGE('',*,*,#19309,.F.);
#28135=ORIENTED_EDGE('',*,*,#19095,.F.);
#28136=ORIENTED_EDGE('',*,*,#19310,.F.);
#28137=ORIENTED_EDGE('',*,*,#18456,.T.);
#28138=ORIENTED_EDGE('',*,*,#19311,.F.);
#28139=ORIENTED_EDGE('',*,*,#19098,.F.);
#28140=ORIENTED_EDGE('',*,*,#19312,.F.);
#28141=ORIENTED_EDGE('',*,*,#18460,.T.);
#28142=ORIENTED_EDGE('',*,*,#19313,.F.);
#28143=ORIENTED_EDGE('',*,*,#19101,.F.);
#28144=ORIENTED_EDGE('',*,*,#19314,.F.);
#28145=ORIENTED_EDGE('',*,*,#18464,.T.);
#28146=ORIENTED_EDGE('',*,*,#19315,.F.);
#28147=ORIENTED_EDGE('',*,*,#19104,.F.);
#28148=ORIENTED_EDGE('',*,*,#19316,.F.);
#28149=ORIENTED_EDGE('',*,*,#18468,.T.);
#28150=ORIENTED_EDGE('',*,*,#19317,.F.);
#28151=ORIENTED_EDGE('',*,*,#19107,.F.);
#28152=ORIENTED_EDGE('',*,*,#19318,.F.);
#28153=ORIENTED_EDGE('',*,*,#18472,.T.);
#28154=ORIENTED_EDGE('',*,*,#19319,.F.);
#28155=ORIENTED_EDGE('',*,*,#19110,.F.);
#28156=ORIENTED_EDGE('',*,*,#19320,.F.);
#28157=ORIENTED_EDGE('',*,*,#18171,.T.);
#28158=ORIENTED_EDGE('',*,*,#19321,.F.);
#28159=ORIENTED_EDGE('',*,*,#19113,.F.);
#28160=ORIENTED_EDGE('',*,*,#19322,.F.);
#28161=ORIENTED_EDGE('',*,*,#18175,.T.);
#28162=ORIENTED_EDGE('',*,*,#19323,.F.);
#28163=ORIENTED_EDGE('',*,*,#19116,.F.);
#28164=ORIENTED_EDGE('',*,*,#19324,.F.);
#28165=ORIENTED_EDGE('',*,*,#18179,.T.);
#28166=ORIENTED_EDGE('',*,*,#19325,.F.);
#28167=ORIENTED_EDGE('',*,*,#19119,.F.);
#28168=ORIENTED_EDGE('',*,*,#19326,.F.);
#28169=ORIENTED_EDGE('',*,*,#18183,.T.);
#28170=ORIENTED_EDGE('',*,*,#19327,.F.);
#28171=ORIENTED_EDGE('',*,*,#19122,.F.);
#28172=ORIENTED_EDGE('',*,*,#19328,.F.);
#28173=ORIENTED_EDGE('',*,*,#18187,.T.);
#28174=ORIENTED_EDGE('',*,*,#19329,.F.);
#28175=ORIENTED_EDGE('',*,*,#19125,.F.);
#28176=ORIENTED_EDGE('',*,*,#19330,.F.);
#28177=ORIENTED_EDGE('',*,*,#18191,.T.);
#28178=ORIENTED_EDGE('',*,*,#19331,.F.);
#28179=ORIENTED_EDGE('',*,*,#19128,.F.);
#28180=ORIENTED_EDGE('',*,*,#19332,.F.);
#28181=ORIENTED_EDGE('',*,*,#18195,.T.);
#28182=ORIENTED_EDGE('',*,*,#19333,.F.);
#28183=ORIENTED_EDGE('',*,*,#19131,.F.);
#28184=ORIENTED_EDGE('',*,*,#19334,.F.);
#28185=ORIENTED_EDGE('',*,*,#18199,.T.);
#28186=ORIENTED_EDGE('',*,*,#19335,.F.);
#28187=ORIENTED_EDGE('',*,*,#19134,.F.);
#28188=ORIENTED_EDGE('',*,*,#19336,.F.);
#28189=ORIENTED_EDGE('',*,*,#18203,.T.);
#28190=ORIENTED_EDGE('',*,*,#19337,.F.);
#28191=ORIENTED_EDGE('',*,*,#19137,.F.);
#28192=ORIENTED_EDGE('',*,*,#19338,.F.);
#28193=ORIENTED_EDGE('',*,*,#18207,.T.);
#28194=ORIENTED_EDGE('',*,*,#19339,.F.);
#28195=ORIENTED_EDGE('',*,*,#19140,.F.);
#28196=ORIENTED_EDGE('',*,*,#19340,.F.);
#28197=ORIENTED_EDGE('',*,*,#18211,.T.);
#28198=ORIENTED_EDGE('',*,*,#19341,.F.);
#28199=ORIENTED_EDGE('',*,*,#19143,.F.);
#28200=ORIENTED_EDGE('',*,*,#19342,.F.);
#28201=ORIENTED_EDGE('',*,*,#18215,.T.);
#28202=ORIENTED_EDGE('',*,*,#19343,.F.);
#28203=ORIENTED_EDGE('',*,*,#19146,.F.);
#28204=ORIENTED_EDGE('',*,*,#19344,.F.);
#28205=ORIENTED_EDGE('',*,*,#18219,.T.);
#28206=ORIENTED_EDGE('',*,*,#19345,.F.);
#28207=ORIENTED_EDGE('',*,*,#19149,.F.);
#28208=ORIENTED_EDGE('',*,*,#19346,.F.);
#28209=ORIENTED_EDGE('',*,*,#18223,.T.);
#28210=ORIENTED_EDGE('',*,*,#19347,.F.);
#28211=ORIENTED_EDGE('',*,*,#19152,.F.);
#28212=ORIENTED_EDGE('',*,*,#19348,.F.);
#28213=ORIENTED_EDGE('',*,*,#18227,.T.);
#28214=ORIENTED_EDGE('',*,*,#19349,.F.);
#28215=ORIENTED_EDGE('',*,*,#19155,.F.);
#28216=ORIENTED_EDGE('',*,*,#19350,.F.);
#28217=ORIENTED_EDGE('',*,*,#18231,.T.);
#28218=ORIENTED_EDGE('',*,*,#19351,.F.);
#28219=ORIENTED_EDGE('',*,*,#19158,.F.);
#28220=ORIENTED_EDGE('',*,*,#19352,.F.);
#28221=ORIENTED_EDGE('',*,*,#18235,.T.);
#28222=ORIENTED_EDGE('',*,*,#19353,.F.);
#28223=ORIENTED_EDGE('',*,*,#19161,.F.);
#28224=ORIENTED_EDGE('',*,*,#19354,.F.);
#28225=ORIENTED_EDGE('',*,*,#18239,.T.);
#28226=ORIENTED_EDGE('',*,*,#19355,.F.);
#28227=ORIENTED_EDGE('',*,*,#19164,.F.);
#28228=ORIENTED_EDGE('',*,*,#19356,.F.);
#28229=ORIENTED_EDGE('',*,*,#18243,.T.);
#28230=ORIENTED_EDGE('',*,*,#19357,.F.);
#28231=ORIENTED_EDGE('',*,*,#19167,.F.);
#28232=ORIENTED_EDGE('',*,*,#19358,.F.);
#28233=ORIENTED_EDGE('',*,*,#18247,.T.);
#28234=ORIENTED_EDGE('',*,*,#19359,.F.);
#28235=ORIENTED_EDGE('',*,*,#19170,.F.);
#28236=ORIENTED_EDGE('',*,*,#19360,.F.);
#28237=ORIENTED_EDGE('',*,*,#18251,.T.);
#28238=ORIENTED_EDGE('',*,*,#19361,.F.);
#28239=ORIENTED_EDGE('',*,*,#19173,.F.);
#28240=ORIENTED_EDGE('',*,*,#19362,.F.);
#28241=ORIENTED_EDGE('',*,*,#18255,.T.);
#28242=ORIENTED_EDGE('',*,*,#19363,.F.);
#28243=ORIENTED_EDGE('',*,*,#19176,.F.);
#28244=ORIENTED_EDGE('',*,*,#19364,.F.);
#28245=ORIENTED_EDGE('',*,*,#18259,.T.);
#28246=ORIENTED_EDGE('',*,*,#19365,.F.);
#28247=ORIENTED_EDGE('',*,*,#19179,.F.);
#28248=ORIENTED_EDGE('',*,*,#19366,.F.);
#28249=ORIENTED_EDGE('',*,*,#18263,.T.);
#28250=ORIENTED_EDGE('',*,*,#19367,.F.);
#28251=ORIENTED_EDGE('',*,*,#19182,.F.);
#28252=ORIENTED_EDGE('',*,*,#19368,.F.);
#28253=ORIENTED_EDGE('',*,*,#18267,.T.);
#28254=ORIENTED_EDGE('',*,*,#19369,.F.);
#28255=ORIENTED_EDGE('',*,*,#19185,.F.);
#28256=ORIENTED_EDGE('',*,*,#19370,.F.);
#28257=ORIENTED_EDGE('',*,*,#18271,.T.);
#28258=ORIENTED_EDGE('',*,*,#19371,.F.);
#28259=ORIENTED_EDGE('',*,*,#19188,.F.);
#28260=ORIENTED_EDGE('',*,*,#19372,.F.);
#28261=ORIENTED_EDGE('',*,*,#18275,.T.);
#28262=ORIENTED_EDGE('',*,*,#19373,.F.);
#28263=ORIENTED_EDGE('',*,*,#19191,.F.);
#28264=ORIENTED_EDGE('',*,*,#19374,.F.);
#28265=ORIENTED_EDGE('',*,*,#18279,.T.);
#28266=ORIENTED_EDGE('',*,*,#19375,.F.);
#28267=ORIENTED_EDGE('',*,*,#19194,.F.);
#28268=ORIENTED_EDGE('',*,*,#19376,.F.);
#28269=ORIENTED_EDGE('',*,*,#18283,.T.);
#28270=ORIENTED_EDGE('',*,*,#19377,.F.);
#28271=ORIENTED_EDGE('',*,*,#19197,.F.);
#28272=ORIENTED_EDGE('',*,*,#19378,.F.);
#28273=ORIENTED_EDGE('',*,*,#18287,.T.);
#28274=ORIENTED_EDGE('',*,*,#19379,.F.);
#28275=ORIENTED_EDGE('',*,*,#19200,.F.);
#28276=ORIENTED_EDGE('',*,*,#19380,.F.);
#28277=ORIENTED_EDGE('',*,*,#18291,.T.);
#28278=ORIENTED_EDGE('',*,*,#19381,.F.);
#28279=ORIENTED_EDGE('',*,*,#19203,.F.);
#28280=ORIENTED_EDGE('',*,*,#19382,.F.);
#28281=ORIENTED_EDGE('',*,*,#18295,.T.);
#28282=ORIENTED_EDGE('',*,*,#19383,.F.);
#28283=ORIENTED_EDGE('',*,*,#19206,.F.);
#28284=ORIENTED_EDGE('',*,*,#19384,.F.);
#28285=ORIENTED_EDGE('',*,*,#18299,.T.);
#28286=ORIENTED_EDGE('',*,*,#19385,.F.);
#28287=ORIENTED_EDGE('',*,*,#19209,.F.);
#28288=ORIENTED_EDGE('',*,*,#19386,.F.);
#28289=ORIENTED_EDGE('',*,*,#18303,.T.);
#28290=ORIENTED_EDGE('',*,*,#19387,.F.);
#28291=ORIENTED_EDGE('',*,*,#19212,.F.);
#28292=ORIENTED_EDGE('',*,*,#19388,.F.);
#28293=ORIENTED_EDGE('',*,*,#18307,.T.);
#28294=ORIENTED_EDGE('',*,*,#19389,.F.);
#28295=ORIENTED_EDGE('',*,*,#19215,.F.);
#28296=ORIENTED_EDGE('',*,*,#19390,.F.);
#28297=ORIENTED_EDGE('',*,*,#18311,.T.);
#28298=ORIENTED_EDGE('',*,*,#19391,.F.);
#28299=ORIENTED_EDGE('',*,*,#19218,.F.);
#28300=ORIENTED_EDGE('',*,*,#19392,.F.);
#28301=ORIENTED_EDGE('',*,*,#18315,.T.);
#28302=ORIENTED_EDGE('',*,*,#19393,.F.);
#28303=ORIENTED_EDGE('',*,*,#19221,.F.);
#28304=ORIENTED_EDGE('',*,*,#19394,.F.);
#28305=ORIENTED_EDGE('',*,*,#18319,.T.);
#28306=ORIENTED_EDGE('',*,*,#19395,.F.);
#28307=ORIENTED_EDGE('',*,*,#18375,.T.);
#28308=ORIENTED_EDGE('',*,*,#19396,.F.);
#28309=ORIENTED_EDGE('',*,*,#19223,.F.);
#28310=ORIENTED_EDGE('',*,*,#19397,.F.);
#28311=ORIENTED_EDGE('',*,*,#18372,.T.);
#28312=ORIENTED_EDGE('',*,*,#19398,.F.);
#28313=ORIENTED_EDGE('',*,*,#19226,.F.);
#28314=ORIENTED_EDGE('',*,*,#19399,.F.);
#28315=ORIENTED_EDGE('',*,*,#18369,.T.);
#28316=ORIENTED_EDGE('',*,*,#19400,.F.);
#28317=ORIENTED_EDGE('',*,*,#19229,.F.);
#28318=ORIENTED_EDGE('',*,*,#19401,.F.);
#28319=ORIENTED_EDGE('',*,*,#18366,.T.);
#28320=ORIENTED_EDGE('',*,*,#19402,.F.);
#28321=ORIENTED_EDGE('',*,*,#19232,.F.);
#28322=ORIENTED_EDGE('',*,*,#19403,.F.);
#28323=ORIENTED_EDGE('',*,*,#18363,.T.);
#28324=ORIENTED_EDGE('',*,*,#19404,.F.);
#28325=ORIENTED_EDGE('',*,*,#19235,.F.);
#28326=ORIENTED_EDGE('',*,*,#19405,.F.);
#28327=ORIENTED_EDGE('',*,*,#18360,.T.);
#28328=ORIENTED_EDGE('',*,*,#19406,.F.);
#28329=ORIENTED_EDGE('',*,*,#19238,.F.);
#28330=ORIENTED_EDGE('',*,*,#19407,.F.);
#28331=ORIENTED_EDGE('',*,*,#18357,.T.);
#28332=ORIENTED_EDGE('',*,*,#19408,.F.);
#28333=ORIENTED_EDGE('',*,*,#19241,.F.);
#28334=ORIENTED_EDGE('',*,*,#19409,.F.);
#28335=ORIENTED_EDGE('',*,*,#18354,.T.);
#28336=ORIENTED_EDGE('',*,*,#19410,.F.);
#28337=ORIENTED_EDGE('',*,*,#19244,.F.);
#28338=ORIENTED_EDGE('',*,*,#19411,.F.);
#28339=ORIENTED_EDGE('',*,*,#18351,.T.);
#28340=ORIENTED_EDGE('',*,*,#19412,.F.);
#28341=ORIENTED_EDGE('',*,*,#19247,.F.);
#28342=ORIENTED_EDGE('',*,*,#19413,.F.);
#28343=ORIENTED_EDGE('',*,*,#18347,.T.);
#28344=ORIENTED_EDGE('',*,*,#19414,.F.);
#28345=ORIENTED_EDGE('',*,*,#19250,.F.);
#28346=ORIENTED_EDGE('',*,*,#19415,.F.);
#28347=ORIENTED_EDGE('',*,*,#18343,.T.);
#28348=ORIENTED_EDGE('',*,*,#19416,.F.);
#28349=ORIENTED_EDGE('',*,*,#19253,.F.);
#28350=ORIENTED_EDGE('',*,*,#19417,.F.);
#28351=ORIENTED_EDGE('',*,*,#18339,.T.);
#28352=ORIENTED_EDGE('',*,*,#19418,.F.);
#28353=ORIENTED_EDGE('',*,*,#19256,.F.);
#28354=ORIENTED_EDGE('',*,*,#19419,.F.);
#28355=ORIENTED_EDGE('',*,*,#18335,.T.);
#28356=ORIENTED_EDGE('',*,*,#19420,.F.);
#28357=ORIENTED_EDGE('',*,*,#19259,.F.);
#28358=ORIENTED_EDGE('',*,*,#19421,.F.);
#28359=ORIENTED_EDGE('',*,*,#18331,.T.);
#28360=ORIENTED_EDGE('',*,*,#19422,.F.);
#28361=ORIENTED_EDGE('',*,*,#19262,.F.);
#28362=ORIENTED_EDGE('',*,*,#19423,.F.);
#28363=ORIENTED_EDGE('',*,*,#19266,.F.);
#28364=ORIENTED_EDGE('',*,*,#19424,.F.);
#28365=ORIENTED_EDGE('',*,*,#18323,.T.);
#28366=ORIENTED_EDGE('',*,*,#18001,.T.);
#28367=ORIENTED_EDGE('',*,*,#18091,.T.);
#28368=ORIENTED_EDGE('',*,*,#17998,.T.);
#28369=ORIENTED_EDGE('',*,*,#18789,.T.);
#28370=ORIENTED_EDGE('',*,*,#18792,.F.);
#28371=ORIENTED_EDGE('',*,*,#19425,.F.);
#28372=ORIENTED_EDGE('',*,*,#18478,.F.);
#28373=ORIENTED_EDGE('',*,*,#19426,.F.);
#28374=ORIENTED_EDGE('',*,*,#19427,.T.);
#28375=ORIENTED_EDGE('',*,*,#19428,.F.);
#28376=ORIENTED_EDGE('',*,*,#19427,.F.);
#28377=ORIENTED_EDGE('',*,*,#19429,.F.);
#28378=ORIENTED_EDGE('',*,*,#19430,.T.);
#28379=ORIENTED_EDGE('',*,*,#19431,.F.);
#28380=ORIENTED_EDGE('',*,*,#19430,.F.);
#28381=ORIENTED_EDGE('',*,*,#19432,.F.);
#28382=ORIENTED_EDGE('',*,*,#18327,.T.);
#28383=ORIENTED_EDGE('',*,*,#18168,.F.);
#28384=ORIENTED_EDGE('',*,*,#18165,.F.);
#28385=ORIENTED_EDGE('',*,*,#19433,.T.);
#28386=ORIENTED_EDGE('',*,*,#19434,.T.);
#28387=ORIENTED_EDGE('',*,*,#19435,.T.);
#28388=ORIENTED_EDGE('',*,*,#19436,.T.);
#28389=ORIENTED_EDGE('',*,*,#19437,.T.);
#28390=ORIENTED_EDGE('',*,*,#19438,.T.);
#28391=ORIENTED_EDGE('',*,*,#19439,.T.);
#28392=ORIENTED_EDGE('',*,*,#18160,.T.);
#28393=ORIENTED_EDGE('',*,*,#19440,.F.);
#28394=ORIENTED_EDGE('',*,*,#19434,.F.);
#28395=ORIENTED_EDGE('',*,*,#19440,.T.);
#28396=ORIENTED_EDGE('',*,*,#18159,.T.);
#28397=ORIENTED_EDGE('',*,*,#19441,.F.);
#28398=ORIENTED_EDGE('',*,*,#19435,.F.);
#28399=ORIENTED_EDGE('',*,*,#19441,.T.);
#28400=ORIENTED_EDGE('',*,*,#18158,.T.);
#28401=ORIENTED_EDGE('',*,*,#19442,.F.);
#28402=ORIENTED_EDGE('',*,*,#19436,.F.);
#28403=ORIENTED_EDGE('',*,*,#19442,.T.);
#28404=ORIENTED_EDGE('',*,*,#18157,.T.);
#28405=ORIENTED_EDGE('',*,*,#18163,.T.);
#28406=ORIENTED_EDGE('',*,*,#19443,.F.);
#28407=ORIENTED_EDGE('',*,*,#19437,.F.);
#28408=ORIENTED_EDGE('',*,*,#19443,.T.);
#28409=ORIENTED_EDGE('',*,*,#18162,.T.);
#28410=ORIENTED_EDGE('',*,*,#19444,.F.);
#28411=ORIENTED_EDGE('',*,*,#19438,.F.);
#28412=ORIENTED_EDGE('',*,*,#19444,.T.);
#28413=ORIENTED_EDGE('',*,*,#18161,.T.);
#28414=ORIENTED_EDGE('',*,*,#19439,.F.);
#28415=ORIENTED_EDGE('',*,*,#19433,.F.);
#28416=ORIENTED_EDGE('',*,*,#19445,.F.);
#28417=ORIENTED_EDGE('',*,*,#18089,.F.);
#28418=ORIENTED_EDGE('',*,*,#18088,.F.);
#28419=ORIENTED_EDGE('',*,*,#18085,.F.);
#28420=ORIENTED_EDGE('',*,*,#18082,.F.);
#28421=ORIENTED_EDGE('',*,*,#18079,.F.);
#28422=ORIENTED_EDGE('',*,*,#18076,.F.);
#28423=ORIENTED_EDGE('',*,*,#18073,.F.);
#28424=ORIENTED_EDGE('',*,*,#18070,.F.);
#28425=ORIENTED_EDGE('',*,*,#18067,.F.);
#28426=ORIENTED_EDGE('',*,*,#18064,.F.);
#28427=ORIENTED_EDGE('',*,*,#18061,.F.);
#28428=ORIENTED_EDGE('',*,*,#18058,.F.);
#28429=ORIENTED_EDGE('',*,*,#18055,.F.);
#28430=ORIENTED_EDGE('',*,*,#18052,.F.);
#28431=ORIENTED_EDGE('',*,*,#18049,.F.);
#28432=ORIENTED_EDGE('',*,*,#18046,.F.);
#28433=ORIENTED_EDGE('',*,*,#18043,.F.);
#28434=ORIENTED_EDGE('',*,*,#18040,.F.);
#28435=ORIENTED_EDGE('',*,*,#18037,.F.);
#28436=ORIENTED_EDGE('',*,*,#18034,.F.);
#28437=ORIENTED_EDGE('',*,*,#18031,.F.);
#28438=ORIENTED_EDGE('',*,*,#18028,.F.);
#28439=ORIENTED_EDGE('',*,*,#18025,.F.);
#28440=ORIENTED_EDGE('',*,*,#18022,.F.);
#28441=ORIENTED_EDGE('',*,*,#18019,.F.);
#28442=ORIENTED_EDGE('',*,*,#18016,.F.);
#28443=ORIENTED_EDGE('',*,*,#18013,.F.);
#28444=ORIENTED_EDGE('',*,*,#18010,.F.);
#28445=ORIENTED_EDGE('',*,*,#18007,.F.);
#28446=ORIENTED_EDGE('',*,*,#18004,.F.);
#28447=ORIENTED_EDGE('',*,*,#17997,.F.);
#28448=ORIENTED_EDGE('',*,*,#18094,.F.);
#28449=ORIENTED_EDGE('',*,*,#18095,.T.);
#28450=ORIENTED_EDGE('',*,*,#17995,.T.);
#28451=ORIENTED_EDGE('',*,*,#17992,.T.);
#28452=ORIENTED_EDGE('',*,*,#17989,.T.);
#28453=ORIENTED_EDGE('',*,*,#17986,.T.);
#28454=ORIENTED_EDGE('',*,*,#17983,.T.);
#28455=ORIENTED_EDGE('',*,*,#17980,.T.);
#28456=ORIENTED_EDGE('',*,*,#17977,.T.);
#28457=ORIENTED_EDGE('',*,*,#17974,.T.);
#28458=ORIENTED_EDGE('',*,*,#17971,.T.);
#28459=ORIENTED_EDGE('',*,*,#17968,.T.);
#28460=ORIENTED_EDGE('',*,*,#17965,.T.);
#28461=ORIENTED_EDGE('',*,*,#17962,.T.);
#28462=ORIENTED_EDGE('',*,*,#17959,.T.);
#28463=ORIENTED_EDGE('',*,*,#17956,.T.);
#28464=ORIENTED_EDGE('',*,*,#17953,.T.);
#28465=ORIENTED_EDGE('',*,*,#17950,.T.);
#28466=ORIENTED_EDGE('',*,*,#17947,.T.);
#28467=ORIENTED_EDGE('',*,*,#17944,.T.);
#28468=ORIENTED_EDGE('',*,*,#17941,.T.);
#28469=ORIENTED_EDGE('',*,*,#17938,.T.);
#28470=ORIENTED_EDGE('',*,*,#17935,.T.);
#28471=ORIENTED_EDGE('',*,*,#17932,.T.);
#28472=ORIENTED_EDGE('',*,*,#17929,.T.);
#28473=ORIENTED_EDGE('',*,*,#17926,.T.);
#28474=ORIENTED_EDGE('',*,*,#17923,.T.);
#28475=ORIENTED_EDGE('',*,*,#17920,.T.);
#28476=ORIENTED_EDGE('',*,*,#17917,.T.);
#28477=ORIENTED_EDGE('',*,*,#17914,.T.);
#28478=ORIENTED_EDGE('',*,*,#19446,.F.);
#28479=ORIENTED_EDGE('',*,*,#17910,.T.);
#28480=ORIENTED_EDGE('',*,*,#17916,.T.);
#28481=ORIENTED_EDGE('',*,*,#17919,.T.);
#28482=ORIENTED_EDGE('',*,*,#17922,.T.);
#28483=ORIENTED_EDGE('',*,*,#17925,.T.);
#28484=ORIENTED_EDGE('',*,*,#17928,.T.);
#28485=ORIENTED_EDGE('',*,*,#17931,.T.);
#28486=ORIENTED_EDGE('',*,*,#17934,.T.);
#28487=ORIENTED_EDGE('',*,*,#17937,.T.);
#28488=ORIENTED_EDGE('',*,*,#17940,.T.);
#28489=ORIENTED_EDGE('',*,*,#17943,.T.);
#28490=ORIENTED_EDGE('',*,*,#17946,.T.);
#28491=ORIENTED_EDGE('',*,*,#17949,.T.);
#28492=ORIENTED_EDGE('',*,*,#17952,.T.);
#28493=ORIENTED_EDGE('',*,*,#17955,.T.);
#28494=ORIENTED_EDGE('',*,*,#17958,.T.);
#28495=ORIENTED_EDGE('',*,*,#17961,.T.);
#28496=ORIENTED_EDGE('',*,*,#17964,.T.);
#28497=ORIENTED_EDGE('',*,*,#17967,.T.);
#28498=ORIENTED_EDGE('',*,*,#17970,.T.);
#28499=ORIENTED_EDGE('',*,*,#17973,.T.);
#28500=ORIENTED_EDGE('',*,*,#17976,.T.);
#28501=ORIENTED_EDGE('',*,*,#17979,.T.);
#28502=ORIENTED_EDGE('',*,*,#17982,.T.);
#28503=ORIENTED_EDGE('',*,*,#17985,.T.);
#28504=ORIENTED_EDGE('',*,*,#17988,.T.);
#28505=ORIENTED_EDGE('',*,*,#17991,.T.);
#28506=ORIENTED_EDGE('',*,*,#17994,.T.);
#28507=ORIENTED_EDGE('',*,*,#18096,.T.);
#28508=ORIENTED_EDGE('',*,*,#18092,.F.);
#28509=ORIENTED_EDGE('',*,*,#18000,.T.);
#28510=ORIENTED_EDGE('',*,*,#18003,.T.);
#28511=ORIENTED_EDGE('',*,*,#18006,.T.);
#28512=ORIENTED_EDGE('',*,*,#18009,.T.);
#28513=ORIENTED_EDGE('',*,*,#18012,.T.);
#28514=ORIENTED_EDGE('',*,*,#18015,.T.);
#28515=ORIENTED_EDGE('',*,*,#18018,.T.);
#28516=ORIENTED_EDGE('',*,*,#18021,.T.);
#28517=ORIENTED_EDGE('',*,*,#18024,.T.);
#28518=ORIENTED_EDGE('',*,*,#18027,.T.);
#28519=ORIENTED_EDGE('',*,*,#18030,.T.);
#28520=ORIENTED_EDGE('',*,*,#18033,.T.);
#28521=ORIENTED_EDGE('',*,*,#18036,.T.);
#28522=ORIENTED_EDGE('',*,*,#18039,.T.);
#28523=ORIENTED_EDGE('',*,*,#18042,.T.);
#28524=ORIENTED_EDGE('',*,*,#18045,.T.);
#28525=ORIENTED_EDGE('',*,*,#18048,.T.);
#28526=ORIENTED_EDGE('',*,*,#18051,.T.);
#28527=ORIENTED_EDGE('',*,*,#18054,.T.);
#28528=ORIENTED_EDGE('',*,*,#18057,.T.);
#28529=ORIENTED_EDGE('',*,*,#18060,.T.);
#28530=ORIENTED_EDGE('',*,*,#18063,.T.);
#28531=ORIENTED_EDGE('',*,*,#18066,.T.);
#28532=ORIENTED_EDGE('',*,*,#18069,.T.);
#28533=ORIENTED_EDGE('',*,*,#18072,.T.);
#28534=ORIENTED_EDGE('',*,*,#18075,.T.);
#28535=ORIENTED_EDGE('',*,*,#18078,.T.);
#28536=ORIENTED_EDGE('',*,*,#18081,.T.);
#28537=ORIENTED_EDGE('',*,*,#18084,.T.);
#28538=ORIENTED_EDGE('',*,*,#18087,.T.);
#28539=ORIENTED_EDGE('',*,*,#18090,.T.);
#28540=ORIENTED_EDGE('',*,*,#19445,.T.);
#28541=ORIENTED_EDGE('',*,*,#17913,.T.);
#28542=ORIENTED_EDGE('',*,*,#19446,.T.);
#28543=ORIENTED_EDGE('',*,*,#18477,.T.);
#28544=ORIENTED_EDGE('',*,*,#19447,.T.);
#28545=ORIENTED_EDGE('',*,*,#18328,.T.);
#28546=ORIENTED_EDGE('',*,*,#19432,.T.);
#28547=ORIENTED_EDGE('',*,*,#19429,.T.);
#28548=ORIENTED_EDGE('',*,*,#19426,.T.);
#28549=ORIENTED_EDGE('',*,*,#18476,.T.);
#28550=ORIENTED_EDGE('',*,*,#18781,.T.);
#28551=ORIENTED_EDGE('',*,*,#19448,.T.);
#28552=ORIENTED_EDGE('',*,*,#18329,.T.);
#28553=ORIENTED_EDGE('',*,*,#19447,.F.);
#28554=ORIENTED_EDGE('',*,*,#18780,.T.);
#28555=ORIENTED_EDGE('',*,*,#19026,.T.);
#28556=ORIENTED_EDGE('',*,*,#19263,.T.);
#28557=ORIENTED_EDGE('',*,*,#19422,.T.);
#28558=ORIENTED_EDGE('',*,*,#18330,.T.);
#28559=ORIENTED_EDGE('',*,*,#19448,.F.);
#28560=ORIENTED_EDGE('',*,*,#18481,.T.);
#28561=ORIENTED_EDGE('',*,*,#19449,.T.);
#28562=ORIENTED_EDGE('',*,*,#18324,.T.);
#28563=ORIENTED_EDGE('',*,*,#19424,.T.);
#28564=ORIENTED_EDGE('',*,*,#19265,.T.);
#28565=ORIENTED_EDGE('',*,*,#19028,.T.);
#28566=ORIENTED_EDGE('',*,*,#18480,.T.);
#28567=ORIENTED_EDGE('',*,*,#19450,.T.);
#28568=ORIENTED_EDGE('',*,*,#18325,.T.);
#28569=ORIENTED_EDGE('',*,*,#19449,.F.);
#28570=ORIENTED_EDGE('',*,*,#18479,.T.);
#28571=ORIENTED_EDGE('',*,*,#19425,.T.);
#28572=ORIENTED_EDGE('',*,*,#19428,.T.);
#28573=ORIENTED_EDGE('',*,*,#19431,.T.);
#28574=ORIENTED_EDGE('',*,*,#18326,.T.);
#28575=ORIENTED_EDGE('',*,*,#19450,.F.);
#28576=ORIENTED_EDGE('',*,*,#18778,.T.);
#28577=ORIENTED_EDGE('',*,*,#19451,.T.);
#28578=ORIENTED_EDGE('',*,*,#18332,.T.);
#28579=ORIENTED_EDGE('',*,*,#19421,.T.);
#28580=ORIENTED_EDGE('',*,*,#19261,.T.);
#28581=ORIENTED_EDGE('',*,*,#19024,.T.);
#28582=ORIENTED_EDGE('',*,*,#18777,.T.);
#28583=ORIENTED_EDGE('',*,*,#19452,.T.);
#28584=ORIENTED_EDGE('',*,*,#18333,.T.);
#28585=ORIENTED_EDGE('',*,*,#19451,.F.);
#28586=ORIENTED_EDGE('',*,*,#18776,.T.);
#28587=ORIENTED_EDGE('',*,*,#19023,.T.);
#28588=ORIENTED_EDGE('',*,*,#19260,.T.);
#28589=ORIENTED_EDGE('',*,*,#19420,.T.);
#28590=ORIENTED_EDGE('',*,*,#18334,.T.);
#28591=ORIENTED_EDGE('',*,*,#19452,.F.);
#28592=ORIENTED_EDGE('',*,*,#18774,.T.);
#28593=ORIENTED_EDGE('',*,*,#19453,.T.);
#28594=ORIENTED_EDGE('',*,*,#18336,.T.);
#28595=ORIENTED_EDGE('',*,*,#19419,.T.);
#28596=ORIENTED_EDGE('',*,*,#19258,.T.);
#28597=ORIENTED_EDGE('',*,*,#19021,.T.);
#28598=ORIENTED_EDGE('',*,*,#18773,.T.);
#28599=ORIENTED_EDGE('',*,*,#19454,.T.);
#28600=ORIENTED_EDGE('',*,*,#18337,.T.);
#28601=ORIENTED_EDGE('',*,*,#19453,.F.);
#28602=ORIENTED_EDGE('',*,*,#18772,.T.);
#28603=ORIENTED_EDGE('',*,*,#19020,.T.);
#28604=ORIENTED_EDGE('',*,*,#19257,.T.);
#28605=ORIENTED_EDGE('',*,*,#19418,.T.);
#28606=ORIENTED_EDGE('',*,*,#18338,.T.);
#28607=ORIENTED_EDGE('',*,*,#19454,.F.);
#28608=ORIENTED_EDGE('',*,*,#18770,.T.);
#28609=ORIENTED_EDGE('',*,*,#19455,.T.);
#28610=ORIENTED_EDGE('',*,*,#18340,.T.);
#28611=ORIENTED_EDGE('',*,*,#19417,.T.);
#28612=ORIENTED_EDGE('',*,*,#19255,.T.);
#28613=ORIENTED_EDGE('',*,*,#19018,.T.);
#28614=ORIENTED_EDGE('',*,*,#18769,.T.);
#28615=ORIENTED_EDGE('',*,*,#19456,.T.);
#28616=ORIENTED_EDGE('',*,*,#18341,.T.);
#28617=ORIENTED_EDGE('',*,*,#19455,.F.);
#28618=ORIENTED_EDGE('',*,*,#18768,.T.);
#28619=ORIENTED_EDGE('',*,*,#19017,.T.);
#28620=ORIENTED_EDGE('',*,*,#19254,.T.);
#28621=ORIENTED_EDGE('',*,*,#19416,.T.);
#28622=ORIENTED_EDGE('',*,*,#18342,.T.);
#28623=ORIENTED_EDGE('',*,*,#19456,.F.);
#28624=ORIENTED_EDGE('',*,*,#18766,.T.);
#28625=ORIENTED_EDGE('',*,*,#19457,.T.);
#28626=ORIENTED_EDGE('',*,*,#18344,.T.);
#28627=ORIENTED_EDGE('',*,*,#19415,.T.);
#28628=ORIENTED_EDGE('',*,*,#19252,.T.);
#28629=ORIENTED_EDGE('',*,*,#19015,.T.);
#28630=ORIENTED_EDGE('',*,*,#18765,.T.);
#28631=ORIENTED_EDGE('',*,*,#19458,.T.);
#28632=ORIENTED_EDGE('',*,*,#18345,.T.);
#28633=ORIENTED_EDGE('',*,*,#19457,.F.);
#28634=ORIENTED_EDGE('',*,*,#18764,.T.);
#28635=ORIENTED_EDGE('',*,*,#19014,.T.);
#28636=ORIENTED_EDGE('',*,*,#19251,.T.);
#28637=ORIENTED_EDGE('',*,*,#19414,.T.);
#28638=ORIENTED_EDGE('',*,*,#18346,.T.);
#28639=ORIENTED_EDGE('',*,*,#19458,.F.);
#28640=ORIENTED_EDGE('',*,*,#18762,.T.);
#28641=ORIENTED_EDGE('',*,*,#19459,.T.);
#28642=ORIENTED_EDGE('',*,*,#18348,.T.);
#28643=ORIENTED_EDGE('',*,*,#19413,.T.);
#28644=ORIENTED_EDGE('',*,*,#19249,.T.);
#28645=ORIENTED_EDGE('',*,*,#19012,.T.);
#28646=ORIENTED_EDGE('',*,*,#18761,.T.);
#28647=ORIENTED_EDGE('',*,*,#19460,.T.);
#28648=ORIENTED_EDGE('',*,*,#18349,.T.);
#28649=ORIENTED_EDGE('',*,*,#19459,.F.);
#28650=ORIENTED_EDGE('',*,*,#18760,.T.);
#28651=ORIENTED_EDGE('',*,*,#19011,.T.);
#28652=ORIENTED_EDGE('',*,*,#19248,.T.);
#28653=ORIENTED_EDGE('',*,*,#19412,.T.);
#28654=ORIENTED_EDGE('',*,*,#18350,.T.);
#28655=ORIENTED_EDGE('',*,*,#19460,.F.);
#28656=ORIENTED_EDGE('',*,*,#18758,.T.);
#28657=ORIENTED_EDGE('',*,*,#18156,.T.);
#28658=ORIENTED_EDGE('',*,*,#18352,.T.);
#28659=ORIENTED_EDGE('',*,*,#19411,.T.);
#28660=ORIENTED_EDGE('',*,*,#19246,.T.);
#28661=ORIENTED_EDGE('',*,*,#19009,.T.);
#28662=ORIENTED_EDGE('',*,*,#18757,.T.);
#28663=ORIENTED_EDGE('',*,*,#19008,.T.);
#28664=ORIENTED_EDGE('',*,*,#19245,.T.);
#28665=ORIENTED_EDGE('',*,*,#19410,.T.);
#28666=ORIENTED_EDGE('',*,*,#18353,.T.);
#28667=ORIENTED_EDGE('',*,*,#18154,.F.);
#28668=ORIENTED_EDGE('',*,*,#18755,.T.);
#28669=ORIENTED_EDGE('',*,*,#18152,.T.);
#28670=ORIENTED_EDGE('',*,*,#18355,.T.);
#28671=ORIENTED_EDGE('',*,*,#19409,.T.);
#28672=ORIENTED_EDGE('',*,*,#19243,.T.);
#28673=ORIENTED_EDGE('',*,*,#19006,.T.);
#28674=ORIENTED_EDGE('',*,*,#18754,.T.);
#28675=ORIENTED_EDGE('',*,*,#19005,.T.);
#28676=ORIENTED_EDGE('',*,*,#19242,.T.);
#28677=ORIENTED_EDGE('',*,*,#19408,.T.);
#28678=ORIENTED_EDGE('',*,*,#18356,.T.);
#28679=ORIENTED_EDGE('',*,*,#18150,.F.);
#28680=ORIENTED_EDGE('',*,*,#18752,.T.);
#28681=ORIENTED_EDGE('',*,*,#18148,.T.);
#28682=ORIENTED_EDGE('',*,*,#18358,.T.);
#28683=ORIENTED_EDGE('',*,*,#19407,.T.);
#28684=ORIENTED_EDGE('',*,*,#19240,.T.);
#28685=ORIENTED_EDGE('',*,*,#19003,.T.);
#28686=ORIENTED_EDGE('',*,*,#18751,.T.);
#28687=ORIENTED_EDGE('',*,*,#19002,.T.);
#28688=ORIENTED_EDGE('',*,*,#19239,.T.);
#28689=ORIENTED_EDGE('',*,*,#19406,.T.);
#28690=ORIENTED_EDGE('',*,*,#18359,.T.);
#28691=ORIENTED_EDGE('',*,*,#18146,.F.);
#28692=ORIENTED_EDGE('',*,*,#18749,.T.);
#28693=ORIENTED_EDGE('',*,*,#18144,.T.);
#28694=ORIENTED_EDGE('',*,*,#18361,.T.);
#28695=ORIENTED_EDGE('',*,*,#19405,.T.);
#28696=ORIENTED_EDGE('',*,*,#19237,.T.);
#28697=ORIENTED_EDGE('',*,*,#19000,.T.);
#28698=ORIENTED_EDGE('',*,*,#18748,.T.);
#28699=ORIENTED_EDGE('',*,*,#18999,.T.);
#28700=ORIENTED_EDGE('',*,*,#19236,.T.);
#28701=ORIENTED_EDGE('',*,*,#19404,.T.);
#28702=ORIENTED_EDGE('',*,*,#18362,.T.);
#28703=ORIENTED_EDGE('',*,*,#18142,.F.);
#28704=ORIENTED_EDGE('',*,*,#18746,.T.);
#28705=ORIENTED_EDGE('',*,*,#18140,.T.);
#28706=ORIENTED_EDGE('',*,*,#18364,.T.);
#28707=ORIENTED_EDGE('',*,*,#19403,.T.);
#28708=ORIENTED_EDGE('',*,*,#19234,.T.);
#28709=ORIENTED_EDGE('',*,*,#18997,.T.);
#28710=ORIENTED_EDGE('',*,*,#18745,.T.);
#28711=ORIENTED_EDGE('',*,*,#18996,.T.);
#28712=ORIENTED_EDGE('',*,*,#19233,.T.);
#28713=ORIENTED_EDGE('',*,*,#19402,.T.);
#28714=ORIENTED_EDGE('',*,*,#18365,.T.);
#28715=ORIENTED_EDGE('',*,*,#18138,.F.);
#28716=ORIENTED_EDGE('',*,*,#18743,.T.);
#28717=ORIENTED_EDGE('',*,*,#18136,.T.);
#28718=ORIENTED_EDGE('',*,*,#18367,.T.);
#28719=ORIENTED_EDGE('',*,*,#19401,.T.);
#28720=ORIENTED_EDGE('',*,*,#19231,.T.);
#28721=ORIENTED_EDGE('',*,*,#18994,.T.);
#28722=ORIENTED_EDGE('',*,*,#18742,.T.);
#28723=ORIENTED_EDGE('',*,*,#18993,.T.);
#28724=ORIENTED_EDGE('',*,*,#19230,.T.);
#28725=ORIENTED_EDGE('',*,*,#19400,.T.);
#28726=ORIENTED_EDGE('',*,*,#18368,.T.);
#28727=ORIENTED_EDGE('',*,*,#18134,.F.);
#28728=ORIENTED_EDGE('',*,*,#18740,.T.);
#28729=ORIENTED_EDGE('',*,*,#18132,.T.);
#28730=ORIENTED_EDGE('',*,*,#18370,.T.);
#28731=ORIENTED_EDGE('',*,*,#19399,.T.);
#28732=ORIENTED_EDGE('',*,*,#19228,.T.);
#28733=ORIENTED_EDGE('',*,*,#18991,.T.);
#28734=ORIENTED_EDGE('',*,*,#18739,.T.);
#28735=ORIENTED_EDGE('',*,*,#18990,.T.);
#28736=ORIENTED_EDGE('',*,*,#19227,.T.);
#28737=ORIENTED_EDGE('',*,*,#19398,.T.);
#28738=ORIENTED_EDGE('',*,*,#18371,.T.);
#28739=ORIENTED_EDGE('',*,*,#18130,.F.);
#28740=ORIENTED_EDGE('',*,*,#18737,.T.);
#28741=ORIENTED_EDGE('',*,*,#18128,.T.);
#28742=ORIENTED_EDGE('',*,*,#18373,.T.);
#28743=ORIENTED_EDGE('',*,*,#19397,.T.);
#28744=ORIENTED_EDGE('',*,*,#19225,.T.);
#28745=ORIENTED_EDGE('',*,*,#18988,.T.);
#28746=ORIENTED_EDGE('',*,*,#18736,.T.);
#28747=ORIENTED_EDGE('',*,*,#18987,.T.);
#28748=ORIENTED_EDGE('',*,*,#19224,.T.);
#28749=ORIENTED_EDGE('',*,*,#19396,.T.);
#28750=ORIENTED_EDGE('',*,*,#18374,.T.);
#28751=ORIENTED_EDGE('',*,*,#18126,.F.);
#28752=ORIENTED_EDGE('',*,*,#18734,.T.);
#28753=ORIENTED_EDGE('',*,*,#18124,.T.);
#28754=ORIENTED_EDGE('',*,*,#18376,.T.);
#28755=ORIENTED_EDGE('',*,*,#19395,.T.);
#28756=ORIENTED_EDGE('',*,*,#19222,.T.);
#28757=ORIENTED_EDGE('',*,*,#18985,.T.);
#28758=ORIENTED_EDGE('',*,*,#18733,.T.);
#28759=ORIENTED_EDGE('',*,*,#18795,.T.);
#28760=ORIENTED_EDGE('',*,*,#19032,.T.);
#28761=ORIENTED_EDGE('',*,*,#19268,.T.);
#28762=ORIENTED_EDGE('',*,*,#18377,.T.);
#28763=ORIENTED_EDGE('',*,*,#18122,.F.);
#28764=ORIENTED_EDGE('',*,*,#18485,.T.);
#28765=ORIENTED_EDGE('',*,*,#19461,.T.);
#28766=ORIENTED_EDGE('',*,*,#18320,.T.);
#28767=ORIENTED_EDGE('',*,*,#19394,.T.);
#28768=ORIENTED_EDGE('',*,*,#19220,.T.);
#28769=ORIENTED_EDGE('',*,*,#18983,.T.);
#28770=ORIENTED_EDGE('',*,*,#18484,.T.);
#28771=ORIENTED_EDGE('',*,*,#19462,.T.);
#28772=ORIENTED_EDGE('',*,*,#18321,.T.);
#28773=ORIENTED_EDGE('',*,*,#19461,.F.);
#28774=ORIENTED_EDGE('',*,*,#18483,.T.);
#28775=ORIENTED_EDGE('',*,*,#19027,.T.);
#28776=ORIENTED_EDGE('',*,*,#19264,.T.);
#28777=ORIENTED_EDGE('',*,*,#19423,.T.);
#28778=ORIENTED_EDGE('',*,*,#18322,.T.);
#28779=ORIENTED_EDGE('',*,*,#19462,.F.);
#28780=ORIENTED_EDGE('',*,*,#18489,.T.);
#28781=ORIENTED_EDGE('',*,*,#19463,.T.);
#28782=ORIENTED_EDGE('',*,*,#18316,.T.);
#28783=ORIENTED_EDGE('',*,*,#19392,.T.);
#28784=ORIENTED_EDGE('',*,*,#19217,.T.);
#28785=ORIENTED_EDGE('',*,*,#18980,.T.);
#28786=ORIENTED_EDGE('',*,*,#18488,.T.);
#28787=ORIENTED_EDGE('',*,*,#19464,.T.);
#28788=ORIENTED_EDGE('',*,*,#18317,.T.);
#28789=ORIENTED_EDGE('',*,*,#19463,.F.);
#28790=ORIENTED_EDGE('',*,*,#18487,.T.);
#28791=ORIENTED_EDGE('',*,*,#18982,.T.);
#28792=ORIENTED_EDGE('',*,*,#19219,.T.);
#28793=ORIENTED_EDGE('',*,*,#19393,.T.);
#28794=ORIENTED_EDGE('',*,*,#18318,.T.);
#28795=ORIENTED_EDGE('',*,*,#19464,.F.);
#28796=ORIENTED_EDGE('',*,*,#18493,.T.);
#28797=ORIENTED_EDGE('',*,*,#19465,.T.);
#28798=ORIENTED_EDGE('',*,*,#18312,.T.);
#28799=ORIENTED_EDGE('',*,*,#19390,.T.);
#28800=ORIENTED_EDGE('',*,*,#19214,.T.);
#28801=ORIENTED_EDGE('',*,*,#18977,.T.);
#28802=ORIENTED_EDGE('',*,*,#18492,.T.);
#28803=ORIENTED_EDGE('',*,*,#19466,.T.);
#28804=ORIENTED_EDGE('',*,*,#18313,.T.);
#28805=ORIENTED_EDGE('',*,*,#19465,.F.);
#28806=ORIENTED_EDGE('',*,*,#18491,.T.);
#28807=ORIENTED_EDGE('',*,*,#18979,.T.);
#28808=ORIENTED_EDGE('',*,*,#19216,.T.);
#28809=ORIENTED_EDGE('',*,*,#19391,.T.);
#28810=ORIENTED_EDGE('',*,*,#18314,.T.);
#28811=ORIENTED_EDGE('',*,*,#19466,.F.);
#28812=ORIENTED_EDGE('',*,*,#18497,.T.);
#28813=ORIENTED_EDGE('',*,*,#19467,.T.);
#28814=ORIENTED_EDGE('',*,*,#18308,.T.);
#28815=ORIENTED_EDGE('',*,*,#19388,.T.);
#28816=ORIENTED_EDGE('',*,*,#19211,.T.);
#28817=ORIENTED_EDGE('',*,*,#18974,.T.);
#28818=ORIENTED_EDGE('',*,*,#18496,.T.);
#28819=ORIENTED_EDGE('',*,*,#19468,.T.);
#28820=ORIENTED_EDGE('',*,*,#18309,.T.);
#28821=ORIENTED_EDGE('',*,*,#19467,.F.);
#28822=ORIENTED_EDGE('',*,*,#18495,.T.);
#28823=ORIENTED_EDGE('',*,*,#18976,.T.);
#28824=ORIENTED_EDGE('',*,*,#19213,.T.);
#28825=ORIENTED_EDGE('',*,*,#19389,.T.);
#28826=ORIENTED_EDGE('',*,*,#18310,.T.);
#28827=ORIENTED_EDGE('',*,*,#19468,.F.);
#28828=ORIENTED_EDGE('',*,*,#18501,.T.);
#28829=ORIENTED_EDGE('',*,*,#19469,.T.);
#28830=ORIENTED_EDGE('',*,*,#18304,.T.);
#28831=ORIENTED_EDGE('',*,*,#19386,.T.);
#28832=ORIENTED_EDGE('',*,*,#19208,.T.);
#28833=ORIENTED_EDGE('',*,*,#18971,.T.);
#28834=ORIENTED_EDGE('',*,*,#18500,.T.);
#28835=ORIENTED_EDGE('',*,*,#19470,.T.);
#28836=ORIENTED_EDGE('',*,*,#18305,.T.);
#28837=ORIENTED_EDGE('',*,*,#19469,.F.);
#28838=ORIENTED_EDGE('',*,*,#18499,.T.);
#28839=ORIENTED_EDGE('',*,*,#18973,.T.);
#28840=ORIENTED_EDGE('',*,*,#19210,.T.);
#28841=ORIENTED_EDGE('',*,*,#19387,.T.);
#28842=ORIENTED_EDGE('',*,*,#18306,.T.);
#28843=ORIENTED_EDGE('',*,*,#19470,.F.);
#28844=ORIENTED_EDGE('',*,*,#18505,.T.);
#28845=ORIENTED_EDGE('',*,*,#19471,.T.);
#28846=ORIENTED_EDGE('',*,*,#18300,.T.);
#28847=ORIENTED_EDGE('',*,*,#19384,.T.);
#28848=ORIENTED_EDGE('',*,*,#19205,.T.);
#28849=ORIENTED_EDGE('',*,*,#18968,.T.);
#28850=ORIENTED_EDGE('',*,*,#18504,.T.);
#28851=ORIENTED_EDGE('',*,*,#19472,.T.);
#28852=ORIENTED_EDGE('',*,*,#18301,.T.);
#28853=ORIENTED_EDGE('',*,*,#19471,.F.);
#28854=ORIENTED_EDGE('',*,*,#18503,.T.);
#28855=ORIENTED_EDGE('',*,*,#18970,.T.);
#28856=ORIENTED_EDGE('',*,*,#19207,.T.);
#28857=ORIENTED_EDGE('',*,*,#19385,.T.);
#28858=ORIENTED_EDGE('',*,*,#18302,.T.);
#28859=ORIENTED_EDGE('',*,*,#19472,.F.);
#28860=ORIENTED_EDGE('',*,*,#18509,.T.);
#28861=ORIENTED_EDGE('',*,*,#19473,.T.);
#28862=ORIENTED_EDGE('',*,*,#18296,.T.);
#28863=ORIENTED_EDGE('',*,*,#19382,.T.);
#28864=ORIENTED_EDGE('',*,*,#19202,.T.);
#28865=ORIENTED_EDGE('',*,*,#18965,.T.);
#28866=ORIENTED_EDGE('',*,*,#18508,.T.);
#28867=ORIENTED_EDGE('',*,*,#19474,.T.);
#28868=ORIENTED_EDGE('',*,*,#18297,.T.);
#28869=ORIENTED_EDGE('',*,*,#19473,.F.);
#28870=ORIENTED_EDGE('',*,*,#18507,.T.);
#28871=ORIENTED_EDGE('',*,*,#18967,.T.);
#28872=ORIENTED_EDGE('',*,*,#19204,.T.);
#28873=ORIENTED_EDGE('',*,*,#19383,.T.);
#28874=ORIENTED_EDGE('',*,*,#18298,.T.);
#28875=ORIENTED_EDGE('',*,*,#19474,.F.);
#28876=ORIENTED_EDGE('',*,*,#18513,.T.);
#28877=ORIENTED_EDGE('',*,*,#19475,.T.);
#28878=ORIENTED_EDGE('',*,*,#18292,.T.);
#28879=ORIENTED_EDGE('',*,*,#19380,.T.);
#28880=ORIENTED_EDGE('',*,*,#19199,.T.);
#28881=ORIENTED_EDGE('',*,*,#18962,.T.);
#28882=ORIENTED_EDGE('',*,*,#18512,.T.);
#28883=ORIENTED_EDGE('',*,*,#19476,.T.);
#28884=ORIENTED_EDGE('',*,*,#18293,.T.);
#28885=ORIENTED_EDGE('',*,*,#19475,.F.);
#28886=ORIENTED_EDGE('',*,*,#18511,.T.);
#28887=ORIENTED_EDGE('',*,*,#18964,.T.);
#28888=ORIENTED_EDGE('',*,*,#19201,.T.);
#28889=ORIENTED_EDGE('',*,*,#19381,.T.);
#28890=ORIENTED_EDGE('',*,*,#18294,.T.);
#28891=ORIENTED_EDGE('',*,*,#19476,.F.);
#28892=ORIENTED_EDGE('',*,*,#18517,.T.);
#28893=ORIENTED_EDGE('',*,*,#19477,.T.);
#28894=ORIENTED_EDGE('',*,*,#18288,.T.);
#28895=ORIENTED_EDGE('',*,*,#19378,.T.);
#28896=ORIENTED_EDGE('',*,*,#19196,.T.);
#28897=ORIENTED_EDGE('',*,*,#18959,.T.);
#28898=ORIENTED_EDGE('',*,*,#18516,.T.);
#28899=ORIENTED_EDGE('',*,*,#19478,.T.);
#28900=ORIENTED_EDGE('',*,*,#18289,.T.);
#28901=ORIENTED_EDGE('',*,*,#19477,.F.);
#28902=ORIENTED_EDGE('',*,*,#18515,.T.);
#28903=ORIENTED_EDGE('',*,*,#18961,.T.);
#28904=ORIENTED_EDGE('',*,*,#19198,.T.);
#28905=ORIENTED_EDGE('',*,*,#19379,.T.);
#28906=ORIENTED_EDGE('',*,*,#18290,.T.);
#28907=ORIENTED_EDGE('',*,*,#19478,.F.);
#28908=ORIENTED_EDGE('',*,*,#18521,.T.);
#28909=ORIENTED_EDGE('',*,*,#19479,.T.);
#28910=ORIENTED_EDGE('',*,*,#18284,.T.);
#28911=ORIENTED_EDGE('',*,*,#19376,.T.);
#28912=ORIENTED_EDGE('',*,*,#19193,.T.);
#28913=ORIENTED_EDGE('',*,*,#18956,.T.);
#28914=ORIENTED_EDGE('',*,*,#18520,.T.);
#28915=ORIENTED_EDGE('',*,*,#19480,.T.);
#28916=ORIENTED_EDGE('',*,*,#18285,.T.);
#28917=ORIENTED_EDGE('',*,*,#19479,.F.);
#28918=ORIENTED_EDGE('',*,*,#18519,.T.);
#28919=ORIENTED_EDGE('',*,*,#18958,.T.);
#28920=ORIENTED_EDGE('',*,*,#19195,.T.);
#28921=ORIENTED_EDGE('',*,*,#19377,.T.);
#28922=ORIENTED_EDGE('',*,*,#18286,.T.);
#28923=ORIENTED_EDGE('',*,*,#19480,.F.);
#28924=ORIENTED_EDGE('',*,*,#18525,.T.);
#28925=ORIENTED_EDGE('',*,*,#19481,.T.);
#28926=ORIENTED_EDGE('',*,*,#18280,.T.);
#28927=ORIENTED_EDGE('',*,*,#19374,.T.);
#28928=ORIENTED_EDGE('',*,*,#19190,.T.);
#28929=ORIENTED_EDGE('',*,*,#18953,.T.);
#28930=ORIENTED_EDGE('',*,*,#18524,.T.);
#28931=ORIENTED_EDGE('',*,*,#19482,.T.);
#28932=ORIENTED_EDGE('',*,*,#18281,.T.);
#28933=ORIENTED_EDGE('',*,*,#19481,.F.);
#28934=ORIENTED_EDGE('',*,*,#18523,.T.);
#28935=ORIENTED_EDGE('',*,*,#18955,.T.);
#28936=ORIENTED_EDGE('',*,*,#19192,.T.);
#28937=ORIENTED_EDGE('',*,*,#19375,.T.);
#28938=ORIENTED_EDGE('',*,*,#18282,.T.);
#28939=ORIENTED_EDGE('',*,*,#19482,.F.);
#28940=ORIENTED_EDGE('',*,*,#18529,.T.);
#28941=ORIENTED_EDGE('',*,*,#19483,.T.);
#28942=ORIENTED_EDGE('',*,*,#18276,.T.);
#28943=ORIENTED_EDGE('',*,*,#19372,.T.);
#28944=ORIENTED_EDGE('',*,*,#19187,.T.);
#28945=ORIENTED_EDGE('',*,*,#18950,.T.);
#28946=ORIENTED_EDGE('',*,*,#18528,.T.);
#28947=ORIENTED_EDGE('',*,*,#19484,.T.);
#28948=ORIENTED_EDGE('',*,*,#18277,.T.);
#28949=ORIENTED_EDGE('',*,*,#19483,.F.);
#28950=ORIENTED_EDGE('',*,*,#18527,.T.);
#28951=ORIENTED_EDGE('',*,*,#18952,.T.);
#28952=ORIENTED_EDGE('',*,*,#19189,.T.);
#28953=ORIENTED_EDGE('',*,*,#19373,.T.);
#28954=ORIENTED_EDGE('',*,*,#18278,.T.);
#28955=ORIENTED_EDGE('',*,*,#19484,.F.);
#28956=ORIENTED_EDGE('',*,*,#18533,.T.);
#28957=ORIENTED_EDGE('',*,*,#19485,.T.);
#28958=ORIENTED_EDGE('',*,*,#18272,.T.);
#28959=ORIENTED_EDGE('',*,*,#19370,.T.);
#28960=ORIENTED_EDGE('',*,*,#19184,.T.);
#28961=ORIENTED_EDGE('',*,*,#18947,.T.);
#28962=ORIENTED_EDGE('',*,*,#18532,.T.);
#28963=ORIENTED_EDGE('',*,*,#19486,.T.);
#28964=ORIENTED_EDGE('',*,*,#18273,.T.);
#28965=ORIENTED_EDGE('',*,*,#19485,.F.);
#28966=ORIENTED_EDGE('',*,*,#18531,.T.);
#28967=ORIENTED_EDGE('',*,*,#18949,.T.);
#28968=ORIENTED_EDGE('',*,*,#19186,.T.);
#28969=ORIENTED_EDGE('',*,*,#19371,.T.);
#28970=ORIENTED_EDGE('',*,*,#18274,.T.);
#28971=ORIENTED_EDGE('',*,*,#19486,.F.);
#28972=ORIENTED_EDGE('',*,*,#18537,.T.);
#28973=ORIENTED_EDGE('',*,*,#19487,.T.);
#28974=ORIENTED_EDGE('',*,*,#18268,.T.);
#28975=ORIENTED_EDGE('',*,*,#19368,.T.);
#28976=ORIENTED_EDGE('',*,*,#19181,.T.);
#28977=ORIENTED_EDGE('',*,*,#18944,.T.);
#28978=ORIENTED_EDGE('',*,*,#18536,.T.);
#28979=ORIENTED_EDGE('',*,*,#19488,.T.);
#28980=ORIENTED_EDGE('',*,*,#18269,.T.);
#28981=ORIENTED_EDGE('',*,*,#19487,.F.);
#28982=ORIENTED_EDGE('',*,*,#18535,.T.);
#28983=ORIENTED_EDGE('',*,*,#18946,.T.);
#28984=ORIENTED_EDGE('',*,*,#19183,.T.);
#28985=ORIENTED_EDGE('',*,*,#19369,.T.);
#28986=ORIENTED_EDGE('',*,*,#18270,.T.);
#28987=ORIENTED_EDGE('',*,*,#19488,.F.);
#28988=ORIENTED_EDGE('',*,*,#18541,.T.);
#28989=ORIENTED_EDGE('',*,*,#19489,.T.);
#28990=ORIENTED_EDGE('',*,*,#18264,.T.);
#28991=ORIENTED_EDGE('',*,*,#19366,.T.);
#28992=ORIENTED_EDGE('',*,*,#19178,.T.);
#28993=ORIENTED_EDGE('',*,*,#18941,.T.);
#28994=ORIENTED_EDGE('',*,*,#18540,.T.);
#28995=ORIENTED_EDGE('',*,*,#19490,.T.);
#28996=ORIENTED_EDGE('',*,*,#18265,.T.);
#28997=ORIENTED_EDGE('',*,*,#19489,.F.);
#28998=ORIENTED_EDGE('',*,*,#18539,.T.);
#28999=ORIENTED_EDGE('',*,*,#18943,.T.);
#29000=ORIENTED_EDGE('',*,*,#19180,.T.);
#29001=ORIENTED_EDGE('',*,*,#19367,.T.);
#29002=ORIENTED_EDGE('',*,*,#18266,.T.);
#29003=ORIENTED_EDGE('',*,*,#19490,.F.);
#29004=ORIENTED_EDGE('',*,*,#18545,.T.);
#29005=ORIENTED_EDGE('',*,*,#19491,.T.);
#29006=ORIENTED_EDGE('',*,*,#18260,.T.);
#29007=ORIENTED_EDGE('',*,*,#19364,.T.);
#29008=ORIENTED_EDGE('',*,*,#19175,.T.);
#29009=ORIENTED_EDGE('',*,*,#18938,.T.);
#29010=ORIENTED_EDGE('',*,*,#18544,.T.);
#29011=ORIENTED_EDGE('',*,*,#19492,.T.);
#29012=ORIENTED_EDGE('',*,*,#18261,.T.);
#29013=ORIENTED_EDGE('',*,*,#19491,.F.);
#29014=ORIENTED_EDGE('',*,*,#18543,.T.);
#29015=ORIENTED_EDGE('',*,*,#18940,.T.);
#29016=ORIENTED_EDGE('',*,*,#19177,.T.);
#29017=ORIENTED_EDGE('',*,*,#19365,.T.);
#29018=ORIENTED_EDGE('',*,*,#18262,.T.);
#29019=ORIENTED_EDGE('',*,*,#19492,.F.);
#29020=ORIENTED_EDGE('',*,*,#18549,.T.);
#29021=ORIENTED_EDGE('',*,*,#19493,.T.);
#29022=ORIENTED_EDGE('',*,*,#18256,.T.);
#29023=ORIENTED_EDGE('',*,*,#19362,.T.);
#29024=ORIENTED_EDGE('',*,*,#19172,.T.);
#29025=ORIENTED_EDGE('',*,*,#18935,.T.);
#29026=ORIENTED_EDGE('',*,*,#18548,.T.);
#29027=ORIENTED_EDGE('',*,*,#19494,.T.);
#29028=ORIENTED_EDGE('',*,*,#18257,.T.);
#29029=ORIENTED_EDGE('',*,*,#19493,.F.);
#29030=ORIENTED_EDGE('',*,*,#18547,.T.);
#29031=ORIENTED_EDGE('',*,*,#18937,.T.);
#29032=ORIENTED_EDGE('',*,*,#19174,.T.);
#29033=ORIENTED_EDGE('',*,*,#19363,.T.);
#29034=ORIENTED_EDGE('',*,*,#18258,.T.);
#29035=ORIENTED_EDGE('',*,*,#19494,.F.);
#29036=ORIENTED_EDGE('',*,*,#18553,.T.);
#29037=ORIENTED_EDGE('',*,*,#19495,.T.);
#29038=ORIENTED_EDGE('',*,*,#18252,.T.);
#29039=ORIENTED_EDGE('',*,*,#19360,.T.);
#29040=ORIENTED_EDGE('',*,*,#19169,.T.);
#29041=ORIENTED_EDGE('',*,*,#18932,.T.);
#29042=ORIENTED_EDGE('',*,*,#18552,.T.);
#29043=ORIENTED_EDGE('',*,*,#19496,.T.);
#29044=ORIENTED_EDGE('',*,*,#18253,.T.);
#29045=ORIENTED_EDGE('',*,*,#19495,.F.);
#29046=ORIENTED_EDGE('',*,*,#18551,.T.);
#29047=ORIENTED_EDGE('',*,*,#18934,.T.);
#29048=ORIENTED_EDGE('',*,*,#19171,.T.);
#29049=ORIENTED_EDGE('',*,*,#19361,.T.);
#29050=ORIENTED_EDGE('',*,*,#18254,.T.);
#29051=ORIENTED_EDGE('',*,*,#19496,.F.);
#29052=ORIENTED_EDGE('',*,*,#18557,.T.);
#29053=ORIENTED_EDGE('',*,*,#19497,.T.);
#29054=ORIENTED_EDGE('',*,*,#18248,.T.);
#29055=ORIENTED_EDGE('',*,*,#19358,.T.);
#29056=ORIENTED_EDGE('',*,*,#19166,.T.);
#29057=ORIENTED_EDGE('',*,*,#18929,.T.);
#29058=ORIENTED_EDGE('',*,*,#18556,.T.);
#29059=ORIENTED_EDGE('',*,*,#19498,.T.);
#29060=ORIENTED_EDGE('',*,*,#18249,.T.);
#29061=ORIENTED_EDGE('',*,*,#19497,.F.);
#29062=ORIENTED_EDGE('',*,*,#18555,.T.);
#29063=ORIENTED_EDGE('',*,*,#18931,.T.);
#29064=ORIENTED_EDGE('',*,*,#19168,.T.);
#29065=ORIENTED_EDGE('',*,*,#19359,.T.);
#29066=ORIENTED_EDGE('',*,*,#18250,.T.);
#29067=ORIENTED_EDGE('',*,*,#19498,.F.);
#29068=ORIENTED_EDGE('',*,*,#18561,.T.);
#29069=ORIENTED_EDGE('',*,*,#19499,.T.);
#29070=ORIENTED_EDGE('',*,*,#18244,.T.);
#29071=ORIENTED_EDGE('',*,*,#19356,.T.);
#29072=ORIENTED_EDGE('',*,*,#19163,.T.);
#29073=ORIENTED_EDGE('',*,*,#18926,.T.);
#29074=ORIENTED_EDGE('',*,*,#18560,.T.);
#29075=ORIENTED_EDGE('',*,*,#19500,.T.);
#29076=ORIENTED_EDGE('',*,*,#18245,.T.);
#29077=ORIENTED_EDGE('',*,*,#19499,.F.);
#29078=ORIENTED_EDGE('',*,*,#18559,.T.);
#29079=ORIENTED_EDGE('',*,*,#18928,.T.);
#29080=ORIENTED_EDGE('',*,*,#19165,.T.);
#29081=ORIENTED_EDGE('',*,*,#19357,.T.);
#29082=ORIENTED_EDGE('',*,*,#18246,.T.);
#29083=ORIENTED_EDGE('',*,*,#19500,.F.);
#29084=ORIENTED_EDGE('',*,*,#18565,.T.);
#29085=ORIENTED_EDGE('',*,*,#19501,.T.);
#29086=ORIENTED_EDGE('',*,*,#18240,.T.);
#29087=ORIENTED_EDGE('',*,*,#19354,.T.);
#29088=ORIENTED_EDGE('',*,*,#19160,.T.);
#29089=ORIENTED_EDGE('',*,*,#18923,.T.);
#29090=ORIENTED_EDGE('',*,*,#18564,.T.);
#29091=ORIENTED_EDGE('',*,*,#19502,.T.);
#29092=ORIENTED_EDGE('',*,*,#18241,.T.);
#29093=ORIENTED_EDGE('',*,*,#19501,.F.);
#29094=ORIENTED_EDGE('',*,*,#18563,.T.);
#29095=ORIENTED_EDGE('',*,*,#18925,.T.);
#29096=ORIENTED_EDGE('',*,*,#19162,.T.);
#29097=ORIENTED_EDGE('',*,*,#19355,.T.);
#29098=ORIENTED_EDGE('',*,*,#18242,.T.);
#29099=ORIENTED_EDGE('',*,*,#19502,.F.);
#29100=ORIENTED_EDGE('',*,*,#18569,.T.);
#29101=ORIENTED_EDGE('',*,*,#19503,.T.);
#29102=ORIENTED_EDGE('',*,*,#18236,.T.);
#29103=ORIENTED_EDGE('',*,*,#19352,.T.);
#29104=ORIENTED_EDGE('',*,*,#19157,.T.);
#29105=ORIENTED_EDGE('',*,*,#18920,.T.);
#29106=ORIENTED_EDGE('',*,*,#18568,.T.);
#29107=ORIENTED_EDGE('',*,*,#19504,.T.);
#29108=ORIENTED_EDGE('',*,*,#18237,.T.);
#29109=ORIENTED_EDGE('',*,*,#19503,.F.);
#29110=ORIENTED_EDGE('',*,*,#18567,.T.);
#29111=ORIENTED_EDGE('',*,*,#18922,.T.);
#29112=ORIENTED_EDGE('',*,*,#19159,.T.);
#29113=ORIENTED_EDGE('',*,*,#19353,.T.);
#29114=ORIENTED_EDGE('',*,*,#18238,.T.);
#29115=ORIENTED_EDGE('',*,*,#19504,.F.);
#29116=ORIENTED_EDGE('',*,*,#18573,.T.);
#29117=ORIENTED_EDGE('',*,*,#19505,.T.);
#29118=ORIENTED_EDGE('',*,*,#18232,.T.);
#29119=ORIENTED_EDGE('',*,*,#19350,.T.);
#29120=ORIENTED_EDGE('',*,*,#19154,.T.);
#29121=ORIENTED_EDGE('',*,*,#18917,.T.);
#29122=ORIENTED_EDGE('',*,*,#18572,.T.);
#29123=ORIENTED_EDGE('',*,*,#19506,.T.);
#29124=ORIENTED_EDGE('',*,*,#18233,.T.);
#29125=ORIENTED_EDGE('',*,*,#19505,.F.);
#29126=ORIENTED_EDGE('',*,*,#18571,.T.);
#29127=ORIENTED_EDGE('',*,*,#18919,.T.);
#29128=ORIENTED_EDGE('',*,*,#19156,.T.);
#29129=ORIENTED_EDGE('',*,*,#19351,.T.);
#29130=ORIENTED_EDGE('',*,*,#18234,.T.);
#29131=ORIENTED_EDGE('',*,*,#19506,.F.);
#29132=ORIENTED_EDGE('',*,*,#18577,.T.);
#29133=ORIENTED_EDGE('',*,*,#19507,.T.);
#29134=ORIENTED_EDGE('',*,*,#18228,.T.);
#29135=ORIENTED_EDGE('',*,*,#19348,.T.);
#29136=ORIENTED_EDGE('',*,*,#19151,.T.);
#29137=ORIENTED_EDGE('',*,*,#18914,.T.);
#29138=ORIENTED_EDGE('',*,*,#18576,.T.);
#29139=ORIENTED_EDGE('',*,*,#19508,.T.);
#29140=ORIENTED_EDGE('',*,*,#18229,.T.);
#29141=ORIENTED_EDGE('',*,*,#19507,.F.);
#29142=ORIENTED_EDGE('',*,*,#18575,.T.);
#29143=ORIENTED_EDGE('',*,*,#18916,.T.);
#29144=ORIENTED_EDGE('',*,*,#19153,.T.);
#29145=ORIENTED_EDGE('',*,*,#19349,.T.);
#29146=ORIENTED_EDGE('',*,*,#18230,.T.);
#29147=ORIENTED_EDGE('',*,*,#19508,.F.);
#29148=ORIENTED_EDGE('',*,*,#18581,.T.);
#29149=ORIENTED_EDGE('',*,*,#19509,.T.);
#29150=ORIENTED_EDGE('',*,*,#18224,.T.);
#29151=ORIENTED_EDGE('',*,*,#19346,.T.);
#29152=ORIENTED_EDGE('',*,*,#19148,.T.);
#29153=ORIENTED_EDGE('',*,*,#18911,.T.);
#29154=ORIENTED_EDGE('',*,*,#18580,.T.);
#29155=ORIENTED_EDGE('',*,*,#19510,.T.);
#29156=ORIENTED_EDGE('',*,*,#18225,.T.);
#29157=ORIENTED_EDGE('',*,*,#19509,.F.);
#29158=ORIENTED_EDGE('',*,*,#18579,.T.);
#29159=ORIENTED_EDGE('',*,*,#18913,.T.);
#29160=ORIENTED_EDGE('',*,*,#19150,.T.);
#29161=ORIENTED_EDGE('',*,*,#19347,.T.);
#29162=ORIENTED_EDGE('',*,*,#18226,.T.);
#29163=ORIENTED_EDGE('',*,*,#19510,.F.);
#29164=ORIENTED_EDGE('',*,*,#18585,.T.);
#29165=ORIENTED_EDGE('',*,*,#19511,.T.);
#29166=ORIENTED_EDGE('',*,*,#18220,.T.);
#29167=ORIENTED_EDGE('',*,*,#19344,.T.);
#29168=ORIENTED_EDGE('',*,*,#19145,.T.);
#29169=ORIENTED_EDGE('',*,*,#18908,.T.);
#29170=ORIENTED_EDGE('',*,*,#18584,.T.);
#29171=ORIENTED_EDGE('',*,*,#19512,.T.);
#29172=ORIENTED_EDGE('',*,*,#18221,.T.);
#29173=ORIENTED_EDGE('',*,*,#19511,.F.);
#29174=ORIENTED_EDGE('',*,*,#18583,.T.);
#29175=ORIENTED_EDGE('',*,*,#18910,.T.);
#29176=ORIENTED_EDGE('',*,*,#19147,.T.);
#29177=ORIENTED_EDGE('',*,*,#19345,.T.);
#29178=ORIENTED_EDGE('',*,*,#18222,.T.);
#29179=ORIENTED_EDGE('',*,*,#19512,.F.);
#29180=ORIENTED_EDGE('',*,*,#18589,.T.);
#29181=ORIENTED_EDGE('',*,*,#19513,.T.);
#29182=ORIENTED_EDGE('',*,*,#18216,.T.);
#29183=ORIENTED_EDGE('',*,*,#19342,.T.);
#29184=ORIENTED_EDGE('',*,*,#19142,.T.);
#29185=ORIENTED_EDGE('',*,*,#18905,.T.);
#29186=ORIENTED_EDGE('',*,*,#18588,.T.);
#29187=ORIENTED_EDGE('',*,*,#19514,.T.);
#29188=ORIENTED_EDGE('',*,*,#18217,.T.);
#29189=ORIENTED_EDGE('',*,*,#19513,.F.);
#29190=ORIENTED_EDGE('',*,*,#18587,.T.);
#29191=ORIENTED_EDGE('',*,*,#18907,.T.);
#29192=ORIENTED_EDGE('',*,*,#19144,.T.);
#29193=ORIENTED_EDGE('',*,*,#19343,.T.);
#29194=ORIENTED_EDGE('',*,*,#18218,.T.);
#29195=ORIENTED_EDGE('',*,*,#19514,.F.);
#29196=ORIENTED_EDGE('',*,*,#18593,.T.);
#29197=ORIENTED_EDGE('',*,*,#19515,.T.);
#29198=ORIENTED_EDGE('',*,*,#18212,.T.);
#29199=ORIENTED_EDGE('',*,*,#19340,.T.);
#29200=ORIENTED_EDGE('',*,*,#19139,.T.);
#29201=ORIENTED_EDGE('',*,*,#18902,.T.);
#29202=ORIENTED_EDGE('',*,*,#18592,.T.);
#29203=ORIENTED_EDGE('',*,*,#19516,.T.);
#29204=ORIENTED_EDGE('',*,*,#18213,.T.);
#29205=ORIENTED_EDGE('',*,*,#19515,.F.);
#29206=ORIENTED_EDGE('',*,*,#18591,.T.);
#29207=ORIENTED_EDGE('',*,*,#18904,.T.);
#29208=ORIENTED_EDGE('',*,*,#19141,.T.);
#29209=ORIENTED_EDGE('',*,*,#19341,.T.);
#29210=ORIENTED_EDGE('',*,*,#18214,.T.);
#29211=ORIENTED_EDGE('',*,*,#19516,.F.);
#29212=ORIENTED_EDGE('',*,*,#18597,.T.);
#29213=ORIENTED_EDGE('',*,*,#19517,.T.);
#29214=ORIENTED_EDGE('',*,*,#18208,.T.);
#29215=ORIENTED_EDGE('',*,*,#19338,.T.);
#29216=ORIENTED_EDGE('',*,*,#19136,.T.);
#29217=ORIENTED_EDGE('',*,*,#18899,.T.);
#29218=ORIENTED_EDGE('',*,*,#18596,.T.);
#29219=ORIENTED_EDGE('',*,*,#19518,.T.);
#29220=ORIENTED_EDGE('',*,*,#18209,.T.);
#29221=ORIENTED_EDGE('',*,*,#19517,.F.);
#29222=ORIENTED_EDGE('',*,*,#18595,.T.);
#29223=ORIENTED_EDGE('',*,*,#18901,.T.);
#29224=ORIENTED_EDGE('',*,*,#19138,.T.);
#29225=ORIENTED_EDGE('',*,*,#19339,.T.);
#29226=ORIENTED_EDGE('',*,*,#18210,.T.);
#29227=ORIENTED_EDGE('',*,*,#19518,.F.);
#29228=ORIENTED_EDGE('',*,*,#18601,.T.);
#29229=ORIENTED_EDGE('',*,*,#19519,.T.);
#29230=ORIENTED_EDGE('',*,*,#18204,.T.);
#29231=ORIENTED_EDGE('',*,*,#19336,.T.);
#29232=ORIENTED_EDGE('',*,*,#19133,.T.);
#29233=ORIENTED_EDGE('',*,*,#18896,.T.);
#29234=ORIENTED_EDGE('',*,*,#18600,.T.);
#29235=ORIENTED_EDGE('',*,*,#19520,.T.);
#29236=ORIENTED_EDGE('',*,*,#18205,.T.);
#29237=ORIENTED_EDGE('',*,*,#19519,.F.);
#29238=ORIENTED_EDGE('',*,*,#18599,.T.);
#29239=ORIENTED_EDGE('',*,*,#18898,.T.);
#29240=ORIENTED_EDGE('',*,*,#19135,.T.);
#29241=ORIENTED_EDGE('',*,*,#19337,.T.);
#29242=ORIENTED_EDGE('',*,*,#18206,.T.);
#29243=ORIENTED_EDGE('',*,*,#19520,.F.);
#29244=ORIENTED_EDGE('',*,*,#18605,.T.);
#29245=ORIENTED_EDGE('',*,*,#19521,.T.);
#29246=ORIENTED_EDGE('',*,*,#18200,.T.);
#29247=ORIENTED_EDGE('',*,*,#19334,.T.);
#29248=ORIENTED_EDGE('',*,*,#19130,.T.);
#29249=ORIENTED_EDGE('',*,*,#18893,.T.);
#29250=ORIENTED_EDGE('',*,*,#18604,.T.);
#29251=ORIENTED_EDGE('',*,*,#19522,.T.);
#29252=ORIENTED_EDGE('',*,*,#18201,.T.);
#29253=ORIENTED_EDGE('',*,*,#19521,.F.);
#29254=ORIENTED_EDGE('',*,*,#18603,.T.);
#29255=ORIENTED_EDGE('',*,*,#18895,.T.);
#29256=ORIENTED_EDGE('',*,*,#19132,.T.);
#29257=ORIENTED_EDGE('',*,*,#19335,.T.);
#29258=ORIENTED_EDGE('',*,*,#18202,.T.);
#29259=ORIENTED_EDGE('',*,*,#19522,.F.);
#29260=ORIENTED_EDGE('',*,*,#18609,.T.);
#29261=ORIENTED_EDGE('',*,*,#19523,.T.);
#29262=ORIENTED_EDGE('',*,*,#18196,.T.);
#29263=ORIENTED_EDGE('',*,*,#19332,.T.);
#29264=ORIENTED_EDGE('',*,*,#19127,.T.);
#29265=ORIENTED_EDGE('',*,*,#18890,.T.);
#29266=ORIENTED_EDGE('',*,*,#18608,.T.);
#29267=ORIENTED_EDGE('',*,*,#19524,.T.);
#29268=ORIENTED_EDGE('',*,*,#18197,.T.);
#29269=ORIENTED_EDGE('',*,*,#19523,.F.);
#29270=ORIENTED_EDGE('',*,*,#18607,.T.);
#29271=ORIENTED_EDGE('',*,*,#18892,.T.);
#29272=ORIENTED_EDGE('',*,*,#19129,.T.);
#29273=ORIENTED_EDGE('',*,*,#19333,.T.);
#29274=ORIENTED_EDGE('',*,*,#18198,.T.);
#29275=ORIENTED_EDGE('',*,*,#19524,.F.);
#29276=ORIENTED_EDGE('',*,*,#18613,.T.);
#29277=ORIENTED_EDGE('',*,*,#19525,.T.);
#29278=ORIENTED_EDGE('',*,*,#18192,.T.);
#29279=ORIENTED_EDGE('',*,*,#19330,.T.);
#29280=ORIENTED_EDGE('',*,*,#19124,.T.);
#29281=ORIENTED_EDGE('',*,*,#18887,.T.);
#29282=ORIENTED_EDGE('',*,*,#18612,.T.);
#29283=ORIENTED_EDGE('',*,*,#19526,.T.);
#29284=ORIENTED_EDGE('',*,*,#18193,.T.);
#29285=ORIENTED_EDGE('',*,*,#19525,.F.);
#29286=ORIENTED_EDGE('',*,*,#18611,.T.);
#29287=ORIENTED_EDGE('',*,*,#18889,.T.);
#29288=ORIENTED_EDGE('',*,*,#19126,.T.);
#29289=ORIENTED_EDGE('',*,*,#19331,.T.);
#29290=ORIENTED_EDGE('',*,*,#18194,.T.);
#29291=ORIENTED_EDGE('',*,*,#19526,.F.);
#29292=ORIENTED_EDGE('',*,*,#18617,.T.);
#29293=ORIENTED_EDGE('',*,*,#19527,.T.);
#29294=ORIENTED_EDGE('',*,*,#18188,.T.);
#29295=ORIENTED_EDGE('',*,*,#19328,.T.);
#29296=ORIENTED_EDGE('',*,*,#19121,.T.);
#29297=ORIENTED_EDGE('',*,*,#18884,.T.);
#29298=ORIENTED_EDGE('',*,*,#18616,.T.);
#29299=ORIENTED_EDGE('',*,*,#19528,.T.);
#29300=ORIENTED_EDGE('',*,*,#18189,.T.);
#29301=ORIENTED_EDGE('',*,*,#19527,.F.);
#29302=ORIENTED_EDGE('',*,*,#18615,.T.);
#29303=ORIENTED_EDGE('',*,*,#18886,.T.);
#29304=ORIENTED_EDGE('',*,*,#19123,.T.);
#29305=ORIENTED_EDGE('',*,*,#19329,.T.);
#29306=ORIENTED_EDGE('',*,*,#18190,.T.);
#29307=ORIENTED_EDGE('',*,*,#19528,.F.);
#29308=ORIENTED_EDGE('',*,*,#18621,.T.);
#29309=ORIENTED_EDGE('',*,*,#19529,.T.);
#29310=ORIENTED_EDGE('',*,*,#18184,.T.);
#29311=ORIENTED_EDGE('',*,*,#19326,.T.);
#29312=ORIENTED_EDGE('',*,*,#19118,.T.);
#29313=ORIENTED_EDGE('',*,*,#18881,.T.);
#29314=ORIENTED_EDGE('',*,*,#18620,.T.);
#29315=ORIENTED_EDGE('',*,*,#19530,.T.);
#29316=ORIENTED_EDGE('',*,*,#18185,.T.);
#29317=ORIENTED_EDGE('',*,*,#19529,.F.);
#29318=ORIENTED_EDGE('',*,*,#18619,.T.);
#29319=ORIENTED_EDGE('',*,*,#18883,.T.);
#29320=ORIENTED_EDGE('',*,*,#19120,.T.);
#29321=ORIENTED_EDGE('',*,*,#19327,.T.);
#29322=ORIENTED_EDGE('',*,*,#18186,.T.);
#29323=ORIENTED_EDGE('',*,*,#19530,.F.);
#29324=ORIENTED_EDGE('',*,*,#18625,.T.);
#29325=ORIENTED_EDGE('',*,*,#19531,.T.);
#29326=ORIENTED_EDGE('',*,*,#18180,.T.);
#29327=ORIENTED_EDGE('',*,*,#19324,.T.);
#29328=ORIENTED_EDGE('',*,*,#19115,.T.);
#29329=ORIENTED_EDGE('',*,*,#18878,.T.);
#29330=ORIENTED_EDGE('',*,*,#18624,.T.);
#29331=ORIENTED_EDGE('',*,*,#19532,.T.);
#29332=ORIENTED_EDGE('',*,*,#18181,.T.);
#29333=ORIENTED_EDGE('',*,*,#19531,.F.);
#29334=ORIENTED_EDGE('',*,*,#18623,.T.);
#29335=ORIENTED_EDGE('',*,*,#18880,.T.);
#29336=ORIENTED_EDGE('',*,*,#19117,.T.);
#29337=ORIENTED_EDGE('',*,*,#19325,.T.);
#29338=ORIENTED_EDGE('',*,*,#18182,.T.);
#29339=ORIENTED_EDGE('',*,*,#19532,.F.);
#29340=ORIENTED_EDGE('',*,*,#18629,.T.);
#29341=ORIENTED_EDGE('',*,*,#19533,.T.);
#29342=ORIENTED_EDGE('',*,*,#18176,.T.);
#29343=ORIENTED_EDGE('',*,*,#19322,.T.);
#29344=ORIENTED_EDGE('',*,*,#19112,.T.);
#29345=ORIENTED_EDGE('',*,*,#18875,.T.);
#29346=ORIENTED_EDGE('',*,*,#18628,.T.);
#29347=ORIENTED_EDGE('',*,*,#19534,.T.);
#29348=ORIENTED_EDGE('',*,*,#18177,.T.);
#29349=ORIENTED_EDGE('',*,*,#19533,.F.);
#29350=ORIENTED_EDGE('',*,*,#18627,.T.);
#29351=ORIENTED_EDGE('',*,*,#18877,.T.);
#29352=ORIENTED_EDGE('',*,*,#19114,.T.);
#29353=ORIENTED_EDGE('',*,*,#19323,.T.);
#29354=ORIENTED_EDGE('',*,*,#18178,.T.);
#29355=ORIENTED_EDGE('',*,*,#19534,.F.);
#29356=ORIENTED_EDGE('',*,*,#18633,.T.);
#29357=ORIENTED_EDGE('',*,*,#19535,.T.);
#29358=ORIENTED_EDGE('',*,*,#18172,.T.);
#29359=ORIENTED_EDGE('',*,*,#19320,.T.);
#29360=ORIENTED_EDGE('',*,*,#19109,.T.);
#29361=ORIENTED_EDGE('',*,*,#18872,.T.);
#29362=ORIENTED_EDGE('',*,*,#18632,.T.);
#29363=ORIENTED_EDGE('',*,*,#19536,.T.);
#29364=ORIENTED_EDGE('',*,*,#18173,.T.);
#29365=ORIENTED_EDGE('',*,*,#19535,.F.);
#29366=ORIENTED_EDGE('',*,*,#18631,.T.);
#29367=ORIENTED_EDGE('',*,*,#18874,.T.);
#29368=ORIENTED_EDGE('',*,*,#19111,.T.);
#29369=ORIENTED_EDGE('',*,*,#19321,.T.);
#29370=ORIENTED_EDGE('',*,*,#18174,.T.);
#29371=ORIENTED_EDGE('',*,*,#19536,.F.);
#29372=ORIENTED_EDGE('',*,*,#18637,.T.);
#29373=ORIENTED_EDGE('',*,*,#19537,.T.);
#29374=ORIENTED_EDGE('',*,*,#18473,.T.);
#29375=ORIENTED_EDGE('',*,*,#19318,.T.);
#29376=ORIENTED_EDGE('',*,*,#19106,.T.);
#29377=ORIENTED_EDGE('',*,*,#18869,.T.);
#29378=ORIENTED_EDGE('',*,*,#18636,.T.);
#29379=ORIENTED_EDGE('',*,*,#19538,.T.);
#29380=ORIENTED_EDGE('',*,*,#18169,.T.);
#29381=ORIENTED_EDGE('',*,*,#18474,.T.);
#29382=ORIENTED_EDGE('',*,*,#19537,.F.);
#29383=ORIENTED_EDGE('',*,*,#18635,.T.);
#29384=ORIENTED_EDGE('',*,*,#18871,.T.);
#29385=ORIENTED_EDGE('',*,*,#19108,.T.);
#29386=ORIENTED_EDGE('',*,*,#19319,.T.);
#29387=ORIENTED_EDGE('',*,*,#18170,.T.);
#29388=ORIENTED_EDGE('',*,*,#19538,.F.);
#29389=ORIENTED_EDGE('',*,*,#18641,.T.);
#29390=ORIENTED_EDGE('',*,*,#19539,.T.);
#29391=ORIENTED_EDGE('',*,*,#18469,.T.);
#29392=ORIENTED_EDGE('',*,*,#19316,.T.);
#29393=ORIENTED_EDGE('',*,*,#19103,.T.);
#29394=ORIENTED_EDGE('',*,*,#18866,.T.);
#29395=ORIENTED_EDGE('',*,*,#18640,.T.);
#29396=ORIENTED_EDGE('',*,*,#19540,.T.);
#29397=ORIENTED_EDGE('',*,*,#18470,.T.);
#29398=ORIENTED_EDGE('',*,*,#19539,.F.);
#29399=ORIENTED_EDGE('',*,*,#18639,.T.);
#29400=ORIENTED_EDGE('',*,*,#18868,.T.);
#29401=ORIENTED_EDGE('',*,*,#19105,.T.);
#29402=ORIENTED_EDGE('',*,*,#19317,.T.);
#29403=ORIENTED_EDGE('',*,*,#18471,.T.);
#29404=ORIENTED_EDGE('',*,*,#19540,.F.);
#29405=ORIENTED_EDGE('',*,*,#18645,.T.);
#29406=ORIENTED_EDGE('',*,*,#19541,.T.);
#29407=ORIENTED_EDGE('',*,*,#18465,.T.);
#29408=ORIENTED_EDGE('',*,*,#19314,.T.);
#29409=ORIENTED_EDGE('',*,*,#19100,.T.);
#29410=ORIENTED_EDGE('',*,*,#18863,.T.);
#29411=ORIENTED_EDGE('',*,*,#18644,.T.);
#29412=ORIENTED_EDGE('',*,*,#19542,.T.);
#29413=ORIENTED_EDGE('',*,*,#18466,.T.);
#29414=ORIENTED_EDGE('',*,*,#19541,.F.);
#29415=ORIENTED_EDGE('',*,*,#18643,.T.);
#29416=ORIENTED_EDGE('',*,*,#18865,.T.);
#29417=ORIENTED_EDGE('',*,*,#19102,.T.);
#29418=ORIENTED_EDGE('',*,*,#19315,.T.);
#29419=ORIENTED_EDGE('',*,*,#18467,.T.);
#29420=ORIENTED_EDGE('',*,*,#19542,.F.);
#29421=ORIENTED_EDGE('',*,*,#18649,.T.);
#29422=ORIENTED_EDGE('',*,*,#19543,.T.);
#29423=ORIENTED_EDGE('',*,*,#18461,.T.);
#29424=ORIENTED_EDGE('',*,*,#19312,.T.);
#29425=ORIENTED_EDGE('',*,*,#19097,.T.);
#29426=ORIENTED_EDGE('',*,*,#18860,.T.);
#29427=ORIENTED_EDGE('',*,*,#18648,.T.);
#29428=ORIENTED_EDGE('',*,*,#19544,.T.);
#29429=ORIENTED_EDGE('',*,*,#18462,.T.);
#29430=ORIENTED_EDGE('',*,*,#19543,.F.);
#29431=ORIENTED_EDGE('',*,*,#18647,.T.);
#29432=ORIENTED_EDGE('',*,*,#18862,.T.);
#29433=ORIENTED_EDGE('',*,*,#19099,.T.);
#29434=ORIENTED_EDGE('',*,*,#19313,.T.);
#29435=ORIENTED_EDGE('',*,*,#18463,.T.);
#29436=ORIENTED_EDGE('',*,*,#19544,.F.);
#29437=ORIENTED_EDGE('',*,*,#18653,.T.);
#29438=ORIENTED_EDGE('',*,*,#19545,.T.);
#29439=ORIENTED_EDGE('',*,*,#18457,.T.);
#29440=ORIENTED_EDGE('',*,*,#19310,.T.);
#29441=ORIENTED_EDGE('',*,*,#19094,.T.);
#29442=ORIENTED_EDGE('',*,*,#18857,.T.);
#29443=ORIENTED_EDGE('',*,*,#18652,.T.);
#29444=ORIENTED_EDGE('',*,*,#19546,.T.);
#29445=ORIENTED_EDGE('',*,*,#18458,.T.);
#29446=ORIENTED_EDGE('',*,*,#19545,.F.);
#29447=ORIENTED_EDGE('',*,*,#18651,.T.);
#29448=ORIENTED_EDGE('',*,*,#18859,.T.);
#29449=ORIENTED_EDGE('',*,*,#19096,.T.);
#29450=ORIENTED_EDGE('',*,*,#19311,.T.);
#29451=ORIENTED_EDGE('',*,*,#18459,.T.);
#29452=ORIENTED_EDGE('',*,*,#19546,.F.);
#29453=ORIENTED_EDGE('',*,*,#18657,.T.);
#29454=ORIENTED_EDGE('',*,*,#19547,.T.);
#29455=ORIENTED_EDGE('',*,*,#18453,.T.);
#29456=ORIENTED_EDGE('',*,*,#19308,.T.);
#29457=ORIENTED_EDGE('',*,*,#19091,.T.);
#29458=ORIENTED_EDGE('',*,*,#18854,.T.);
#29459=ORIENTED_EDGE('',*,*,#18656,.T.);
#29460=ORIENTED_EDGE('',*,*,#19548,.T.);
#29461=ORIENTED_EDGE('',*,*,#18454,.T.);
#29462=ORIENTED_EDGE('',*,*,#19547,.F.);
#29463=ORIENTED_EDGE('',*,*,#18655,.T.);
#29464=ORIENTED_EDGE('',*,*,#18856,.T.);
#29465=ORIENTED_EDGE('',*,*,#19093,.T.);
#29466=ORIENTED_EDGE('',*,*,#19309,.T.);
#29467=ORIENTED_EDGE('',*,*,#18455,.T.);
#29468=ORIENTED_EDGE('',*,*,#19548,.F.);
#29469=ORIENTED_EDGE('',*,*,#18661,.T.);
#29470=ORIENTED_EDGE('',*,*,#19549,.T.);
#29471=ORIENTED_EDGE('',*,*,#18449,.T.);
#29472=ORIENTED_EDGE('',*,*,#19306,.T.);
#29473=ORIENTED_EDGE('',*,*,#19088,.T.);
#29474=ORIENTED_EDGE('',*,*,#18851,.T.);
#29475=ORIENTED_EDGE('',*,*,#18660,.T.);
#29476=ORIENTED_EDGE('',*,*,#19550,.T.);
#29477=ORIENTED_EDGE('',*,*,#18450,.T.);
#29478=ORIENTED_EDGE('',*,*,#19549,.F.);
#29479=ORIENTED_EDGE('',*,*,#18659,.T.);
#29480=ORIENTED_EDGE('',*,*,#18853,.T.);
#29481=ORIENTED_EDGE('',*,*,#19090,.T.);
#29482=ORIENTED_EDGE('',*,*,#19307,.T.);
#29483=ORIENTED_EDGE('',*,*,#18451,.T.);
#29484=ORIENTED_EDGE('',*,*,#19550,.F.);
#29485=ORIENTED_EDGE('',*,*,#18665,.T.);
#29486=ORIENTED_EDGE('',*,*,#19551,.T.);
#29487=ORIENTED_EDGE('',*,*,#18445,.T.);
#29488=ORIENTED_EDGE('',*,*,#19304,.T.);
#29489=ORIENTED_EDGE('',*,*,#19085,.T.);
#29490=ORIENTED_EDGE('',*,*,#18848,.T.);
#29491=ORIENTED_EDGE('',*,*,#18664,.T.);
#29492=ORIENTED_EDGE('',*,*,#19552,.T.);
#29493=ORIENTED_EDGE('',*,*,#18446,.T.);
#29494=ORIENTED_EDGE('',*,*,#19551,.F.);
#29495=ORIENTED_EDGE('',*,*,#18663,.T.);
#29496=ORIENTED_EDGE('',*,*,#18850,.T.);
#29497=ORIENTED_EDGE('',*,*,#19087,.T.);
#29498=ORIENTED_EDGE('',*,*,#19305,.T.);
#29499=ORIENTED_EDGE('',*,*,#18447,.T.);
#29500=ORIENTED_EDGE('',*,*,#19552,.F.);
#29501=ORIENTED_EDGE('',*,*,#18669,.T.);
#29502=ORIENTED_EDGE('',*,*,#19553,.T.);
#29503=ORIENTED_EDGE('',*,*,#18441,.T.);
#29504=ORIENTED_EDGE('',*,*,#19302,.T.);
#29505=ORIENTED_EDGE('',*,*,#19082,.T.);
#29506=ORIENTED_EDGE('',*,*,#18845,.T.);
#29507=ORIENTED_EDGE('',*,*,#18668,.T.);
#29508=ORIENTED_EDGE('',*,*,#19554,.T.);
#29509=ORIENTED_EDGE('',*,*,#18442,.T.);
#29510=ORIENTED_EDGE('',*,*,#19553,.F.);
#29511=ORIENTED_EDGE('',*,*,#18667,.T.);
#29512=ORIENTED_EDGE('',*,*,#18847,.T.);
#29513=ORIENTED_EDGE('',*,*,#19084,.T.);
#29514=ORIENTED_EDGE('',*,*,#19303,.T.);
#29515=ORIENTED_EDGE('',*,*,#18443,.T.);
#29516=ORIENTED_EDGE('',*,*,#19554,.F.);
#29517=ORIENTED_EDGE('',*,*,#18673,.T.);
#29518=ORIENTED_EDGE('',*,*,#19555,.T.);
#29519=ORIENTED_EDGE('',*,*,#18437,.T.);
#29520=ORIENTED_EDGE('',*,*,#19300,.T.);
#29521=ORIENTED_EDGE('',*,*,#19079,.T.);
#29522=ORIENTED_EDGE('',*,*,#18842,.T.);
#29523=ORIENTED_EDGE('',*,*,#18672,.T.);
#29524=ORIENTED_EDGE('',*,*,#19556,.T.);
#29525=ORIENTED_EDGE('',*,*,#18438,.T.);
#29526=ORIENTED_EDGE('',*,*,#19555,.F.);
#29527=ORIENTED_EDGE('',*,*,#18671,.T.);
#29528=ORIENTED_EDGE('',*,*,#18844,.T.);
#29529=ORIENTED_EDGE('',*,*,#19081,.T.);
#29530=ORIENTED_EDGE('',*,*,#19301,.T.);
#29531=ORIENTED_EDGE('',*,*,#18439,.T.);
#29532=ORIENTED_EDGE('',*,*,#19556,.F.);
#29533=ORIENTED_EDGE('',*,*,#18677,.T.);
#29534=ORIENTED_EDGE('',*,*,#19557,.T.);
#29535=ORIENTED_EDGE('',*,*,#18433,.T.);
#29536=ORIENTED_EDGE('',*,*,#19298,.T.);
#29537=ORIENTED_EDGE('',*,*,#19076,.T.);
#29538=ORIENTED_EDGE('',*,*,#18839,.T.);
#29539=ORIENTED_EDGE('',*,*,#18676,.T.);
#29540=ORIENTED_EDGE('',*,*,#19558,.T.);
#29541=ORIENTED_EDGE('',*,*,#18434,.T.);
#29542=ORIENTED_EDGE('',*,*,#19557,.F.);
#29543=ORIENTED_EDGE('',*,*,#18675,.T.);
#29544=ORIENTED_EDGE('',*,*,#18841,.T.);
#29545=ORIENTED_EDGE('',*,*,#19078,.T.);
#29546=ORIENTED_EDGE('',*,*,#19299,.T.);
#29547=ORIENTED_EDGE('',*,*,#18435,.T.);
#29548=ORIENTED_EDGE('',*,*,#19558,.F.);
#29549=ORIENTED_EDGE('',*,*,#18681,.T.);
#29550=ORIENTED_EDGE('',*,*,#19559,.T.);
#29551=ORIENTED_EDGE('',*,*,#18429,.T.);
#29552=ORIENTED_EDGE('',*,*,#19296,.T.);
#29553=ORIENTED_EDGE('',*,*,#19073,.T.);
#29554=ORIENTED_EDGE('',*,*,#18836,.T.);
#29555=ORIENTED_EDGE('',*,*,#18680,.T.);
#29556=ORIENTED_EDGE('',*,*,#19560,.T.);
#29557=ORIENTED_EDGE('',*,*,#18430,.T.);
#29558=ORIENTED_EDGE('',*,*,#19559,.F.);
#29559=ORIENTED_EDGE('',*,*,#18679,.T.);
#29560=ORIENTED_EDGE('',*,*,#18838,.T.);
#29561=ORIENTED_EDGE('',*,*,#19075,.T.);
#29562=ORIENTED_EDGE('',*,*,#19297,.T.);
#29563=ORIENTED_EDGE('',*,*,#18431,.T.);
#29564=ORIENTED_EDGE('',*,*,#19560,.F.);
#29565=ORIENTED_EDGE('',*,*,#18685,.T.);
#29566=ORIENTED_EDGE('',*,*,#19561,.T.);
#29567=ORIENTED_EDGE('',*,*,#18425,.T.);
#29568=ORIENTED_EDGE('',*,*,#19294,.T.);
#29569=ORIENTED_EDGE('',*,*,#19070,.T.);
#29570=ORIENTED_EDGE('',*,*,#18833,.T.);
#29571=ORIENTED_EDGE('',*,*,#18684,.T.);
#29572=ORIENTED_EDGE('',*,*,#19562,.T.);
#29573=ORIENTED_EDGE('',*,*,#18426,.T.);
#29574=ORIENTED_EDGE('',*,*,#19561,.F.);
#29575=ORIENTED_EDGE('',*,*,#18683,.T.);
#29576=ORIENTED_EDGE('',*,*,#18835,.T.);
#29577=ORIENTED_EDGE('',*,*,#19072,.T.);
#29578=ORIENTED_EDGE('',*,*,#19295,.T.);
#29579=ORIENTED_EDGE('',*,*,#18427,.T.);
#29580=ORIENTED_EDGE('',*,*,#19562,.F.);
#29581=ORIENTED_EDGE('',*,*,#18689,.T.);
#29582=ORIENTED_EDGE('',*,*,#19563,.T.);
#29583=ORIENTED_EDGE('',*,*,#18421,.T.);
#29584=ORIENTED_EDGE('',*,*,#19292,.T.);
#29585=ORIENTED_EDGE('',*,*,#19067,.T.);
#29586=ORIENTED_EDGE('',*,*,#18830,.T.);
#29587=ORIENTED_EDGE('',*,*,#18688,.T.);
#29588=ORIENTED_EDGE('',*,*,#19564,.T.);
#29589=ORIENTED_EDGE('',*,*,#18422,.T.);
#29590=ORIENTED_EDGE('',*,*,#19563,.F.);
#29591=ORIENTED_EDGE('',*,*,#18687,.T.);
#29592=ORIENTED_EDGE('',*,*,#18832,.T.);
#29593=ORIENTED_EDGE('',*,*,#19069,.T.);
#29594=ORIENTED_EDGE('',*,*,#19293,.T.);
#29595=ORIENTED_EDGE('',*,*,#18423,.T.);
#29596=ORIENTED_EDGE('',*,*,#19564,.F.);
#29597=ORIENTED_EDGE('',*,*,#18693,.T.);
#29598=ORIENTED_EDGE('',*,*,#19565,.T.);
#29599=ORIENTED_EDGE('',*,*,#18417,.T.);
#29600=ORIENTED_EDGE('',*,*,#19290,.T.);
#29601=ORIENTED_EDGE('',*,*,#19064,.T.);
#29602=ORIENTED_EDGE('',*,*,#18827,.T.);
#29603=ORIENTED_EDGE('',*,*,#18692,.T.);
#29604=ORIENTED_EDGE('',*,*,#19566,.T.);
#29605=ORIENTED_EDGE('',*,*,#18418,.T.);
#29606=ORIENTED_EDGE('',*,*,#19565,.F.);
#29607=ORIENTED_EDGE('',*,*,#18691,.T.);
#29608=ORIENTED_EDGE('',*,*,#18829,.T.);
#29609=ORIENTED_EDGE('',*,*,#19066,.T.);
#29610=ORIENTED_EDGE('',*,*,#19291,.T.);
#29611=ORIENTED_EDGE('',*,*,#18419,.T.);
#29612=ORIENTED_EDGE('',*,*,#19566,.F.);
#29613=ORIENTED_EDGE('',*,*,#18697,.T.);
#29614=ORIENTED_EDGE('',*,*,#19567,.T.);
#29615=ORIENTED_EDGE('',*,*,#18413,.T.);
#29616=ORIENTED_EDGE('',*,*,#19288,.T.);
#29617=ORIENTED_EDGE('',*,*,#19061,.T.);
#29618=ORIENTED_EDGE('',*,*,#18824,.T.);
#29619=ORIENTED_EDGE('',*,*,#18696,.T.);
#29620=ORIENTED_EDGE('',*,*,#19568,.T.);
#29621=ORIENTED_EDGE('',*,*,#18414,.T.);
#29622=ORIENTED_EDGE('',*,*,#19567,.F.);
#29623=ORIENTED_EDGE('',*,*,#18695,.T.);
#29624=ORIENTED_EDGE('',*,*,#18826,.T.);
#29625=ORIENTED_EDGE('',*,*,#19063,.T.);
#29626=ORIENTED_EDGE('',*,*,#19289,.T.);
#29627=ORIENTED_EDGE('',*,*,#18415,.T.);
#29628=ORIENTED_EDGE('',*,*,#19568,.F.);
#29629=ORIENTED_EDGE('',*,*,#18701,.T.);
#29630=ORIENTED_EDGE('',*,*,#19569,.T.);
#29631=ORIENTED_EDGE('',*,*,#18409,.T.);
#29632=ORIENTED_EDGE('',*,*,#19286,.T.);
#29633=ORIENTED_EDGE('',*,*,#19058,.T.);
#29634=ORIENTED_EDGE('',*,*,#18821,.T.);
#29635=ORIENTED_EDGE('',*,*,#18700,.T.);
#29636=ORIENTED_EDGE('',*,*,#19570,.T.);
#29637=ORIENTED_EDGE('',*,*,#18410,.T.);
#29638=ORIENTED_EDGE('',*,*,#19569,.F.);
#29639=ORIENTED_EDGE('',*,*,#18699,.T.);
#29640=ORIENTED_EDGE('',*,*,#18823,.T.);
#29641=ORIENTED_EDGE('',*,*,#19060,.T.);
#29642=ORIENTED_EDGE('',*,*,#19287,.T.);
#29643=ORIENTED_EDGE('',*,*,#18411,.T.);
#29644=ORIENTED_EDGE('',*,*,#19570,.F.);
#29645=ORIENTED_EDGE('',*,*,#18705,.T.);
#29646=ORIENTED_EDGE('',*,*,#19571,.T.);
#29647=ORIENTED_EDGE('',*,*,#18405,.T.);
#29648=ORIENTED_EDGE('',*,*,#19284,.T.);
#29649=ORIENTED_EDGE('',*,*,#19055,.T.);
#29650=ORIENTED_EDGE('',*,*,#18818,.T.);
#29651=ORIENTED_EDGE('',*,*,#18704,.T.);
#29652=ORIENTED_EDGE('',*,*,#19572,.T.);
#29653=ORIENTED_EDGE('',*,*,#18406,.T.);
#29654=ORIENTED_EDGE('',*,*,#19571,.F.);
#29655=ORIENTED_EDGE('',*,*,#18703,.T.);
#29656=ORIENTED_EDGE('',*,*,#18820,.T.);
#29657=ORIENTED_EDGE('',*,*,#19057,.T.);
#29658=ORIENTED_EDGE('',*,*,#19285,.T.);
#29659=ORIENTED_EDGE('',*,*,#18407,.T.);
#29660=ORIENTED_EDGE('',*,*,#19572,.F.);
#29661=ORIENTED_EDGE('',*,*,#18709,.T.);
#29662=ORIENTED_EDGE('',*,*,#19573,.T.);
#29663=ORIENTED_EDGE('',*,*,#18401,.T.);
#29664=ORIENTED_EDGE('',*,*,#19282,.T.);
#29665=ORIENTED_EDGE('',*,*,#19052,.T.);
#29666=ORIENTED_EDGE('',*,*,#18815,.T.);
#29667=ORIENTED_EDGE('',*,*,#18708,.T.);
#29668=ORIENTED_EDGE('',*,*,#19574,.T.);
#29669=ORIENTED_EDGE('',*,*,#18402,.T.);
#29670=ORIENTED_EDGE('',*,*,#19573,.F.);
#29671=ORIENTED_EDGE('',*,*,#18707,.T.);
#29672=ORIENTED_EDGE('',*,*,#18817,.T.);
#29673=ORIENTED_EDGE('',*,*,#19054,.T.);
#29674=ORIENTED_EDGE('',*,*,#19283,.T.);
#29675=ORIENTED_EDGE('',*,*,#18403,.T.);
#29676=ORIENTED_EDGE('',*,*,#19574,.F.);
#29677=ORIENTED_EDGE('',*,*,#18713,.T.);
#29678=ORIENTED_EDGE('',*,*,#19575,.T.);
#29679=ORIENTED_EDGE('',*,*,#18397,.T.);
#29680=ORIENTED_EDGE('',*,*,#19280,.T.);
#29681=ORIENTED_EDGE('',*,*,#19049,.T.);
#29682=ORIENTED_EDGE('',*,*,#18812,.T.);
#29683=ORIENTED_EDGE('',*,*,#18712,.T.);
#29684=ORIENTED_EDGE('',*,*,#19576,.T.);
#29685=ORIENTED_EDGE('',*,*,#18398,.T.);
#29686=ORIENTED_EDGE('',*,*,#19575,.F.);
#29687=ORIENTED_EDGE('',*,*,#18711,.T.);
#29688=ORIENTED_EDGE('',*,*,#18814,.T.);
#29689=ORIENTED_EDGE('',*,*,#19051,.T.);
#29690=ORIENTED_EDGE('',*,*,#19281,.T.);
#29691=ORIENTED_EDGE('',*,*,#18399,.T.);
#29692=ORIENTED_EDGE('',*,*,#19576,.F.);
#29693=ORIENTED_EDGE('',*,*,#18716,.T.);
#29694=ORIENTED_EDGE('',*,*,#18120,.T.);
#29695=ORIENTED_EDGE('',*,*,#18394,.T.);
#29696=ORIENTED_EDGE('',*,*,#19278,.T.);
#29697=ORIENTED_EDGE('',*,*,#19046,.T.);
#29698=ORIENTED_EDGE('',*,*,#18809,.T.);
#29699=ORIENTED_EDGE('',*,*,#18715,.T.);
#29700=ORIENTED_EDGE('',*,*,#18811,.T.);
#29701=ORIENTED_EDGE('',*,*,#19048,.T.);
#29702=ORIENTED_EDGE('',*,*,#19279,.T.);
#29703=ORIENTED_EDGE('',*,*,#18395,.T.);
#29704=ORIENTED_EDGE('',*,*,#18118,.F.);
#29705=ORIENTED_EDGE('',*,*,#18719,.T.);
#29706=ORIENTED_EDGE('',*,*,#18116,.T.);
#29707=ORIENTED_EDGE('',*,*,#18391,.T.);
#29708=ORIENTED_EDGE('',*,*,#19276,.T.);
#29709=ORIENTED_EDGE('',*,*,#19043,.T.);
#29710=ORIENTED_EDGE('',*,*,#18806,.T.);
#29711=ORIENTED_EDGE('',*,*,#18718,.T.);
#29712=ORIENTED_EDGE('',*,*,#18808,.T.);
#29713=ORIENTED_EDGE('',*,*,#19045,.T.);
#29714=ORIENTED_EDGE('',*,*,#19277,.T.);
#29715=ORIENTED_EDGE('',*,*,#18392,.T.);
#29716=ORIENTED_EDGE('',*,*,#18114,.F.);
#29717=ORIENTED_EDGE('',*,*,#18722,.T.);
#29718=ORIENTED_EDGE('',*,*,#18112,.T.);
#29719=ORIENTED_EDGE('',*,*,#18388,.T.);
#29720=ORIENTED_EDGE('',*,*,#19274,.T.);
#29721=ORIENTED_EDGE('',*,*,#19040,.T.);
#29722=ORIENTED_EDGE('',*,*,#18803,.T.);
#29723=ORIENTED_EDGE('',*,*,#18721,.T.);
#29724=ORIENTED_EDGE('',*,*,#18805,.T.);
#29725=ORIENTED_EDGE('',*,*,#19042,.T.);
#29726=ORIENTED_EDGE('',*,*,#19275,.T.);
#29727=ORIENTED_EDGE('',*,*,#18389,.T.);
#29728=ORIENTED_EDGE('',*,*,#18110,.F.);
#29729=ORIENTED_EDGE('',*,*,#18725,.T.);
#29730=ORIENTED_EDGE('',*,*,#18108,.T.);
#29731=ORIENTED_EDGE('',*,*,#18385,.T.);
#29732=ORIENTED_EDGE('',*,*,#19272,.T.);
#29733=ORIENTED_EDGE('',*,*,#19037,.T.);
#29734=ORIENTED_EDGE('',*,*,#18800,.T.);
#29735=ORIENTED_EDGE('',*,*,#18724,.T.);
#29736=ORIENTED_EDGE('',*,*,#18802,.T.);
#29737=ORIENTED_EDGE('',*,*,#19039,.T.);
#29738=ORIENTED_EDGE('',*,*,#19273,.T.);
#29739=ORIENTED_EDGE('',*,*,#18386,.T.);
#29740=ORIENTED_EDGE('',*,*,#18106,.F.);
#29741=ORIENTED_EDGE('',*,*,#18728,.T.);
#29742=ORIENTED_EDGE('',*,*,#18104,.T.);
#29743=ORIENTED_EDGE('',*,*,#18382,.T.);
#29744=ORIENTED_EDGE('',*,*,#19270,.T.);
#29745=ORIENTED_EDGE('',*,*,#19034,.T.);
#29746=ORIENTED_EDGE('',*,*,#18797,.T.);
#29747=ORIENTED_EDGE('',*,*,#18727,.T.);
#29748=ORIENTED_EDGE('',*,*,#18799,.T.);
#29749=ORIENTED_EDGE('',*,*,#19036,.T.);
#29750=ORIENTED_EDGE('',*,*,#19271,.T.);
#29751=ORIENTED_EDGE('',*,*,#18383,.T.);
#29752=ORIENTED_EDGE('',*,*,#18102,.F.);
#29753=ORIENTED_EDGE('',*,*,#18731,.T.);
#29754=ORIENTED_EDGE('',*,*,#18100,.T.);
#29755=ORIENTED_EDGE('',*,*,#18379,.T.);
#29756=ORIENTED_EDGE('',*,*,#19267,.T.);
#29757=ORIENTED_EDGE('',*,*,#19030,.T.);
#29758=ORIENTED_EDGE('',*,*,#18793,.T.);
#29759=ORIENTED_EDGE('',*,*,#18730,.T.);
#29760=ORIENTED_EDGE('',*,*,#18796,.T.);
#29761=ORIENTED_EDGE('',*,*,#19033,.T.);
#29762=ORIENTED_EDGE('',*,*,#19269,.T.);
#29763=ORIENTED_EDGE('',*,*,#18380,.T.);
#29764=ORIENTED_EDGE('',*,*,#18098,.F.);
#30124=PLANE('',#36092);
#30125=PLANE('',#36093);
#30126=PLANE('',#36103);
#30127=PLANE('',#36104);
#30128=PLANE('',#36105);
#30129=PLANE('',#36106);
#30130=PLANE('',#36107);
#30131=PLANE('',#36108);
#30132=PLANE('',#36109);
#30133=PLANE('',#36110);
#30134=PLANE('',#36112);
#30135=PLANE('',#36114);
#30136=PLANE('',#36115);
#30137=PLANE('',#36117);
#30138=PLANE('',#36118);
#30139=PLANE('',#36120);
#30140=PLANE('',#36121);
#30141=PLANE('',#36123);
#30142=PLANE('',#36124);
#30143=PLANE('',#36126);
#30144=PLANE('',#36127);
#30145=PLANE('',#36129);
#30146=PLANE('',#36130);
#30147=PLANE('',#36132);
#30148=PLANE('',#36133);
#30149=PLANE('',#36134);
#30150=PLANE('',#36135);
#30151=PLANE('',#36136);
#30152=PLANE('',#36137);
#30153=PLANE('',#36138);
#30154=PLANE('',#36139);
#30155=PLANE('',#36140);
#30156=PLANE('',#36141);
#30157=PLANE('',#36142);
#30158=PLANE('',#36143);
#30159=PLANE('',#36144);
#30160=PLANE('',#36145);
#30161=PLANE('',#36146);
#30162=PLANE('',#36147);
#30163=PLANE('',#36148);
#30164=PLANE('',#36149);
#30165=PLANE('',#36150);
#30166=PLANE('',#36151);
#30167=PLANE('',#36153);
#30168=PLANE('',#36154);
#30169=PLANE('',#36156);
#30170=PLANE('',#36157);
#30171=PLANE('',#36159);
#30172=PLANE('',#36160);
#30173=PLANE('',#36162);
#30174=PLANE('',#36163);
#30175=PLANE('',#36165);
#30176=PLANE('',#36166);
#30177=PLANE('',#36168);
#30178=PLANE('',#36169);
#30179=PLANE('',#36171);
#30180=PLANE('',#36172);
#30181=PLANE('',#36174);
#30182=PLANE('',#36175);
#30183=PLANE('',#36177);
#30184=PLANE('',#36178);
#30185=PLANE('',#36180);
#30186=PLANE('',#36181);
#30187=PLANE('',#36183);
#30188=PLANE('',#36184);
#30189=PLANE('',#36186);
#30190=PLANE('',#36187);
#30191=PLANE('',#36189);
#30192=PLANE('',#36190);
#30193=PLANE('',#36192);
#30194=PLANE('',#36193);
#30195=PLANE('',#36195);
#30196=PLANE('',#36196);
#30197=PLANE('',#36198);
#30198=PLANE('',#36199);
#30199=PLANE('',#36201);
#30200=PLANE('',#36202);
#30201=PLANE('',#36204);
#30202=PLANE('',#36205);
#30203=PLANE('',#36207);
#30204=PLANE('',#36208);
#30205=PLANE('',#36210);
#30206=PLANE('',#36211);
#30207=PLANE('',#36213);
#30208=PLANE('',#36214);
#30209=PLANE('',#36216);
#30210=PLANE('',#36217);
#30211=PLANE('',#36219);
#30212=PLANE('',#36220);
#30213=PLANE('',#36222);
#30214=PLANE('',#36223);
#30215=PLANE('',#36225);
#30216=PLANE('',#36226);
#30217=PLANE('',#36228);
#30218=PLANE('',#36229);
#30219=PLANE('',#36231);
#30220=PLANE('',#36232);
#30221=PLANE('',#36234);
#30222=PLANE('',#36235);
#30223=PLANE('',#36237);
#30224=PLANE('',#36238);
#30225=PLANE('',#36240);
#30226=PLANE('',#36241);
#30227=PLANE('',#36243);
#30228=PLANE('',#36244);
#30229=PLANE('',#36246);
#30230=PLANE('',#36247);
#30231=PLANE('',#36249);
#30232=PLANE('',#36250);
#30233=PLANE('',#36252);
#30234=PLANE('',#36253);
#30235=PLANE('',#36255);
#30236=PLANE('',#36256);
#30237=PLANE('',#36258);
#30238=PLANE('',#36259);
#30239=PLANE('',#36261);
#30240=PLANE('',#36262);
#30241=PLANE('',#36264);
#30242=PLANE('',#36265);
#30243=PLANE('',#36267);
#30244=PLANE('',#36268);
#30245=PLANE('',#36270);
#30246=PLANE('',#36271);
#30247=PLANE('',#36273);
#30248=PLANE('',#36274);
#30249=PLANE('',#36276);
#30250=PLANE('',#36277);
#30251=PLANE('',#36279);
#30252=PLANE('',#36280);
#30253=PLANE('',#36282);
#30254=PLANE('',#36283);
#30255=PLANE('',#36285);
#30256=PLANE('',#36286);
#30257=PLANE('',#36288);
#30258=PLANE('',#36289);
#30259=PLANE('',#36291);
#30260=PLANE('',#36292);
#30261=PLANE('',#36294);
#30262=PLANE('',#36295);
#30263=PLANE('',#36297);
#30264=PLANE('',#36298);
#30265=PLANE('',#36300);
#30266=PLANE('',#36301);
#30267=PLANE('',#36303);
#30268=PLANE('',#36304);
#30269=PLANE('',#36306);
#30270=PLANE('',#36307);
#30271=PLANE('',#36309);
#30272=PLANE('',#36310);
#30273=PLANE('',#36312);
#30274=PLANE('',#36313);
#30275=PLANE('',#36315);
#30276=PLANE('',#36316);
#30277=PLANE('',#36318);
#30278=PLANE('',#36319);
#30279=PLANE('',#36321);
#30280=PLANE('',#36322);
#30281=PLANE('',#36324);
#30282=PLANE('',#36325);
#30283=PLANE('',#36326);
#30284=PLANE('',#36327);
#30285=PLANE('',#36328);
#30286=PLANE('',#36329);
#30287=PLANE('',#36330);
#30288=PLANE('',#36331);
#30289=PLANE('',#36332);
#30290=PLANE('',#36333);
#30291=PLANE('',#36334);
#30292=PLANE('',#36335);
#30293=PLANE('',#36336);
#31458=ADVANCED_FACE('',(#6298),#4913,.T.);
#31459=ADVANCED_FACE('',(#6299),#4914,.T.);
#31460=ADVANCED_FACE('',(#6300),#4915,.T.);
#31461=ADVANCED_FACE('',(#6301),#4916,.T.);
#31462=ADVANCED_FACE('',(#6302),#4917,.T.);
#31463=ADVANCED_FACE('',(#6303),#4918,.T.);
#31464=ADVANCED_FACE('',(#6304),#4919,.T.);
#31465=ADVANCED_FACE('',(#6305),#4920,.T.);
#31466=ADVANCED_FACE('',(#6306),#4921,.T.);
#31467=ADVANCED_FACE('',(#6307),#4922,.T.);
#31468=ADVANCED_FACE('',(#6308),#4923,.T.);
#31469=ADVANCED_FACE('',(#6309),#4924,.T.);
#31470=ADVANCED_FACE('',(#6310),#4925,.T.);
#31471=ADVANCED_FACE('',(#6311),#4926,.T.);
#31472=ADVANCED_FACE('',(#6312),#4927,.T.);
#31473=ADVANCED_FACE('',(#6313),#4928,.T.);
#31474=ADVANCED_FACE('',(#6314),#4929,.T.);
#31475=ADVANCED_FACE('',(#6315),#4930,.T.);
#31476=ADVANCED_FACE('',(#6316),#4931,.T.);
#31477=ADVANCED_FACE('',(#6317),#4932,.T.);
#31478=ADVANCED_FACE('',(#6318),#4933,.T.);
#31479=ADVANCED_FACE('',(#6319),#4934,.T.);
#31480=ADVANCED_FACE('',(#6320),#4935,.T.);
#31481=ADVANCED_FACE('',(#6321),#4936,.T.);
#31482=ADVANCED_FACE('',(#6322),#4937,.T.);
#31483=ADVANCED_FACE('',(#6323),#4938,.T.);
#31484=ADVANCED_FACE('',(#6324),#4939,.T.);
#31485=ADVANCED_FACE('',(#6325),#4940,.T.);
#31486=ADVANCED_FACE('',(#6326),#2968,.T.);
#31487=ADVANCED_FACE('',(#6327),#4941,.T.);
#31488=ADVANCED_FACE('',(#6328),#4942,.T.);
#31489=ADVANCED_FACE('',(#6329),#4943,.T.);
#31490=ADVANCED_FACE('',(#6330),#4944,.T.);
#31491=ADVANCED_FACE('',(#6331),#4945,.T.);
#31492=ADVANCED_FACE('',(#6332),#4946,.T.);
#31493=ADVANCED_FACE('',(#6333),#4947,.T.);
#31494=ADVANCED_FACE('',(#6334),#4948,.T.);
#31495=ADVANCED_FACE('',(#6335),#4949,.T.);
#31496=ADVANCED_FACE('',(#6336),#4950,.T.);
#31497=ADVANCED_FACE('',(#6337),#4951,.T.);
#31498=ADVANCED_FACE('',(#6338),#4952,.T.);
#31499=ADVANCED_FACE('',(#6339),#4953,.T.);
#31500=ADVANCED_FACE('',(#6340),#4954,.T.);
#31501=ADVANCED_FACE('',(#6341),#4955,.T.);
#31502=ADVANCED_FACE('',(#6342),#4956,.T.);
#31503=ADVANCED_FACE('',(#6343),#4957,.T.);
#31504=ADVANCED_FACE('',(#6344),#4958,.T.);
#31505=ADVANCED_FACE('',(#6345),#4959,.T.);
#31506=ADVANCED_FACE('',(#6346),#4960,.T.);
#31507=ADVANCED_FACE('',(#6347),#4961,.T.);
#31508=ADVANCED_FACE('',(#6348),#4962,.T.);
#31509=ADVANCED_FACE('',(#6349),#4963,.T.);
#31510=ADVANCED_FACE('',(#6350),#4964,.T.);
#31511=ADVANCED_FACE('',(#6351),#4965,.T.);
#31512=ADVANCED_FACE('',(#6352),#4966,.T.);
#31513=ADVANCED_FACE('',(#6353),#4967,.T.);
#31514=ADVANCED_FACE('',(#6354),#4968,.T.);
#31515=ADVANCED_FACE('',(#6355),#4969,.T.);
#31516=ADVANCED_FACE('',(#6356),#4970,.T.);
#31517=ADVANCED_FACE('',(#6357),#4971,.T.);
#31518=ADVANCED_FACE('',(#6358),#2969,.T.);
#31519=ADVANCED_FACE('',(#6359),#4972,.T.);
#31520=ADVANCED_FACE('',(#6360),#4973,.F.);
#31521=ADVANCED_FACE('',(#6361),#4974,.F.);
#31522=ADVANCED_FACE('',(#6362),#4975,.F.);
#31523=ADVANCED_FACE('',(#6363),#4976,.F.);
#31524=ADVANCED_FACE('',(#6364),#4977,.F.);
#31525=ADVANCED_FACE('',(#6365),#4978,.F.);
#31526=ADVANCED_FACE('',(#6366),#4979,.F.);
#31527=ADVANCED_FACE('',(#6367),#4980,.F.);
#31528=ADVANCED_FACE('',(#6368),#4981,.F.);
#31529=ADVANCED_FACE('',(#6369),#4982,.F.);
#31530=ADVANCED_FACE('',(#6370),#4983,.F.);
#31531=ADVANCED_FACE('',(#6371),#4984,.F.);
#31532=ADVANCED_FACE('',(#6372),#4985,.F.);
#31533=ADVANCED_FACE('',(#6373),#4986,.F.);
#31534=ADVANCED_FACE('',(#6374),#4987,.F.);
#31535=ADVANCED_FACE('',(#6375),#2970,.F.);
#31536=ADVANCED_FACE('',(#6376),#377,.T.);
#31537=ADVANCED_FACE('',(#6377),#2971,.T.);
#31538=ADVANCED_FACE('',(#6378),#2972,.T.);
#31539=ADVANCED_FACE('',(#6379),#378,.F.);
#31540=ADVANCED_FACE('',(#6380),#4988,.T.);
#31541=ADVANCED_FACE('',(#6381),#379,.T.);
#31542=ADVANCED_FACE('',(#6382),#380,.F.);
#31543=ADVANCED_FACE('',(#6383),#381,.T.);
#31544=ADVANCED_FACE('',(#6384),#382,.T.);
#31545=ADVANCED_FACE('',(#6385),#383,.T.);
#31546=ADVANCED_FACE('',(#6386),#384,.T.);
#31547=ADVANCED_FACE('',(#6387),#385,.T.);
#31548=ADVANCED_FACE('',(#6388),#386,.T.);
#31549=ADVANCED_FACE('',(#6389),#387,.T.);
#31550=ADVANCED_FACE('',(#6390),#388,.T.);
#31551=ADVANCED_FACE('',(#6391),#389,.T.);
#31552=ADVANCED_FACE('',(#6392),#390,.T.);
#31553=ADVANCED_FACE('',(#6393),#391,.T.);
#31554=ADVANCED_FACE('',(#6394),#392,.T.);
#31555=ADVANCED_FACE('',(#6395),#393,.T.);
#31556=ADVANCED_FACE('',(#6396),#394,.T.);
#31557=ADVANCED_FACE('',(#6397),#395,.T.);
#31558=ADVANCED_FACE('',(#6398),#396,.T.);
#31559=ADVANCED_FACE('',(#6399),#397,.T.);
#31560=ADVANCED_FACE('',(#6400),#398,.T.);
#31561=ADVANCED_FACE('',(#6401),#399,.T.);
#31562=ADVANCED_FACE('',(#6402),#400,.T.);
#31563=ADVANCED_FACE('',(#6403),#401,.T.);
#31564=ADVANCED_FACE('',(#6404),#402,.T.);
#31565=ADVANCED_FACE('',(#6405),#403,.T.);
#31566=ADVANCED_FACE('',(#6406),#404,.T.);
#31567=ADVANCED_FACE('',(#6407),#405,.T.);
#31568=ADVANCED_FACE('',(#6408),#406,.T.);
#31569=ADVANCED_FACE('',(#6409),#407,.T.);
#31570=ADVANCED_FACE('',(#6410),#408,.T.);
#31571=ADVANCED_FACE('',(#6411),#409,.T.);
#31572=ADVANCED_FACE('',(#6412),#410,.T.);
#31573=ADVANCED_FACE('',(#6413),#411,.T.);
#31574=ADVANCED_FACE('',(#6414),#412,.T.);
#31575=ADVANCED_FACE('',(#6415),#413,.T.);
#31576=ADVANCED_FACE('',(#6416),#414,.T.);
#31577=ADVANCED_FACE('',(#6417),#415,.T.);
#31578=ADVANCED_FACE('',(#6418),#416,.T.);
#31579=ADVANCED_FACE('',(#6419),#417,.T.);
#31580=ADVANCED_FACE('',(#6420),#418,.T.);
#31581=ADVANCED_FACE('',(#6421),#419,.T.);
#31582=ADVANCED_FACE('',(#6422),#420,.T.);
#31583=ADVANCED_FACE('',(#6423),#421,.T.);
#31584=ADVANCED_FACE('',(#6424),#422,.T.);
#31585=ADVANCED_FACE('',(#6425),#423,.T.);
#31586=ADVANCED_FACE('',(#6426),#424,.T.);
#31587=ADVANCED_FACE('',(#6427),#425,.T.);
#31588=ADVANCED_FACE('',(#6428),#426,.T.);
#31589=ADVANCED_FACE('',(#6429),#427,.T.);
#31590=ADVANCED_FACE('',(#6430),#428,.T.);
#31591=ADVANCED_FACE('',(#6431),#429,.T.);
#31592=ADVANCED_FACE('',(#6432),#430,.T.);
#31593=ADVANCED_FACE('',(#6433),#431,.T.);
#31594=ADVANCED_FACE('',(#6434),#432,.T.);
#31595=ADVANCED_FACE('',(#6435),#433,.T.);
#31596=ADVANCED_FACE('',(#6436),#434,.T.);
#31597=ADVANCED_FACE('',(#6437),#435,.T.);
#31598=ADVANCED_FACE('',(#6438),#436,.T.);
#31599=ADVANCED_FACE('',(#6439),#437,.T.);
#31600=ADVANCED_FACE('',(#6440),#438,.T.);
#31601=ADVANCED_FACE('',(#6441),#439,.T.);
#31602=ADVANCED_FACE('',(#6442),#440,.T.);
#31603=ADVANCED_FACE('',(#6443),#441,.T.);
#31604=ADVANCED_FACE('',(#6444),#442,.T.);
#31605=ADVANCED_FACE('',(#6445),#443,.T.);
#31606=ADVANCED_FACE('',(#6446),#444,.T.);
#31607=ADVANCED_FACE('',(#6447),#445,.T.);
#31608=ADVANCED_FACE('',(#6448),#446,.T.);
#31609=ADVANCED_FACE('',(#6449),#447,.T.);
#31610=ADVANCED_FACE('',(#6450),#448,.T.);
#31611=ADVANCED_FACE('',(#6451),#449,.T.);
#31612=ADVANCED_FACE('',(#6452),#450,.T.);
#31613=ADVANCED_FACE('',(#6453),#451,.T.);
#31614=ADVANCED_FACE('',(#6454),#452,.T.);
#31615=ADVANCED_FACE('',(#6455),#453,.T.);
#31616=ADVANCED_FACE('',(#6456),#454,.T.);
#31617=ADVANCED_FACE('',(#6457),#455,.T.);
#31618=ADVANCED_FACE('',(#6458),#456,.T.);
#31619=ADVANCED_FACE('',(#6459),#457,.T.);
#31620=ADVANCED_FACE('',(#6460),#458,.T.);
#31621=ADVANCED_FACE('',(#6461),#459,.T.);
#31622=ADVANCED_FACE('',(#6462),#4989,.T.);
#31623=ADVANCED_FACE('',(#6463),#4990,.T.);
#31624=ADVANCED_FACE('',(#6464),#4991,.T.);
#31625=ADVANCED_FACE('',(#6465),#4992,.T.);
#31626=ADVANCED_FACE('',(#6466),#4993,.T.);
#31627=ADVANCED_FACE('',(#6467),#4994,.T.);
#31628=ADVANCED_FACE('',(#6468),#4995,.T.);
#31629=ADVANCED_FACE('',(#6469),#4996,.T.);
#31630=ADVANCED_FACE('',(#6470),#4997,.T.);
#31631=ADVANCED_FACE('',(#6471),#4998,.T.);
#31632=ADVANCED_FACE('',(#6472),#4999,.T.);
#31633=ADVANCED_FACE('',(#6473),#5000,.T.);
#31634=ADVANCED_FACE('',(#6474),#5001,.T.);
#31635=ADVANCED_FACE('',(#6475),#5002,.T.);
#31636=ADVANCED_FACE('',(#6476),#5003,.T.);
#31637=ADVANCED_FACE('',(#6477),#5004,.T.);
#31638=ADVANCED_FACE('',(#6478),#5005,.T.);
#31639=ADVANCED_FACE('',(#6479),#5006,.T.);
#31640=ADVANCED_FACE('',(#6480),#5007,.T.);
#31641=ADVANCED_FACE('',(#6481),#5008,.T.);
#31642=ADVANCED_FACE('',(#6482),#5009,.T.);
#31643=ADVANCED_FACE('',(#6483),#5010,.T.);
#31644=ADVANCED_FACE('',(#6484),#5011,.T.);
#31645=ADVANCED_FACE('',(#6485),#5012,.T.);
#31646=ADVANCED_FACE('',(#6486),#5013,.T.);
#31647=ADVANCED_FACE('',(#6487),#5014,.T.);
#31648=ADVANCED_FACE('',(#6488),#5015,.T.);
#31649=ADVANCED_FACE('',(#6489),#5016,.T.);
#31650=ADVANCED_FACE('',(#6490),#5017,.T.);
#31651=ADVANCED_FACE('',(#6491),#5018,.T.);
#31652=ADVANCED_FACE('',(#6492),#5019,.T.);
#31653=ADVANCED_FACE('',(#6493),#5020,.T.);
#31654=ADVANCED_FACE('',(#6494),#5021,.T.);
#31655=ADVANCED_FACE('',(#6495),#5022,.T.);
#31656=ADVANCED_FACE('',(#6496),#5023,.T.);
#31657=ADVANCED_FACE('',(#6497),#5024,.T.);
#31658=ADVANCED_FACE('',(#6498),#5025,.T.);
#31659=ADVANCED_FACE('',(#6499),#5026,.T.);
#31660=ADVANCED_FACE('',(#6500),#5027,.T.);
#31661=ADVANCED_FACE('',(#6501),#5028,.T.);
#31662=ADVANCED_FACE('',(#6502),#5029,.T.);
#31663=ADVANCED_FACE('',(#6503),#5030,.T.);
#31664=ADVANCED_FACE('',(#6504),#5031,.T.);
#31665=ADVANCED_FACE('',(#6505),#5032,.T.);
#31666=ADVANCED_FACE('',(#6506),#5033,.T.);
#31667=ADVANCED_FACE('',(#6507),#5034,.T.);
#31668=ADVANCED_FACE('',(#6508),#5035,.T.);
#31669=ADVANCED_FACE('',(#6509),#5036,.T.);
#31670=ADVANCED_FACE('',(#6510),#5037,.T.);
#31671=ADVANCED_FACE('',(#6511),#5038,.T.);
#31672=ADVANCED_FACE('',(#6512),#5039,.T.);
#31673=ADVANCED_FACE('',(#6513),#5040,.T.);
#31674=ADVANCED_FACE('',(#6514),#5041,.T.);
#31675=ADVANCED_FACE('',(#6515),#5042,.T.);
#31676=ADVANCED_FACE('',(#6516),#5043,.T.);
#31677=ADVANCED_FACE('',(#6517),#5044,.T.);
#31678=ADVANCED_FACE('',(#6518),#5045,.T.);
#31679=ADVANCED_FACE('',(#6519),#5046,.T.);
#31680=ADVANCED_FACE('',(#6520),#5047,.T.);
#31681=ADVANCED_FACE('',(#6521),#5048,.T.);
#31682=ADVANCED_FACE('',(#6522),#5049,.T.);
#31683=ADVANCED_FACE('',(#6523),#5050,.T.);
#31684=ADVANCED_FACE('',(#6524),#5051,.T.);
#31685=ADVANCED_FACE('',(#6525),#5052,.T.);
#31686=ADVANCED_FACE('',(#6526),#5053,.T.);
#31687=ADVANCED_FACE('',(#6527),#5054,.T.);
#31688=ADVANCED_FACE('',(#6528),#5055,.T.);
#31689=ADVANCED_FACE('',(#6529),#5056,.T.);
#31690=ADVANCED_FACE('',(#6530),#5057,.T.);
#31691=ADVANCED_FACE('',(#6531),#5058,.T.);
#31692=ADVANCED_FACE('',(#6532),#5059,.T.);
#31693=ADVANCED_FACE('',(#6533),#5060,.T.);
#31694=ADVANCED_FACE('',(#6534),#5061,.T.);
#31695=ADVANCED_FACE('',(#6535),#5062,.T.);
#31696=ADVANCED_FACE('',(#6536),#5063,.T.);
#31697=ADVANCED_FACE('',(#6537),#5064,.T.);
#31698=ADVANCED_FACE('',(#6538),#5065,.T.);
#31699=ADVANCED_FACE('',(#6539),#5066,.T.);
#31700=ADVANCED_FACE('',(#6540),#5067,.T.);
#31701=ADVANCED_FACE('',(#6541),#460,.T.);
#31702=ADVANCED_FACE('',(#6542),#461,.T.);
#31703=ADVANCED_FACE('',(#6543),#462,.T.);
#31704=ADVANCED_FACE('',(#6544),#463,.T.);
#31705=ADVANCED_FACE('',(#6545),#464,.T.);
#31706=ADVANCED_FACE('',(#6546),#465,.T.);
#31707=ADVANCED_FACE('',(#6547),#466,.T.);
#31708=ADVANCED_FACE('',(#6548),#467,.T.);
#31709=ADVANCED_FACE('',(#6549),#468,.T.);
#31710=ADVANCED_FACE('',(#6550),#469,.T.);
#31711=ADVANCED_FACE('',(#6551),#470,.T.);
#31712=ADVANCED_FACE('',(#6552),#471,.T.);
#31713=ADVANCED_FACE('',(#6553),#472,.T.);
#31714=ADVANCED_FACE('',(#6554),#473,.T.);
#31715=ADVANCED_FACE('',(#6555),#474,.T.);
#31716=ADVANCED_FACE('',(#6556),#475,.T.);
#31717=ADVANCED_FACE('',(#6557),#476,.T.);
#31718=ADVANCED_FACE('',(#6558),#477,.T.);
#31719=ADVANCED_FACE('',(#6559),#478,.T.);
#31720=ADVANCED_FACE('',(#6560),#479,.T.);
#31721=ADVANCED_FACE('',(#6561),#480,.T.);
#31722=ADVANCED_FACE('',(#6562),#481,.T.);
#31723=ADVANCED_FACE('',(#6563),#482,.T.);
#31724=ADVANCED_FACE('',(#6564),#483,.T.);
#31725=ADVANCED_FACE('',(#6565),#484,.T.);
#31726=ADVANCED_FACE('',(#6566),#485,.T.);
#31727=ADVANCED_FACE('',(#6567),#486,.T.);
#31728=ADVANCED_FACE('',(#6568),#487,.T.);
#31729=ADVANCED_FACE('',(#6569),#488,.T.);
#31730=ADVANCED_FACE('',(#6570),#489,.T.);
#31731=ADVANCED_FACE('',(#6571),#490,.T.);
#31732=ADVANCED_FACE('',(#6572),#491,.T.);
#31733=ADVANCED_FACE('',(#6573),#492,.T.);
#31734=ADVANCED_FACE('',(#6574),#493,.T.);
#31735=ADVANCED_FACE('',(#6575),#494,.T.);
#31736=ADVANCED_FACE('',(#6576),#495,.T.);
#31737=ADVANCED_FACE('',(#6577),#496,.T.);
#31738=ADVANCED_FACE('',(#6578),#497,.T.);
#31739=ADVANCED_FACE('',(#6579),#498,.T.);
#31740=ADVANCED_FACE('',(#6580),#499,.T.);
#31741=ADVANCED_FACE('',(#6581),#500,.T.);
#31742=ADVANCED_FACE('',(#6582),#501,.T.);
#31743=ADVANCED_FACE('',(#6583),#502,.T.);
#31744=ADVANCED_FACE('',(#6584),#503,.T.);
#31745=ADVANCED_FACE('',(#6585),#504,.T.);
#31746=ADVANCED_FACE('',(#6586),#505,.T.);
#31747=ADVANCED_FACE('',(#6587),#506,.T.);
#31748=ADVANCED_FACE('',(#6588),#507,.T.);
#31749=ADVANCED_FACE('',(#6589),#508,.T.);
#31750=ADVANCED_FACE('',(#6590),#509,.T.);
#31751=ADVANCED_FACE('',(#6591),#510,.T.);
#31752=ADVANCED_FACE('',(#6592),#511,.T.);
#31753=ADVANCED_FACE('',(#6593),#512,.T.);
#31754=ADVANCED_FACE('',(#6594),#513,.T.);
#31755=ADVANCED_FACE('',(#6595),#514,.T.);
#31756=ADVANCED_FACE('',(#6596),#515,.T.);
#31757=ADVANCED_FACE('',(#6597),#516,.T.);
#31758=ADVANCED_FACE('',(#6598),#517,.T.);
#31759=ADVANCED_FACE('',(#6599),#518,.T.);
#31760=ADVANCED_FACE('',(#6600),#519,.T.);
#31761=ADVANCED_FACE('',(#6601),#520,.T.);
#31762=ADVANCED_FACE('',(#6602),#521,.T.);
#31763=ADVANCED_FACE('',(#6603),#522,.T.);
#31764=ADVANCED_FACE('',(#6604),#523,.T.);
#31765=ADVANCED_FACE('',(#6605),#524,.T.);
#31766=ADVANCED_FACE('',(#6606),#525,.T.);
#31767=ADVANCED_FACE('',(#6607),#526,.T.);
#31768=ADVANCED_FACE('',(#6608),#527,.T.);
#31769=ADVANCED_FACE('',(#6609),#528,.T.);
#31770=ADVANCED_FACE('',(#6610),#529,.T.);
#31771=ADVANCED_FACE('',(#6611),#530,.T.);
#31772=ADVANCED_FACE('',(#6612),#531,.T.);
#31773=ADVANCED_FACE('',(#6613),#532,.T.);
#31774=ADVANCED_FACE('',(#6614),#533,.T.);
#31775=ADVANCED_FACE('',(#6615),#534,.T.);
#31776=ADVANCED_FACE('',(#6616),#535,.T.);
#31777=ADVANCED_FACE('',(#6617),#536,.T.);
#31778=ADVANCED_FACE('',(#6618),#537,.T.);
#31779=ADVANCED_FACE('',(#6619),#538,.T.);
#31780=ADVANCED_FACE('',(#6620),#30124,.T.);
#31781=ADVANCED_FACE('',(#6621,#3398),#30125,.T.);
#31782=ADVANCED_FACE('',(#6622),#539,.T.);
#31783=ADVANCED_FACE('',(#6623),#5068,.T.);
#31784=ADVANCED_FACE('',(#6624),#540,.T.);
#31785=ADVANCED_FACE('',(#6625,#3399),#30126,.T.);
#31786=ADVANCED_FACE('',(#6626),#30127,.T.);
#31787=ADVANCED_FACE('',(#6627),#30128,.F.);
#31788=ADVANCED_FACE('',(#6628),#30129,.F.);
#31789=ADVANCED_FACE('',(#6629),#30130,.F.);
#31790=ADVANCED_FACE('',(#6630),#30131,.F.);
#31791=ADVANCED_FACE('',(#6631),#30132,.F.);
#31792=ADVANCED_FACE('',(#6632),#30133,.F.);
#31793=ADVANCED_FACE('',(#6633),#47,.T.);
#31794=ADVANCED_FACE('',(#6634),#48,.T.);
#31795=ADVANCED_FACE('',(#6635),#2973,.T.);
#31796=ADVANCED_FACE('',(#6636),#30134,.F.);
#31797=ADVANCED_FACE('',(#6637),#5069,.F.);
#31798=ADVANCED_FACE('',(#6638),#30135,.F.);
#31799=ADVANCED_FACE('',(#6639),#30136,.F.);
#31800=ADVANCED_FACE('',(#6640),#5070,.F.);
#31801=ADVANCED_FACE('',(#6641),#30137,.F.);
#31802=ADVANCED_FACE('',(#6642),#30138,.F.);
#31803=ADVANCED_FACE('',(#6643),#5071,.F.);
#31804=ADVANCED_FACE('',(#6644),#30139,.F.);
#31805=ADVANCED_FACE('',(#6645),#30140,.F.);
#31806=ADVANCED_FACE('',(#6646),#5072,.F.);
#31807=ADVANCED_FACE('',(#6647),#30141,.F.);
#31808=ADVANCED_FACE('',(#6648),#30142,.F.);
#31809=ADVANCED_FACE('',(#6649),#5073,.F.);
#31810=ADVANCED_FACE('',(#6650),#30143,.F.);
#31811=ADVANCED_FACE('',(#6651),#30144,.F.);
#31812=ADVANCED_FACE('',(#6652),#5074,.F.);
#31813=ADVANCED_FACE('',(#6653),#30145,.F.);
#31814=ADVANCED_FACE('',(#6654),#30146,.F.);
#31815=ADVANCED_FACE('',(#6655),#5075,.F.);
#31816=ADVANCED_FACE('',(#6656),#30147,.F.);
#31817=ADVANCED_FACE('',(#6657),#30148,.F.);
#31818=ADVANCED_FACE('',(#6658),#30149,.F.);
#31819=ADVANCED_FACE('',(#6659),#30150,.F.);
#31820=ADVANCED_FACE('',(#6660),#30151,.F.);
#31821=ADVANCED_FACE('',(#6661),#30152,.F.);
#31822=ADVANCED_FACE('',(#6662),#30153,.F.);
#31823=ADVANCED_FACE('',(#6663),#30154,.F.);
#31824=ADVANCED_FACE('',(#6664),#30155,.F.);
#31825=ADVANCED_FACE('',(#6665),#30156,.F.);
#31826=ADVANCED_FACE('',(#6666),#30157,.F.);
#31827=ADVANCED_FACE('',(#6667),#30158,.F.);
#31828=ADVANCED_FACE('',(#6668),#30159,.F.);
#31829=ADVANCED_FACE('',(#6669),#30160,.F.);
#31830=ADVANCED_FACE('',(#6670),#30161,.F.);
#31831=ADVANCED_FACE('',(#6671),#30162,.F.);
#31832=ADVANCED_FACE('',(#6672),#30163,.F.);
#31833=ADVANCED_FACE('',(#6673),#30164,.F.);
#31834=ADVANCED_FACE('',(#6674),#30165,.F.);
#31835=ADVANCED_FACE('',(#6675),#30166,.F.);
#31836=ADVANCED_FACE('',(#6676),#5076,.F.);
#31837=ADVANCED_FACE('',(#6677),#30167,.F.);
#31838=ADVANCED_FACE('',(#6678),#30168,.F.);
#31839=ADVANCED_FACE('',(#6679),#5077,.F.);
#31840=ADVANCED_FACE('',(#6680),#30169,.F.);
#31841=ADVANCED_FACE('',(#6681),#30170,.F.);
#31842=ADVANCED_FACE('',(#6682),#5078,.F.);
#31843=ADVANCED_FACE('',(#6683),#30171,.F.);
#31844=ADVANCED_FACE('',(#6684),#30172,.F.);
#31845=ADVANCED_FACE('',(#6685),#5079,.F.);
#31846=ADVANCED_FACE('',(#6686),#30173,.F.);
#31847=ADVANCED_FACE('',(#6687),#30174,.F.);
#31848=ADVANCED_FACE('',(#6688),#5080,.F.);
#31849=ADVANCED_FACE('',(#6689),#30175,.F.);
#31850=ADVANCED_FACE('',(#6690),#30176,.F.);
#31851=ADVANCED_FACE('',(#6691),#5081,.F.);
#31852=ADVANCED_FACE('',(#6692),#30177,.F.);
#31853=ADVANCED_FACE('',(#6693),#30178,.F.);
#31854=ADVANCED_FACE('',(#6694),#5082,.F.);
#31855=ADVANCED_FACE('',(#6695),#30179,.F.);
#31856=ADVANCED_FACE('',(#6696),#30180,.F.);
#31857=ADVANCED_FACE('',(#6697),#5083,.F.);
#31858=ADVANCED_FACE('',(#6698),#30181,.F.);
#31859=ADVANCED_FACE('',(#6699),#30182,.F.);
#31860=ADVANCED_FACE('',(#6700),#5084,.F.);
#31861=ADVANCED_FACE('',(#6701),#30183,.F.);
#31862=ADVANCED_FACE('',(#6702),#30184,.F.);
#31863=ADVANCED_FACE('',(#6703),#5085,.F.);
#31864=ADVANCED_FACE('',(#6704),#30185,.F.);
#31865=ADVANCED_FACE('',(#6705),#30186,.F.);
#31866=ADVANCED_FACE('',(#6706),#5086,.F.);
#31867=ADVANCED_FACE('',(#6707),#30187,.F.);
#31868=ADVANCED_FACE('',(#6708),#30188,.F.);
#31869=ADVANCED_FACE('',(#6709),#5087,.F.);
#31870=ADVANCED_FACE('',(#6710),#30189,.F.);
#31871=ADVANCED_FACE('',(#6711),#30190,.F.);
#31872=ADVANCED_FACE('',(#6712),#5088,.F.);
#31873=ADVANCED_FACE('',(#6713),#30191,.F.);
#31874=ADVANCED_FACE('',(#6714),#30192,.F.);
#31875=ADVANCED_FACE('',(#6715),#5089,.F.);
#31876=ADVANCED_FACE('',(#6716),#30193,.F.);
#31877=ADVANCED_FACE('',(#6717),#30194,.F.);
#31878=ADVANCED_FACE('',(#6718),#5090,.F.);
#31879=ADVANCED_FACE('',(#6719),#30195,.F.);
#31880=ADVANCED_FACE('',(#6720),#30196,.F.);
#31881=ADVANCED_FACE('',(#6721),#5091,.F.);
#31882=ADVANCED_FACE('',(#6722),#30197,.F.);
#31883=ADVANCED_FACE('',(#6723),#30198,.F.);
#31884=ADVANCED_FACE('',(#6724),#5092,.F.);
#31885=ADVANCED_FACE('',(#6725),#30199,.F.);
#31886=ADVANCED_FACE('',(#6726),#30200,.F.);
#31887=ADVANCED_FACE('',(#6727),#5093,.F.);
#31888=ADVANCED_FACE('',(#6728),#30201,.F.);
#31889=ADVANCED_FACE('',(#6729),#30202,.F.);
#31890=ADVANCED_FACE('',(#6730),#5094,.F.);
#31891=ADVANCED_FACE('',(#6731),#30203,.F.);
#31892=ADVANCED_FACE('',(#6732),#30204,.F.);
#31893=ADVANCED_FACE('',(#6733),#5095,.F.);
#31894=ADVANCED_FACE('',(#6734),#30205,.F.);
#31895=ADVANCED_FACE('',(#6735),#30206,.F.);
#31896=ADVANCED_FACE('',(#6736),#5096,.F.);
#31897=ADVANCED_FACE('',(#6737),#30207,.F.);
#31898=ADVANCED_FACE('',(#6738),#30208,.F.);
#31899=ADVANCED_FACE('',(#6739),#5097,.F.);
#31900=ADVANCED_FACE('',(#6740),#30209,.F.);
#31901=ADVANCED_FACE('',(#6741),#30210,.F.);
#31902=ADVANCED_FACE('',(#6742),#5098,.F.);
#31903=ADVANCED_FACE('',(#6743),#30211,.F.);
#31904=ADVANCED_FACE('',(#6744),#30212,.F.);
#31905=ADVANCED_FACE('',(#6745),#5099,.F.);
#31906=ADVANCED_FACE('',(#6746),#30213,.F.);
#31907=ADVANCED_FACE('',(#6747),#30214,.F.);
#31908=ADVANCED_FACE('',(#6748),#5100,.F.);
#31909=ADVANCED_FACE('',(#6749),#30215,.F.);
#31910=ADVANCED_FACE('',(#6750),#30216,.F.);
#31911=ADVANCED_FACE('',(#6751),#5101,.F.);
#31912=ADVANCED_FACE('',(#6752),#30217,.F.);
#31913=ADVANCED_FACE('',(#6753),#30218,.F.);
#31914=ADVANCED_FACE('',(#6754),#5102,.F.);
#31915=ADVANCED_FACE('',(#6755),#30219,.F.);
#31916=ADVANCED_FACE('',(#6756),#30220,.F.);
#31917=ADVANCED_FACE('',(#6757),#5103,.F.);
#31918=ADVANCED_FACE('',(#6758),#30221,.F.);
#31919=ADVANCED_FACE('',(#6759),#30222,.F.);
#31920=ADVANCED_FACE('',(#6760),#5104,.F.);
#31921=ADVANCED_FACE('',(#6761),#30223,.F.);
#31922=ADVANCED_FACE('',(#6762),#30224,.F.);
#31923=ADVANCED_FACE('',(#6763),#5105,.F.);
#31924=ADVANCED_FACE('',(#6764),#30225,.F.);
#31925=ADVANCED_FACE('',(#6765),#30226,.F.);
#31926=ADVANCED_FACE('',(#6766),#5106,.F.);
#31927=ADVANCED_FACE('',(#6767),#30227,.F.);
#31928=ADVANCED_FACE('',(#6768),#30228,.F.);
#31929=ADVANCED_FACE('',(#6769),#5107,.F.);
#31930=ADVANCED_FACE('',(#6770),#30229,.F.);
#31931=ADVANCED_FACE('',(#6771),#30230,.F.);
#31932=ADVANCED_FACE('',(#6772),#5108,.F.);
#31933=ADVANCED_FACE('',(#6773),#30231,.F.);
#31934=ADVANCED_FACE('',(#6774),#30232,.F.);
#31935=ADVANCED_FACE('',(#6775),#5109,.F.);
#31936=ADVANCED_FACE('',(#6776),#30233,.F.);
#31937=ADVANCED_FACE('',(#6777),#30234,.F.);
#31938=ADVANCED_FACE('',(#6778),#5110,.F.);
#31939=ADVANCED_FACE('',(#6779),#30235,.F.);
#31940=ADVANCED_FACE('',(#6780),#30236,.F.);
#31941=ADVANCED_FACE('',(#6781),#5111,.F.);
#31942=ADVANCED_FACE('',(#6782),#30237,.F.);
#31943=ADVANCED_FACE('',(#6783),#30238,.F.);
#31944=ADVANCED_FACE('',(#6784),#5112,.F.);
#31945=ADVANCED_FACE('',(#6785),#30239,.F.);
#31946=ADVANCED_FACE('',(#6786),#30240,.F.);
#31947=ADVANCED_FACE('',(#6787),#5113,.F.);
#31948=ADVANCED_FACE('',(#6788),#30241,.F.);
#31949=ADVANCED_FACE('',(#6789),#30242,.F.);
#31950=ADVANCED_FACE('',(#6790),#5114,.F.);
#31951=ADVANCED_FACE('',(#6791),#30243,.F.);
#31952=ADVANCED_FACE('',(#6792),#30244,.F.);
#31953=ADVANCED_FACE('',(#6793),#5115,.F.);
#31954=ADVANCED_FACE('',(#6794),#30245,.F.);
#31955=ADVANCED_FACE('',(#6795),#30246,.F.);
#31956=ADVANCED_FACE('',(#6796),#5116,.F.);
#31957=ADVANCED_FACE('',(#6797),#30247,.F.);
#31958=ADVANCED_FACE('',(#6798),#30248,.F.);
#31959=ADVANCED_FACE('',(#6799),#5117,.F.);
#31960=ADVANCED_FACE('',(#6800),#30249,.F.);
#31961=ADVANCED_FACE('',(#6801),#30250,.F.);
#31962=ADVANCED_FACE('',(#6802),#5118,.F.);
#31963=ADVANCED_FACE('',(#6803),#30251,.F.);
#31964=ADVANCED_FACE('',(#6804),#30252,.F.);
#31965=ADVANCED_FACE('',(#6805),#5119,.F.);
#31966=ADVANCED_FACE('',(#6806),#30253,.F.);
#31967=ADVANCED_FACE('',(#6807),#30254,.F.);
#31968=ADVANCED_FACE('',(#6808),#5120,.F.);
#31969=ADVANCED_FACE('',(#6809),#30255,.F.);
#31970=ADVANCED_FACE('',(#6810),#30256,.F.);
#31971=ADVANCED_FACE('',(#6811),#5121,.F.);
#31972=ADVANCED_FACE('',(#6812),#30257,.F.);
#31973=ADVANCED_FACE('',(#6813),#30258,.F.);
#31974=ADVANCED_FACE('',(#6814),#5122,.F.);
#31975=ADVANCED_FACE('',(#6815),#30259,.F.);
#31976=ADVANCED_FACE('',(#6816),#30260,.F.);
#31977=ADVANCED_FACE('',(#6817),#5123,.F.);
#31978=ADVANCED_FACE('',(#6818),#30261,.F.);
#31979=ADVANCED_FACE('',(#6819),#30262,.F.);
#31980=ADVANCED_FACE('',(#6820),#5124,.F.);
#31981=ADVANCED_FACE('',(#6821),#30263,.F.);
#31982=ADVANCED_FACE('',(#6822),#30264,.F.);
#31983=ADVANCED_FACE('',(#6823),#5125,.F.);
#31984=ADVANCED_FACE('',(#6824),#30265,.F.);
#31985=ADVANCED_FACE('',(#6825),#30266,.F.);
#31986=ADVANCED_FACE('',(#6826),#5126,.F.);
#31987=ADVANCED_FACE('',(#6827),#30267,.F.);
#31988=ADVANCED_FACE('',(#6828),#30268,.F.);
#31989=ADVANCED_FACE('',(#6829),#5127,.F.);
#31990=ADVANCED_FACE('',(#6830),#30269,.F.);
#31991=ADVANCED_FACE('',(#6831),#30270,.F.);
#31992=ADVANCED_FACE('',(#6832),#5128,.F.);
#31993=ADVANCED_FACE('',(#6833),#30271,.F.);
#31994=ADVANCED_FACE('',(#6834),#30272,.F.);
#31995=ADVANCED_FACE('',(#6835),#5129,.F.);
#31996=ADVANCED_FACE('',(#6836),#30273,.F.);
#31997=ADVANCED_FACE('',(#6837),#30274,.F.);
#31998=ADVANCED_FACE('',(#6838),#5130,.F.);
#31999=ADVANCED_FACE('',(#6839),#30275,.F.);
#32000=ADVANCED_FACE('',(#6840),#30276,.F.);
#32001=ADVANCED_FACE('',(#6841),#5131,.F.);
#32002=ADVANCED_FACE('',(#6842),#30277,.F.);
#32003=ADVANCED_FACE('',(#6843),#30278,.F.);
#32004=ADVANCED_FACE('',(#6844),#5132,.F.);
#32005=ADVANCED_FACE('',(#6845),#30279,.F.);
#32006=ADVANCED_FACE('',(#6846),#30280,.F.);
#32007=ADVANCED_FACE('',(#6847),#5133,.F.);
#32008=ADVANCED_FACE('',(#6848),#30281,.F.);
#32009=ADVANCED_FACE('',(#6849),#30282,.F.);
#32010=ADVANCED_FACE('',(#6850),#30283,.F.);
#32011=ADVANCED_FACE('',(#6851),#30284,.F.);
#32012=ADVANCED_FACE('',(#6852),#30285,.F.);
#32013=ADVANCED_FACE('',(#6853),#30286,.F.);
#32014=ADVANCED_FACE('',(#6854),#30287,.F.);
#32015=ADVANCED_FACE('',(#6855),#30288,.F.);
#32016=ADVANCED_FACE('',(#6856),#30289,.F.);
#32017=ADVANCED_FACE('',(#6857),#30290,.F.);
#32018=ADVANCED_FACE('',(#6858),#30291,.F.);
#32019=ADVANCED_FACE('',(#6859),#30292,.F.);
#32020=ADVANCED_FACE('',(#6860),#30293,.F.);
#32028=CLOSED_SHELL('',(#31458,#31459,#31460,#31461,#31462,#31463,#31464,
#31465,#31466,#31467,#31468,#31469,#31470,#31471,#31472,#31473,#31474,#31475,
#31476,#31477,#31478,#31479,#31480,#31481,#31482,#31483,#31484,#31485,#31486,
#31487,#31488,#31489,#31490,#31491,#31492,#31493,#31494,#31495,#31496,#31497,
#31498,#31499,#31500,#31501,#31502,#31503,#31504,#31505,#31506,#31507,#31508,
#31509,#31510,#31511,#31512,#31513,#31514,#31515,#31516,#31517,#31518,#31519,
#31520,#31521,#31522,#31523,#31524,#31525,#31526,#31527,#31528,#31529,#31530,
#31531,#31532,#31533,#31534,#31535,#31536,#31537,#31538,#31539,#31540,#31541,
#31542,#31543,#31544,#31545,#31546,#31547,#31548,#31549,#31550,#31551,#31552,
#31553,#31554,#31555,#31556,#31557,#31558,#31559,#31560,#31561,#31562,#31563,
#31564,#31565,#31566,#31567,#31568,#31569,#31570,#31571,#31572,#31573,#31574,
#31575,#31576,#31577,#31578,#31579,#31580,#31581,#31582,#31583,#31584,#31585,
#31586,#31587,#31588,#31589,#31590,#31591,#31592,#31593,#31594,#31595,#31596,
#31597,#31598,#31599,#31600,#31601,#31602,#31603,#31604,#31605,#31606,#31607,
#31608,#31609,#31610,#31611,#31612,#31613,#31614,#31615,#31616,#31617,#31618,
#31619,#31620,#31621,#31622,#31623,#31624,#31625,#31626,#31627,#31628,#31629,
#31630,#31631,#31632,#31633,#31634,#31635,#31636,#31637,#31638,#31639,#31640,
#31641,#31642,#31643,#31644,#31645,#31646,#31647,#31648,#31649,#31650,#31651,
#31652,#31653,#31654,#31655,#31656,#31657,#31658,#31659,#31660,#31661,#31662,
#31663,#31664,#31665,#31666,#31667,#31668,#31669,#31670,#31671,#31672,#31673,
#31674,#31675,#31676,#31677,#31678,#31679,#31680,#31681,#31682,#31683,#31684,
#31685,#31686,#31687,#31688,#31689,#31690,#31691,#31692,#31693,#31694,#31695,
#31696,#31697,#31698,#31699,#31700,#31701,#31702,#31703,#31704,#31705,#31706,
#31707,#31708,#31709,#31710,#31711,#31712,#31713,#31714,#31715,#31716,#31717,
#31718,#31719,#31720,#31721,#31722,#31723,#31724,#31725,#31726,#31727,#31728,
#31729,#31730,#31731,#31732,#31733,#31734,#31735,#31736,#31737,#31738,#31739,
#31740,#31741,#31742,#31743,#31744,#31745,#31746,#31747,#31748,#31749,#31750,
#31751,#31752,#31753,#31754,#31755,#31756,#31757,#31758,#31759,#31760,#31761,
#31762,#31763,#31764,#31765,#31766,#31767,#31768,#31769,#31770,#31771,#31772,
#31773,#31774,#31775,#31776,#31777,#31778,#31779,#31780,#31781,#31782,#31783,
#31784,#31785,#31786,#31787,#31788,#31789,#31790,#31791,#31792,#31793,#31794,
#31795,#31796,#31797,#31798,#31799,#31800,#31801,#31802,#31803,#31804,#31805,
#31806,#31807,#31808,#31809,#31810,#31811,#31812,#31813,#31814,#31815,#31816,
#31817,#31818,#31819,#31820,#31821,#31822,#31823,#31824,#31825,#31826,#31827,
#31828,#31829,#31830,#31831,#31832,#31833,#31834,#31835,#31836,#31837,#31838,
#31839,#31840,#31841,#31842,#31843,#31844,#31845,#31846,#31847,#31848,#31849,
#31850,#31851,#31852,#31853,#31854,#31855,#31856,#31857,#31858,#31859,#31860,
#31861,#31862,#31863,#31864,#31865,#31866,#31867,#31868,#31869,#31870,#31871,
#31872,#31873,#31874,#31875,#31876,#31877,#31878,#31879,#31880,#31881,#31882,
#31883,#31884,#31885,#31886,#31887,#31888,#31889,#31890,#31891,#31892,#31893,
#31894,#31895,#31896,#31897,#31898,#31899,#31900,#31901,#31902,#31903,#31904,
#31905,#31906,#31907,#31908,#31909,#31910,#31911,#31912,#31913,#31914,#31915,
#31916,#31917,#31918,#31919,#31920,#31921,#31922,#31923,#31924,#31925,#31926,
#31927,#31928,#31929,#31930,#31931,#31932,#31933,#31934,#31935,#31936,#31937,
#31938,#31939,#31940,#31941,#31942,#31943,#31944,#31945,#31946,#31947,#31948,
#31949,#31950,#31951,#31952,#31953,#31954,#31955,#31956,#31957,#31958,#31959,
#31960,#31961,#31962,#31963,#31964,#31965,#31966,#31967,#31968,#31969,#31970,
#31971,#31972,#31973,#31974,#31975,#31976,#31977,#31978,#31979,#31980,#31981,
#31982,#31983,#31984,#31985,#31986,#31987,#31988,#31989,#31990,#31991,#31992,
#31993,#31994,#31995,#31996,#31997,#31998,#31999,#32000,#32001,#32002,#32003,
#32004,#32005,#32006,#32007,#32008,#32009,#32010,#32011,#32012,#32013,#32014,
#32015,#32016,#32017,#32018,#32019,#32020));
#34957=AXIS2_PLACEMENT_3D('',#65620,#42872,#42873);
#34958=AXIS2_PLACEMENT_3D('',#65621,#42874,#42875);
#34959=AXIS2_PLACEMENT_3D('',#65664,#42878,#42879);
#34960=AXIS2_PLACEMENT_3D('',#65666,#42880,#42881);
#34961=AXIS2_PLACEMENT_3D('',#65701,#42882,#42883);
#34962=AXIS2_PLACEMENT_3D('',#65777,#42885,#42886);
#34963=AXIS2_PLACEMENT_3D('',#65855,#42888,#42889);
#34964=AXIS2_PLACEMENT_3D('',#65931,#42891,#42892);
#34965=AXIS2_PLACEMENT_3D('',#66007,#42894,#42895);
#34966=AXIS2_PLACEMENT_3D('',#66083,#42897,#42898);
#34967=AXIS2_PLACEMENT_3D('',#66159,#42900,#42901);
#34968=AXIS2_PLACEMENT_3D('',#66237,#42903,#42904);
#34969=AXIS2_PLACEMENT_3D('',#66315,#42906,#42907);
#34970=AXIS2_PLACEMENT_3D('',#66391,#42909,#42910);
#34971=AXIS2_PLACEMENT_3D('',#66467,#42912,#42913);
#34972=AXIS2_PLACEMENT_3D('',#66543,#42915,#42916);
#34973=AXIS2_PLACEMENT_3D('',#66619,#42918,#42919);
#34974=AXIS2_PLACEMENT_3D('',#66697,#42921,#42922);
#34975=AXIS2_PLACEMENT_3D('',#66773,#42924,#42925);
#34976=AXIS2_PLACEMENT_3D('',#66851,#42927,#42928);
#34977=AXIS2_PLACEMENT_3D('',#66927,#42930,#42931);
#34978=AXIS2_PLACEMENT_3D('',#67003,#42933,#42934);
#34979=AXIS2_PLACEMENT_3D('',#67079,#42936,#42937);
#34980=AXIS2_PLACEMENT_3D('',#67155,#42939,#42940);
#34981=AXIS2_PLACEMENT_3D('',#67233,#42942,#42943);
#34982=AXIS2_PLACEMENT_3D('',#67311,#42945,#42946);
#34983=AXIS2_PLACEMENT_3D('',#67387,#42948,#42949);
#34984=AXIS2_PLACEMENT_3D('',#67463,#42951,#42952);
#34985=AXIS2_PLACEMENT_3D('',#67539,#42954,#42955);
#34986=AXIS2_PLACEMENT_3D('',#67615,#42957,#42958);
#34987=AXIS2_PLACEMENT_3D('',#67693,#42960,#42961);
#34988=AXIS2_PLACEMENT_3D('',#67769,#42963,#42964);
#34989=AXIS2_PLACEMENT_3D('',#67794,#42966,#42967);
#34990=AXIS2_PLACEMENT_3D('',#67795,#42968,#42969);
#34991=AXIS2_PLACEMENT_3D('',#67807,#42971,#42972);
#34992=AXIS2_PLACEMENT_3D('',#67808,#42973,#42974);
#34993=AXIS2_PLACEMENT_3D('',#67884,#42976,#42977);
#34994=AXIS2_PLACEMENT_3D('',#67960,#42979,#42980);
#34995=AXIS2_PLACEMENT_3D('',#68038,#42982,#42983);
#34996=AXIS2_PLACEMENT_3D('',#68114,#42985,#42986);
#34997=AXIS2_PLACEMENT_3D('',#68192,#42988,#42989);
#34998=AXIS2_PLACEMENT_3D('',#68268,#42991,#42992);
#34999=AXIS2_PLACEMENT_3D('',#68344,#42994,#42995);
#35000=AXIS2_PLACEMENT_3D('',#68420,#42997,#42998);
#35001=AXIS2_PLACEMENT_3D('',#68496,#43000,#43001);
#35002=AXIS2_PLACEMENT_3D('',#68574,#43003,#43004);
#35003=AXIS2_PLACEMENT_3D('',#68650,#43006,#43007);
#35004=AXIS2_PLACEMENT_3D('',#68728,#43009,#43010);
#35005=AXIS2_PLACEMENT_3D('',#68804,#43012,#43013);
#35006=AXIS2_PLACEMENT_3D('',#68880,#43015,#43016);
#35007=AXIS2_PLACEMENT_3D('',#68956,#43018,#43019);
#35008=AXIS2_PLACEMENT_3D('',#69032,#43021,#43022);
#35009=AXIS2_PLACEMENT_3D('',#69108,#43024,#43025);
#35010=AXIS2_PLACEMENT_3D('',#69186,#43027,#43028);
#35011=AXIS2_PLACEMENT_3D('',#69262,#43030,#43031);
#35012=AXIS2_PLACEMENT_3D('',#69340,#43033,#43034);
#35013=AXIS2_PLACEMENT_3D('',#69416,#43036,#43037);
#35014=AXIS2_PLACEMENT_3D('',#69492,#43039,#43040);
#35015=AXIS2_PLACEMENT_3D('',#69568,#43042,#43043);
#35016=AXIS2_PLACEMENT_3D('',#69644,#43045,#43046);
#35017=AXIS2_PLACEMENT_3D('',#69722,#43048,#43049);
#35018=AXIS2_PLACEMENT_3D('',#69798,#43051,#43052);
#35019=AXIS2_PLACEMENT_3D('',#69876,#43054,#43055);
#35020=AXIS2_PLACEMENT_3D('',#69952,#43057,#43058);
#35021=AXIS2_PLACEMENT_3D('',#70028,#43060,#43061);
#35022=AXIS2_PLACEMENT_3D('',#70038,#43062,#43063);
#35023=AXIS2_PLACEMENT_3D('',#70039,#43064,#43065);
#35024=AXIS2_PLACEMENT_3D('',#70040,#43066,#43067);
#35025=AXIS2_PLACEMENT_3D('',#70055,#43068,#43069);
#35026=AXIS2_PLACEMENT_3D('',#70078,#43070,#43071);
#35027=AXIS2_PLACEMENT_3D('',#70145,#43072,#43073);
#35028=AXIS2_PLACEMENT_3D('',#70148,#43074,#43075);
#35029=AXIS2_PLACEMENT_3D('',#70152,#43077,#43078);
#35030=AXIS2_PLACEMENT_3D('',#70154,#43080,#43081);
#35031=AXIS2_PLACEMENT_3D('',#70157,#43082,#43083);
#35032=AXIS2_PLACEMENT_3D('',#70161,#43085,#43086);
#35033=AXIS2_PLACEMENT_3D('',#70163,#43088,#43089);
#35034=AXIS2_PLACEMENT_3D('',#70166,#43090,#43091);
#35035=AXIS2_PLACEMENT_3D('',#70170,#43093,#43094);
#35036=AXIS2_PLACEMENT_3D('',#70172,#43096,#43097);
#35037=AXIS2_PLACEMENT_3D('',#70175,#43098,#43099);
#35038=AXIS2_PLACEMENT_3D('',#70179,#43101,#43102);
#35039=AXIS2_PLACEMENT_3D('',#70181,#43104,#43105);
#35040=AXIS2_PLACEMENT_3D('',#70184,#43106,#43107);
#35041=AXIS2_PLACEMENT_3D('',#70188,#43109,#43110);
#35042=AXIS2_PLACEMENT_3D('',#70190,#43112,#43113);
#35043=AXIS2_PLACEMENT_3D('',#70193,#43114,#43115);
#35044=AXIS2_PLACEMENT_3D('',#70197,#43117,#43118);
#35045=AXIS2_PLACEMENT_3D('',#70199,#43120,#43121);
#35046=AXIS2_PLACEMENT_3D('',#70202,#43122,#43123);
#35047=AXIS2_PLACEMENT_3D('',#70206,#43125,#43126);
#35048=AXIS2_PLACEMENT_3D('',#70208,#43128,#43129);
#35049=AXIS2_PLACEMENT_3D('',#70211,#43130,#43131);
#35050=AXIS2_PLACEMENT_3D('',#70215,#43133,#43134);
#35051=AXIS2_PLACEMENT_3D('',#70217,#43136,#43137);
#35052=AXIS2_PLACEMENT_3D('',#70220,#43138,#43139);
#35053=AXIS2_PLACEMENT_3D('',#70224,#43141,#43142);
#35054=AXIS2_PLACEMENT_3D('',#70226,#43144,#43145);
#35055=AXIS2_PLACEMENT_3D('',#70229,#43146,#43147);
#35056=AXIS2_PLACEMENT_3D('',#70233,#43149,#43150);
#35057=AXIS2_PLACEMENT_3D('',#70235,#43152,#43153);
#35058=AXIS2_PLACEMENT_3D('',#70238,#43154,#43155);
#35059=AXIS2_PLACEMENT_3D('',#70242,#43157,#43158);
#35060=AXIS2_PLACEMENT_3D('',#70244,#43160,#43161);
#35061=AXIS2_PLACEMENT_3D('',#70247,#43162,#43163);
#35062=AXIS2_PLACEMENT_3D('',#70251,#43165,#43166);
#35063=AXIS2_PLACEMENT_3D('',#70253,#43168,#43169);
#35064=AXIS2_PLACEMENT_3D('',#70256,#43170,#43171);
#35065=AXIS2_PLACEMENT_3D('',#70260,#43173,#43174);
#35066=AXIS2_PLACEMENT_3D('',#70262,#43176,#43177);
#35067=AXIS2_PLACEMENT_3D('',#70265,#43178,#43179);
#35068=AXIS2_PLACEMENT_3D('',#70269,#43181,#43182);
#35069=AXIS2_PLACEMENT_3D('',#70271,#43184,#43185);
#35070=AXIS2_PLACEMENT_3D('',#70274,#43186,#43187);
#35071=AXIS2_PLACEMENT_3D('',#70278,#43189,#43190);
#35072=AXIS2_PLACEMENT_3D('',#70280,#43192,#43193);
#35073=AXIS2_PLACEMENT_3D('',#70311,#43195,#43196);
#35074=AXIS2_PLACEMENT_3D('',#70312,#43197,#43198);
#35075=AXIS2_PLACEMENT_3D('',#70314,#43199,#43200);
#35076=AXIS2_PLACEMENT_3D('',#70316,#43201,#43202);
#35077=AXIS2_PLACEMENT_3D('',#70317,#43203,#43204);
#35078=AXIS2_PLACEMENT_3D('',#70318,#43205,#43206);
#35079=AXIS2_PLACEMENT_3D('',#70334,#43207,#43208);
#35080=AXIS2_PLACEMENT_3D('',#70340,#43209,#43210);
#35081=AXIS2_PLACEMENT_3D('',#70346,#43211,#43212);
#35082=AXIS2_PLACEMENT_3D('',#70352,#43213,#43214);
#35083=AXIS2_PLACEMENT_3D('',#70358,#43215,#43216);
#35084=AXIS2_PLACEMENT_3D('',#70364,#43217,#43218);
#35085=AXIS2_PLACEMENT_3D('',#70370,#43219,#43220);
#35086=AXIS2_PLACEMENT_3D('',#70376,#43221,#43222);
#35087=AXIS2_PLACEMENT_3D('',#70382,#43223,#43224);
#35088=AXIS2_PLACEMENT_3D('',#70388,#43225,#43226);
#35089=AXIS2_PLACEMENT_3D('',#70394,#43227,#43228);
#35090=AXIS2_PLACEMENT_3D('',#70400,#43229,#43230);
#35091=AXIS2_PLACEMENT_3D('',#70406,#43231,#43232);
#35092=AXIS2_PLACEMENT_3D('',#70412,#43233,#43234);
#35093=AXIS2_PLACEMENT_3D('',#70418,#43235,#43236);
#35094=AXIS2_PLACEMENT_3D('',#70424,#43237,#43238);
#35095=AXIS2_PLACEMENT_3D('',#70430,#43239,#43240);
#35096=AXIS2_PLACEMENT_3D('',#70436,#43241,#43242);
#35097=AXIS2_PLACEMENT_3D('',#70442,#43243,#43244);
#35098=AXIS2_PLACEMENT_3D('',#70448,#43245,#43246);
#35099=AXIS2_PLACEMENT_3D('',#70454,#43247,#43248);
#35100=AXIS2_PLACEMENT_3D('',#70460,#43249,#43250);
#35101=AXIS2_PLACEMENT_3D('',#70466,#43251,#43252);
#35102=AXIS2_PLACEMENT_3D('',#70472,#43253,#43254);
#35103=AXIS2_PLACEMENT_3D('',#70478,#43255,#43256);
#35104=AXIS2_PLACEMENT_3D('',#70484,#43257,#43258);
#35105=AXIS2_PLACEMENT_3D('',#70490,#43259,#43260);
#35106=AXIS2_PLACEMENT_3D('',#70496,#43261,#43262);
#35107=AXIS2_PLACEMENT_3D('',#70502,#43263,#43264);
#35108=AXIS2_PLACEMENT_3D('',#70508,#43265,#43266);
#35109=AXIS2_PLACEMENT_3D('',#70514,#43267,#43268);
#35110=AXIS2_PLACEMENT_3D('',#70520,#43269,#43270);
#35111=AXIS2_PLACEMENT_3D('',#70526,#43271,#43272);
#35112=AXIS2_PLACEMENT_3D('',#70532,#43273,#43274);
#35113=AXIS2_PLACEMENT_3D('',#70538,#43275,#43276);
#35114=AXIS2_PLACEMENT_3D('',#70544,#43277,#43278);
#35115=AXIS2_PLACEMENT_3D('',#70550,#43279,#43280);
#35116=AXIS2_PLACEMENT_3D('',#70556,#43281,#43282);
#35117=AXIS2_PLACEMENT_3D('',#70562,#43283,#43284);
#35118=AXIS2_PLACEMENT_3D('',#70568,#43285,#43286);
#35119=AXIS2_PLACEMENT_3D('',#70574,#43287,#43288);
#35120=AXIS2_PLACEMENT_3D('',#70580,#43289,#43290);
#35121=AXIS2_PLACEMENT_3D('',#70586,#43291,#43292);
#35122=AXIS2_PLACEMENT_3D('',#70592,#43293,#43294);
#35123=AXIS2_PLACEMENT_3D('',#70598,#43295,#43296);
#35124=AXIS2_PLACEMENT_3D('',#70604,#43297,#43298);
#35125=AXIS2_PLACEMENT_3D('',#70610,#43299,#43300);
#35126=AXIS2_PLACEMENT_3D('',#70616,#43301,#43302);
#35127=AXIS2_PLACEMENT_3D('',#70622,#43303,#43304);
#35128=AXIS2_PLACEMENT_3D('',#70628,#43305,#43306);
#35129=AXIS2_PLACEMENT_3D('',#70634,#43307,#43308);
#35130=AXIS2_PLACEMENT_3D('',#70640,#43309,#43310);
#35131=AXIS2_PLACEMENT_3D('',#70646,#43311,#43312);
#35132=AXIS2_PLACEMENT_3D('',#70652,#43313,#43314);
#35133=AXIS2_PLACEMENT_3D('',#70658,#43315,#43316);
#35134=AXIS2_PLACEMENT_3D('',#70664,#43317,#43318);
#35135=AXIS2_PLACEMENT_3D('',#70670,#43319,#43320);
#35136=AXIS2_PLACEMENT_3D('',#70676,#43321,#43322);
#35137=AXIS2_PLACEMENT_3D('',#70682,#43323,#43324);
#35138=AXIS2_PLACEMENT_3D('',#70688,#43325,#43326);
#35139=AXIS2_PLACEMENT_3D('',#70694,#43327,#43328);
#35140=AXIS2_PLACEMENT_3D('',#70700,#43329,#43330);
#35141=AXIS2_PLACEMENT_3D('',#70706,#43331,#43332);
#35142=AXIS2_PLACEMENT_3D('',#70712,#43333,#43334);
#35143=AXIS2_PLACEMENT_3D('',#70718,#43335,#43336);
#35144=AXIS2_PLACEMENT_3D('',#70724,#43337,#43338);
#35145=AXIS2_PLACEMENT_3D('',#70730,#43339,#43340);
#35146=AXIS2_PLACEMENT_3D('',#70736,#43341,#43342);
#35147=AXIS2_PLACEMENT_3D('',#70742,#43343,#43344);
#35148=AXIS2_PLACEMENT_3D('',#70748,#43345,#43346);
#35149=AXIS2_PLACEMENT_3D('',#70754,#43347,#43348);
#35150=AXIS2_PLACEMENT_3D('',#70760,#43349,#43350);
#35151=AXIS2_PLACEMENT_3D('',#70766,#43351,#43352);
#35152=AXIS2_PLACEMENT_3D('',#70772,#43353,#43354);
#35153=AXIS2_PLACEMENT_3D('',#70778,#43355,#43356);
#35154=AXIS2_PLACEMENT_3D('',#70784,#43357,#43358);
#35155=AXIS2_PLACEMENT_3D('',#70790,#43359,#43360);
#35156=AXIS2_PLACEMENT_3D('',#70796,#43361,#43362);
#35157=AXIS2_PLACEMENT_3D('',#70802,#43363,#43364);
#35158=AXIS2_PLACEMENT_3D('',#70808,#43365,#43366);
#35159=AXIS2_PLACEMENT_3D('',#70814,#43367,#43368);
#35160=AXIS2_PLACEMENT_3D('',#70820,#43369,#43370);
#35161=AXIS2_PLACEMENT_3D('',#70826,#43371,#43372);
#35162=AXIS2_PLACEMENT_3D('',#70832,#43373,#43374);
#35163=AXIS2_PLACEMENT_3D('',#70838,#43375,#43376);
#35164=AXIS2_PLACEMENT_3D('',#70844,#43377,#43378);
#35165=AXIS2_PLACEMENT_3D('',#70850,#43379,#43380);
#35166=AXIS2_PLACEMENT_3D('',#70856,#43381,#43382);
#35167=AXIS2_PLACEMENT_3D('',#70862,#43383,#43384);
#35168=AXIS2_PLACEMENT_3D('',#70868,#43385,#43386);
#35169=AXIS2_PLACEMENT_3D('',#70874,#43387,#43388);
#35170=AXIS2_PLACEMENT_3D('',#70883,#43389,#43390);
#35171=AXIS2_PLACEMENT_3D('',#70892,#43391,#43392);
#35172=AXIS2_PLACEMENT_3D('',#70901,#43393,#43394);
#35173=AXIS2_PLACEMENT_3D('',#70910,#43395,#43396);
#35174=AXIS2_PLACEMENT_3D('',#70919,#43397,#43398);
#35175=AXIS2_PLACEMENT_3D('',#70928,#43399,#43400);
#35176=AXIS2_PLACEMENT_3D('',#70937,#43401,#43402);
#35177=AXIS2_PLACEMENT_3D('',#70946,#43403,#43404);
#35178=AXIS2_PLACEMENT_3D('',#70955,#43405,#43406);
#35179=AXIS2_PLACEMENT_3D('',#70964,#43407,#43408);
#35180=AXIS2_PLACEMENT_3D('',#70973,#43409,#43410);
#35181=AXIS2_PLACEMENT_3D('',#70982,#43411,#43412);
#35182=AXIS2_PLACEMENT_3D('',#70991,#43413,#43414);
#35183=AXIS2_PLACEMENT_3D('',#71000,#43415,#43416);
#35184=AXIS2_PLACEMENT_3D('',#71009,#43417,#43418);
#35185=AXIS2_PLACEMENT_3D('',#71015,#43419,#43420);
#35186=AXIS2_PLACEMENT_3D('',#71021,#43421,#43422);
#35187=AXIS2_PLACEMENT_3D('',#71027,#43423,#43424);
#35188=AXIS2_PLACEMENT_3D('',#71033,#43425,#43426);
#35189=AXIS2_PLACEMENT_3D('',#71039,#43427,#43428);
#35190=AXIS2_PLACEMENT_3D('',#71045,#43429,#43430);
#35191=AXIS2_PLACEMENT_3D('',#71051,#43431,#43432);
#35192=AXIS2_PLACEMENT_3D('',#71057,#43433,#43434);
#35193=AXIS2_PLACEMENT_3D('',#71063,#43435,#43436);
#35194=AXIS2_PLACEMENT_3D('',#71069,#43437,#43438);
#35195=AXIS2_PLACEMENT_3D('',#71075,#43439,#43440);
#35196=AXIS2_PLACEMENT_3D('',#71081,#43441,#43442);
#35197=AXIS2_PLACEMENT_3D('',#71087,#43443,#43444);
#35198=AXIS2_PLACEMENT_3D('',#71093,#43445,#43446);
#35199=AXIS2_PLACEMENT_3D('',#71099,#43447,#43448);
#35200=AXIS2_PLACEMENT_3D('',#71105,#43449,#43450);
#35201=AXIS2_PLACEMENT_3D('',#71111,#43451,#43452);
#35202=AXIS2_PLACEMENT_3D('',#71117,#43453,#43454);
#35203=AXIS2_PLACEMENT_3D('',#71123,#43455,#43456);
#35204=AXIS2_PLACEMENT_3D('',#71129,#43457,#43458);
#35205=AXIS2_PLACEMENT_3D('',#71135,#43459,#43460);
#35206=AXIS2_PLACEMENT_3D('',#71141,#43461,#43462);
#35207=AXIS2_PLACEMENT_3D('',#71147,#43463,#43464);
#35208=AXIS2_PLACEMENT_3D('',#71153,#43465,#43466);
#35209=AXIS2_PLACEMENT_3D('',#71159,#43467,#43468);
#35210=AXIS2_PLACEMENT_3D('',#71165,#43469,#43470);
#35211=AXIS2_PLACEMENT_3D('',#71171,#43471,#43472);
#35212=AXIS2_PLACEMENT_3D('',#71177,#43473,#43474);
#35213=AXIS2_PLACEMENT_3D('',#71183,#43475,#43476);
#35214=AXIS2_PLACEMENT_3D('',#71189,#43477,#43478);
#35215=AXIS2_PLACEMENT_3D('',#71195,#43479,#43480);
#35216=AXIS2_PLACEMENT_3D('',#71201,#43481,#43482);
#35217=AXIS2_PLACEMENT_3D('',#71207,#43483,#43484);
#35218=AXIS2_PLACEMENT_3D('',#71213,#43485,#43486);
#35219=AXIS2_PLACEMENT_3D('',#71219,#43487,#43488);
#35220=AXIS2_PLACEMENT_3D('',#71225,#43489,#43490);
#35221=AXIS2_PLACEMENT_3D('',#71231,#43491,#43492);
#35222=AXIS2_PLACEMENT_3D('',#71237,#43493,#43494);
#35223=AXIS2_PLACEMENT_3D('',#71251,#43496,#43497);
#35224=AXIS2_PLACEMENT_3D('',#71267,#43498,#43499);
#35225=AXIS2_PLACEMENT_3D('',#71273,#43500,#43501);
#35226=AXIS2_PLACEMENT_3D('',#71279,#43502,#43503);
#35227=AXIS2_PLACEMENT_3D('',#71285,#43504,#43505);
#35228=AXIS2_PLACEMENT_3D('',#71291,#43506,#43507);
#35229=AXIS2_PLACEMENT_3D('',#71297,#43508,#43509);
#35230=AXIS2_PLACEMENT_3D('',#71303,#43510,#43511);
#35231=AXIS2_PLACEMENT_3D('',#71309,#43512,#43513);
#35232=AXIS2_PLACEMENT_3D('',#71315,#43514,#43515);
#35233=AXIS2_PLACEMENT_3D('',#71321,#43516,#43517);
#35234=AXIS2_PLACEMENT_3D('',#71327,#43518,#43519);
#35235=AXIS2_PLACEMENT_3D('',#71333,#43520,#43521);
#35236=AXIS2_PLACEMENT_3D('',#71339,#43522,#43523);
#35237=AXIS2_PLACEMENT_3D('',#71345,#43524,#43525);
#35238=AXIS2_PLACEMENT_3D('',#71351,#43526,#43527);
#35239=AXIS2_PLACEMENT_3D('',#71357,#43528,#43529);
#35240=AXIS2_PLACEMENT_3D('',#71363,#43530,#43531);
#35241=AXIS2_PLACEMENT_3D('',#71369,#43532,#43533);
#35242=AXIS2_PLACEMENT_3D('',#71375,#43534,#43535);
#35243=AXIS2_PLACEMENT_3D('',#71381,#43536,#43537);
#35244=AXIS2_PLACEMENT_3D('',#71387,#43538,#43539);
#35245=AXIS2_PLACEMENT_3D('',#71393,#43540,#43541);
#35246=AXIS2_PLACEMENT_3D('',#71399,#43542,#43543);
#35247=AXIS2_PLACEMENT_3D('',#71405,#43544,#43545);
#35248=AXIS2_PLACEMENT_3D('',#71411,#43546,#43547);
#35249=AXIS2_PLACEMENT_3D('',#71417,#43548,#43549);
#35250=AXIS2_PLACEMENT_3D('',#71423,#43550,#43551);
#35251=AXIS2_PLACEMENT_3D('',#71429,#43552,#43553);
#35252=AXIS2_PLACEMENT_3D('',#71435,#43554,#43555);
#35253=AXIS2_PLACEMENT_3D('',#71441,#43556,#43557);
#35254=AXIS2_PLACEMENT_3D('',#71447,#43558,#43559);
#35255=AXIS2_PLACEMENT_3D('',#71453,#43560,#43561);
#35256=AXIS2_PLACEMENT_3D('',#71459,#43562,#43563);
#35257=AXIS2_PLACEMENT_3D('',#71465,#43564,#43565);
#35258=AXIS2_PLACEMENT_3D('',#71471,#43566,#43567);
#35259=AXIS2_PLACEMENT_3D('',#71477,#43568,#43569);
#35260=AXIS2_PLACEMENT_3D('',#71483,#43570,#43571);
#35261=AXIS2_PLACEMENT_3D('',#71489,#43572,#43573);
#35262=AXIS2_PLACEMENT_3D('',#71495,#43574,#43575);
#35263=AXIS2_PLACEMENT_3D('',#71501,#43576,#43577);
#35264=AXIS2_PLACEMENT_3D('',#71507,#43578,#43579);
#35265=AXIS2_PLACEMENT_3D('',#71513,#43580,#43581);
#35266=AXIS2_PLACEMENT_3D('',#71519,#43582,#43583);
#35267=AXIS2_PLACEMENT_3D('',#71525,#43584,#43585);
#35268=AXIS2_PLACEMENT_3D('',#71531,#43586,#43587);
#35269=AXIS2_PLACEMENT_3D('',#71537,#43588,#43589);
#35270=AXIS2_PLACEMENT_3D('',#71543,#43590,#43591);
#35271=AXIS2_PLACEMENT_3D('',#71549,#43592,#43593);
#35272=AXIS2_PLACEMENT_3D('',#71555,#43594,#43595);
#35273=AXIS2_PLACEMENT_3D('',#71561,#43596,#43597);
#35274=AXIS2_PLACEMENT_3D('',#71567,#43598,#43599);
#35275=AXIS2_PLACEMENT_3D('',#71573,#43600,#43601);
#35276=AXIS2_PLACEMENT_3D('',#71579,#43602,#43603);
#35277=AXIS2_PLACEMENT_3D('',#71585,#43604,#43605);
#35278=AXIS2_PLACEMENT_3D('',#71591,#43606,#43607);
#35279=AXIS2_PLACEMENT_3D('',#71597,#43608,#43609);
#35280=AXIS2_PLACEMENT_3D('',#71603,#43610,#43611);
#35281=AXIS2_PLACEMENT_3D('',#71609,#43612,#43613);
#35282=AXIS2_PLACEMENT_3D('',#71615,#43614,#43615);
#35283=AXIS2_PLACEMENT_3D('',#71621,#43616,#43617);
#35284=AXIS2_PLACEMENT_3D('',#71627,#43618,#43619);
#35285=AXIS2_PLACEMENT_3D('',#71633,#43620,#43621);
#35286=AXIS2_PLACEMENT_3D('',#71639,#43622,#43623);
#35287=AXIS2_PLACEMENT_3D('',#71645,#43624,#43625);
#35288=AXIS2_PLACEMENT_3D('',#71651,#43626,#43627);
#35289=AXIS2_PLACEMENT_3D('',#71657,#43628,#43629);
#35290=AXIS2_PLACEMENT_3D('',#71663,#43630,#43631);
#35291=AXIS2_PLACEMENT_3D('',#71669,#43632,#43633);
#35292=AXIS2_PLACEMENT_3D('',#71675,#43634,#43635);
#35293=AXIS2_PLACEMENT_3D('',#71681,#43636,#43637);
#35294=AXIS2_PLACEMENT_3D('',#71687,#43638,#43639);
#35295=AXIS2_PLACEMENT_3D('',#71693,#43640,#43641);
#35296=AXIS2_PLACEMENT_3D('',#71699,#43642,#43643);
#35297=AXIS2_PLACEMENT_3D('',#71705,#43644,#43645);
#35298=AXIS2_PLACEMENT_3D('',#71711,#43646,#43647);
#35299=AXIS2_PLACEMENT_3D('',#71717,#43648,#43649);
#35300=AXIS2_PLACEMENT_3D('',#71723,#43650,#43651);
#35301=AXIS2_PLACEMENT_3D('',#71729,#43652,#43653);
#35302=AXIS2_PLACEMENT_3D('',#71735,#43654,#43655);
#35303=AXIS2_PLACEMENT_3D('',#71741,#43656,#43657);
#35304=AXIS2_PLACEMENT_3D('',#71747,#43658,#43659);
#35305=AXIS2_PLACEMENT_3D('',#71753,#43660,#43661);
#35306=AXIS2_PLACEMENT_3D('',#71759,#43662,#43663);
#35307=AXIS2_PLACEMENT_3D('',#71765,#43664,#43665);
#35308=AXIS2_PLACEMENT_3D('',#71771,#43666,#43667);
#35309=AXIS2_PLACEMENT_3D('',#71777,#43668,#43669);
#35310=AXIS2_PLACEMENT_3D('',#71783,#43670,#43671);
#35311=AXIS2_PLACEMENT_3D('',#71789,#43672,#43673);
#35312=AXIS2_PLACEMENT_3D('',#71795,#43674,#43675);
#35313=AXIS2_PLACEMENT_3D('',#71801,#43676,#43677);
#35314=AXIS2_PLACEMENT_3D('',#71807,#43678,#43679);
#35315=AXIS2_PLACEMENT_3D('',#71813,#43680,#43681);
#35316=AXIS2_PLACEMENT_3D('',#71819,#43682,#43683);
#35317=AXIS2_PLACEMENT_3D('',#71825,#43684,#43685);
#35318=AXIS2_PLACEMENT_3D('',#71831,#43686,#43687);
#35319=AXIS2_PLACEMENT_3D('',#71837,#43688,#43689);
#35320=AXIS2_PLACEMENT_3D('',#71843,#43690,#43691);
#35321=AXIS2_PLACEMENT_3D('',#71849,#43692,#43693);
#35322=AXIS2_PLACEMENT_3D('',#71855,#43694,#43695);
#35323=AXIS2_PLACEMENT_3D('',#71861,#43696,#43697);
#35324=AXIS2_PLACEMENT_3D('',#71867,#43698,#43699);
#35325=AXIS2_PLACEMENT_3D('',#71873,#43700,#43701);
#35326=AXIS2_PLACEMENT_3D('',#71879,#43702,#43703);
#35327=AXIS2_PLACEMENT_3D('',#71885,#43704,#43705);
#35328=AXIS2_PLACEMENT_3D('',#71891,#43706,#43707);
#35329=AXIS2_PLACEMENT_3D('',#71897,#43708,#43709);
#35330=AXIS2_PLACEMENT_3D('',#71903,#43710,#43711);
#35331=AXIS2_PLACEMENT_3D('',#71909,#43712,#43713);
#35332=AXIS2_PLACEMENT_3D('',#71915,#43714,#43715);
#35333=AXIS2_PLACEMENT_3D('',#71921,#43716,#43717);
#35334=AXIS2_PLACEMENT_3D('',#71927,#43718,#43719);
#35335=AXIS2_PLACEMENT_3D('',#71933,#43720,#43721);
#35336=AXIS2_PLACEMENT_3D('',#71939,#43722,#43723);
#35337=AXIS2_PLACEMENT_3D('',#71945,#43724,#43725);
#35338=AXIS2_PLACEMENT_3D('',#71951,#43726,#43727);
#35339=AXIS2_PLACEMENT_3D('',#71957,#43728,#43729);
#35340=AXIS2_PLACEMENT_3D('',#71963,#43730,#43731);
#35341=AXIS2_PLACEMENT_3D('',#71969,#43732,#43733);
#35342=AXIS2_PLACEMENT_3D('',#71975,#43734,#43735);
#35343=AXIS2_PLACEMENT_3D('',#71984,#43736,#43737);
#35344=AXIS2_PLACEMENT_3D('',#71993,#43738,#43739);
#35345=AXIS2_PLACEMENT_3D('',#72002,#43740,#43741);
#35346=AXIS2_PLACEMENT_3D('',#72011,#43742,#43743);
#35347=AXIS2_PLACEMENT_3D('',#72020,#43744,#43745);
#35348=AXIS2_PLACEMENT_3D('',#72029,#43746,#43747);
#35349=AXIS2_PLACEMENT_3D('',#72038,#43748,#43749);
#35350=AXIS2_PLACEMENT_3D('',#72047,#43750,#43751);
#35351=AXIS2_PLACEMENT_3D('',#72056,#43752,#43753);
#35352=AXIS2_PLACEMENT_3D('',#72065,#43754,#43755);
#35353=AXIS2_PLACEMENT_3D('',#72074,#43756,#43757);
#35354=AXIS2_PLACEMENT_3D('',#72083,#43758,#43759);
#35355=AXIS2_PLACEMENT_3D('',#72092,#43760,#43761);
#35356=AXIS2_PLACEMENT_3D('',#72101,#43762,#43763);
#35357=AXIS2_PLACEMENT_3D('',#72110,#43764,#43765);
#35358=AXIS2_PLACEMENT_3D('',#72116,#43766,#43767);
#35359=AXIS2_PLACEMENT_3D('',#72122,#43768,#43769);
#35360=AXIS2_PLACEMENT_3D('',#72128,#43770,#43771);
#35361=AXIS2_PLACEMENT_3D('',#72134,#43772,#43773);
#35362=AXIS2_PLACEMENT_3D('',#72140,#43774,#43775);
#35363=AXIS2_PLACEMENT_3D('',#72146,#43776,#43777);
#35364=AXIS2_PLACEMENT_3D('',#72152,#43778,#43779);
#35365=AXIS2_PLACEMENT_3D('',#72158,#43780,#43781);
#35366=AXIS2_PLACEMENT_3D('',#72164,#43782,#43783);
#35367=AXIS2_PLACEMENT_3D('',#72170,#43784,#43785);
#35368=AXIS2_PLACEMENT_3D('',#72186,#43787,#43788);
#35369=AXIS2_PLACEMENT_3D('',#72187,#43789,#43790);
#35370=AXIS2_PLACEMENT_3D('',#72188,#43791,#43792);
#35371=AXIS2_PLACEMENT_3D('',#72190,#43793,#43794);
#35372=AXIS2_PLACEMENT_3D('',#72191,#43795,#43796);
#35373=AXIS2_PLACEMENT_3D('',#72192,#43797,#43798);
#35374=AXIS2_PLACEMENT_3D('',#72194,#43799,#43800);
#35375=AXIS2_PLACEMENT_3D('',#72196,#43802,#43803);
#35376=AXIS2_PLACEMENT_3D('',#72198,#43804,#43805);
#35377=AXIS2_PLACEMENT_3D('',#72199,#43806,#43807);
#35378=AXIS2_PLACEMENT_3D('',#72200,#43808,#43809);
#35379=AXIS2_PLACEMENT_3D('',#72202,#43810,#43811);
#35380=AXIS2_PLACEMENT_3D('',#72203,#43812,#43813);
#35381=AXIS2_PLACEMENT_3D('',#72204,#43814,#43815);
#35382=AXIS2_PLACEMENT_3D('',#72206,#43816,#43817);
#35383=AXIS2_PLACEMENT_3D('',#72208,#43818,#43819);
#35384=AXIS2_PLACEMENT_3D('',#72209,#43820,#43821);
#35385=AXIS2_PLACEMENT_3D('',#72210,#43822,#43823);
#35386=AXIS2_PLACEMENT_3D('',#72212,#43824,#43825);
#35387=AXIS2_PLACEMENT_3D('',#72214,#43826,#43827);
#35388=AXIS2_PLACEMENT_3D('',#72215,#43828,#43829);
#35389=AXIS2_PLACEMENT_3D('',#72216,#43830,#43831);
#35390=AXIS2_PLACEMENT_3D('',#72218,#43832,#43833);
#35391=AXIS2_PLACEMENT_3D('',#72220,#43834,#43835);
#35392=AXIS2_PLACEMENT_3D('',#72221,#43836,#43837);
#35393=AXIS2_PLACEMENT_3D('',#72222,#43838,#43839);
#35394=AXIS2_PLACEMENT_3D('',#72224,#43840,#43841);
#35395=AXIS2_PLACEMENT_3D('',#72226,#43842,#43843);
#35396=AXIS2_PLACEMENT_3D('',#72227,#43844,#43845);
#35397=AXIS2_PLACEMENT_3D('',#72228,#43846,#43847);
#35398=AXIS2_PLACEMENT_3D('',#72230,#43848,#43849);
#35399=AXIS2_PLACEMENT_3D('',#72232,#43850,#43851);
#35400=AXIS2_PLACEMENT_3D('',#72233,#43852,#43853);
#35401=AXIS2_PLACEMENT_3D('',#72234,#43854,#43855);
#35402=AXIS2_PLACEMENT_3D('',#72236,#43856,#43857);
#35403=AXIS2_PLACEMENT_3D('',#72238,#43858,#43859);
#35404=AXIS2_PLACEMENT_3D('',#72239,#43860,#43861);
#35405=AXIS2_PLACEMENT_3D('',#72240,#43862,#43863);
#35406=AXIS2_PLACEMENT_3D('',#72242,#43864,#43865);
#35407=AXIS2_PLACEMENT_3D('',#72244,#43866,#43867);
#35408=AXIS2_PLACEMENT_3D('',#72245,#43868,#43869);
#35409=AXIS2_PLACEMENT_3D('',#72246,#43870,#43871);
#35410=AXIS2_PLACEMENT_3D('',#72248,#43872,#43873);
#35411=AXIS2_PLACEMENT_3D('',#72250,#43874,#43875);
#35412=AXIS2_PLACEMENT_3D('',#72251,#43876,#43877);
#35413=AXIS2_PLACEMENT_3D('',#72252,#43878,#43879);
#35414=AXIS2_PLACEMENT_3D('',#72254,#43880,#43881);
#35415=AXIS2_PLACEMENT_3D('',#72256,#43882,#43883);
#35416=AXIS2_PLACEMENT_3D('',#72257,#43884,#43885);
#35417=AXIS2_PLACEMENT_3D('',#72258,#43886,#43887);
#35418=AXIS2_PLACEMENT_3D('',#72260,#43888,#43889);
#35419=AXIS2_PLACEMENT_3D('',#72262,#43890,#43891);
#35420=AXIS2_PLACEMENT_3D('',#72263,#43892,#43893);
#35421=AXIS2_PLACEMENT_3D('',#72264,#43894,#43895);
#35422=AXIS2_PLACEMENT_3D('',#72266,#43896,#43897);
#35423=AXIS2_PLACEMENT_3D('',#72268,#43898,#43899);
#35424=AXIS2_PLACEMENT_3D('',#72269,#43900,#43901);
#35425=AXIS2_PLACEMENT_3D('',#72270,#43902,#43903);
#35426=AXIS2_PLACEMENT_3D('',#72272,#43904,#43905);
#35427=AXIS2_PLACEMENT_3D('',#72274,#43906,#43907);
#35428=AXIS2_PLACEMENT_3D('',#72275,#43908,#43909);
#35429=AXIS2_PLACEMENT_3D('',#72276,#43910,#43911);
#35430=AXIS2_PLACEMENT_3D('',#72278,#43912,#43913);
#35431=AXIS2_PLACEMENT_3D('',#72280,#43914,#43915);
#35432=AXIS2_PLACEMENT_3D('',#72281,#43916,#43917);
#35433=AXIS2_PLACEMENT_3D('',#72282,#43918,#43919);
#35434=AXIS2_PLACEMENT_3D('',#72284,#43920,#43921);
#35435=AXIS2_PLACEMENT_3D('',#72286,#43922,#43923);
#35436=AXIS2_PLACEMENT_3D('',#72287,#43924,#43925);
#35437=AXIS2_PLACEMENT_3D('',#72288,#43926,#43927);
#35438=AXIS2_PLACEMENT_3D('',#72290,#43928,#43929);
#35439=AXIS2_PLACEMENT_3D('',#72292,#43930,#43931);
#35440=AXIS2_PLACEMENT_3D('',#72293,#43932,#43933);
#35441=AXIS2_PLACEMENT_3D('',#72294,#43934,#43935);
#35442=AXIS2_PLACEMENT_3D('',#72296,#43936,#43937);
#35443=AXIS2_PLACEMENT_3D('',#72298,#43938,#43939);
#35444=AXIS2_PLACEMENT_3D('',#72299,#43940,#43941);
#35445=AXIS2_PLACEMENT_3D('',#72300,#43942,#43943);
#35446=AXIS2_PLACEMENT_3D('',#72302,#43944,#43945);
#35447=AXIS2_PLACEMENT_3D('',#72304,#43946,#43947);
#35448=AXIS2_PLACEMENT_3D('',#72305,#43948,#43949);
#35449=AXIS2_PLACEMENT_3D('',#72306,#43950,#43951);
#35450=AXIS2_PLACEMENT_3D('',#72308,#43952,#43953);
#35451=AXIS2_PLACEMENT_3D('',#72310,#43954,#43955);
#35452=AXIS2_PLACEMENT_3D('',#72311,#43956,#43957);
#35453=AXIS2_PLACEMENT_3D('',#72312,#43958,#43959);
#35454=AXIS2_PLACEMENT_3D('',#72314,#43960,#43961);
#35455=AXIS2_PLACEMENT_3D('',#72316,#43962,#43963);
#35456=AXIS2_PLACEMENT_3D('',#72317,#43964,#43965);
#35457=AXIS2_PLACEMENT_3D('',#72318,#43966,#43967);
#35458=AXIS2_PLACEMENT_3D('',#72320,#43968,#43969);
#35459=AXIS2_PLACEMENT_3D('',#72322,#43970,#43971);
#35460=AXIS2_PLACEMENT_3D('',#72323,#43972,#43973);
#35461=AXIS2_PLACEMENT_3D('',#72324,#43974,#43975);
#35462=AXIS2_PLACEMENT_3D('',#72326,#43976,#43977);
#35463=AXIS2_PLACEMENT_3D('',#72328,#43978,#43979);
#35464=AXIS2_PLACEMENT_3D('',#72329,#43980,#43981);
#35465=AXIS2_PLACEMENT_3D('',#72330,#43982,#43983);
#35466=AXIS2_PLACEMENT_3D('',#72332,#43984,#43985);
#35467=AXIS2_PLACEMENT_3D('',#72334,#43986,#43987);
#35468=AXIS2_PLACEMENT_3D('',#72335,#43988,#43989);
#35469=AXIS2_PLACEMENT_3D('',#72336,#43990,#43991);
#35470=AXIS2_PLACEMENT_3D('',#72338,#43992,#43993);
#35471=AXIS2_PLACEMENT_3D('',#72340,#43994,#43995);
#35472=AXIS2_PLACEMENT_3D('',#72341,#43996,#43997);
#35473=AXIS2_PLACEMENT_3D('',#72342,#43998,#43999);
#35474=AXIS2_PLACEMENT_3D('',#72344,#44000,#44001);
#35475=AXIS2_PLACEMENT_3D('',#72346,#44002,#44003);
#35476=AXIS2_PLACEMENT_3D('',#72347,#44004,#44005);
#35477=AXIS2_PLACEMENT_3D('',#72348,#44006,#44007);
#35478=AXIS2_PLACEMENT_3D('',#72350,#44008,#44009);
#35479=AXIS2_PLACEMENT_3D('',#72352,#44010,#44011);
#35480=AXIS2_PLACEMENT_3D('',#72353,#44012,#44013);
#35481=AXIS2_PLACEMENT_3D('',#72354,#44014,#44015);
#35482=AXIS2_PLACEMENT_3D('',#72356,#44016,#44017);
#35483=AXIS2_PLACEMENT_3D('',#72358,#44018,#44019);
#35484=AXIS2_PLACEMENT_3D('',#72359,#44020,#44021);
#35485=AXIS2_PLACEMENT_3D('',#72360,#44022,#44023);
#35486=AXIS2_PLACEMENT_3D('',#72362,#44024,#44025);
#35487=AXIS2_PLACEMENT_3D('',#72364,#44026,#44027);
#35488=AXIS2_PLACEMENT_3D('',#72365,#44028,#44029);
#35489=AXIS2_PLACEMENT_3D('',#72366,#44030,#44031);
#35490=AXIS2_PLACEMENT_3D('',#72368,#44032,#44033);
#35491=AXIS2_PLACEMENT_3D('',#72370,#44034,#44035);
#35492=AXIS2_PLACEMENT_3D('',#72371,#44036,#44037);
#35493=AXIS2_PLACEMENT_3D('',#72372,#44038,#44039);
#35494=AXIS2_PLACEMENT_3D('',#72374,#44040,#44041);
#35495=AXIS2_PLACEMENT_3D('',#72376,#44042,#44043);
#35496=AXIS2_PLACEMENT_3D('',#72377,#44044,#44045);
#35497=AXIS2_PLACEMENT_3D('',#72378,#44046,#44047);
#35498=AXIS2_PLACEMENT_3D('',#72380,#44048,#44049);
#35499=AXIS2_PLACEMENT_3D('',#72382,#44050,#44051);
#35500=AXIS2_PLACEMENT_3D('',#72383,#44052,#44053);
#35501=AXIS2_PLACEMENT_3D('',#72384,#44054,#44055);
#35502=AXIS2_PLACEMENT_3D('',#72386,#44056,#44057);
#35503=AXIS2_PLACEMENT_3D('',#72388,#44058,#44059);
#35504=AXIS2_PLACEMENT_3D('',#72389,#44060,#44061);
#35505=AXIS2_PLACEMENT_3D('',#72390,#44062,#44063);
#35506=AXIS2_PLACEMENT_3D('',#72392,#44064,#44065);
#35507=AXIS2_PLACEMENT_3D('',#72394,#44066,#44067);
#35508=AXIS2_PLACEMENT_3D('',#72395,#44068,#44069);
#35509=AXIS2_PLACEMENT_3D('',#72396,#44070,#44071);
#35510=AXIS2_PLACEMENT_3D('',#72398,#44072,#44073);
#35511=AXIS2_PLACEMENT_3D('',#72400,#44074,#44075);
#35512=AXIS2_PLACEMENT_3D('',#72401,#44076,#44077);
#35513=AXIS2_PLACEMENT_3D('',#72402,#44078,#44079);
#35514=AXIS2_PLACEMENT_3D('',#72404,#44080,#44081);
#35515=AXIS2_PLACEMENT_3D('',#72406,#44082,#44083);
#35516=AXIS2_PLACEMENT_3D('',#72407,#44084,#44085);
#35517=AXIS2_PLACEMENT_3D('',#72408,#44086,#44087);
#35518=AXIS2_PLACEMENT_3D('',#72410,#44088,#44089);
#35519=AXIS2_PLACEMENT_3D('',#72412,#44090,#44091);
#35520=AXIS2_PLACEMENT_3D('',#72413,#44092,#44093);
#35521=AXIS2_PLACEMENT_3D('',#72414,#44094,#44095);
#35522=AXIS2_PLACEMENT_3D('',#72416,#44096,#44097);
#35523=AXIS2_PLACEMENT_3D('',#72418,#44098,#44099);
#35524=AXIS2_PLACEMENT_3D('',#72419,#44100,#44101);
#35525=AXIS2_PLACEMENT_3D('',#72420,#44102,#44103);
#35526=AXIS2_PLACEMENT_3D('',#72422,#44104,#44105);
#35527=AXIS2_PLACEMENT_3D('',#72424,#44106,#44107);
#35528=AXIS2_PLACEMENT_3D('',#72425,#44108,#44109);
#35529=AXIS2_PLACEMENT_3D('',#72426,#44110,#44111);
#35530=AXIS2_PLACEMENT_3D('',#72428,#44112,#44113);
#35531=AXIS2_PLACEMENT_3D('',#72430,#44114,#44115);
#35532=AXIS2_PLACEMENT_3D('',#72431,#44116,#44117);
#35533=AXIS2_PLACEMENT_3D('',#72432,#44118,#44119);
#35534=AXIS2_PLACEMENT_3D('',#72434,#44120,#44121);
#35535=AXIS2_PLACEMENT_3D('',#72436,#44122,#44123);
#35536=AXIS2_PLACEMENT_3D('',#72437,#44124,#44125);
#35537=AXIS2_PLACEMENT_3D('',#72438,#44126,#44127);
#35538=AXIS2_PLACEMENT_3D('',#72440,#44128,#44129);
#35539=AXIS2_PLACEMENT_3D('',#72442,#44130,#44131);
#35540=AXIS2_PLACEMENT_3D('',#72443,#44132,#44133);
#35541=AXIS2_PLACEMENT_3D('',#72444,#44134,#44135);
#35542=AXIS2_PLACEMENT_3D('',#72446,#44136,#44137);
#35543=AXIS2_PLACEMENT_3D('',#72448,#44138,#44139);
#35544=AXIS2_PLACEMENT_3D('',#72449,#44140,#44141);
#35545=AXIS2_PLACEMENT_3D('',#72450,#44142,#44143);
#35546=AXIS2_PLACEMENT_3D('',#72452,#44144,#44145);
#35547=AXIS2_PLACEMENT_3D('',#72454,#44146,#44147);
#35548=AXIS2_PLACEMENT_3D('',#72455,#44148,#44149);
#35549=AXIS2_PLACEMENT_3D('',#72456,#44150,#44151);
#35550=AXIS2_PLACEMENT_3D('',#72458,#44152,#44153);
#35551=AXIS2_PLACEMENT_3D('',#72460,#44154,#44155);
#35552=AXIS2_PLACEMENT_3D('',#72461,#44156,#44157);
#35553=AXIS2_PLACEMENT_3D('',#72462,#44158,#44159);
#35554=AXIS2_PLACEMENT_3D('',#72464,#44160,#44161);
#35555=AXIS2_PLACEMENT_3D('',#72466,#44162,#44163);
#35556=AXIS2_PLACEMENT_3D('',#72467,#44164,#44165);
#35557=AXIS2_PLACEMENT_3D('',#72468,#44166,#44167);
#35558=AXIS2_PLACEMENT_3D('',#72470,#44168,#44169);
#35559=AXIS2_PLACEMENT_3D('',#72472,#44170,#44171);
#35560=AXIS2_PLACEMENT_3D('',#72473,#44172,#44173);
#35561=AXIS2_PLACEMENT_3D('',#72474,#44174,#44175);
#35562=AXIS2_PLACEMENT_3D('',#72476,#44176,#44177);
#35563=AXIS2_PLACEMENT_3D('',#72478,#44178,#44179);
#35564=AXIS2_PLACEMENT_3D('',#72479,#44180,#44181);
#35565=AXIS2_PLACEMENT_3D('',#72480,#44182,#44183);
#35566=AXIS2_PLACEMENT_3D('',#72482,#44184,#44185);
#35567=AXIS2_PLACEMENT_3D('',#72484,#44186,#44187);
#35568=AXIS2_PLACEMENT_3D('',#72485,#44188,#44189);
#35569=AXIS2_PLACEMENT_3D('',#72486,#44190,#44191);
#35570=AXIS2_PLACEMENT_3D('',#72488,#44192,#44193);
#35571=AXIS2_PLACEMENT_3D('',#72490,#44194,#44195);
#35572=AXIS2_PLACEMENT_3D('',#72491,#44196,#44197);
#35573=AXIS2_PLACEMENT_3D('',#72492,#44198,#44199);
#35574=AXIS2_PLACEMENT_3D('',#72494,#44200,#44201);
#35575=AXIS2_PLACEMENT_3D('',#72496,#44202,#44203);
#35576=AXIS2_PLACEMENT_3D('',#72497,#44204,#44205);
#35577=AXIS2_PLACEMENT_3D('',#72498,#44206,#44207);
#35578=AXIS2_PLACEMENT_3D('',#72500,#44208,#44209);
#35579=AXIS2_PLACEMENT_3D('',#72502,#44210,#44211);
#35580=AXIS2_PLACEMENT_3D('',#72503,#44212,#44213);
#35581=AXIS2_PLACEMENT_3D('',#72504,#44214,#44215);
#35582=AXIS2_PLACEMENT_3D('',#72506,#44216,#44217);
#35583=AXIS2_PLACEMENT_3D('',#72508,#44218,#44219);
#35584=AXIS2_PLACEMENT_3D('',#72509,#44220,#44221);
#35585=AXIS2_PLACEMENT_3D('',#72510,#44222,#44223);
#35586=AXIS2_PLACEMENT_3D('',#72512,#44224,#44225);
#35587=AXIS2_PLACEMENT_3D('',#72514,#44226,#44227);
#35588=AXIS2_PLACEMENT_3D('',#72515,#44228,#44229);
#35589=AXIS2_PLACEMENT_3D('',#72516,#44230,#44231);
#35590=AXIS2_PLACEMENT_3D('',#72518,#44232,#44233);
#35591=AXIS2_PLACEMENT_3D('',#72520,#44234,#44235);
#35592=AXIS2_PLACEMENT_3D('',#72521,#44236,#44237);
#35593=AXIS2_PLACEMENT_3D('',#72522,#44238,#44239);
#35594=AXIS2_PLACEMENT_3D('',#72524,#44240,#44241);
#35595=AXIS2_PLACEMENT_3D('',#72526,#44242,#44243);
#35596=AXIS2_PLACEMENT_3D('',#72527,#44244,#44245);
#35597=AXIS2_PLACEMENT_3D('',#72528,#44246,#44247);
#35598=AXIS2_PLACEMENT_3D('',#72530,#44248,#44249);
#35599=AXIS2_PLACEMENT_3D('',#72532,#44250,#44251);
#35600=AXIS2_PLACEMENT_3D('',#72533,#44252,#44253);
#35601=AXIS2_PLACEMENT_3D('',#72534,#44254,#44255);
#35602=AXIS2_PLACEMENT_3D('',#72536,#44256,#44257);
#35603=AXIS2_PLACEMENT_3D('',#72538,#44258,#44259);
#35604=AXIS2_PLACEMENT_3D('',#72539,#44260,#44261);
#35605=AXIS2_PLACEMENT_3D('',#72540,#44262,#44263);
#35606=AXIS2_PLACEMENT_3D('',#72542,#44264,#44265);
#35607=AXIS2_PLACEMENT_3D('',#72544,#44266,#44267);
#35608=AXIS2_PLACEMENT_3D('',#72545,#44268,#44269);
#35609=AXIS2_PLACEMENT_3D('',#72546,#44270,#44271);
#35610=AXIS2_PLACEMENT_3D('',#72548,#44272,#44273);
#35611=AXIS2_PLACEMENT_3D('',#72550,#44274,#44275);
#35612=AXIS2_PLACEMENT_3D('',#72551,#44276,#44277);
#35613=AXIS2_PLACEMENT_3D('',#72552,#44278,#44279);
#35614=AXIS2_PLACEMENT_3D('',#72554,#44280,#44281);
#35615=AXIS2_PLACEMENT_3D('',#72556,#44282,#44283);
#35616=AXIS2_PLACEMENT_3D('',#72557,#44284,#44285);
#35617=AXIS2_PLACEMENT_3D('',#72558,#44286,#44287);
#35618=AXIS2_PLACEMENT_3D('',#72560,#44288,#44289);
#35619=AXIS2_PLACEMENT_3D('',#72562,#44290,#44291);
#35620=AXIS2_PLACEMENT_3D('',#72563,#44292,#44293);
#35621=AXIS2_PLACEMENT_3D('',#72564,#44294,#44295);
#35622=AXIS2_PLACEMENT_3D('',#72566,#44296,#44297);
#35623=AXIS2_PLACEMENT_3D('',#72568,#44298,#44299);
#35624=AXIS2_PLACEMENT_3D('',#72569,#44300,#44301);
#35625=AXIS2_PLACEMENT_3D('',#72570,#44302,#44303);
#35626=AXIS2_PLACEMENT_3D('',#72572,#44304,#44305);
#35627=AXIS2_PLACEMENT_3D('',#72574,#44306,#44307);
#35628=AXIS2_PLACEMENT_3D('',#72575,#44308,#44309);
#35629=AXIS2_PLACEMENT_3D('',#72576,#44310,#44311);
#35630=AXIS2_PLACEMENT_3D('',#72578,#44312,#44313);
#35631=AXIS2_PLACEMENT_3D('',#72580,#44314,#44315);
#35632=AXIS2_PLACEMENT_3D('',#72581,#44316,#44317);
#35633=AXIS2_PLACEMENT_3D('',#72582,#44318,#44319);
#35634=AXIS2_PLACEMENT_3D('',#72584,#44320,#44321);
#35635=AXIS2_PLACEMENT_3D('',#72586,#44322,#44323);
#35636=AXIS2_PLACEMENT_3D('',#72587,#44324,#44325);
#35637=AXIS2_PLACEMENT_3D('',#72588,#44326,#44327);
#35638=AXIS2_PLACEMENT_3D('',#72590,#44328,#44329);
#35639=AXIS2_PLACEMENT_3D('',#72592,#44330,#44331);
#35640=AXIS2_PLACEMENT_3D('',#72593,#44332,#44333);
#35641=AXIS2_PLACEMENT_3D('',#72594,#44334,#44335);
#35642=AXIS2_PLACEMENT_3D('',#72596,#44336,#44337);
#35643=AXIS2_PLACEMENT_3D('',#72598,#44338,#44339);
#35644=AXIS2_PLACEMENT_3D('',#72599,#44340,#44341);
#35645=AXIS2_PLACEMENT_3D('',#72600,#44342,#44343);
#35646=AXIS2_PLACEMENT_3D('',#72602,#44344,#44345);
#35647=AXIS2_PLACEMENT_3D('',#72604,#44346,#44347);
#35648=AXIS2_PLACEMENT_3D('',#72605,#44348,#44349);
#35649=AXIS2_PLACEMENT_3D('',#72606,#44350,#44351);
#35650=AXIS2_PLACEMENT_3D('',#72608,#44352,#44353);
#35651=AXIS2_PLACEMENT_3D('',#72610,#44354,#44355);
#35652=AXIS2_PLACEMENT_3D('',#72611,#44356,#44357);
#35653=AXIS2_PLACEMENT_3D('',#72612,#44358,#44359);
#35654=AXIS2_PLACEMENT_3D('',#72614,#44360,#44361);
#35655=AXIS2_PLACEMENT_3D('',#72616,#44362,#44363);
#35656=AXIS2_PLACEMENT_3D('',#72617,#44364,#44365);
#35657=AXIS2_PLACEMENT_3D('',#72618,#44366,#44367);
#35658=AXIS2_PLACEMENT_3D('',#72620,#44368,#44369);
#35659=AXIS2_PLACEMENT_3D('',#72622,#44370,#44371);
#35660=AXIS2_PLACEMENT_3D('',#72623,#44372,#44373);
#35661=AXIS2_PLACEMENT_3D('',#72624,#44374,#44375);
#35662=AXIS2_PLACEMENT_3D('',#72626,#44376,#44377);
#35663=AXIS2_PLACEMENT_3D('',#72628,#44378,#44379);
#35664=AXIS2_PLACEMENT_3D('',#72629,#44380,#44381);
#35665=AXIS2_PLACEMENT_3D('',#72630,#44382,#44383);
#35666=AXIS2_PLACEMENT_3D('',#72632,#44384,#44385);
#35667=AXIS2_PLACEMENT_3D('',#72634,#44386,#44387);
#35668=AXIS2_PLACEMENT_3D('',#72635,#44388,#44389);
#35669=AXIS2_PLACEMENT_3D('',#72636,#44390,#44391);
#35670=AXIS2_PLACEMENT_3D('',#72638,#44392,#44393);
#35671=AXIS2_PLACEMENT_3D('',#72640,#44394,#44395);
#35672=AXIS2_PLACEMENT_3D('',#72641,#44396,#44397);
#35673=AXIS2_PLACEMENT_3D('',#72642,#44398,#44399);
#35674=AXIS2_PLACEMENT_3D('',#72644,#44400,#44401);
#35675=AXIS2_PLACEMENT_3D('',#72646,#44402,#44403);
#35676=AXIS2_PLACEMENT_3D('',#72647,#44404,#44405);
#35677=AXIS2_PLACEMENT_3D('',#72648,#44406,#44407);
#35678=AXIS2_PLACEMENT_3D('',#72650,#44408,#44409);
#35679=AXIS2_PLACEMENT_3D('',#72652,#44410,#44411);
#35680=AXIS2_PLACEMENT_3D('',#72653,#44412,#44413);
#35681=AXIS2_PLACEMENT_3D('',#72654,#44414,#44415);
#35682=AXIS2_PLACEMENT_3D('',#72656,#44416,#44417);
#35683=AXIS2_PLACEMENT_3D('',#72658,#44418,#44419);
#35684=AXIS2_PLACEMENT_3D('',#72659,#44420,#44421);
#35685=AXIS2_PLACEMENT_3D('',#72660,#44422,#44423);
#35686=AXIS2_PLACEMENT_3D('',#72662,#44424,#44425);
#35687=AXIS2_PLACEMENT_3D('',#72664,#44426,#44427);
#35688=AXIS2_PLACEMENT_3D('',#72665,#44428,#44429);
#35689=AXIS2_PLACEMENT_3D('',#72666,#44430,#44431);
#35690=AXIS2_PLACEMENT_3D('',#72668,#44432,#44433);
#35691=AXIS2_PLACEMENT_3D('',#72670,#44434,#44435);
#35692=AXIS2_PLACEMENT_3D('',#72671,#44436,#44437);
#35693=AXIS2_PLACEMENT_3D('',#72672,#44438,#44439);
#35694=AXIS2_PLACEMENT_3D('',#72674,#44440,#44441);
#35695=AXIS2_PLACEMENT_3D('',#72676,#44442,#44443);
#35696=AXIS2_PLACEMENT_3D('',#72677,#44444,#44445);
#35697=AXIS2_PLACEMENT_3D('',#72678,#44446,#44447);
#35698=AXIS2_PLACEMENT_3D('',#72682,#44449,#44450);
#35699=AXIS2_PLACEMENT_3D('',#72684,#44452,#44453);
#35700=AXIS2_PLACEMENT_3D('',#72689,#44456,#44457);
#35701=AXIS2_PLACEMENT_3D('',#72690,#44458,#44459);
#35702=AXIS2_PLACEMENT_3D('',#72695,#44462,#44463);
#35703=AXIS2_PLACEMENT_3D('',#72696,#44464,#44465);
#35704=AXIS2_PLACEMENT_3D('',#72701,#44468,#44469);
#35705=AXIS2_PLACEMENT_3D('',#72702,#44470,#44471);
#35706=AXIS2_PLACEMENT_3D('',#72707,#44474,#44475);
#35707=AXIS2_PLACEMENT_3D('',#72708,#44476,#44477);
#35708=AXIS2_PLACEMENT_3D('',#72713,#44480,#44481);
#35709=AXIS2_PLACEMENT_3D('',#72714,#44482,#44483);
#35710=AXIS2_PLACEMENT_3D('',#72719,#44486,#44487);
#35711=AXIS2_PLACEMENT_3D('',#72720,#44488,#44489);
#35712=AXIS2_PLACEMENT_3D('',#72725,#44492,#44493);
#35713=AXIS2_PLACEMENT_3D('',#72726,#44494,#44495);
#35714=AXIS2_PLACEMENT_3D('',#72731,#44498,#44499);
#35715=AXIS2_PLACEMENT_3D('',#72732,#44500,#44501);
#35716=AXIS2_PLACEMENT_3D('',#72737,#44504,#44505);
#35717=AXIS2_PLACEMENT_3D('',#72738,#44506,#44507);
#35718=AXIS2_PLACEMENT_3D('',#72743,#44510,#44511);
#35719=AXIS2_PLACEMENT_3D('',#72744,#44512,#44513);
#35720=AXIS2_PLACEMENT_3D('',#72749,#44516,#44517);
#35721=AXIS2_PLACEMENT_3D('',#72750,#44518,#44519);
#35722=AXIS2_PLACEMENT_3D('',#72755,#44522,#44523);
#35723=AXIS2_PLACEMENT_3D('',#72756,#44524,#44525);
#35724=AXIS2_PLACEMENT_3D('',#72761,#44528,#44529);
#35725=AXIS2_PLACEMENT_3D('',#72762,#44530,#44531);
#35726=AXIS2_PLACEMENT_3D('',#72767,#44534,#44535);
#35727=AXIS2_PLACEMENT_3D('',#72768,#44536,#44537);
#35728=AXIS2_PLACEMENT_3D('',#72773,#44540,#44541);
#35729=AXIS2_PLACEMENT_3D('',#72774,#44542,#44543);
#35730=AXIS2_PLACEMENT_3D('',#72779,#44546,#44547);
#35731=AXIS2_PLACEMENT_3D('',#72780,#44548,#44549);
#35732=AXIS2_PLACEMENT_3D('',#72785,#44552,#44553);
#35733=AXIS2_PLACEMENT_3D('',#72786,#44554,#44555);
#35734=AXIS2_PLACEMENT_3D('',#72791,#44558,#44559);
#35735=AXIS2_PLACEMENT_3D('',#72792,#44560,#44561);
#35736=AXIS2_PLACEMENT_3D('',#72797,#44564,#44565);
#35737=AXIS2_PLACEMENT_3D('',#72798,#44566,#44567);
#35738=AXIS2_PLACEMENT_3D('',#72803,#44570,#44571);
#35739=AXIS2_PLACEMENT_3D('',#72804,#44572,#44573);
#35740=AXIS2_PLACEMENT_3D('',#72809,#44576,#44577);
#35741=AXIS2_PLACEMENT_3D('',#72810,#44578,#44579);
#35742=AXIS2_PLACEMENT_3D('',#72815,#44582,#44583);
#35743=AXIS2_PLACEMENT_3D('',#72816,#44584,#44585);
#35744=AXIS2_PLACEMENT_3D('',#72821,#44588,#44589);
#35745=AXIS2_PLACEMENT_3D('',#72822,#44590,#44591);
#35746=AXIS2_PLACEMENT_3D('',#72827,#44594,#44595);
#35747=AXIS2_PLACEMENT_3D('',#72828,#44596,#44597);
#35748=AXIS2_PLACEMENT_3D('',#72833,#44600,#44601);
#35749=AXIS2_PLACEMENT_3D('',#72834,#44602,#44603);
#35750=AXIS2_PLACEMENT_3D('',#72839,#44606,#44607);
#35751=AXIS2_PLACEMENT_3D('',#72840,#44608,#44609);
#35752=AXIS2_PLACEMENT_3D('',#72845,#44612,#44613);
#35753=AXIS2_PLACEMENT_3D('',#72846,#44614,#44615);
#35754=AXIS2_PLACEMENT_3D('',#72851,#44618,#44619);
#35755=AXIS2_PLACEMENT_3D('',#72852,#44620,#44621);
#35756=AXIS2_PLACEMENT_3D('',#72857,#44624,#44625);
#35757=AXIS2_PLACEMENT_3D('',#72858,#44626,#44627);
#35758=AXIS2_PLACEMENT_3D('',#72863,#44630,#44631);
#35759=AXIS2_PLACEMENT_3D('',#72864,#44632,#44633);
#35760=AXIS2_PLACEMENT_3D('',#72869,#44636,#44637);
#35761=AXIS2_PLACEMENT_3D('',#72870,#44638,#44639);
#35762=AXIS2_PLACEMENT_3D('',#72875,#44642,#44643);
#35763=AXIS2_PLACEMENT_3D('',#72876,#44644,#44645);
#35764=AXIS2_PLACEMENT_3D('',#72881,#44648,#44649);
#35765=AXIS2_PLACEMENT_3D('',#72882,#44650,#44651);
#35766=AXIS2_PLACEMENT_3D('',#72887,#44654,#44655);
#35767=AXIS2_PLACEMENT_3D('',#72888,#44656,#44657);
#35768=AXIS2_PLACEMENT_3D('',#72893,#44660,#44661);
#35769=AXIS2_PLACEMENT_3D('',#72894,#44662,#44663);
#35770=AXIS2_PLACEMENT_3D('',#72899,#44666,#44667);
#35771=AXIS2_PLACEMENT_3D('',#72900,#44668,#44669);
#35772=AXIS2_PLACEMENT_3D('',#72905,#44672,#44673);
#35773=AXIS2_PLACEMENT_3D('',#72906,#44674,#44675);
#35774=AXIS2_PLACEMENT_3D('',#72911,#44678,#44679);
#35775=AXIS2_PLACEMENT_3D('',#72912,#44680,#44681);
#35776=AXIS2_PLACEMENT_3D('',#72917,#44684,#44685);
#35777=AXIS2_PLACEMENT_3D('',#72918,#44686,#44687);
#35778=AXIS2_PLACEMENT_3D('',#72923,#44690,#44691);
#35779=AXIS2_PLACEMENT_3D('',#72924,#44692,#44693);
#35780=AXIS2_PLACEMENT_3D('',#72929,#44696,#44697);
#35781=AXIS2_PLACEMENT_3D('',#72930,#44698,#44699);
#35782=AXIS2_PLACEMENT_3D('',#72935,#44702,#44703);
#35783=AXIS2_PLACEMENT_3D('',#72936,#44704,#44705);
#35784=AXIS2_PLACEMENT_3D('',#72941,#44708,#44709);
#35785=AXIS2_PLACEMENT_3D('',#72942,#44710,#44711);
#35786=AXIS2_PLACEMENT_3D('',#72947,#44714,#44715);
#35787=AXIS2_PLACEMENT_3D('',#72948,#44716,#44717);
#35788=AXIS2_PLACEMENT_3D('',#72953,#44720,#44721);
#35789=AXIS2_PLACEMENT_3D('',#72954,#44722,#44723);
#35790=AXIS2_PLACEMENT_3D('',#72959,#44726,#44727);
#35791=AXIS2_PLACEMENT_3D('',#72960,#44728,#44729);
#35792=AXIS2_PLACEMENT_3D('',#72965,#44732,#44733);
#35793=AXIS2_PLACEMENT_3D('',#72966,#44734,#44735);
#35794=AXIS2_PLACEMENT_3D('',#72971,#44738,#44739);
#35795=AXIS2_PLACEMENT_3D('',#72972,#44740,#44741);
#35796=AXIS2_PLACEMENT_3D('',#72977,#44744,#44745);
#35797=AXIS2_PLACEMENT_3D('',#72978,#44746,#44747);
#35798=AXIS2_PLACEMENT_3D('',#72983,#44750,#44751);
#35799=AXIS2_PLACEMENT_3D('',#72984,#44752,#44753);
#35800=AXIS2_PLACEMENT_3D('',#72989,#44756,#44757);
#35801=AXIS2_PLACEMENT_3D('',#72990,#44758,#44759);
#35802=AXIS2_PLACEMENT_3D('',#72995,#44762,#44763);
#35803=AXIS2_PLACEMENT_3D('',#72996,#44764,#44765);
#35804=AXIS2_PLACEMENT_3D('',#73001,#44768,#44769);
#35805=AXIS2_PLACEMENT_3D('',#73002,#44770,#44771);
#35806=AXIS2_PLACEMENT_3D('',#73007,#44774,#44775);
#35807=AXIS2_PLACEMENT_3D('',#73008,#44776,#44777);
#35808=AXIS2_PLACEMENT_3D('',#73013,#44780,#44781);
#35809=AXIS2_PLACEMENT_3D('',#73014,#44782,#44783);
#35810=AXIS2_PLACEMENT_3D('',#73019,#44786,#44787);
#35811=AXIS2_PLACEMENT_3D('',#73020,#44788,#44789);
#35812=AXIS2_PLACEMENT_3D('',#73025,#44792,#44793);
#35813=AXIS2_PLACEMENT_3D('',#73026,#44794,#44795);
#35814=AXIS2_PLACEMENT_3D('',#73031,#44798,#44799);
#35815=AXIS2_PLACEMENT_3D('',#73032,#44800,#44801);
#35816=AXIS2_PLACEMENT_3D('',#73037,#44804,#44805);
#35817=AXIS2_PLACEMENT_3D('',#73038,#44806,#44807);
#35818=AXIS2_PLACEMENT_3D('',#73043,#44810,#44811);
#35819=AXIS2_PLACEMENT_3D('',#73044,#44812,#44813);
#35820=AXIS2_PLACEMENT_3D('',#73049,#44816,#44817);
#35821=AXIS2_PLACEMENT_3D('',#73050,#44818,#44819);
#35822=AXIS2_PLACEMENT_3D('',#73055,#44822,#44823);
#35823=AXIS2_PLACEMENT_3D('',#73056,#44824,#44825);
#35824=AXIS2_PLACEMENT_3D('',#73061,#44828,#44829);
#35825=AXIS2_PLACEMENT_3D('',#73062,#44830,#44831);
#35826=AXIS2_PLACEMENT_3D('',#73066,#44833,#44834);
#35827=AXIS2_PLACEMENT_3D('',#73068,#44836,#44837);
#35828=AXIS2_PLACEMENT_3D('',#73072,#44839,#44840);
#35829=AXIS2_PLACEMENT_3D('',#73074,#44842,#44843);
#35830=AXIS2_PLACEMENT_3D('',#73078,#44845,#44846);
#35831=AXIS2_PLACEMENT_3D('',#73080,#44848,#44849);
#35832=AXIS2_PLACEMENT_3D('',#73084,#44851,#44852);
#35833=AXIS2_PLACEMENT_3D('',#73086,#44854,#44855);
#35834=AXIS2_PLACEMENT_3D('',#73090,#44857,#44858);
#35835=AXIS2_PLACEMENT_3D('',#73092,#44860,#44861);
#35836=AXIS2_PLACEMENT_3D('',#73096,#44863,#44864);
#35837=AXIS2_PLACEMENT_3D('',#73098,#44866,#44867);
#35838=AXIS2_PLACEMENT_3D('',#73102,#44869,#44870);
#35839=AXIS2_PLACEMENT_3D('',#73104,#44872,#44873);
#35840=AXIS2_PLACEMENT_3D('',#73108,#44875,#44876);
#35841=AXIS2_PLACEMENT_3D('',#73110,#44878,#44879);
#35842=AXIS2_PLACEMENT_3D('',#73114,#44881,#44882);
#35843=AXIS2_PLACEMENT_3D('',#73116,#44884,#44885);
#35844=AXIS2_PLACEMENT_3D('',#73120,#44887,#44888);
#35845=AXIS2_PLACEMENT_3D('',#73122,#44890,#44891);
#35846=AXIS2_PLACEMENT_3D('',#73126,#44893,#44894);
#35847=AXIS2_PLACEMENT_3D('',#73128,#44896,#44897);
#35848=AXIS2_PLACEMENT_3D('',#73132,#44899,#44900);
#35849=AXIS2_PLACEMENT_3D('',#73134,#44902,#44903);
#35850=AXIS2_PLACEMENT_3D('',#73138,#44905,#44906);
#35851=AXIS2_PLACEMENT_3D('',#73140,#44908,#44909);
#35852=AXIS2_PLACEMENT_3D('',#73144,#44911,#44912);
#35853=AXIS2_PLACEMENT_3D('',#73146,#44914,#44915);
#35854=AXIS2_PLACEMENT_3D('',#73151,#44918,#44919);
#35855=AXIS2_PLACEMENT_3D('',#73152,#44920,#44921);
#35856=AXIS2_PLACEMENT_3D('',#73153,#44922,#44923);
#35857=AXIS2_PLACEMENT_3D('',#73154,#44924,#44925);
#35858=AXIS2_PLACEMENT_3D('',#73155,#44926,#44927);
#35859=AXIS2_PLACEMENT_3D('',#73156,#44928,#44929);
#35860=AXIS2_PLACEMENT_3D('',#73157,#44930,#44931);
#35861=AXIS2_PLACEMENT_3D('',#73158,#44932,#44933);
#35862=AXIS2_PLACEMENT_3D('',#73159,#44934,#44935);
#35863=AXIS2_PLACEMENT_3D('',#73160,#44936,#44937);
#35864=AXIS2_PLACEMENT_3D('',#73161,#44938,#44939);
#35865=AXIS2_PLACEMENT_3D('',#73162,#44940,#44941);
#35866=AXIS2_PLACEMENT_3D('',#73163,#44942,#44943);
#35867=AXIS2_PLACEMENT_3D('',#73164,#44944,#44945);
#35868=AXIS2_PLACEMENT_3D('',#73165,#44946,#44947);
#35869=AXIS2_PLACEMENT_3D('',#73166,#44948,#44949);
#35870=AXIS2_PLACEMENT_3D('',#73167,#44950,#44951);
#35871=AXIS2_PLACEMENT_3D('',#73168,#44952,#44953);
#35872=AXIS2_PLACEMENT_3D('',#73169,#44954,#44955);
#35873=AXIS2_PLACEMENT_3D('',#73170,#44956,#44957);
#35874=AXIS2_PLACEMENT_3D('',#73171,#44958,#44959);
#35875=AXIS2_PLACEMENT_3D('',#73172,#44960,#44961);
#35876=AXIS2_PLACEMENT_3D('',#73173,#44962,#44963);
#35877=AXIS2_PLACEMENT_3D('',#73174,#44964,#44965);
#35878=AXIS2_PLACEMENT_3D('',#73175,#44966,#44967);
#35879=AXIS2_PLACEMENT_3D('',#73176,#44968,#44969);
#35880=AXIS2_PLACEMENT_3D('',#73177,#44970,#44971);
#35881=AXIS2_PLACEMENT_3D('',#73178,#44972,#44973);
#35882=AXIS2_PLACEMENT_3D('',#73179,#44974,#44975);
#35883=AXIS2_PLACEMENT_3D('',#73180,#44976,#44977);
#35884=AXIS2_PLACEMENT_3D('',#73181,#44978,#44979);
#35885=AXIS2_PLACEMENT_3D('',#73182,#44980,#44981);
#35886=AXIS2_PLACEMENT_3D('',#73183,#44982,#44983);
#35887=AXIS2_PLACEMENT_3D('',#73184,#44984,#44985);
#35888=AXIS2_PLACEMENT_3D('',#73185,#44986,#44987);
#35889=AXIS2_PLACEMENT_3D('',#73186,#44988,#44989);
#35890=AXIS2_PLACEMENT_3D('',#73187,#44990,#44991);
#35891=AXIS2_PLACEMENT_3D('',#73188,#44992,#44993);
#35892=AXIS2_PLACEMENT_3D('',#73189,#44994,#44995);
#35893=AXIS2_PLACEMENT_3D('',#73190,#44996,#44997);
#35894=AXIS2_PLACEMENT_3D('',#73191,#44998,#44999);
#35895=AXIS2_PLACEMENT_3D('',#73192,#45000,#45001);
#35896=AXIS2_PLACEMENT_3D('',#73193,#45002,#45003);
#35897=AXIS2_PLACEMENT_3D('',#73194,#45004,#45005);
#35898=AXIS2_PLACEMENT_3D('',#73195,#45006,#45007);
#35899=AXIS2_PLACEMENT_3D('',#73196,#45008,#45009);
#35900=AXIS2_PLACEMENT_3D('',#73197,#45010,#45011);
#35901=AXIS2_PLACEMENT_3D('',#73198,#45012,#45013);
#35902=AXIS2_PLACEMENT_3D('',#73199,#45014,#45015);
#35903=AXIS2_PLACEMENT_3D('',#73200,#45016,#45017);
#35904=AXIS2_PLACEMENT_3D('',#73201,#45018,#45019);
#35905=AXIS2_PLACEMENT_3D('',#73202,#45020,#45021);
#35906=AXIS2_PLACEMENT_3D('',#73203,#45022,#45023);
#35907=AXIS2_PLACEMENT_3D('',#73204,#45024,#45025);
#35908=AXIS2_PLACEMENT_3D('',#73205,#45026,#45027);
#35909=AXIS2_PLACEMENT_3D('',#73206,#45028,#45029);
#35910=AXIS2_PLACEMENT_3D('',#73207,#45030,#45031);
#35911=AXIS2_PLACEMENT_3D('',#73208,#45032,#45033);
#35912=AXIS2_PLACEMENT_3D('',#73209,#45034,#45035);
#35913=AXIS2_PLACEMENT_3D('',#73210,#45036,#45037);
#35914=AXIS2_PLACEMENT_3D('',#73211,#45038,#45039);
#35915=AXIS2_PLACEMENT_3D('',#73212,#45040,#45041);
#35916=AXIS2_PLACEMENT_3D('',#73213,#45042,#45043);
#35917=AXIS2_PLACEMENT_3D('',#73214,#45044,#45045);
#35918=AXIS2_PLACEMENT_3D('',#73215,#45046,#45047);
#35919=AXIS2_PLACEMENT_3D('',#73216,#45048,#45049);
#35920=AXIS2_PLACEMENT_3D('',#73217,#45050,#45051);
#35921=AXIS2_PLACEMENT_3D('',#73218,#45052,#45053);
#35922=AXIS2_PLACEMENT_3D('',#73219,#45054,#45055);
#35923=AXIS2_PLACEMENT_3D('',#73220,#45056,#45057);
#35924=AXIS2_PLACEMENT_3D('',#73221,#45058,#45059);
#35925=AXIS2_PLACEMENT_3D('',#73222,#45060,#45061);
#35926=AXIS2_PLACEMENT_3D('',#73223,#45062,#45063);
#35927=AXIS2_PLACEMENT_3D('',#73224,#45064,#45065);
#35928=AXIS2_PLACEMENT_3D('',#73225,#45066,#45067);
#35929=AXIS2_PLACEMENT_3D('',#73226,#45068,#45069);
#35930=AXIS2_PLACEMENT_3D('',#73227,#45070,#45071);
#35931=AXIS2_PLACEMENT_3D('',#73228,#45072,#45073);
#35932=AXIS2_PLACEMENT_3D('',#73229,#45074,#45075);
#35933=AXIS2_PLACEMENT_3D('',#73230,#45076,#45077);
#35934=AXIS2_PLACEMENT_3D('',#73231,#45078,#45079);
#35935=AXIS2_PLACEMENT_3D('',#73232,#45080,#45081);
#35936=AXIS2_PLACEMENT_3D('',#73233,#45082,#45083);
#35937=AXIS2_PLACEMENT_3D('',#73234,#45084,#45085);
#35938=AXIS2_PLACEMENT_3D('',#73235,#45086,#45087);
#35939=AXIS2_PLACEMENT_3D('',#73236,#45088,#45089);
#35940=AXIS2_PLACEMENT_3D('',#73237,#45090,#45091);
#35941=AXIS2_PLACEMENT_3D('',#73238,#45092,#45093);
#35942=AXIS2_PLACEMENT_3D('',#73239,#45094,#45095);
#35943=AXIS2_PLACEMENT_3D('',#73240,#45096,#45097);
#35944=AXIS2_PLACEMENT_3D('',#73241,#45098,#45099);
#35945=AXIS2_PLACEMENT_3D('',#73242,#45100,#45101);
#35946=AXIS2_PLACEMENT_3D('',#73243,#45102,#45103);
#35947=AXIS2_PLACEMENT_3D('',#73244,#45104,#45105);
#35948=AXIS2_PLACEMENT_3D('',#73245,#45106,#45107);
#35949=AXIS2_PLACEMENT_3D('',#73246,#45108,#45109);
#35950=AXIS2_PLACEMENT_3D('',#73247,#45110,#45111);
#35951=AXIS2_PLACEMENT_3D('',#73248,#45112,#45113);
#35952=AXIS2_PLACEMENT_3D('',#73249,#45114,#45115);
#35953=AXIS2_PLACEMENT_3D('',#73250,#45116,#45117);
#35954=AXIS2_PLACEMENT_3D('',#73251,#45118,#45119);
#35955=AXIS2_PLACEMENT_3D('',#73252,#45120,#45121);
#35956=AXIS2_PLACEMENT_3D('',#73253,#45122,#45123);
#35957=AXIS2_PLACEMENT_3D('',#73254,#45124,#45125);
#35958=AXIS2_PLACEMENT_3D('',#73255,#45126,#45127);
#35959=AXIS2_PLACEMENT_3D('',#73256,#45128,#45129);
#35960=AXIS2_PLACEMENT_3D('',#73257,#45130,#45131);
#35961=AXIS2_PLACEMENT_3D('',#73258,#45132,#45133);
#35962=AXIS2_PLACEMENT_3D('',#73259,#45134,#45135);
#35963=AXIS2_PLACEMENT_3D('',#73260,#45136,#45137);
#35964=AXIS2_PLACEMENT_3D('',#73261,#45138,#45139);
#35965=AXIS2_PLACEMENT_3D('',#73262,#45140,#45141);
#35966=AXIS2_PLACEMENT_3D('',#73263,#45142,#45143);
#35967=AXIS2_PLACEMENT_3D('',#73264,#45144,#45145);
#35968=AXIS2_PLACEMENT_3D('',#73265,#45146,#45147);
#35969=AXIS2_PLACEMENT_3D('',#73266,#45148,#45149);
#35970=AXIS2_PLACEMENT_3D('',#73267,#45150,#45151);
#35971=AXIS2_PLACEMENT_3D('',#73268,#45152,#45153);
#35972=AXIS2_PLACEMENT_3D('',#73269,#45154,#45155);
#35973=AXIS2_PLACEMENT_3D('',#73270,#45156,#45157);
#35974=AXIS2_PLACEMENT_3D('',#73271,#45158,#45159);
#35975=AXIS2_PLACEMENT_3D('',#73272,#45160,#45161);
#35976=AXIS2_PLACEMENT_3D('',#73273,#45162,#45163);
#35977=AXIS2_PLACEMENT_3D('',#73274,#45164,#45165);
#35978=AXIS2_PLACEMENT_3D('',#73275,#45166,#45167);
#35979=AXIS2_PLACEMENT_3D('',#73276,#45168,#45169);
#35980=AXIS2_PLACEMENT_3D('',#73277,#45170,#45171);
#35981=AXIS2_PLACEMENT_3D('',#73278,#45172,#45173);
#35982=AXIS2_PLACEMENT_3D('',#73279,#45174,#45175);
#35983=AXIS2_PLACEMENT_3D('',#73280,#45176,#45177);
#35984=AXIS2_PLACEMENT_3D('',#73281,#45178,#45179);
#35985=AXIS2_PLACEMENT_3D('',#73282,#45180,#45181);
#35986=AXIS2_PLACEMENT_3D('',#73283,#45182,#45183);
#35987=AXIS2_PLACEMENT_3D('',#73284,#45184,#45185);
#35988=AXIS2_PLACEMENT_3D('',#73285,#45186,#45187);
#35989=AXIS2_PLACEMENT_3D('',#73286,#45188,#45189);
#35990=AXIS2_PLACEMENT_3D('',#73287,#45190,#45191);
#35991=AXIS2_PLACEMENT_3D('',#73288,#45192,#45193);
#35992=AXIS2_PLACEMENT_3D('',#73289,#45194,#45195);
#35993=AXIS2_PLACEMENT_3D('',#73290,#45196,#45197);
#35994=AXIS2_PLACEMENT_3D('',#73291,#45198,#45199);
#35995=AXIS2_PLACEMENT_3D('',#73292,#45200,#45201);
#35996=AXIS2_PLACEMENT_3D('',#73293,#45202,#45203);
#35997=AXIS2_PLACEMENT_3D('',#73294,#45204,#45205);
#35998=AXIS2_PLACEMENT_3D('',#73295,#45206,#45207);
#35999=AXIS2_PLACEMENT_3D('',#73296,#45208,#45209);
#36000=AXIS2_PLACEMENT_3D('',#73297,#45210,#45211);
#36001=AXIS2_PLACEMENT_3D('',#73298,#45212,#45213);
#36002=AXIS2_PLACEMENT_3D('',#73299,#45214,#45215);
#36003=AXIS2_PLACEMENT_3D('',#73300,#45216,#45217);
#36004=AXIS2_PLACEMENT_3D('',#73301,#45218,#45219);
#36005=AXIS2_PLACEMENT_3D('',#73302,#45220,#45221);
#36006=AXIS2_PLACEMENT_3D('',#73303,#45222,#45223);
#36007=AXIS2_PLACEMENT_3D('',#73304,#45224,#45225);
#36008=AXIS2_PLACEMENT_3D('',#73305,#45226,#45227);
#36009=AXIS2_PLACEMENT_3D('',#73306,#45228,#45229);
#36010=AXIS2_PLACEMENT_3D('',#73307,#45230,#45231);
#36011=AXIS2_PLACEMENT_3D('',#73308,#45232,#45233);
#36012=AXIS2_PLACEMENT_3D('',#73309,#45234,#45235);
#36013=AXIS2_PLACEMENT_3D('',#73310,#45236,#45237);
#36014=AXIS2_PLACEMENT_3D('',#73311,#45238,#45239);
#36015=AXIS2_PLACEMENT_3D('',#73312,#45240,#45241);
#36016=AXIS2_PLACEMENT_3D('',#73313,#45242,#45243);
#36017=AXIS2_PLACEMENT_3D('',#73314,#45244,#45245);
#36018=AXIS2_PLACEMENT_3D('',#73315,#45246,#45247);
#36019=AXIS2_PLACEMENT_3D('',#73316,#45248,#45249);
#36020=AXIS2_PLACEMENT_3D('',#73317,#45250,#45251);
#36021=AXIS2_PLACEMENT_3D('',#73318,#45252,#45253);
#36022=AXIS2_PLACEMENT_3D('',#73319,#45254,#45255);
#36023=AXIS2_PLACEMENT_3D('',#73320,#45256,#45257);
#36024=AXIS2_PLACEMENT_3D('',#73321,#45258,#45259);
#36025=AXIS2_PLACEMENT_3D('',#73322,#45260,#45261);
#36026=AXIS2_PLACEMENT_3D('',#73323,#45262,#45263);
#36027=AXIS2_PLACEMENT_3D('',#73324,#45264,#45265);
#36028=AXIS2_PLACEMENT_3D('',#73325,#45266,#45267);
#36029=AXIS2_PLACEMENT_3D('',#73326,#45268,#45269);
#36030=AXIS2_PLACEMENT_3D('',#73327,#45270,#45271);
#36031=AXIS2_PLACEMENT_3D('',#73328,#45272,#45273);
#36032=AXIS2_PLACEMENT_3D('',#73329,#45274,#45275);
#36033=AXIS2_PLACEMENT_3D('',#73330,#45276,#45277);
#36034=AXIS2_PLACEMENT_3D('',#73331,#45278,#45279);
#36035=AXIS2_PLACEMENT_3D('',#73332,#45280,#45281);
#36036=AXIS2_PLACEMENT_3D('',#73333,#45282,#45283);
#36037=AXIS2_PLACEMENT_3D('',#73334,#45284,#45285);
#36038=AXIS2_PLACEMENT_3D('',#73335,#45286,#45287);
#36039=AXIS2_PLACEMENT_3D('',#73336,#45288,#45289);
#36040=AXIS2_PLACEMENT_3D('',#73337,#45290,#45291);
#36041=AXIS2_PLACEMENT_3D('',#73338,#45292,#45293);
#36042=AXIS2_PLACEMENT_3D('',#73339,#45294,#45295);
#36043=AXIS2_PLACEMENT_3D('',#73340,#45296,#45297);
#36044=AXIS2_PLACEMENT_3D('',#73341,#45298,#45299);
#36045=AXIS2_PLACEMENT_3D('',#73342,#45300,#45301);
#36046=AXIS2_PLACEMENT_3D('',#73343,#45302,#45303);
#36047=AXIS2_PLACEMENT_3D('',#73344,#45304,#45305);
#36048=AXIS2_PLACEMENT_3D('',#73345,#45306,#45307);
#36049=AXIS2_PLACEMENT_3D('',#73346,#45308,#45309);
#36050=AXIS2_PLACEMENT_3D('',#73347,#45310,#45311);
#36051=AXIS2_PLACEMENT_3D('',#73348,#45312,#45313);
#36052=AXIS2_PLACEMENT_3D('',#73349,#45314,#45315);
#36053=AXIS2_PLACEMENT_3D('',#73350,#45316,#45317);
#36054=AXIS2_PLACEMENT_3D('',#73351,#45318,#45319);
#36055=AXIS2_PLACEMENT_3D('',#73352,#45320,#45321);
#36056=AXIS2_PLACEMENT_3D('',#73353,#45322,#45323);
#36057=AXIS2_PLACEMENT_3D('',#73354,#45324,#45325);
#36058=AXIS2_PLACEMENT_3D('',#73355,#45326,#45327);
#36059=AXIS2_PLACEMENT_3D('',#73356,#45328,#45329);
#36060=AXIS2_PLACEMENT_3D('',#73357,#45330,#45331);
#36061=AXIS2_PLACEMENT_3D('',#73358,#45332,#45333);
#36062=AXIS2_PLACEMENT_3D('',#73359,#45334,#45335);
#36063=AXIS2_PLACEMENT_3D('',#73360,#45336,#45337);
#36064=AXIS2_PLACEMENT_3D('',#73361,#45338,#45339);
#36065=AXIS2_PLACEMENT_3D('',#73362,#45340,#45341);
#36066=AXIS2_PLACEMENT_3D('',#73363,#45342,#45343);
#36067=AXIS2_PLACEMENT_3D('',#73364,#45344,#45345);
#36068=AXIS2_PLACEMENT_3D('',#73365,#45346,#45347);
#36069=AXIS2_PLACEMENT_3D('',#73366,#45348,#45349);
#36070=AXIS2_PLACEMENT_3D('',#73367,#45350,#45351);
#36071=AXIS2_PLACEMENT_3D('',#73368,#45352,#45353);
#36072=AXIS2_PLACEMENT_3D('',#73369,#45354,#45355);
#36073=AXIS2_PLACEMENT_3D('',#73370,#45356,#45357);
#36074=AXIS2_PLACEMENT_3D('',#73371,#45358,#45359);
#36075=AXIS2_PLACEMENT_3D('',#73372,#45360,#45361);
#36076=AXIS2_PLACEMENT_3D('',#73373,#45362,#45363);
#36077=AXIS2_PLACEMENT_3D('',#73374,#45364,#45365);
#36078=AXIS2_PLACEMENT_3D('',#73375,#45366,#45367);
#36079=AXIS2_PLACEMENT_3D('',#73376,#45368,#45369);
#36080=AXIS2_PLACEMENT_3D('',#73377,#45370,#45371);
#36081=AXIS2_PLACEMENT_3D('',#73378,#45372,#45373);
#36082=AXIS2_PLACEMENT_3D('',#73379,#45374,#45375);
#36083=AXIS2_PLACEMENT_3D('',#73380,#45376,#45377);
#36084=AXIS2_PLACEMENT_3D('',#73381,#45378,#45379);
#36085=AXIS2_PLACEMENT_3D('',#73382,#45380,#45381);
#36086=AXIS2_PLACEMENT_3D('',#73383,#45382,#45383);
#36087=AXIS2_PLACEMENT_3D('',#73384,#45384,#45385);
#36088=AXIS2_PLACEMENT_3D('',#73385,#45386,#45387);
#36089=AXIS2_PLACEMENT_3D('',#73386,#45388,#45389);
#36090=AXIS2_PLACEMENT_3D('',#73387,#45390,#45391);
#36091=AXIS2_PLACEMENT_3D('',#73388,#45392,#45393);
#36092=AXIS2_PLACEMENT_3D('',#73389,#45394,#45395);
#36093=AXIS2_PLACEMENT_3D('',#73390,#45396,#45397);
#36094=AXIS2_PLACEMENT_3D('',#73391,#45398,#45399);
#36095=AXIS2_PLACEMENT_3D('',#73393,#45400,#45401);
#36096=AXIS2_PLACEMENT_3D('',#73395,#45402,#45403);
#36097=AXIS2_PLACEMENT_3D('',#73396,#45404,#45405);
#36098=AXIS2_PLACEMENT_3D('',#73397,#45406,#45407);
#36099=AXIS2_PLACEMENT_3D('',#73402,#45410,#45411);
#36100=AXIS2_PLACEMENT_3D('',#73403,#45412,#45413);
#36101=AXIS2_PLACEMENT_3D('',#73404,#45414,#45415);
#36102=AXIS2_PLACEMENT_3D('',#73405,#45416,#45417);
#36103=AXIS2_PLACEMENT_3D('',#73406,#45418,#45419);
#36104=AXIS2_PLACEMENT_3D('',#73407,#45420,#45421);
#36105=AXIS2_PLACEMENT_3D('',#73420,#45428,#45429);
#36106=AXIS2_PLACEMENT_3D('',#73423,#45432,#45433);
#36107=AXIS2_PLACEMENT_3D('',#73425,#45435,#45436);
#36108=AXIS2_PLACEMENT_3D('',#73427,#45438,#45439);
#36109=AXIS2_PLACEMENT_3D('',#73429,#45441,#45442);
#36110=AXIS2_PLACEMENT_3D('',#73431,#45444,#45445);
#36111=AXIS2_PLACEMENT_3D('',#74953,#45447,#45448);
#36112=AXIS2_PLACEMENT_3D('',#74954,#45449,#45450);
#36113=AXIS2_PLACEMENT_3D('',#74956,#45452,#45453);
#36114=AXIS2_PLACEMENT_3D('',#74958,#45455,#45456);
#36115=AXIS2_PLACEMENT_3D('',#74959,#45457,#45458);
#36116=AXIS2_PLACEMENT_3D('',#74961,#45460,#45461);
#36117=AXIS2_PLACEMENT_3D('',#74963,#45463,#45464);
#36118=AXIS2_PLACEMENT_3D('',#74964,#45465,#45466);
#36119=AXIS2_PLACEMENT_3D('',#74966,#45468,#45469);
#36120=AXIS2_PLACEMENT_3D('',#74968,#45471,#45472);
#36121=AXIS2_PLACEMENT_3D('',#74969,#45473,#45474);
#36122=AXIS2_PLACEMENT_3D('',#74971,#45476,#45477);
#36123=AXIS2_PLACEMENT_3D('',#74973,#45479,#45480);
#36124=AXIS2_PLACEMENT_3D('',#74974,#45481,#45482);
#36125=AXIS2_PLACEMENT_3D('',#74976,#45484,#45485);
#36126=AXIS2_PLACEMENT_3D('',#74978,#45487,#45488);
#36127=AXIS2_PLACEMENT_3D('',#74979,#45489,#45490);
#36128=AXIS2_PLACEMENT_3D('',#74981,#45492,#45493);
#36129=AXIS2_PLACEMENT_3D('',#74983,#45495,#45496);
#36130=AXIS2_PLACEMENT_3D('',#74984,#45497,#45498);
#36131=AXIS2_PLACEMENT_3D('',#74986,#45500,#45501);
#36132=AXIS2_PLACEMENT_3D('',#74988,#45503,#45504);
#36133=AXIS2_PLACEMENT_3D('',#74989,#45505,#45506);
#36134=AXIS2_PLACEMENT_3D('',#74990,#45507,#45508);
#36135=AXIS2_PLACEMENT_3D('',#74991,#45509,#45510);
#36136=AXIS2_PLACEMENT_3D('',#74992,#45511,#45512);
#36137=AXIS2_PLACEMENT_3D('',#74993,#45513,#45514);
#36138=AXIS2_PLACEMENT_3D('',#74994,#45515,#45516);
#36139=AXIS2_PLACEMENT_3D('',#74995,#45517,#45518);
#36140=AXIS2_PLACEMENT_3D('',#74996,#45519,#45520);
#36141=AXIS2_PLACEMENT_3D('',#74997,#45521,#45522);
#36142=AXIS2_PLACEMENT_3D('',#74998,#45523,#45524);
#36143=AXIS2_PLACEMENT_3D('',#74999,#45525,#45526);
#36144=AXIS2_PLACEMENT_3D('',#75000,#45527,#45528);
#36145=AXIS2_PLACEMENT_3D('',#75001,#45529,#45530);
#36146=AXIS2_PLACEMENT_3D('',#75002,#45531,#45532);
#36147=AXIS2_PLACEMENT_3D('',#75003,#45533,#45534);
#36148=AXIS2_PLACEMENT_3D('',#75004,#45535,#45536);
#36149=AXIS2_PLACEMENT_3D('',#75005,#45537,#45538);
#36150=AXIS2_PLACEMENT_3D('',#75006,#45539,#45540);
#36151=AXIS2_PLACEMENT_3D('',#75007,#45541,#45542);
#36152=AXIS2_PLACEMENT_3D('',#75009,#45544,#45545);
#36153=AXIS2_PLACEMENT_3D('',#75011,#45547,#45548);
#36154=AXIS2_PLACEMENT_3D('',#75012,#45549,#45550);
#36155=AXIS2_PLACEMENT_3D('',#75014,#45552,#45553);
#36156=AXIS2_PLACEMENT_3D('',#75016,#45555,#45556);
#36157=AXIS2_PLACEMENT_3D('',#75017,#45557,#45558);
#36158=AXIS2_PLACEMENT_3D('',#75019,#45560,#45561);
#36159=AXIS2_PLACEMENT_3D('',#75021,#45563,#45564);
#36160=AXIS2_PLACEMENT_3D('',#75022,#45565,#45566);
#36161=AXIS2_PLACEMENT_3D('',#75024,#45568,#45569);
#36162=AXIS2_PLACEMENT_3D('',#75026,#45571,#45572);
#36163=AXIS2_PLACEMENT_3D('',#75027,#45573,#45574);
#36164=AXIS2_PLACEMENT_3D('',#75029,#45576,#45577);
#36165=AXIS2_PLACEMENT_3D('',#75031,#45579,#45580);
#36166=AXIS2_PLACEMENT_3D('',#75032,#45581,#45582);
#36167=AXIS2_PLACEMENT_3D('',#75034,#45584,#45585);
#36168=AXIS2_PLACEMENT_3D('',#75036,#45587,#45588);
#36169=AXIS2_PLACEMENT_3D('',#75037,#45589,#45590);
#36170=AXIS2_PLACEMENT_3D('',#75039,#45592,#45593);
#36171=AXIS2_PLACEMENT_3D('',#75041,#45595,#45596);
#36172=AXIS2_PLACEMENT_3D('',#75042,#45597,#45598);
#36173=AXIS2_PLACEMENT_3D('',#75044,#45600,#45601);
#36174=AXIS2_PLACEMENT_3D('',#75046,#45603,#45604);
#36175=AXIS2_PLACEMENT_3D('',#75047,#45605,#45606);
#36176=AXIS2_PLACEMENT_3D('',#75049,#45608,#45609);
#36177=AXIS2_PLACEMENT_3D('',#75051,#45611,#45612);
#36178=AXIS2_PLACEMENT_3D('',#75052,#45613,#45614);
#36179=AXIS2_PLACEMENT_3D('',#75054,#45616,#45617);
#36180=AXIS2_PLACEMENT_3D('',#75056,#45619,#45620);
#36181=AXIS2_PLACEMENT_3D('',#75057,#45621,#45622);
#36182=AXIS2_PLACEMENT_3D('',#75059,#45624,#45625);
#36183=AXIS2_PLACEMENT_3D('',#75061,#45627,#45628);
#36184=AXIS2_PLACEMENT_3D('',#75062,#45629,#45630);
#36185=AXIS2_PLACEMENT_3D('',#75064,#45632,#45633);
#36186=AXIS2_PLACEMENT_3D('',#75066,#45635,#45636);
#36187=AXIS2_PLACEMENT_3D('',#75067,#45637,#45638);
#36188=AXIS2_PLACEMENT_3D('',#75069,#45640,#45641);
#36189=AXIS2_PLACEMENT_3D('',#75071,#45643,#45644);
#36190=AXIS2_PLACEMENT_3D('',#75072,#45645,#45646);
#36191=AXIS2_PLACEMENT_3D('',#75074,#45648,#45649);
#36192=AXIS2_PLACEMENT_3D('',#75076,#45651,#45652);
#36193=AXIS2_PLACEMENT_3D('',#75077,#45653,#45654);
#36194=AXIS2_PLACEMENT_3D('',#75079,#45656,#45657);
#36195=AXIS2_PLACEMENT_3D('',#75081,#45659,#45660);
#36196=AXIS2_PLACEMENT_3D('',#75082,#45661,#45662);
#36197=AXIS2_PLACEMENT_3D('',#75084,#45664,#45665);
#36198=AXIS2_PLACEMENT_3D('',#75086,#45667,#45668);
#36199=AXIS2_PLACEMENT_3D('',#75087,#45669,#45670);
#36200=AXIS2_PLACEMENT_3D('',#75089,#45672,#45673);
#36201=AXIS2_PLACEMENT_3D('',#75091,#45675,#45676);
#36202=AXIS2_PLACEMENT_3D('',#75092,#45677,#45678);
#36203=AXIS2_PLACEMENT_3D('',#75094,#45680,#45681);
#36204=AXIS2_PLACEMENT_3D('',#75096,#45683,#45684);
#36205=AXIS2_PLACEMENT_3D('',#75097,#45685,#45686);
#36206=AXIS2_PLACEMENT_3D('',#75099,#45688,#45689);
#36207=AXIS2_PLACEMENT_3D('',#75101,#45691,#45692);
#36208=AXIS2_PLACEMENT_3D('',#75102,#45693,#45694);
#36209=AXIS2_PLACEMENT_3D('',#75104,#45696,#45697);
#36210=AXIS2_PLACEMENT_3D('',#75106,#45699,#45700);
#36211=AXIS2_PLACEMENT_3D('',#75107,#45701,#45702);
#36212=AXIS2_PLACEMENT_3D('',#75109,#45704,#45705);
#36213=AXIS2_PLACEMENT_3D('',#75111,#45707,#45708);
#36214=AXIS2_PLACEMENT_3D('',#75112,#45709,#45710);
#36215=AXIS2_PLACEMENT_3D('',#75114,#45712,#45713);
#36216=AXIS2_PLACEMENT_3D('',#75116,#45715,#45716);
#36217=AXIS2_PLACEMENT_3D('',#75117,#45717,#45718);
#36218=AXIS2_PLACEMENT_3D('',#75119,#45720,#45721);
#36219=AXIS2_PLACEMENT_3D('',#75121,#45723,#45724);
#36220=AXIS2_PLACEMENT_3D('',#75122,#45725,#45726);
#36221=AXIS2_PLACEMENT_3D('',#75124,#45728,#45729);
#36222=AXIS2_PLACEMENT_3D('',#75126,#45731,#45732);
#36223=AXIS2_PLACEMENT_3D('',#75127,#45733,#45734);
#36224=AXIS2_PLACEMENT_3D('',#75129,#45736,#45737);
#36225=AXIS2_PLACEMENT_3D('',#75131,#45739,#45740);
#36226=AXIS2_PLACEMENT_3D('',#75132,#45741,#45742);
#36227=AXIS2_PLACEMENT_3D('',#75134,#45744,#45745);
#36228=AXIS2_PLACEMENT_3D('',#75136,#45747,#45748);
#36229=AXIS2_PLACEMENT_3D('',#75137,#45749,#45750);
#36230=AXIS2_PLACEMENT_3D('',#75139,#45752,#45753);
#36231=AXIS2_PLACEMENT_3D('',#75141,#45755,#45756);
#36232=AXIS2_PLACEMENT_3D('',#75142,#45757,#45758);
#36233=AXIS2_PLACEMENT_3D('',#75144,#45760,#45761);
#36234=AXIS2_PLACEMENT_3D('',#75146,#45763,#45764);
#36235=AXIS2_PLACEMENT_3D('',#75147,#45765,#45766);
#36236=AXIS2_PLACEMENT_3D('',#75149,#45768,#45769);
#36237=AXIS2_PLACEMENT_3D('',#75151,#45771,#45772);
#36238=AXIS2_PLACEMENT_3D('',#75152,#45773,#45774);
#36239=AXIS2_PLACEMENT_3D('',#75154,#45776,#45777);
#36240=AXIS2_PLACEMENT_3D('',#75156,#45779,#45780);
#36241=AXIS2_PLACEMENT_3D('',#75157,#45781,#45782);
#36242=AXIS2_PLACEMENT_3D('',#75159,#45784,#45785);
#36243=AXIS2_PLACEMENT_3D('',#75161,#45787,#45788);
#36244=AXIS2_PLACEMENT_3D('',#75162,#45789,#45790);
#36245=AXIS2_PLACEMENT_3D('',#75164,#45792,#45793);
#36246=AXIS2_PLACEMENT_3D('',#75166,#45795,#45796);
#36247=AXIS2_PLACEMENT_3D('',#75167,#45797,#45798);
#36248=AXIS2_PLACEMENT_3D('',#75169,#45800,#45801);
#36249=AXIS2_PLACEMENT_3D('',#75171,#45803,#45804);
#36250=AXIS2_PLACEMENT_3D('',#75172,#45805,#45806);
#36251=AXIS2_PLACEMENT_3D('',#75174,#45808,#45809);
#36252=AXIS2_PLACEMENT_3D('',#75176,#45811,#45812);
#36253=AXIS2_PLACEMENT_3D('',#75177,#45813,#45814);
#36254=AXIS2_PLACEMENT_3D('',#75179,#45816,#45817);
#36255=AXIS2_PLACEMENT_3D('',#75181,#45819,#45820);
#36256=AXIS2_PLACEMENT_3D('',#75182,#45821,#45822);
#36257=AXIS2_PLACEMENT_3D('',#75184,#45824,#45825);
#36258=AXIS2_PLACEMENT_3D('',#75186,#45827,#45828);
#36259=AXIS2_PLACEMENT_3D('',#75187,#45829,#45830);
#36260=AXIS2_PLACEMENT_3D('',#75189,#45832,#45833);
#36261=AXIS2_PLACEMENT_3D('',#75191,#45835,#45836);
#36262=AXIS2_PLACEMENT_3D('',#75192,#45837,#45838);
#36263=AXIS2_PLACEMENT_3D('',#75194,#45840,#45841);
#36264=AXIS2_PLACEMENT_3D('',#75196,#45843,#45844);
#36265=AXIS2_PLACEMENT_3D('',#75197,#45845,#45846);
#36266=AXIS2_PLACEMENT_3D('',#75199,#45848,#45849);
#36267=AXIS2_PLACEMENT_3D('',#75201,#45851,#45852);
#36268=AXIS2_PLACEMENT_3D('',#75202,#45853,#45854);
#36269=AXIS2_PLACEMENT_3D('',#75204,#45856,#45857);
#36270=AXIS2_PLACEMENT_3D('',#75206,#45859,#45860);
#36271=AXIS2_PLACEMENT_3D('',#75207,#45861,#45862);
#36272=AXIS2_PLACEMENT_3D('',#75209,#45864,#45865);
#36273=AXIS2_PLACEMENT_3D('',#75211,#45867,#45868);
#36274=AXIS2_PLACEMENT_3D('',#75212,#45869,#45870);
#36275=AXIS2_PLACEMENT_3D('',#75214,#45872,#45873);
#36276=AXIS2_PLACEMENT_3D('',#75216,#45875,#45876);
#36277=AXIS2_PLACEMENT_3D('',#75217,#45877,#45878);
#36278=AXIS2_PLACEMENT_3D('',#75219,#45880,#45881);
#36279=AXIS2_PLACEMENT_3D('',#75221,#45883,#45884);
#36280=AXIS2_PLACEMENT_3D('',#75222,#45885,#45886);
#36281=AXIS2_PLACEMENT_3D('',#75224,#45888,#45889);
#36282=AXIS2_PLACEMENT_3D('',#75226,#45891,#45892);
#36283=AXIS2_PLACEMENT_3D('',#75227,#45893,#45894);
#36284=AXIS2_PLACEMENT_3D('',#75229,#45896,#45897);
#36285=AXIS2_PLACEMENT_3D('',#75231,#45899,#45900);
#36286=AXIS2_PLACEMENT_3D('',#75232,#45901,#45902);
#36287=AXIS2_PLACEMENT_3D('',#75234,#45904,#45905);
#36288=AXIS2_PLACEMENT_3D('',#75236,#45907,#45908);
#36289=AXIS2_PLACEMENT_3D('',#75237,#45909,#45910);
#36290=AXIS2_PLACEMENT_3D('',#75239,#45912,#45913);
#36291=AXIS2_PLACEMENT_3D('',#75241,#45915,#45916);
#36292=AXIS2_PLACEMENT_3D('',#75242,#45917,#45918);
#36293=AXIS2_PLACEMENT_3D('',#75244,#45920,#45921);
#36294=AXIS2_PLACEMENT_3D('',#75246,#45923,#45924);
#36295=AXIS2_PLACEMENT_3D('',#75247,#45925,#45926);
#36296=AXIS2_PLACEMENT_3D('',#75249,#45928,#45929);
#36297=AXIS2_PLACEMENT_3D('',#75251,#45931,#45932);
#36298=AXIS2_PLACEMENT_3D('',#75252,#45933,#45934);
#36299=AXIS2_PLACEMENT_3D('',#75254,#45936,#45937);
#36300=AXIS2_PLACEMENT_3D('',#75256,#45939,#45940);
#36301=AXIS2_PLACEMENT_3D('',#75257,#45941,#45942);
#36302=AXIS2_PLACEMENT_3D('',#75259,#45944,#45945);
#36303=AXIS2_PLACEMENT_3D('',#75261,#45947,#45948);
#36304=AXIS2_PLACEMENT_3D('',#75262,#45949,#45950);
#36305=AXIS2_PLACEMENT_3D('',#75264,#45952,#45953);
#36306=AXIS2_PLACEMENT_3D('',#75266,#45955,#45956);
#36307=AXIS2_PLACEMENT_3D('',#75267,#45957,#45958);
#36308=AXIS2_PLACEMENT_3D('',#75269,#45960,#45961);
#36309=AXIS2_PLACEMENT_3D('',#75271,#45963,#45964);
#36310=AXIS2_PLACEMENT_3D('',#75272,#45965,#45966);
#36311=AXIS2_PLACEMENT_3D('',#75274,#45968,#45969);
#36312=AXIS2_PLACEMENT_3D('',#75276,#45971,#45972);
#36313=AXIS2_PLACEMENT_3D('',#75277,#45973,#45974);
#36314=AXIS2_PLACEMENT_3D('',#75279,#45976,#45977);
#36315=AXIS2_PLACEMENT_3D('',#75281,#45979,#45980);
#36316=AXIS2_PLACEMENT_3D('',#75282,#45981,#45982);
#36317=AXIS2_PLACEMENT_3D('',#75284,#45984,#45985);
#36318=AXIS2_PLACEMENT_3D('',#75286,#45987,#45988);
#36319=AXIS2_PLACEMENT_3D('',#75287,#45989,#45990);
#36320=AXIS2_PLACEMENT_3D('',#75289,#45992,#45993);
#36321=AXIS2_PLACEMENT_3D('',#75291,#45995,#45996);
#36322=AXIS2_PLACEMENT_3D('',#75292,#45997,#45998);
#36323=AXIS2_PLACEMENT_3D('',#75294,#46000,#46001);
#36324=AXIS2_PLACEMENT_3D('',#75296,#46003,#46004);
#36325=AXIS2_PLACEMENT_3D('',#75297,#46005,#46006);
#36326=AXIS2_PLACEMENT_3D('',#75298,#46007,#46008);
#36327=AXIS2_PLACEMENT_3D('',#75299,#46009,#46010);
#36328=AXIS2_PLACEMENT_3D('',#75300,#46011,#46012);
#36329=AXIS2_PLACEMENT_3D('',#75301,#46013,#46014);
#36330=AXIS2_PLACEMENT_3D('',#75302,#46015,#46016);
#36331=AXIS2_PLACEMENT_3D('',#75303,#46017,#46018);
#36332=AXIS2_PLACEMENT_3D('',#75304,#46019,#46020);
#36333=AXIS2_PLACEMENT_3D('',#75305,#46021,#46022);
#36334=AXIS2_PLACEMENT_3D('',#75306,#46023,#46024);
#36335=AXIS2_PLACEMENT_3D('',#75307,#46025,#46026);
#36336=AXIS2_PLACEMENT_3D('',#75308,#46027,#46028);
#42872=DIRECTION('axis',(0.,0.,1.));
#42873=DIRECTION('refdir',(1.,0.,0.));
#42874=DIRECTION('center_axis',(5.15167520928809E-67,-1.18789542670764E-48,
-1.));
#42875=DIRECTION('ref_axis',(-4.33680868994202E-19,1.,-1.18789542670764E-48));
#42876=DIRECTION('',(-5.15167520928809E-67,1.18789542670764E-48,1.));
#42877=DIRECTION('',(-5.15167520928809E-67,1.18789542670764E-48,1.));
#42878=DIRECTION('center_axis',(5.15167520928809E-67,-1.18789542670764E-48,
-1.));
#42879=DIRECTION('ref_axis',(-4.33680868994202E-19,1.,-1.18789542670764E-48));
#42880=DIRECTION('center_axis',(-4.70261923768679E-35,1.08435016942139E-16,
-1.));
#42881=DIRECTION('ref_axis',(-4.33680868994202E-19,1.,1.08435016942139E-16));
#42882=DIRECTION('center_axis',(5.15167520928809E-67,-1.18789542670764E-48,
-1.));
#42883=DIRECTION('ref_axis',(-4.33680868994202E-19,1.,-1.18789542670764E-48));
#42884=DIRECTION('',(-5.15167520928809E-67,1.18789542670764E-48,1.));
#42885=DIRECTION('center_axis',(5.15167520928809E-67,-1.18789542670764E-48,
-1.));
#42886=DIRECTION('ref_axis',(-4.33680868994202E-19,1.,-1.18789542670764E-48));
#42887=DIRECTION('',(-5.15167520928809E-67,1.18789542670764E-48,1.));
#42888=DIRECTION('center_axis',(5.15167520928809E-67,-1.18789542670764E-48,
-1.));
#42889=DIRECTION('ref_axis',(-4.33680868994202E-19,1.,-1.18789542670764E-48));
#42890=DIRECTION('',(-5.15167520928809E-67,1.18789542670764E-48,1.));
#42891=DIRECTION('center_axis',(5.15167520928809E-67,-1.18789542670764E-48,
-1.));
#42892=DIRECTION('ref_axis',(-4.33680868994202E-19,1.,-1.18789542670764E-48));
#42893=DIRECTION('',(-5.15167520928809E-67,1.18789542670764E-48,1.));
#42894=DIRECTION('center_axis',(5.15167520928809E-67,-1.18789542670764E-48,
-1.));
#42895=DIRECTION('ref_axis',(-4.33680868994202E-19,1.,-1.18789542670764E-48));
#42896=DIRECTION('',(-5.15167520928809E-67,1.18789542670764E-48,1.));
#42897=DIRECTION('center_axis',(5.15167520928809E-67,-1.18789542670764E-48,
-1.));
#42898=DIRECTION('ref_axis',(-4.33680868994202E-19,1.,-1.18789542670764E-48));
#42899=DIRECTION('',(-5.15167520928809E-67,1.18789542670764E-48,1.));
#42900=DIRECTION('center_axis',(5.15167520928809E-67,-1.18789542670764E-48,
-1.));
#42901=DIRECTION('ref_axis',(-4.33680868994202E-19,1.,-1.18789542670764E-48));
#42902=DIRECTION('',(-5.15167520928809E-67,1.18789542670764E-48,1.));
#42903=DIRECTION('center_axis',(5.15167520928809E-67,-1.18789542670764E-48,
-1.));
#42904=DIRECTION('ref_axis',(-4.33680868994202E-19,1.,-1.18789542670764E-48));
#42905=DIRECTION('',(-5.15167520928809E-67,1.18789542670764E-48,1.));
#42906=DIRECTION('center_axis',(5.15167520928809E-67,-1.18789542670764E-48,
-1.));
#42907=DIRECTION('ref_axis',(-4.33680868994202E-19,1.,-1.18789542670764E-48));
#42908=DIRECTION('',(-5.15167520928809E-67,1.18789542670764E-48,1.));
#42909=DIRECTION('center_axis',(5.15167520928809E-67,-1.18789542670764E-48,
-1.));
#42910=DIRECTION('ref_axis',(-4.33680868994202E-19,1.,-1.18789542670764E-48));
#42911=DIRECTION('',(-5.15167520928809E-67,1.18789542670764E-48,1.));
#42912=DIRECTION('center_axis',(5.15167520928809E-67,-1.18789542670764E-48,
-1.));
#42913=DIRECTION('ref_axis',(-4.33680868994202E-19,1.,-1.18789542670764E-48));
#42914=DIRECTION('',(-5.15167520928809E-67,1.18789542670764E-48,1.));
#42915=DIRECTION('center_axis',(5.15167520928809E-67,-1.18789542670764E-48,
-1.));
#42916=DIRECTION('ref_axis',(-4.33680868994202E-19,1.,-1.18789542670764E-48));
#42917=DIRECTION('',(-5.15167520928809E-67,1.18789542670764E-48,1.));
#42918=DIRECTION('center_axis',(5.15167520928809E-67,-1.18789542670764E-48,
-1.));
#42919=DIRECTION('ref_axis',(-4.33680868994202E-19,1.,-1.18789542670764E-48));
#42920=DIRECTION('',(-5.15167520928809E-67,1.18789542670764E-48,1.));
#42921=DIRECTION('center_axis',(5.15167520928809E-67,-1.18789542670764E-48,
-1.));
#42922=DIRECTION('ref_axis',(-4.33680868994202E-19,1.,-1.18789542670764E-48));
#42923=DIRECTION('',(-5.15167520928809E-67,1.18789542670764E-48,1.));
#42924=DIRECTION('center_axis',(5.15167520928809E-67,-1.18789542670764E-48,
-1.));
#42925=DIRECTION('ref_axis',(-4.33680868994202E-19,1.,-1.18789542670764E-48));
#42926=DIRECTION('',(-5.15167520928809E-67,1.18789542670764E-48,1.));
#42927=DIRECTION('center_axis',(5.15167520928809E-67,-1.18789542670764E-48,
-1.));
#42928=DIRECTION('ref_axis',(-4.33680868994202E-19,1.,-1.18789542670764E-48));
#42929=DIRECTION('',(-5.15167520928809E-67,1.18789542670764E-48,1.));
#42930=DIRECTION('center_axis',(5.15167520928809E-67,-1.18789542670764E-48,
-1.));
#42931=DIRECTION('ref_axis',(-4.33680868994202E-19,1.,-1.18789542670764E-48));
#42932=DIRECTION('',(-5.15167520928809E-67,1.18789542670764E-48,1.));
#42933=DIRECTION('center_axis',(5.15167520928809E-67,-1.18789542670764E-48,
-1.));
#42934=DIRECTION('ref_axis',(-4.33680868994202E-19,1.,-1.18789542670764E-48));
#42935=DIRECTION('',(-5.15167520928809E-67,1.18789542670764E-48,1.));
#42936=DIRECTION('center_axis',(5.15167520928809E-67,-1.18789542670764E-48,
-1.));
#42937=DIRECTION('ref_axis',(-4.33680868994202E-19,1.,-1.18789542670764E-48));
#42938=DIRECTION('',(-5.15167520928809E-67,1.18789542670764E-48,1.));
#42939=DIRECTION('center_axis',(5.15167520928809E-67,-1.18789542670764E-48,
-1.));
#42940=DIRECTION('ref_axis',(-4.33680868994202E-19,1.,-1.18789542670764E-48));
#42941=DIRECTION('',(-5.15167520928809E-67,1.18789542670764E-48,1.));
#42942=DIRECTION('center_axis',(5.15167520928809E-67,-1.18789542670764E-48,
-1.));
#42943=DIRECTION('ref_axis',(-4.33680868994202E-19,1.,-1.18789542670764E-48));
#42944=DIRECTION('',(-5.15167520928809E-67,1.18789542670764E-48,1.));
#42945=DIRECTION('center_axis',(5.15167520928809E-67,-1.18789542670764E-48,
-1.));
#42946=DIRECTION('ref_axis',(-4.33680868994202E-19,1.,-1.18789542670764E-48));
#42947=DIRECTION('',(-5.15167520928809E-67,1.18789542670764E-48,1.));
#42948=DIRECTION('center_axis',(5.15167520928809E-67,-1.18789542670764E-48,
-1.));
#42949=DIRECTION('ref_axis',(-4.33680868994202E-19,1.,-1.18789542670764E-48));
#42950=DIRECTION('',(-5.15167520928809E-67,1.18789542670764E-48,1.));
#42951=DIRECTION('center_axis',(5.15167520928809E-67,-1.18789542670764E-48,
-1.));
#42952=DIRECTION('ref_axis',(-4.33680868994202E-19,1.,-1.18789542670764E-48));
#42953=DIRECTION('',(-5.15167520928809E-67,1.18789542670764E-48,1.));
#42954=DIRECTION('center_axis',(5.15167520928809E-67,-1.18789542670764E-48,
-1.));
#42955=DIRECTION('ref_axis',(-4.33680868994202E-19,1.,-1.18789542670764E-48));
#42956=DIRECTION('',(-5.15167520928809E-67,1.18789542670764E-48,1.));
#42957=DIRECTION('center_axis',(5.15167520928809E-67,-1.18789542670764E-48,
-1.));
#42958=DIRECTION('ref_axis',(-4.33680868994202E-19,1.,-1.18789542670764E-48));
#42959=DIRECTION('',(-5.15167520928809E-67,1.18789542670764E-48,1.));
#42960=DIRECTION('center_axis',(5.15167520928809E-67,-1.18789542670764E-48,
-1.));
#42961=DIRECTION('ref_axis',(-4.33680868994202E-19,1.,-1.18789542670764E-48));
#42962=DIRECTION('',(-5.15167520928809E-67,1.18789542670764E-48,1.));
#42963=DIRECTION('center_axis',(-5.15167520928809E-67,1.18789542670764E-48,
1.));
#42964=DIRECTION('ref_axis',(4.33680868994202E-19,-1.,1.18789542670764E-48));
#42965=DIRECTION('',(8.69022643068855E-17,-0.707106781186544,-0.707106781186551));
#42966=DIRECTION('center_axis',(5.15167520928809E-67,-1.18789542670764E-48,
-1.));
#42967=DIRECTION('ref_axis',(-4.33680868994202E-19,1.,-1.18789542670764E-48));
#42968=DIRECTION('center_axis',(0.,0.,1.));
#42969=DIRECTION('ref_axis',(5.30947313395831E-16,1.,0.));
#42970=DIRECTION('',(0.,0.,-1.));
#42971=DIRECTION('center_axis',(5.15167520928809E-67,-1.18789542670764E-48,
-1.));
#42972=DIRECTION('ref_axis',(-4.33680868994202E-19,1.,-1.18789542670764E-48));
#42973=DIRECTION('center_axis',(0.,0.,1.));
#42974=DIRECTION('ref_axis',(5.30947313395831E-16,1.,0.));
#42975=DIRECTION('',(0.,0.,-1.));
#42976=DIRECTION('center_axis',(0.,0.,1.));
#42977=DIRECTION('ref_axis',(5.30947313395831E-16,1.,0.));
#42978=DIRECTION('',(0.,0.,-1.));
#42979=DIRECTION('center_axis',(0.,0.,1.));
#42980=DIRECTION('ref_axis',(5.30947313395831E-16,1.,0.));
#42981=DIRECTION('',(0.,0.,-1.));
#42982=DIRECTION('center_axis',(0.,0.,1.));
#42983=DIRECTION('ref_axis',(5.30947313395831E-16,1.,0.));
#42984=DIRECTION('',(0.,0.,-1.));
#42985=DIRECTION('center_axis',(0.,0.,1.));
#42986=DIRECTION('ref_axis',(5.30947313395831E-16,1.,0.));
#42987=DIRECTION('',(0.,0.,-1.));
#42988=DIRECTION('center_axis',(0.,0.,1.));
#42989=DIRECTION('ref_axis',(5.30947313395831E-16,1.,0.));
#42990=DIRECTION('',(0.,0.,-1.));
#42991=DIRECTION('center_axis',(0.,0.,1.));
#42992=DIRECTION('ref_axis',(5.30947313395831E-16,1.,0.));
#42993=DIRECTION('',(0.,0.,-1.));
#42994=DIRECTION('center_axis',(0.,0.,1.));
#42995=DIRECTION('ref_axis',(5.30947313395831E-16,1.,0.));
#42996=DIRECTION('',(0.,0.,-1.));
#42997=DIRECTION('center_axis',(0.,0.,1.));
#42998=DIRECTION('ref_axis',(5.30947313395831E-16,1.,0.));
#42999=DIRECTION('',(0.,0.,-1.));
#43000=DIRECTION('center_axis',(0.,0.,1.));
#43001=DIRECTION('ref_axis',(5.30947313395831E-16,1.,0.));
#43002=DIRECTION('',(0.,0.,-1.));
#43003=DIRECTION('center_axis',(0.,0.,1.));
#43004=DIRECTION('ref_axis',(5.30947313395831E-16,1.,0.));
#43005=DIRECTION('',(0.,0.,-1.));
#43006=DIRECTION('center_axis',(0.,0.,1.));
#43007=DIRECTION('ref_axis',(5.30947313395831E-16,1.,0.));
#43008=DIRECTION('',(0.,0.,-1.));
#43009=DIRECTION('center_axis',(0.,0.,1.));
#43010=DIRECTION('ref_axis',(5.30947313395831E-16,1.,0.));
#43011=DIRECTION('',(0.,0.,-1.));
#43012=DIRECTION('center_axis',(0.,0.,1.));
#43013=DIRECTION('ref_axis',(5.30947313395831E-16,1.,0.));
#43014=DIRECTION('',(0.,0.,-1.));
#43015=DIRECTION('center_axis',(0.,0.,1.));
#43016=DIRECTION('ref_axis',(5.30947313395831E-16,1.,0.));
#43017=DIRECTION('',(0.,0.,-1.));
#43018=DIRECTION('center_axis',(0.,0.,1.));
#43019=DIRECTION('ref_axis',(5.30947313395831E-16,1.,0.));
#43020=DIRECTION('',(0.,0.,-1.));
#43021=DIRECTION('center_axis',(0.,0.,1.));
#43022=DIRECTION('ref_axis',(5.30947313395831E-16,1.,0.));
#43023=DIRECTION('',(0.,0.,-1.));
#43024=DIRECTION('center_axis',(0.,0.,1.));
#43025=DIRECTION('ref_axis',(5.30947313395831E-16,1.,0.));
#43026=DIRECTION('',(0.,0.,-1.));
#43027=DIRECTION('center_axis',(0.,0.,1.));
#43028=DIRECTION('ref_axis',(5.30947313395831E-16,1.,0.));
#43029=DIRECTION('',(0.,0.,-1.));
#43030=DIRECTION('center_axis',(0.,0.,1.));
#43031=DIRECTION('ref_axis',(5.30947313395831E-16,1.,0.));
#43032=DIRECTION('',(0.,0.,-1.));
#43033=DIRECTION('center_axis',(0.,0.,1.));
#43034=DIRECTION('ref_axis',(5.30947313395831E-16,1.,0.));
#43035=DIRECTION('',(0.,0.,-1.));
#43036=DIRECTION('center_axis',(0.,0.,1.));
#43037=DIRECTION('ref_axis',(5.30947313395831E-16,1.,0.));
#43038=DIRECTION('',(0.,0.,-1.));
#43039=DIRECTION('center_axis',(0.,0.,1.));
#43040=DIRECTION('ref_axis',(5.30947313395831E-16,1.,0.));
#43041=DIRECTION('',(0.,0.,-1.));
#43042=DIRECTION('center_axis',(0.,0.,1.));
#43043=DIRECTION('ref_axis',(5.30947313395831E-16,1.,0.));
#43044=DIRECTION('',(0.,0.,-1.));
#43045=DIRECTION('center_axis',(0.,0.,1.));
#43046=DIRECTION('ref_axis',(5.30947313395831E-16,1.,0.));
#43047=DIRECTION('',(0.,0.,-1.));
#43048=DIRECTION('center_axis',(0.,0.,1.));
#43049=DIRECTION('ref_axis',(5.30947313395831E-16,1.,0.));
#43050=DIRECTION('',(0.,0.,-1.));
#43051=DIRECTION('center_axis',(0.,0.,1.));
#43052=DIRECTION('ref_axis',(5.30947313395831E-16,1.,0.));
#43053=DIRECTION('',(0.,0.,-1.));
#43054=DIRECTION('center_axis',(0.,0.,1.));
#43055=DIRECTION('ref_axis',(5.30947313395831E-16,1.,0.));
#43056=DIRECTION('',(0.,0.,-1.));
#43057=DIRECTION('center_axis',(0.,0.,1.));
#43058=DIRECTION('ref_axis',(5.30947313395831E-16,1.,0.));
#43059=DIRECTION('',(0.,0.,-1.));
#43060=DIRECTION('center_axis',(0.,0.,1.));
#43061=DIRECTION('ref_axis',(5.30947313395831E-16,1.,0.));
#43062=DIRECTION('center_axis',(0.,0.,1.));
#43063=DIRECTION('ref_axis',(0.700629269222058,-0.7135254915624,0.));
#43064=DIRECTION('center_axis',(-5.15167520928809E-67,1.18789542670764E-48,
1.));
#43065=DIRECTION('ref_axis',(4.33680868994202E-19,-1.,1.18789542670764E-48));
#43066=DIRECTION('center_axis',(5.15167520928809E-67,-1.18789542670764E-48,
-1.));
#43067=DIRECTION('ref_axis',(-4.33680868994202E-19,1.,-1.18789542670764E-48));
#43068=DIRECTION('center_axis',(5.15167520928809E-67,-1.18789542670764E-48,
-1.));
#43069=DIRECTION('ref_axis',(-4.33680868994202E-19,1.,-1.18789542670764E-48));
#43070=DIRECTION('center_axis',(5.15167520928809E-67,-1.18789542670764E-48,
-1.));
#43071=DIRECTION('ref_axis',(-4.33680868994202E-19,1.,-1.18789542670764E-48));
#43072=DIRECTION('center_axis',(1.09747227149895E-48,7.33307527524356E-49,
1.));
#43073=DIRECTION('ref_axis',(1.,4.33680868994202E-19,-1.09747227149895E-48));
#43074=DIRECTION('center_axis',(-0.654448706060852,0.271081529927754,-0.705841126081008));
#43075=DIRECTION('ref_axis',(0.652112169591586,-0.270113704831613,-0.708370174931649));
#43076=DIRECTION('',(1.09747227149895E-48,7.33307527524356E-49,1.));
#43077=DIRECTION('center_axis',(-0.654448706060939,0.271081529927973,0.705841126080843));
#43078=DIRECTION('ref_axis',(0.652112169592024,-0.270113704830126,0.708370174931813));
#43079=DIRECTION('',(1.09747227149895E-48,7.33307527524356E-49,1.));
#43080=DIRECTION('center_axis',(1.12975568624751E-48,8.20815552314688E-49,
1.));
#43081=DIRECTION('ref_axis',(1.,4.33680868994202E-19,-1.12975568624751E-48));
#43082=DIRECTION('center_axis',(-0.673700070814156,0.218898422362917,-0.705841126084352));
#43083=DIRECTION('ref_axis',(0.671294802430975,-0.218116903290839,-0.708370174928316));
#43084=DIRECTION('',(1.12975568624751E-48,8.20815552314688E-49,1.));
#43085=DIRECTION('center_axis',(-0.673700070814201,0.218898422363249,0.705841126084207));
#43086=DIRECTION('ref_axis',(0.671294802430673,-0.218116903291296,0.708370174928462));
#43087=DIRECTION('',(1.12975568624751E-48,8.20815552314688E-49,1.));
#43088=DIRECTION('center_axis',(1.15507378150847E-48,9.10586746597098E-49,
1.));
#43089=DIRECTION('ref_axis',(1.,4.33680868994202E-19,-1.15507378150847E-48));
#43090=DIRECTION('center_axis',(-0.688797850611722,0.165365733230951,-0.705841126079843));
#43091=DIRECTION('ref_axis',(0.686338679579581,-0.164775338502517,-0.708370174932809));
#43092=DIRECTION('',(1.15507378150847E-48,9.10586746597098E-49,1.));
#43093=DIRECTION('center_axis',(-0.688797850609436,0.165365733233163,0.705841126081556));
#43094=DIRECTION('ref_axis',(0.68633867958204,-0.164775338499612,0.708370174931102));
#43095=DIRECTION('',(1.15507378150847E-48,9.10586746597098E-49,1.));
#43096=DIRECTION('center_axis',(1.17327046280542E-48,1.00206764110688E-48,
1.));
#43097=DIRECTION('ref_axis',(1.,4.33680868994202E-19,-1.17327046280542E-48));
#43098=DIRECTION('center_axis',(-0.699648962604041,0.110813509366852,-0.705841126082132));
#43099=DIRECTION('ref_axis',(0.697151050543932,-0.11041787896162,-0.708370174930529));
#43100=DIRECTION('',(1.17327046280542E-48,1.00206764110688E-48,1.));
#43101=DIRECTION('center_axis',(-0.699648962604175,0.110813509367011,0.705841126081974));
#43102=DIRECTION('ref_axis',(0.697151050543496,-0.110417878963368,0.708370174930686));
#43103=DIRECTION('',(1.17327046280542E-48,1.00206764110688E-48,1.));
#43104=DIRECTION('center_axis',(1.18423354154716E-48,1.09469422570891E-48,
1.));
#43105=DIRECTION('ref_axis',(1.,4.33680868994202E-19,-1.18423354154716E-48));
#43106=DIRECTION('center_axis',(-0.706186506088737,0.0555780833649064,-0.705841126081264));
#43107=DIRECTION('ref_axis',(0.703665253451942,-0.0553796564821394,-0.708370174931394));
#43108=DIRECTION('',(1.18423354154716E-48,1.09469422570891E-48,1.));
#43109=DIRECTION('center_axis',(-0.706186506088284,0.0555780833648712,0.705841126081719));
#43110=DIRECTION('ref_axis',(0.703665253452317,-0.0553796564831855,0.70837017493094));
#43111=DIRECTION('',(1.18423354154716E-48,1.09469422570891E-48,1.));
#43112=DIRECTION('center_axis',(1.18789542670764E-48,1.18789542670763E-48,
1.));
#43113=DIRECTION('ref_axis',(1.,4.33680868994202E-19,-1.18789542670764E-48));
#43114=DIRECTION('center_axis',(-0.70837017493089,-1.25340662871076E-13,
-0.70584112608177));
#43115=DIRECTION('ref_axis',(0.70584112608177,-2.88506822019813E-13,-0.708370174930889));
#43116=DIRECTION('',(1.18789542670764E-48,1.18789542670763E-48,1.));
#43117=DIRECTION('center_axis',(-0.70837017493089,1.25340662871076E-13,
0.70584112608177));
#43118=DIRECTION('ref_axis',(0.70584112608177,2.61497947465894E-13,0.708370174930889));
#43119=DIRECTION('',(1.18789542670764E-48,1.18789542670763E-48,1.));
#43120=DIRECTION('center_axis',(1.05842257525003E-48,6.48602188298306E-49,
1.));
#43121=DIRECTION('ref_axis',(1.,4.33680868994202E-19,-1.05842257525003E-48));
#43122=DIRECTION('center_axis',(-0.631162447404585,0.321593329715507,-0.70584112608203));
#43123=DIRECTION('ref_axis',(0.628909048379288,-0.320445165567225,-0.708370174930631));
#43124=DIRECTION('',(1.05842257525003E-48,6.48602188298306E-49,1.));
#43125=DIRECTION('center_axis',(-0.631162447404969,0.32159332971786,0.705841126080614));
#43126=DIRECTION('ref_axis',(0.628909048378923,-0.320445165564824,0.708370174932041));
#43127=DIRECTION('',(1.05842257525003E-48,6.48602188298306E-49,1.));
#43128=DIRECTION('center_axis',(1.01284735186347E-48,5.67221771220248E-49,
1.));
#43129=DIRECTION('ref_axis',(1.,4.33680868994202E-19,-1.01284735186347E-48));
#43130=DIRECTION('center_axis',(-0.603984862377595,0.370122399687911,-0.705841126081486));
#43131=DIRECTION('ref_axis',(0.601828493750374,-0.368800975294447,-0.708370174931173));
#43132=DIRECTION('',(1.01284735186347E-48,5.67221771220248E-49,1.));
#43133=DIRECTION('center_axis',(-0.603984862377492,0.370122399687834,0.705841126081615));
#43134=DIRECTION('ref_axis',(0.60182849375054,-0.368800975294424,0.708370174931044));
#43135=DIRECTION('',(1.01284735186347E-48,5.67221771220248E-49,1.));
#43136=DIRECTION('center_axis',(9.61027587746754E-49,4.89668013623204E-49,
1.));
#43137=DIRECTION('ref_axis',(1.,4.33680868994202E-19,-9.61027587746754E-49));
#43138=DIRECTION('center_axis',(-0.57308350982942,0.416369541987989,-0.705841126080299));
#43139=DIRECTION('ref_axis',(-0.571037466327478,0.414883004371834,0.708370174932355));
#43140=DIRECTION('',(9.61027587746754E-49,4.89668013623204E-49,1.));
#43141=DIRECTION('center_axis',(-0.573083509826005,0.416369541988967,0.705841126082495));
#43142=DIRECTION('ref_axis',(0.571037466331126,-0.41488300437055,0.708370174930167));
#43143=DIRECTION('',(9.61027587746754E-49,4.89668013623204E-49,1.));
#43144=DIRECTION('center_axis',(9.03282768977476E-49,4.16419060212002E-49,
1.));
#43145=DIRECTION('ref_axis',(1.,4.33680868994202E-19,-9.03282768977476E-49));
#43146=DIRECTION('center_axis',(-0.538648906869708,0.460049627603881,-0.705841126082633));
#43147=DIRECTION('ref_axis',(-0.536725803041031,0.458407141763258,0.70837017493003));
#43148=DIRECTION('',(9.03282768977476E-49,4.16419060212002E-49,1.));
#43149=DIRECTION('center_axis',(-0.53864890686968,0.460049627604191,0.705841126082452));
#43150=DIRECTION('ref_axis',(0.536725803040381,-0.45840714176374,0.70837017493021));
#43151=DIRECTION('',(9.03282768977476E-49,4.16419060212002E-49,1.));
#43152=DIRECTION('center_axis',(8.39968911565451E-49,3.47926515142171E-49,
1.));
#43153=DIRECTION('ref_axis',(1.,4.33680868994202E-19,-8.39968911565451E-49));
#43154=DIRECTION('center_axis',(-0.500893354284786,0.500893354283015,-0.705841126081816));
#43155=DIRECTION('ref_axis',(-0.499105046691526,0.499105046694076,0.708370174930843));
#43156=DIRECTION('',(8.39968911565451E-49,3.47926515142171E-49,1.));
#43157=DIRECTION('center_axis',(-0.500893354285066,0.500893354283687,0.70584112608114));
#43158=DIRECTION('ref_axis',(0.49910504669045,-0.499105046694196,0.708370174931517));
#43159=DIRECTION('',(8.39968911565451E-49,3.47926515142171E-49,1.));
#43160=DIRECTION('center_axis',(7.71476366495618E-49,2.84612657730147E-49,
1.));
#43161=DIRECTION('ref_axis',(1.,4.33680868994202E-19,-7.71476366495618E-49));
#43162=DIRECTION('center_axis',(-0.460049627606723,0.538648906869542,-0.705841126080907));
#43163=DIRECTION('ref_axis',(-0.458407141764148,0.536725803038001,0.708370174931749));
#43164=DIRECTION('',(7.71476366495618E-49,2.84612657730147E-49,1.));
#43165=DIRECTION('center_axis',(-0.460049627603276,0.538648906871872,0.705841126081376));
#43166=DIRECTION('ref_axis',(0.458407141768044,-0.53672580303529,0.708370174931282));
#43167=DIRECTION('',(7.71476366495618E-49,2.84612657730147E-49,1.));
#43168=DIRECTION('center_axis',(6.98227413084414E-49,2.26867838960871E-49,
1.));
#43169=DIRECTION('ref_axis',(1.,4.33680868994202E-19,-6.98227413084414E-49));
#43170=DIRECTION('center_axis',(-0.416369541989573,0.573083509826983,-0.705841126081344));
#43171=DIRECTION('ref_axis',(-0.414883004369422,0.571037466330522,0.708370174931314));
#43172=DIRECTION('',(6.98227413084414E-49,2.26867838960871E-49,1.));
#43173=DIRECTION('center_axis',(-0.416369541986537,0.573083509827722,0.705841126082535));
#43174=DIRECTION('ref_axis',(0.414883004374377,-0.571037466328393,0.708370174930127));
#43175=DIRECTION('',(6.98227413084414E-49,2.26867838960871E-49,1.));
#43176=DIRECTION('center_axis',(6.2067365548737E-49,1.75048074844156E-49,
1.));
#43177=DIRECTION('ref_axis',(1.,4.33680868994202E-19,-6.2067365548737E-49));
#43178=DIRECTION('center_axis',(-0.370122399687787,0.603984862376041,-0.70584112608288));
#43179=DIRECTION('ref_axis',(-0.368800975294937,0.60182849375171,0.708370174929783));
#43180=DIRECTION('',(6.2067365548737E-49,1.75048074844156E-49,1.));
#43181=DIRECTION('center_axis',(-0.370122399687792,0.603984862376936,0.705841126082112));
#43182=DIRECTION('ref_axis',(0.368800975294942,-0.601828493750806,0.708370174930549));
#43183=DIRECTION('',(6.2067365548737E-49,1.75048074844156E-49,1.));
#43184=DIRECTION('center_axis',(5.39293238409311E-49,1.29472851457601E-49,
1.));
#43185=DIRECTION('ref_axis',(1.,4.33680868994202E-19,-5.39293238409311E-49));
#43186=DIRECTION('center_axis',(-0.321593329717153,0.63116244740346,-0.705841126082286));
#43187=DIRECTION('ref_axis',(-0.320445165567263,0.628909048379556,0.708370174930376));
#43188=DIRECTION('',(5.39293238409311E-49,1.29472851457601E-49,1.));
#43189=DIRECTION('center_axis',(-0.321593329716558,0.631162447403966,0.705841126082104));
#43190=DIRECTION('ref_axis',(0.320445165566995,-0.628909048379489,0.708370174930556));
#43191=DIRECTION('',(5.39293238409311E-49,1.29472851457601E-49,1.));
#43192=DIRECTION('center_axis',(0.,0.,1.));
#43193=DIRECTION('ref_axis',(1.,4.33680868994202E-19,0.));
#43194=DIRECTION('',(-0.707106781186549,-8.69022643068862E-17,0.707106781186546));
#43195=DIRECTION('center_axis',(0.,0.,1.));
#43196=DIRECTION('ref_axis',(1.,4.33680868994202E-19,0.));
#43197=DIRECTION('center_axis',(5.15167520928809E-67,-1.18789542670764E-48,
-1.));
#43198=DIRECTION('ref_axis',(0.,1.,0.));
#43199=DIRECTION('center_axis',(5.15167520928809E-67,-1.18789542670764E-48,
-1.));
#43200=DIRECTION('ref_axis',(-4.33680868994202E-19,1.,-1.18789542670764E-48));
#43201=DIRECTION('center_axis',(-1.,0.,-5.15167520928809E-67));
#43202=DIRECTION('ref_axis',(0.,-1.,0.));
#43203=DIRECTION('center_axis',(5.15167520928809E-67,-1.18789542670764E-48,
-1.));
#43204=DIRECTION('ref_axis',(-4.33680868994202E-19,1.,-1.18789542670764E-48));
#43205=DIRECTION('center_axis',(5.15167520928809E-67,-1.18789542670764E-48,
-1.));
#43206=DIRECTION('ref_axis',(-4.33680868994202E-19,1.,-1.18789542670764E-48));
#43207=DIRECTION('center_axis',(5.15167520928809E-67,-1.18789542670764E-48,
-1.));
#43208=DIRECTION('ref_axis',(-4.33680868994202E-19,1.,-1.18789542670764E-48));
#43209=DIRECTION('center_axis',(0.0555758110363288,-0.706157633406642,0.705870190622316));
#43210=DIRECTION('ref_axis',(0.0553775799352608,-0.703694571287346,-0.708341212962532));
#43211=DIRECTION('center_axis',(5.15167520928809E-67,-1.18789542670764E-48,
-1.));
#43212=DIRECTION('ref_axis',(-4.33680868994202E-19,1.,-1.18789542670764E-48));
#43213=DIRECTION('center_axis',(0.11080862020158,-0.699618093636883,0.705872490429338));
#43214=DIRECTION('ref_axis',(0.110419233095995,-0.697182591373234,-0.708338921173046));
#43215=DIRECTION('center_axis',(5.15167520928809E-67,-1.18789542670764E-48,
-1.));
#43216=DIRECTION('ref_axis',(-4.33680868994202E-19,1.,-1.18789542670764E-48));
#43217=DIRECTION('center_axis',(0.165358045050138,-0.688765827029971,0.705874176077378));
#43218=DIRECTION('ref_axis',(0.164780094681068,-0.686371526838389,-0.708337241391723));
#43219=DIRECTION('center_axis',(5.15167520928809E-67,-1.18789542670764E-48,
-1.));
#43220=DIRECTION('ref_axis',(-4.33680868994202E-19,1.,-1.18789542670764E-48));
#43221=DIRECTION('center_axis',(0.218887852522913,-0.673667540197498,0.705875451692549));
#43222=DIRECTION('ref_axis',(0.218125006053852,-0.671328261761447,-0.708335970210719));
#43223=DIRECTION('center_axis',(5.15167520928809E-67,-1.18789542670764E-48,
-1.));
#43224=DIRECTION('ref_axis',(-4.33680868994202E-19,1.,-1.18789542670764E-48));
#43225=DIRECTION('center_axis',(0.271068063822855,-0.654416196007407,0.705876439030603));
#43226=DIRECTION('ref_axis',(0.270125073931967,-0.65214568281518,-0.708334986301518));
#43227=DIRECTION('center_axis',(5.15167520928809E-67,-1.18789542670764E-48,
-1.));
#43228=DIRECTION('ref_axis',(-4.33680868994202E-19,1.,-1.18789542670764E-48));
#43229=DIRECTION('center_axis',(0.321577003370555,-0.631130405143931,0.705877214964523));
#43230=DIRECTION('ref_axis',(0.320459697262731,-0.628942147608601,-0.708334213060304));
#43231=DIRECTION('center_axis',(5.15167520928809E-67,-1.18789542670764E-48,
-1.));
#43232=DIRECTION('ref_axis',(-4.33680868994202E-19,1.,-1.18789542670764E-48));
#43233=DIRECTION('center_axis',(0.370103289326652,-0.603953677099404,0.705877830185721));
#43234=DIRECTION('ref_axis',(0.368818543504099,-0.601860775526205,-0.708333599972859));
#43235=DIRECTION('center_axis',(5.15167520928809E-67,-1.18789542670764E-48,
-1.));
#43236=DIRECTION('ref_axis',(-4.33680868994202E-19,1.,-1.18789542670764E-48));
#43237=DIRECTION('center_axis',(0.416347757295498,-0.573053525770462,0.705878319256975));
#43238=DIRECTION('ref_axis',(0.414903461782555,-0.571068576441932,-0.708333112597058));
#43239=DIRECTION('center_axis',(5.15167520928809E-67,-1.18789542670764E-48,
-1.));
#43240=DIRECTION('ref_axis',(-4.33680868994202E-19,1.,-1.18789542670764E-48));
#43241=DIRECTION('center_axis',(0.460025307051016,-0.538620431161506,0.705878706300177));
#43242=DIRECTION('ref_axis',(0.458430320957564,-0.536755427393206,-0.708332726895123));
#43243=DIRECTION('center_axis',(5.15167520928809E-67,-1.18789542670764E-48,
-1.));
#43244=DIRECTION('ref_axis',(-4.33680868994202E-19,1.,-1.18789542670764E-48));
#43245=DIRECTION('center_axis',(0.500866661619323,-0.500866661619323,0.705879008440277));
#43246=DIRECTION('ref_axis',(0.499130761357991,-0.499132905771573,-0.708332425801768));
#43247=DIRECTION('center_axis',(5.15167520928809E-67,-1.18789542670764E-48,
-1.));
#43248=DIRECTION('ref_axis',(-4.33680868994202E-19,1.,-1.18789542670764E-48));
#43249=DIRECTION('center_axis',(0.53862002836901,-0.46002496303376,0.705879237848482));
#43250=DIRECTION('ref_axis',(0.536753849182443,-0.458432987266868,-0.708332197188161));
#43251=DIRECTION('center_axis',(5.15167520928809E-67,-1.18789542670764E-48,
-1.));
#43252=DIRECTION('ref_axis',(-4.33680868994202E-19,1.,-1.18789542670764E-48));
#43253=DIRECTION('center_axis',(0.573052651970297,-0.416347122442612,0.705879403087785));
#43254=DIRECTION('ref_axis',(0.571067623542823,-0.414906617259439,-0.708332032521106));
#43255=DIRECTION('center_axis',(5.15167520928809E-67,-1.18789542670764E-48,
-1.));
#43256=DIRECTION('ref_axis',(-4.33680868994202E-19,1.,-1.18789542670764E-48));
#43257=DIRECTION('center_axis',(0.603952249837211,-0.370102414699222,0.705879509938047));
#43258=DIRECTION('ref_axis',(0.601860526500507,-0.368822164724135,-0.708331926040847));
#43259=DIRECTION('center_axis',(5.15167520928809E-67,-1.18789542670764E-48,
-1.));
#43260=DIRECTION('ref_axis',(-4.33680868994202E-19,1.,-1.18789542670764E-48));
#43261=DIRECTION('center_axis',(0.631128321247012,-0.321575941572045,0.705879561909807));
#43262=DIRECTION('ref_axis',(0.628942707293582,-0.320463768412346,-0.708331874249054));
#43263=DIRECTION('center_axis',(5.15167520928809E-67,-1.18789542670764E-48,
-1.));
#43264=DIRECTION('ref_axis',(-4.33680868994202E-19,1.,-1.18789542670764E-48));
#43265=DIRECTION('center_axis',(0.654413322126613,-0.271066873422487,0.70587956051735));
#43266=DIRECTION('ref_axis',(0.652147192704133,-0.270129585579022,-0.708331875636714));
#43267=DIRECTION('center_axis',(5.15167520928809E-67,-1.18789542670764E-48,
-1.));
#43268=DIRECTION('ref_axis',(-4.33680868994202E-19,1.,-1.18789542670764E-48));
#43269=DIRECTION('center_axis',(0.673663698306673,-0.218886604216949,0.705879505353533));
#43270=DIRECTION('ref_axis',(0.671330916306432,-0.218129954133086,-0.708331930609559));
#43271=DIRECTION('center_axis',(5.15167520928809E-67,-1.18789542670764E-48,
-1.));
#43272=DIRECTION('ref_axis',(-4.33680868994202E-19,1.,-1.18789542670764E-48));
#43273=DIRECTION('center_axis',(0.688760770927107,-0.165356831187235,0.705879393955946));
#43274=DIRECTION('ref_axis',(0.686375600198304,-0.164785479532649,-0.708332041621451));
#43275=DIRECTION('center_axis',(5.15167520928809E-67,-1.18789542670764E-48,
-1.));
#43276=DIRECTION('ref_axis',(-4.33680868994202E-19,1.,-1.18789542670764E-48));
#43277=DIRECTION('center_axis',(0.699611468639781,-0.110807570905153,0.705879221381242));
#43278=DIRECTION('ref_axis',(0.697188483633051,-0.110425058152577,-0.708332213598567));
#43279=DIRECTION('center_axis',(5.15167520928809E-67,-1.18789542670764E-48,
-1.));
#43280=DIRECTION('ref_axis',(-4.33680868994202E-19,1.,-1.18789542670764E-48));
#43281=DIRECTION('center_axis',(0.706148902304913,-0.0555751238837372,0.705878979272562));
#43282=DIRECTION('ref_axis',(0.703702893729778,-0.0553838490533553,-0.708332454868737));
#43283=DIRECTION('center_axis',(5.15167520928809E-67,-1.18789542670764E-48,
-1.));
#43284=DIRECTION('ref_axis',(-4.33680868994202E-19,1.,-1.18789542670764E-48));
#43285=DIRECTION('center_axis',(0.708332577472403,3.07190287735134E-19,
0.705878856243267));
#43286=DIRECTION('ref_axis',(0.705878856242412,-1.55615277571261E-6,-0.708332577471545));
#43287=DIRECTION('center_axis',(5.15167520928809E-67,-1.18789542670764E-48,
-1.));
#43288=DIRECTION('ref_axis',(-4.33680868994202E-19,1.,-1.18789542670764E-48));
#43289=DIRECTION('center_axis',(0.706157633406551,0.0555758110364317,0.705870190622399));
#43290=DIRECTION('ref_axis',(0.703694571287442,0.0553775799351074,-0.70834121296245));
#43291=DIRECTION('center_axis',(5.15167520928809E-67,-1.18789542670764E-48,
-1.));
#43292=DIRECTION('ref_axis',(-4.33680868994202E-19,1.,-1.18789542670764E-48));
#43293=DIRECTION('center_axis',(0.699618093637069,0.110808620201609,0.705872490429149));
#43294=DIRECTION('ref_axis',(0.697182591372912,0.11041923309682,-0.708338921173234));
#43295=DIRECTION('center_axis',(5.15167520928809E-67,-1.18789542670764E-48,
-1.));
#43296=DIRECTION('ref_axis',(-4.33680868994202E-19,1.,-1.18789542670764E-48));
#43297=DIRECTION('center_axis',(0.688765827030135,0.165358045050174,0.705874176077209));
#43298=DIRECTION('ref_axis',(0.686371526838244,0.16478009468095,-0.708337241391891));
#43299=DIRECTION('center_axis',(5.15167520928809E-67,-1.18789542670764E-48,
-1.));
#43300=DIRECTION('ref_axis',(-4.33680868994202E-19,1.,-1.18789542670764E-48));
#43301=DIRECTION('center_axis',(0.673667540197388,0.21888785252289,0.705875451692661));
#43302=DIRECTION('ref_axis',(0.671328261761852,0.21812500605297,-0.708335970210607));
#43303=DIRECTION('center_axis',(5.15167520928809E-67,-1.18789542670764E-48,
-1.));
#43304=DIRECTION('ref_axis',(-4.33680868994202E-19,1.,-1.18789542670764E-48));
#43305=DIRECTION('center_axis',(0.654416196007382,0.271068063822859,0.705876439030624));
#43306=DIRECTION('ref_axis',(0.652145682814771,0.270125073933009,-0.708334986301497));
#43307=DIRECTION('center_axis',(5.15167520928809E-67,-1.18789542670764E-48,
-1.));
#43308=DIRECTION('ref_axis',(-4.33680868994202E-19,1.,-1.18789542670764E-48));
#43309=DIRECTION('center_axis',(0.631130405143941,0.321577003370555,0.705877214964514));
#43310=DIRECTION('ref_axis',(0.628942147608526,0.320459697262857,-0.708334213060313));
#43311=DIRECTION('center_axis',(5.15167520928809E-67,-1.18789542670764E-48,
-1.));
#43312=DIRECTION('ref_axis',(-4.33680868994202E-19,1.,-1.18789542670764E-48));
#43313=DIRECTION('center_axis',(0.603953677099555,0.370103289326611,0.705877830185613));
#43314=DIRECTION('ref_axis',(0.601860775525942,0.368818543504321,-0.708333599972967));
#43315=DIRECTION('center_axis',(5.15167520928809E-67,-1.18789542670764E-48,
-1.));
#43316=DIRECTION('ref_axis',(-4.33680868994202E-19,1.,-1.18789542670764E-48));
#43317=DIRECTION('center_axis',(0.573053525770564,0.41634775729573,0.705878319256755));
#43318=DIRECTION('ref_axis',(-0.571068576442187,-0.414903461781831,0.708333112597277));
#43319=DIRECTION('center_axis',(5.15167520928809E-67,-1.18789542670764E-48,
-1.));
#43320=DIRECTION('ref_axis',(-4.33680868994202E-19,1.,-1.18789542670764E-48));
#43321=DIRECTION('center_axis',(0.538620431161647,0.46002530705115,0.705878706299982));
#43322=DIRECTION('ref_axis',(-0.536755427393011,-0.458430320957492,0.708332726895318));
#43323=DIRECTION('center_axis',(5.15167520928809E-67,-1.18789542670764E-48,
-1.));
#43324=DIRECTION('ref_axis',(-4.33680868994202E-19,1.,-1.18789542670764E-48));
#43325=DIRECTION('center_axis',(0.500866661619527,0.500866661619527,0.705879008439988));
#43326=DIRECTION('ref_axis',(-0.49913290577155,-0.499130761357605,0.708332425802057));
#43327=DIRECTION('center_axis',(5.15167520928809E-67,-1.18789542670764E-48,
-1.));
#43328=DIRECTION('ref_axis',(-4.33680868994202E-19,1.,-1.18789542670764E-48));
#43329=DIRECTION('center_axis',(0.460024963033642,0.538620028368862,0.705879237848672));
#43330=DIRECTION('ref_axis',(-0.45843298726639,-0.536753849183101,0.708332197187972));
#43331=DIRECTION('center_axis',(5.15167520928809E-67,-1.18789542670764E-48,
-1.));
#43332=DIRECTION('ref_axis',(-4.33680868994202E-19,1.,-1.18789542670764E-48));
#43333=DIRECTION('center_axis',(0.416347122442686,0.573052651970292,0.705879403087744));
#43334=DIRECTION('ref_axis',(-0.414906617258984,-0.571067623543104,0.708332032521146));
#43335=DIRECTION('center_axis',(5.15167520928809E-67,-1.18789542670764E-48,
-1.));
#43336=DIRECTION('ref_axis',(-4.33680868994202E-19,1.,-1.18789542670764E-48));
#43337=DIRECTION('center_axis',(0.370102414699172,0.603952249837277,0.705879509938016));
#43338=DIRECTION('ref_axis',(-0.368822164724246,-0.601860526500403,0.708331926040877));
#43339=DIRECTION('center_axis',(5.15167520928809E-67,-1.18789542670764E-48,
-1.));
#43340=DIRECTION('ref_axis',(-4.33680868994202E-19,1.,-1.18789542670764E-48));
#43341=DIRECTION('center_axis',(0.321575941571924,0.631128321246917,0.705879561909948));
#43342=DIRECTION('ref_axis',(-0.320463768412656,-0.628942707293582,0.708331874248914));
#43343=DIRECTION('center_axis',(5.15167520928809E-67,-1.18789542670764E-48,
-1.));
#43344=DIRECTION('ref_axis',(-4.33680868994202E-19,1.,-1.18789542670764E-48));
#43345=DIRECTION('center_axis',(0.271066873422485,0.654413322126598,0.705879560517365));
#43346=DIRECTION('ref_axis',(-0.270129585579224,-0.652147192704065,0.708331875636699));
#43347=DIRECTION('center_axis',(5.15167520928809E-67,-1.18789542670764E-48,
-1.));
#43348=DIRECTION('ref_axis',(-4.33680868994202E-19,1.,-1.18789542670764E-48));
#43349=DIRECTION('center_axis',(0.218886604216952,0.67366369830668,0.705879505353526));
#43350=DIRECTION('ref_axis',(-0.218129954132996,-0.671330916306453,0.708331930609566));
#43351=DIRECTION('center_axis',(5.15167520928809E-67,-1.18789542670764E-48,
-1.));
#43352=DIRECTION('ref_axis',(-4.33680868994202E-19,1.,-1.18789542670764E-48));
#43353=DIRECTION('center_axis',(0.16535683118711,0.68876077092705,0.705879393956031));
#43354=DIRECTION('ref_axis',(-0.164785479532882,-0.686375600198336,0.708332041621366));
#43355=DIRECTION('center_axis',(5.15167520928809E-67,-1.18789542670764E-48,
-1.));
#43356=DIRECTION('ref_axis',(-4.33680868994202E-19,1.,-1.18789542670764E-48));
#43357=DIRECTION('center_axis',(0.110807570905159,0.699611468639805,0.705879221381218));
#43358=DIRECTION('ref_axis',(-0.11042505815257,-0.697188483633028,0.708332213598592));
#43359=DIRECTION('center_axis',(5.15167520928809E-67,-1.18789542670764E-48,
-1.));
#43360=DIRECTION('ref_axis',(-4.33680868994202E-19,1.,-1.18789542670764E-48));
#43361=DIRECTION('center_axis',(0.055575123883674,0.706148902304893,0.705878979272587));
#43362=DIRECTION('ref_axis',(-0.0553838490533958,-0.7037028937298,0.708332454868712));
#43363=DIRECTION('center_axis',(5.15167520928809E-67,-1.18789542670764E-48,
-1.));
#43364=DIRECTION('ref_axis',(-4.33680868994202E-19,1.,-1.18789542670764E-48));
#43365=DIRECTION('center_axis',(4.84352581305682E-13,0.70837017493119,0.705841126081468));
#43366=DIRECTION('ref_axis',(-1.41156745807278E-12,-0.705841126081468,0.70837017493119));
#43367=DIRECTION('center_axis',(5.15167520928809E-67,-1.18789542670764E-48,
-1.));
#43368=DIRECTION('ref_axis',(-4.33680868994202E-19,1.,-1.18789542670764E-48));
#43369=DIRECTION('center_axis',(-0.0555758110363152,0.706157633406656,0.705870190622303));
#43370=DIRECTION('ref_axis',(0.0553775799350914,-0.703694571287347,0.708341212962545));
#43371=DIRECTION('center_axis',(5.15167520928809E-67,-1.18789542670764E-48,
-1.));
#43372=DIRECTION('ref_axis',(-4.33680868994202E-19,1.,-1.18789542670764E-48));
#43373=DIRECTION('center_axis',(-0.110808620201596,0.699618093636976,0.705872490429243));
#43374=DIRECTION('ref_axis',(0.11041923309583,-0.697182591373165,0.70833892117314));
#43375=DIRECTION('center_axis',(5.15167520928809E-67,-1.18789542670764E-48,
-1.));
#43376=DIRECTION('ref_axis',(-4.33680868994202E-19,1.,-1.18789542670764E-48));
#43377=DIRECTION('center_axis',(-0.165358045050154,0.688765827030126,0.705874176077223));
#43378=DIRECTION('ref_axis',(0.164780094680844,-0.686371526838284,0.708337241391878));
#43379=DIRECTION('center_axis',(5.15167520928809E-67,-1.18789542670764E-48,
-1.));
#43380=DIRECTION('ref_axis',(-4.33680868994202E-19,1.,-1.18789542670764E-48));
#43381=DIRECTION('center_axis',(-0.218887852522867,0.673667540197309,0.705875451692744));
#43382=DIRECTION('ref_axis',(0.218125006054104,-0.67132826176157,0.708335970210525));
#43383=DIRECTION('center_axis',(5.15167520928809E-67,-1.18789542670764E-48,
-1.));
#43384=DIRECTION('ref_axis',(-4.33680868994202E-19,1.,-1.18789542670764E-48));
#43385=DIRECTION('center_axis',(-0.271068063822887,0.654416196007496,0.705876439030507));
#43386=DIRECTION('ref_axis',(0.270125073932604,-0.652145682814813,0.708334986301614));
#43387=DIRECTION('center_axis',(5.15167520928809E-67,-1.18789542670764E-48,
-1.));
#43388=DIRECTION('ref_axis',(-4.33680868994202E-19,1.,-1.18789542670764E-48));
#43389=DIRECTION('center_axis',(5.15167520928809E-67,-1.18789542670764E-48,
-1.));
#43390=DIRECTION('ref_axis',(-4.33680868994202E-19,1.,-1.18789542670764E-48));
#43391=DIRECTION('center_axis',(5.15167520928809E-67,-1.18789542670764E-48,
-1.));
#43392=DIRECTION('ref_axis',(-4.33680868994202E-19,1.,-1.18789542670764E-48));
#43393=DIRECTION('center_axis',(5.15167520928809E-67,-1.18789542670764E-48,
-1.));
#43394=DIRECTION('ref_axis',(-4.33680868994202E-19,1.,-1.18789542670764E-48));
#43395=DIRECTION('center_axis',(5.15167520928809E-67,-1.18789542670764E-48,
-1.));
#43396=DIRECTION('ref_axis',(-4.33680868994202E-19,1.,-1.18789542670764E-48));
#43397=DIRECTION('center_axis',(5.15167520928809E-67,-1.18789542670764E-48,
-1.));
#43398=DIRECTION('ref_axis',(-4.33680868994202E-19,1.,-1.18789542670764E-48));
#43399=DIRECTION('center_axis',(5.15167520928809E-67,-1.18789542670764E-48,
-1.));
#43400=DIRECTION('ref_axis',(-4.33680868994202E-19,1.,-1.18789542670764E-48));
#43401=DIRECTION('center_axis',(5.15167520928809E-67,-1.18789542670764E-48,
-1.));
#43402=DIRECTION('ref_axis',(-4.33680868994202E-19,1.,-1.18789542670764E-48));
#43403=DIRECTION('center_axis',(5.15167520928809E-67,-1.18789542670764E-48,
-1.));
#43404=DIRECTION('ref_axis',(-4.33680868994202E-19,1.,-1.18789542670764E-48));
#43405=DIRECTION('center_axis',(5.15167520928809E-67,-1.18789542670764E-48,
-1.));
#43406=DIRECTION('ref_axis',(-4.33680868994202E-19,1.,-1.18789542670764E-48));
#43407=DIRECTION('center_axis',(5.15167520928809E-67,-1.18789542670764E-48,
-1.));
#43408=DIRECTION('ref_axis',(-4.33680868994202E-19,1.,-1.18789542670764E-48));
#43409=DIRECTION('center_axis',(5.15167520928809E-67,-1.18789542670764E-48,
-1.));
#43410=DIRECTION('ref_axis',(-4.33680868994202E-19,1.,-1.18789542670764E-48));
#43411=DIRECTION('center_axis',(5.15167520928809E-67,-1.18789542670764E-48,
-1.));
#43412=DIRECTION('ref_axis',(-4.33680868994202E-19,1.,-1.18789542670764E-48));
#43413=DIRECTION('center_axis',(5.15167520928809E-67,-1.18789542670764E-48,
-1.));
#43414=DIRECTION('ref_axis',(-4.33680868994202E-19,1.,-1.18789542670764E-48));
#43415=DIRECTION('center_axis',(5.15167520928809E-67,-1.18789542670764E-48,
-1.));
#43416=DIRECTION('ref_axis',(-4.33680868994202E-19,1.,-1.18789542670764E-48));
#43417=DIRECTION('center_axis',(5.15167520928809E-67,-1.18789542670764E-48,
-1.));
#43418=DIRECTION('ref_axis',(-4.33680868994202E-19,1.,-1.18789542670764E-48));
#43419=DIRECTION('center_axis',(-0.7061576334064,-0.0555758110363729,0.705870190622555));
#43420=DIRECTION('ref_axis',(0.703694571287618,0.0553775799348557,0.708341212962294));
#43421=DIRECTION('center_axis',(5.15167520928809E-67,-1.18789542670764E-48,
-1.));
#43422=DIRECTION('ref_axis',(-4.33680868994202E-19,1.,-1.18789542670764E-48));
#43423=DIRECTION('center_axis',(-0.699618093637056,-0.110808620201623,0.70587249042916));
#43424=DIRECTION('ref_axis',(0.697182591373085,0.110419233095803,0.708338921173223));
#43425=DIRECTION('center_axis',(5.15167520928809E-67,-1.18789542670764E-48,
-1.));
#43426=DIRECTION('ref_axis',(-4.33680868994202E-19,1.,-1.18789542670764E-48));
#43427=DIRECTION('center_axis',(-0.68876582703002,-0.165358045050145,0.705874176077329));
#43428=DIRECTION('ref_axis',(0.686371526838198,0.164780094681657,0.708337241391772));
#43429=DIRECTION('center_axis',(5.15167520928809E-67,-1.18789542670764E-48,
-1.));
#43430=DIRECTION('ref_axis',(-4.33680868994202E-19,1.,-1.18789542670764E-48));
#43431=DIRECTION('center_axis',(-0.673667540197642,-0.218887852522971,0.705875451692394));
#43432=DIRECTION('ref_axis',(0.671328261761337,0.218125006053688,0.708335970210874));
#43433=DIRECTION('center_axis',(5.15167520928809E-67,-1.18789542670764E-48,
-1.));
#43434=DIRECTION('ref_axis',(-4.33680868994202E-19,1.,-1.18789542670764E-48));
#43435=DIRECTION('center_axis',(-0.654416196007479,-0.271068063822885,0.705876439030525));
#43436=DIRECTION('ref_axis',(0.652145682815046,0.270125073932086,0.708334986301596));
#43437=DIRECTION('center_axis',(5.15167520928809E-67,-1.18789542670764E-48,
-1.));
#43438=DIRECTION('ref_axis',(-4.33680868994202E-19,1.,-1.18789542670764E-48));
#43439=DIRECTION('center_axis',(-0.631130405143739,-0.321577003370466,0.705877214964735));
#43440=DIRECTION('ref_axis',(0.628942147608447,0.3204596972635,0.708334213060093));
#43441=DIRECTION('center_axis',(5.15167520928809E-67,-1.18789542670764E-48,
-1.));
#43442=DIRECTION('ref_axis',(-4.33680868994202E-19,1.,-1.18789542670764E-48));
#43443=DIRECTION('center_axis',(-0.603953677099563,-0.37010328932661,0.705877830185607));
#43444=DIRECTION('ref_axis',(0.601860775526009,0.3688185435042,0.708333599972973));
#43445=DIRECTION('center_axis',(5.15167520928809E-67,-1.18789542670764E-48,
-1.));
#43446=DIRECTION('ref_axis',(-4.33680868994202E-19,1.,-1.18789542670764E-48));
#43447=DIRECTION('center_axis',(-0.573053525770468,-0.416347757295655,0.705878319256877));
#43448=DIRECTION('ref_axis',(-0.571068576442267,-0.414903461781928,-0.708333112597156));
#43449=DIRECTION('center_axis',(5.15167520928809E-67,-1.18789542670764E-48,
-1.));
#43450=DIRECTION('ref_axis',(-4.33680868994202E-19,1.,-1.18789542670764E-48));
#43451=DIRECTION('center_axis',(-0.5386204311615,-0.460025307051025,0.705878706300176));
#43452=DIRECTION('ref_axis',(-0.53675542739315,-0.458430320957627,-0.708332726895124));
#43453=DIRECTION('center_axis',(5.15167520928809E-67,-1.18789542670764E-48,
-1.));
#43454=DIRECTION('ref_axis',(-4.33680868994202E-19,1.,-1.18789542670764E-48));
#43455=DIRECTION('center_axis',(-0.500866661619536,-0.500866661619512,0.705879008439992));
#43456=DIRECTION('ref_axis',(-0.499132905770748,-0.499130761358414,-0.708332425802052));
#43457=DIRECTION('center_axis',(5.15167520928809E-67,-1.18789542670764E-48,
-1.));
#43458=DIRECTION('ref_axis',(-4.33680868994202E-19,1.,-1.18789542670764E-48));
#43459=DIRECTION('center_axis',(-0.460024963033767,-0.538620028369008,0.70587923784848));
#43460=DIRECTION('ref_axis',(-0.45843298726701,-0.536753849182318,-0.708332197188163));
#43461=DIRECTION('center_axis',(5.15167520928809E-67,-1.18789542670764E-48,
-1.));
#43462=DIRECTION('ref_axis',(-4.33680868994202E-19,1.,-1.18789542670764E-48));
#43463=DIRECTION('center_axis',(-0.416347122442742,-0.573052651970378,0.705879403087642));
#43464=DIRECTION('ref_axis',(-0.414906617259033,-0.571067623542942,-0.708332032521248));
#43465=DIRECTION('center_axis',(5.15167520928809E-67,-1.18789542670764E-48,
-1.));
#43466=DIRECTION('ref_axis',(-4.33680868994202E-19,1.,-1.18789542670764E-48));
#43467=DIRECTION('center_axis',(-0.370102414699178,-0.603952249837274,0.705879509938015));
#43468=DIRECTION('ref_axis',(-0.368822164723695,-0.601860526500739,-0.708331926040878));
#43469=DIRECTION('center_axis',(5.15167520928809E-67,-1.18789542670764E-48,
-1.));
#43470=DIRECTION('ref_axis',(-4.33680868994202E-19,1.,-1.18789542670764E-48));
#43471=DIRECTION('center_axis',(-0.321575941572111,-0.631128321247095,0.705879561909702));
#43472=DIRECTION('ref_axis',(-0.320463768412258,-0.628942707293509,-0.708331874249159));
#43473=DIRECTION('center_axis',(5.15167520928809E-67,-1.18789542670764E-48,
-1.));
#43474=DIRECTION('ref_axis',(-4.33680868994202E-19,1.,-1.18789542670764E-48));
#43475=DIRECTION('center_axis',(-0.271066873422704,-0.654413322126826,0.70587956051707));
#43476=DIRECTION('ref_axis',(-0.270129585579653,-0.652147192703568,-0.708331875636993));
#43477=DIRECTION('center_axis',(5.15167520928809E-67,-1.18789542670764E-48,
-1.));
#43478=DIRECTION('ref_axis',(-4.33680868994202E-19,1.,-1.18789542670764E-48));
#43479=DIRECTION('center_axis',(-0.218886604216915,-0.673663698306575,0.705879505353637));
#43480=DIRECTION('ref_axis',(-0.218129954131654,-0.671330916307006,-0.708331930609455));
#43481=DIRECTION('center_axis',(5.15167520928809E-67,-1.18789542670764E-48,
-1.));
#43482=DIRECTION('ref_axis',(-4.33680868994202E-19,1.,-1.18789542670764E-48));
#43483=DIRECTION('center_axis',(-0.165356831187205,-0.688760770926913,0.705879393956142));
#43484=DIRECTION('ref_axis',(-0.164785479532657,-0.686375600198504,-0.708332041621255));
#43485=DIRECTION('center_axis',(5.15167520928809E-67,-1.18789542670764E-48,
-1.));
#43486=DIRECTION('ref_axis',(-4.33680868994202E-19,1.,-1.18789542670764E-48));
#43487=DIRECTION('center_axis',(-0.110807570905278,-0.699611468639872,0.705879221381132));
#43488=DIRECTION('ref_axis',(-0.110425058152835,-0.697188483632899,-0.708332213598677));
#43489=DIRECTION('center_axis',(5.15167520928809E-67,-1.18789542670764E-48,
-1.));
#43490=DIRECTION('ref_axis',(-4.33680868994202E-19,1.,-1.18789542670764E-48));
#43491=DIRECTION('center_axis',(-0.0555751238837442,-0.706148902305009,
0.705878979272465));
#43492=DIRECTION('ref_axis',(-0.0553838490528384,-0.703702893729722,-0.708332454868834));
#43493=DIRECTION('center_axis',(5.15167520928809E-67,-1.18789542670764E-48,
-1.));
#43494=DIRECTION('ref_axis',(-4.33680868994202E-19,1.,-1.18789542670764E-48));
#43495=DIRECTION('',(8.62889469402126E-17,0.707106781186547,0.707106781186548));
#43496=DIRECTION('center_axis',(-5.15167520928809E-67,1.18789542670764E-48,
1.));
#43497=DIRECTION('ref_axis',(4.33680868994202E-19,-1.,1.18789542670764E-48));
#43498=DIRECTION('center_axis',(5.15167520928809E-67,-1.18789542670764E-48,
-1.));
#43499=DIRECTION('ref_axis',(-4.33680868994202E-19,1.,-1.18789542670764E-48));
#43500=DIRECTION('center_axis',(0.0555758110363494,0.706157633406676,-0.705870190622281));
#43501=DIRECTION('ref_axis',(0.0553775799347821,0.703694571287349,0.708341212962568));
#43502=DIRECTION('center_axis',(5.15167520928809E-67,-1.18789542670764E-48,
-1.));
#43503=DIRECTION('ref_axis',(-4.33680868994202E-19,1.,-1.18789542670764E-48));
#43504=DIRECTION('center_axis',(0.110808620201597,0.699618093636782,-0.705872490429435));
#43505=DIRECTION('ref_axis',(0.110419233096536,0.697182591373247,0.708338921172949));
#43506=DIRECTION('center_axis',(5.15167520928809E-67,-1.18789542670764E-48,
-1.));
#43507=DIRECTION('ref_axis',(-4.33680868994202E-19,1.,-1.18789542670764E-48));
#43508=DIRECTION('center_axis',(0.165358045050176,0.688765827030065,-0.705874176077277));
#43509=DIRECTION('ref_axis',(0.164780094681565,0.686371526838166,0.708337241391824));
#43510=DIRECTION('center_axis',(5.15167520928809E-67,-1.18789542670764E-48,
-1.));
#43511=DIRECTION('ref_axis',(-4.33680868994202E-19,1.,-1.18789542670764E-48));
#43512=DIRECTION('center_axis',(0.218887852522828,0.673667540197125,-0.705875451692931));
#43513=DIRECTION('ref_axis',(0.218125006053502,0.671328261761963,0.708335970210338));
#43514=DIRECTION('center_axis',(5.15167520928809E-67,-1.18789542670764E-48,
-1.));
#43515=DIRECTION('ref_axis',(-4.33680868994202E-19,1.,-1.18789542670764E-48));
#43516=DIRECTION('center_axis',(0.271068063822916,0.654416196007463,-0.705876439030527));
#43517=DIRECTION('ref_axis',(0.270125073931817,0.65214568281516,0.708334986301594));
#43518=DIRECTION('center_axis',(5.15167520928809E-67,-1.18789542670764E-48,
-1.));
#43519=DIRECTION('ref_axis',(-4.33680868994202E-19,1.,-1.18789542670764E-48));
#43520=DIRECTION('center_axis',(0.321577003370433,0.631130405143686,-0.705877214964798));
#43521=DIRECTION('ref_axis',(0.320459697263181,0.62894214760868,0.70833421306003));
#43522=DIRECTION('center_axis',(5.15167520928809E-67,-1.18789542670764E-48,
-1.));
#43523=DIRECTION('ref_axis',(-4.33680868994202E-19,1.,-1.18789542670764E-48));
#43524=DIRECTION('center_axis',(0.37010328932647,0.603953677099309,-0.705877830185898));
#43525=DIRECTION('ref_axis',(0.368818543504439,0.601860775526204,0.708333599972683));
#43526=DIRECTION('center_axis',(5.15167520928809E-67,-1.18789542670764E-48,
-1.));
#43527=DIRECTION('ref_axis',(-4.33680868994202E-19,1.,-1.18789542670764E-48));
#43528=DIRECTION('center_axis',(0.416347757295563,0.573053525770315,-0.705878319257056));
#43529=DIRECTION('ref_axis',(0.414903461782186,0.5710685764423,0.708333112596977));
#43530=DIRECTION('center_axis',(5.15167520928809E-67,-1.18789542670764E-48,
-1.));
#43531=DIRECTION('ref_axis',(-4.33680868994202E-19,1.,-1.18789542670764E-48));
#43532=DIRECTION('center_axis',(0.46002530705103,0.538620431161473,-0.705878706300193));
#43533=DIRECTION('ref_axis',(0.458430320957387,0.536755427393379,0.708332726895108));
#43534=DIRECTION('center_axis',(5.15167520928809E-67,-1.18789542670764E-48,
-1.));
#43535=DIRECTION('ref_axis',(-4.33680868994202E-19,1.,-1.18789542670764E-48));
#43536=DIRECTION('center_axis',(0.500866661619595,0.500866661619595,-0.705879008439891));
#43537=DIRECTION('ref_axis',(0.499130761358023,0.499132905770996,0.708332425802153));
#43538=DIRECTION('center_axis',(5.15167520928809E-67,-1.18789542670764E-48,
-1.));
#43539=DIRECTION('ref_axis',(-4.33680868994202E-19,1.,-1.18789542670764E-48));
#43540=DIRECTION('center_axis',(0.538620028368889,0.460024963033635,-0.705879237848656));
#43541=DIRECTION('ref_axis',(0.536753849182959,0.458432987266531,0.708332197187987));
#43542=DIRECTION('center_axis',(5.15167520928809E-67,-1.18789542670764E-48,
-1.));
#43543=DIRECTION('ref_axis',(-4.33680868994202E-19,1.,-1.18789542670764E-48));
#43544=DIRECTION('center_axis',(0.573052651970233,0.416347122442629,-0.705879403087826));
#43545=DIRECTION('ref_axis',(0.57106762354309,0.414906617259142,0.708332032521065));
#43546=DIRECTION('center_axis',(5.15167520928809E-67,-1.18789542670764E-48,
-1.));
#43547=DIRECTION('ref_axis',(-4.33680868994202E-19,1.,-1.18789542670764E-48));
#43548=DIRECTION('center_axis',(0.603952249837032,0.370102414699012,-0.70587950993831));
#43549=DIRECTION('ref_axis',(0.601860526500475,0.36882216472469,0.708331926040585));
#43550=DIRECTION('center_axis',(5.15167520928809E-67,-1.18789542670764E-48,
-1.));
#43551=DIRECTION('ref_axis',(-4.33680868994202E-19,1.,-1.18789542670764E-48));
#43552=DIRECTION('center_axis',(0.631128321246922,0.32157594157199,-0.705879561909913));
#43553=DIRECTION('ref_axis',(0.628942707293632,0.32046376841248,0.708331874248949));
#43554=DIRECTION('center_axis',(5.15167520928809E-67,-1.18789542670764E-48,
-1.));
#43555=DIRECTION('ref_axis',(-4.33680868994202E-19,1.,-1.18789542670764E-48));
#43556=DIRECTION('center_axis',(0.654413322126609,0.271066873422466,-0.705879560517362));
#43557=DIRECTION('ref_axis',(0.652147192704168,0.270129585578968,0.708331875636702));
#43558=DIRECTION('center_axis',(5.15167520928809E-67,-1.18789542670764E-48,
-1.));
#43559=DIRECTION('ref_axis',(-4.33680868994202E-19,1.,-1.18789542670764E-48));
#43560=DIRECTION('center_axis',(0.673663698306398,0.218886604216837,-0.70587950535383));
#43561=DIRECTION('ref_axis',(0.671330916306662,0.218129954133339,0.708331930609263));
#43562=DIRECTION('center_axis',(5.15167520928809E-67,-1.18789542670764E-48,
-1.));
#43563=DIRECTION('ref_axis',(-4.33680868994202E-19,1.,-1.18789542670764E-48));
#43564=DIRECTION('center_axis',(0.688760770927087,0.165356831187229,-0.705879393955967));
#43565=DIRECTION('ref_axis',(0.686375600198292,0.164785479532791,0.70833204162143));
#43566=DIRECTION('center_axis',(5.15167520928809E-67,-1.18789542670764E-48,
-1.));
#43567=DIRECTION('ref_axis',(-4.33680868994202E-19,1.,-1.18789542670764E-48));
#43568=DIRECTION('center_axis',(0.699611468639904,0.110807570905141,-0.705879221381122));
#43569=DIRECTION('ref_axis',(0.697188483632864,0.11042505815299,0.708332213598687));
#43570=DIRECTION('center_axis',(5.15167520928809E-67,-1.18789542670764E-48,
-1.));
#43571=DIRECTION('ref_axis',(-4.33680868994202E-19,1.,-1.18789542670764E-48));
#43572=DIRECTION('center_axis',(0.706148902304704,0.0555751238836885,-0.705878979272775));
#43573=DIRECTION('ref_axis',(0.703702893729991,0.0553838490533688,0.708332454868525));
#43574=DIRECTION('center_axis',(5.15167520928809E-67,-1.18789542670764E-48,
-1.));
#43575=DIRECTION('ref_axis',(-4.33680868994202E-19,1.,-1.18789542670764E-48));
#43576=DIRECTION('center_axis',(0.708332577472139,3.0719028773502E-19,-0.705878856243532));
#43577=DIRECTION('ref_axis',(0.705878856242677,1.5561538090606E-6,0.708332577471281));
#43578=DIRECTION('center_axis',(5.15167520928809E-67,-1.18789542670764E-48,
-1.));
#43579=DIRECTION('ref_axis',(-4.33680868994202E-19,1.,-1.18789542670764E-48));
#43580=DIRECTION('center_axis',(0.706157633406651,-0.0555758110363464,-0.705870190622306));
#43581=DIRECTION('ref_axis',(0.703694571287399,-0.0553775799344575,0.708341212962543));
#43582=DIRECTION('center_axis',(5.15167520928809E-67,-1.18789542670764E-48,
-1.));
#43583=DIRECTION('ref_axis',(-4.33680868994202E-19,1.,-1.18789542670764E-48));
#43584=DIRECTION('center_axis',(0.699618093636944,-0.110808620201621,-0.705872490429271));
#43585=DIRECTION('ref_axis',(0.697182591373154,-0.110419233096072,0.708338921173112));
#43586=DIRECTION('center_axis',(5.15167520928809E-67,-1.18789542670764E-48,
-1.));
#43587=DIRECTION('ref_axis',(-4.33680868994202E-19,1.,-1.18789542670764E-48));
#43588=DIRECTION('center_axis',(0.688765827030149,-0.165358045050179,-0.705874176077195));
#43589=DIRECTION('ref_axis',(0.686371526838092,-0.164780094681522,0.708337241391906));
#43590=DIRECTION('center_axis',(5.15167520928809E-67,-1.18789542670764E-48,
-1.));
#43591=DIRECTION('ref_axis',(-4.33680868994202E-19,1.,-1.18789542670764E-48));
#43592=DIRECTION('center_axis',(0.673667540197491,-0.218887852522947,-0.705875451692545));
#43593=DIRECTION('ref_axis',(0.671328261761432,-0.218125006053886,0.708335970210723));
#43594=DIRECTION('center_axis',(5.15167520928809E-67,-1.18789542670764E-48,
-1.));
#43595=DIRECTION('ref_axis',(-4.33680868994202E-19,1.,-1.18789542670764E-48));
#43596=DIRECTION('center_axis',(0.654416196007489,-0.271068063822922,-0.705876439030501));
#43597=DIRECTION('ref_axis',(0.652145682814786,-0.270125073932652,0.70833498630162));
#43598=DIRECTION('center_axis',(5.15167520928809E-67,-1.18789542670764E-48,
-1.));
#43599=DIRECTION('ref_axis',(-4.33680868994202E-19,1.,-1.18789542670764E-48));
#43600=DIRECTION('center_axis',(0.631130405143858,-0.321577003370522,-0.705877214964604));
#43601=DIRECTION('ref_axis',(0.628942147608515,-0.320459697263077,0.708334213060224));
#43602=DIRECTION('center_axis',(5.15167520928809E-67,-1.18789542670764E-48,
-1.));
#43603=DIRECTION('ref_axis',(-4.33680868994202E-19,1.,-1.18789542670764E-48));
#43604=DIRECTION('center_axis',(0.603953677099314,-0.37010328932649,-0.705877830185883));
#43605=DIRECTION('ref_axis',(0.60186077552563,-0.368818543505346,0.708333599972698));
#43606=DIRECTION('center_axis',(5.15167520928809E-67,-1.18789542670764E-48,
-1.));
#43607=DIRECTION('ref_axis',(-4.33680868994202E-19,1.,-1.18789542670764E-48));
#43608=DIRECTION('center_axis',(0.573053525770311,-0.416347757295561,-0.70587831925706));
#43609=DIRECTION('ref_axis',(-0.571068576442179,0.41490346178236,-0.708333112596973));
#43610=DIRECTION('center_axis',(5.15167520928809E-67,-1.18789542670764E-48,
-1.));
#43611=DIRECTION('ref_axis',(-4.33680868994202E-19,1.,-1.18789542670764E-48));
#43612=DIRECTION('center_axis',(0.53862043116148,-0.460025307051029,-0.705878706300189));
#43613=DIRECTION('ref_axis',(-0.536755427393413,0.45843032095734,-0.708332726895112));
#43614=DIRECTION('center_axis',(5.15167520928809E-67,-1.18789542670764E-48,
-1.));
#43615=DIRECTION('ref_axis',(-4.33680868994202E-19,1.,-1.18789542670764E-48));
#43616=DIRECTION('center_axis',(0.500866661619453,-0.500866661619453,-0.705879008440093));
#43617=DIRECTION('ref_axis',(-0.499132905770974,0.49913076135833,-0.708332425801952));
#43618=DIRECTION('center_axis',(5.15167520928809E-67,-1.18789542670764E-48,
-1.));
#43619=DIRECTION('ref_axis',(-4.33680868994202E-19,1.,-1.18789542670764E-48));
#43620=DIRECTION('center_axis',(0.460024963033751,-0.538620028369041,-0.705879237848464));
#43621=DIRECTION('ref_axis',(-0.458432987266724,0.536753849182542,-0.708332197188179));
#43622=DIRECTION('center_axis',(5.15167520928809E-67,-1.18789542670764E-48,
-1.));
#43623=DIRECTION('ref_axis',(-4.33680868994202E-19,1.,-1.18789542670764E-48));
#43624=DIRECTION('center_axis',(0.416347122442499,-0.573052651970059,-0.705879403088044));
#43625=DIRECTION('ref_axis',(-0.414906617258677,0.571067623543698,-0.708332032520848));
#43626=DIRECTION('center_axis',(5.15167520928809E-67,-1.18789542670764E-48,
-1.));
#43627=DIRECTION('ref_axis',(-4.33680868994202E-19,1.,-1.18789542670764E-48));
#43628=DIRECTION('center_axis',(0.370102414698996,-0.603952249837027,-0.705879509938322));
#43629=DIRECTION('ref_axis',(-0.36882216472453,0.601860526500588,-0.708331926040572));
#43630=DIRECTION('center_axis',(5.15167520928809E-67,-1.18789542670764E-48,
-1.));
#43631=DIRECTION('ref_axis',(-4.33680868994202E-19,1.,-1.18789542670764E-48));
#43632=DIRECTION('center_axis',(0.321575941571994,-0.631128321246919,-0.705879561909914));
#43633=DIRECTION('ref_axis',(-0.320463768412686,0.628942707293528,-0.708331874248948));
#43634=DIRECTION('center_axis',(5.15167520928809E-67,-1.18789542670764E-48,
-1.));
#43635=DIRECTION('ref_axis',(-4.33680868994202E-19,1.,-1.18789542670764E-48));
#43636=DIRECTION('center_axis',(0.27106687342253,-0.654413322126797,-0.705879560517163));
#43637=DIRECTION('ref_axis',(-0.270129585579053,0.652147192703917,-0.7083318756369));
#43638=DIRECTION('center_axis',(5.15167520928809E-67,-1.18789542670764E-48,
-1.));
#43639=DIRECTION('ref_axis',(-4.33680868994202E-19,1.,-1.18789542670764E-48));
#43640=DIRECTION('center_axis',(0.218886604216888,-0.673663698306596,-0.705879505353626));
#43641=DIRECTION('ref_axis',(-0.218129954133397,0.671330916306428,-0.708331930609466));
#43642=DIRECTION('center_axis',(5.15167520928809E-67,-1.18789542670764E-48,
-1.));
#43643=DIRECTION('ref_axis',(-4.33680868994202E-19,1.,-1.18789542670764E-48));
#43644=DIRECTION('center_axis',(0.165356831187193,-0.688760770926925,-0.705879393956133));
#43645=DIRECTION('ref_axis',(-0.164785479532379,0.686375600198561,-0.708332041621264));
#43646=DIRECTION('center_axis',(5.15167520928809E-67,-1.18789542670764E-48,
-1.));
#43647=DIRECTION('ref_axis',(-4.33680868994202E-19,1.,-1.18789542670764E-48));
#43648=DIRECTION('center_axis',(0.110807570905112,-0.699611468639716,-0.705879221381312));
#43649=DIRECTION('ref_axis',(-0.110425058152835,0.697188483633082,-0.708332213598497));
#43650=DIRECTION('center_axis',(5.15167520928809E-67,-1.18789542670764E-48,
-1.));
#43651=DIRECTION('ref_axis',(-4.33680868994202E-19,1.,-1.18789542670764E-48));
#43652=DIRECTION('center_axis',(0.0555751238837179,-0.706148902304883,-0.705878979272593));
#43653=DIRECTION('ref_axis',(-0.0553838490533129,0.703702893729813,-0.708332454868706));
#43654=DIRECTION('center_axis',(5.15167520928809E-67,-1.18789542670764E-48,
-1.));
#43655=DIRECTION('ref_axis',(-4.33680868994202E-19,1.,-1.18789542670764E-48));
#43656=DIRECTION('center_axis',(4.22129745643424E-13,-0.708370174930854,
-0.705841126081805));
#43657=DIRECTION('ref_axis',(-3.47233154276107E-12,0.705841126081805,-0.708370174930854));
#43658=DIRECTION('center_axis',(5.15167520928809E-67,-1.18789542670764E-48,
-1.));
#43659=DIRECTION('ref_axis',(-4.33680868994202E-19,1.,-1.18789542670764E-48));
#43660=DIRECTION('center_axis',(-0.0555758110363383,-0.706157633406556,
-0.705870190622402));
#43661=DIRECTION('ref_axis',(0.0553775799352142,0.703694571287436,-0.708341212962447));
#43662=DIRECTION('center_axis',(5.15167520928809E-67,-1.18789542670764E-48,
-1.));
#43663=DIRECTION('ref_axis',(-4.33680868994202E-19,1.,-1.18789542670764E-48));
#43664=DIRECTION('center_axis',(-0.110808620201578,-0.699618093636773,-0.705872490429447));
#43665=DIRECTION('ref_axis',(0.110419233096311,0.697182591373295,-0.708338921172937));
#43666=DIRECTION('center_axis',(5.15167520928809E-67,-1.18789542670764E-48,
-1.));
#43667=DIRECTION('ref_axis',(-4.33680868994202E-19,1.,-1.18789542670764E-48));
#43668=DIRECTION('center_axis',(-0.165358045050148,-0.688765827029952,-0.705874176077394));
#43669=DIRECTION('ref_axis',(0.164780094682061,0.686371526838168,-0.708337241391707));
#43670=DIRECTION('center_axis',(5.15167520928809E-67,-1.18789542670764E-48,
-1.));
#43671=DIRECTION('ref_axis',(-4.33680868994202E-19,1.,-1.18789542670764E-48));
#43672=DIRECTION('center_axis',(-0.218887852522884,-0.673667540197305,-0.705875451692742));
#43673=DIRECTION('ref_axis',(0.218125006053241,0.671328261761849,-0.708335970210527));
#43674=DIRECTION('center_axis',(5.15167520928809E-67,-1.18789542670764E-48,
-1.));
#43675=DIRECTION('ref_axis',(-4.33680868994202E-19,1.,-1.18789542670764E-48));
#43676=DIRECTION('center_axis',(-0.271068063822912,-0.654416196007481,-0.705876439030512));
#43677=DIRECTION('ref_axis',(0.270125073931987,0.652145682815073,-0.708334986301609));
#43678=DIRECTION('center_axis',(5.15167520928809E-67,-1.18789542670764E-48,
-1.));
#43679=DIRECTION('ref_axis',(-4.33680868994202E-19,1.,-1.18789542670764E-48));
#43680=DIRECTION('center_axis',(-0.321577003370454,-0.631130405143677,-0.705877214964797));
#43681=DIRECTION('ref_axis',(0.32045969726294,0.628942147608801,-0.708334213060031));
#43682=DIRECTION('center_axis',(5.15167520928809E-67,-1.18789542670764E-48,
-1.));
#43683=DIRECTION('ref_axis',(-4.33680868994202E-19,1.,-1.18789542670764E-48));
#43684=DIRECTION('center_axis',(-0.370103289326527,-0.60395367709939,-0.705877830185799));
#43685=DIRECTION('ref_axis',(0.368818543504467,0.601860775526071,-0.708333599972782));
#43686=DIRECTION('center_axis',(5.15167520928809E-67,-1.18789542670764E-48,
-1.));
#43687=DIRECTION('ref_axis',(-4.33680868994202E-19,1.,-1.18789542670764E-48));
#43688=DIRECTION('center_axis',(-0.41634775729562,-0.5730535257704,-0.705878319256953));
#43689=DIRECTION('ref_axis',(0.414903461781904,0.571068576442378,-0.70833311259708));
#43690=DIRECTION('center_axis',(5.15167520928809E-67,-1.18789542670764E-48,
-1.));
#43691=DIRECTION('ref_axis',(-4.33680868994202E-19,1.,-1.18789542670764E-48));
#43692=DIRECTION('center_axis',(-0.460025307050912,-0.538620431161332,-0.705878706300378));
#43693=DIRECTION('ref_axis',(0.458430320957773,0.536755427393291,-0.708332726894923));
#43694=DIRECTION('center_axis',(5.15167520928809E-67,-1.18789542670764E-48,
-1.));
#43695=DIRECTION('ref_axis',(-4.33680868994202E-19,1.,-1.18789542670764E-48));
#43696=DIRECTION('center_axis',(-0.500866661619468,-0.500866661619444,-0.705879008440089));
#43697=DIRECTION('ref_axis',(0.499130761358181,0.499132905771117,-0.708332425801956));
#43698=DIRECTION('center_axis',(5.15167520928809E-67,-1.18789542670764E-48,
-1.));
#43699=DIRECTION('ref_axis',(-4.33680868994202E-19,1.,-1.18789542670764E-48));
#43700=DIRECTION('center_axis',(-0.538620028368883,-0.46002496303363,-0.705879237848664));
#43701=DIRECTION('ref_axis',(0.536753849182796,0.458432987266734,-0.70833219718798));
#43702=DIRECTION('center_axis',(5.15167520928809E-67,-1.18789542670764E-48,
-1.));
#43703=DIRECTION('ref_axis',(-4.33680868994202E-19,1.,-1.18789542670764E-48));
#43704=DIRECTION('center_axis',(-0.573052651970218,-0.416347122442612,-0.705879403087848));
#43705=DIRECTION('ref_axis',(0.571067623543181,0.414906617259055,-0.708332032521043));
#43706=DIRECTION('center_axis',(5.15167520928809E-67,-1.18789542670764E-48,
-1.));
#43707=DIRECTION('ref_axis',(-4.33680868994202E-19,1.,-1.18789542670764E-48));
#43708=DIRECTION('center_axis',(-0.603952249837038,-0.37010241469901,-0.705879509938305));
#43709=DIRECTION('ref_axis',(0.601860526500551,0.368822164724558,-0.708331926040589));
#43710=DIRECTION('center_axis',(5.15167520928809E-67,-1.18789542670764E-48,
-1.));
#43711=DIRECTION('ref_axis',(-4.33680868994202E-19,1.,-1.18789542670764E-48));
#43712=DIRECTION('center_axis',(-0.631128321246897,-0.32157594157199,-0.705879561909935));
#43713=DIRECTION('ref_axis',(0.628942707294004,0.320463768411799,-0.708331874248927));
#43714=DIRECTION('center_axis',(5.15167520928809E-67,-1.18789542670764E-48,
-1.));
#43715=DIRECTION('ref_axis',(-4.33680868994202E-19,1.,-1.18789542670764E-48));
#43716=DIRECTION('center_axis',(-0.654413322126778,-0.271066873422522,-0.705879560517184));
#43717=DIRECTION('ref_axis',(0.65214719270402,0.270129585578859,-0.708331875636879));
#43718=DIRECTION('center_axis',(5.15167520928809E-67,-1.18789542670764E-48,
-1.));
#43719=DIRECTION('ref_axis',(-4.33680868994202E-19,1.,-1.18789542670764E-48));
#43720=DIRECTION('center_axis',(-0.673663698306464,-0.218886604216857,-0.705879505353761));
#43721=DIRECTION('ref_axis',(0.671330916306719,0.218129954132939,-0.708331930609331));
#43722=DIRECTION('center_axis',(5.15167520928809E-67,-1.18789542670764E-48,
-1.));
#43723=DIRECTION('ref_axis',(-4.33680868994202E-19,1.,-1.18789542670764E-48));
#43724=DIRECTION('center_axis',(-0.688760770927255,-0.165356831187267,-0.705879393955794));
#43725=DIRECTION('ref_axis',(0.686375600198197,0.164785479532444,-0.708332041621602));
#43726=DIRECTION('center_axis',(5.15167520928809E-67,-1.18789542670764E-48,
-1.));
#43727=DIRECTION('ref_axis',(-4.33680868994202E-19,1.,-1.18789542670764E-48));
#43728=DIRECTION('center_axis',(-0.699611468639891,-0.110807570905155,-0.705879221381132));
#43729=DIRECTION('ref_axis',(0.697188483632974,0.110425058152362,-0.708332213598677));
#43730=DIRECTION('center_axis',(5.15167520928809E-67,-1.18789542670764E-48,
-1.));
#43731=DIRECTION('ref_axis',(-4.33680868994202E-19,1.,-1.18789542670764E-48));
#43732=DIRECTION('center_axis',(-0.706148902304619,-0.0555751238836977,
-0.705878979272859));
#43733=DIRECTION('ref_axis',(0.703702893730101,0.0553838490530483,-0.708332454868441));
#43734=DIRECTION('center_axis',(5.15167520928809E-67,-1.18789542670764E-48,
-1.));
#43735=DIRECTION('ref_axis',(-4.33680868994202E-19,1.,-1.18789542670764E-48));
#43736=DIRECTION('center_axis',(5.15167520928809E-67,-1.18789542670764E-48,
-1.));
#43737=DIRECTION('ref_axis',(-4.33680868994202E-19,1.,-1.18789542670764E-48));
#43738=DIRECTION('center_axis',(5.15167520928809E-67,-1.18789542670764E-48,
-1.));
#43739=DIRECTION('ref_axis',(-4.33680868994202E-19,1.,-1.18789542670764E-48));
#43740=DIRECTION('center_axis',(5.15167520928809E-67,-1.18789542670764E-48,
-1.));
#43741=DIRECTION('ref_axis',(-4.33680868994202E-19,1.,-1.18789542670764E-48));
#43742=DIRECTION('center_axis',(5.15167520928809E-67,-1.18789542670764E-48,
-1.));
#43743=DIRECTION('ref_axis',(-4.33680868994202E-19,1.,-1.18789542670764E-48));
#43744=DIRECTION('center_axis',(5.15167520928809E-67,-1.18789542670764E-48,
-1.));
#43745=DIRECTION('ref_axis',(-4.33680868994202E-19,1.,-1.18789542670764E-48));
#43746=DIRECTION('center_axis',(5.15167520928809E-67,-1.18789542670764E-48,
-1.));
#43747=DIRECTION('ref_axis',(-4.33680868994202E-19,1.,-1.18789542670764E-48));
#43748=DIRECTION('center_axis',(5.15167520928809E-67,-1.18789542670764E-48,
-1.));
#43749=DIRECTION('ref_axis',(-4.33680868994202E-19,1.,-1.18789542670764E-48));
#43750=DIRECTION('center_axis',(5.15167520928809E-67,-1.18789542670764E-48,
-1.));
#43751=DIRECTION('ref_axis',(-4.33680868994202E-19,1.,-1.18789542670764E-48));
#43752=DIRECTION('center_axis',(5.15167520928809E-67,-1.18789542670764E-48,
-1.));
#43753=DIRECTION('ref_axis',(-4.33680868994202E-19,1.,-1.18789542670764E-48));
#43754=DIRECTION('center_axis',(5.15167520928809E-67,-1.18789542670764E-48,
-1.));
#43755=DIRECTION('ref_axis',(-4.33680868994202E-19,1.,-1.18789542670764E-48));
#43756=DIRECTION('center_axis',(5.15167520928809E-67,-1.18789542670764E-48,
-1.));
#43757=DIRECTION('ref_axis',(-4.33680868994202E-19,1.,-1.18789542670764E-48));
#43758=DIRECTION('center_axis',(5.15167520928809E-67,-1.18789542670764E-48,
-1.));
#43759=DIRECTION('ref_axis',(-4.33680868994202E-19,1.,-1.18789542670764E-48));
#43760=DIRECTION('center_axis',(5.15167520928809E-67,-1.18789542670764E-48,
-1.));
#43761=DIRECTION('ref_axis',(-4.33680868994202E-19,1.,-1.18789542670764E-48));
#43762=DIRECTION('center_axis',(5.15167520928809E-67,-1.18789542670764E-48,
-1.));
#43763=DIRECTION('ref_axis',(-4.33680868994202E-19,1.,-1.18789542670764E-48));
#43764=DIRECTION('center_axis',(5.15167520928809E-67,-1.18789542670764E-48,
-1.));
#43765=DIRECTION('ref_axis',(-4.33680868994202E-19,1.,-1.18789542670764E-48));
#43766=DIRECTION('center_axis',(-0.271066873422527,0.654413322126802,-0.70587956051716));
#43767=DIRECTION('ref_axis',(-0.270129585578839,0.652147192704003,0.708331875636903));
#43768=DIRECTION('center_axis',(5.15167520928809E-67,-1.18789542670764E-48,
-1.));
#43769=DIRECTION('ref_axis',(-4.33680868994202E-19,1.,-1.18789542670764E-48));
#43770=DIRECTION('center_axis',(-0.218886604216929,0.673663698306674,-0.705879505353539));
#43771=DIRECTION('ref_axis',(-0.218129954131946,0.671330916306808,0.708331930609553));
#43772=DIRECTION('center_axis',(5.15167520928809E-67,-1.18789542670764E-48,
-1.));
#43773=DIRECTION('ref_axis',(-4.33680868994202E-19,1.,-1.18789542670764E-48));
#43774=DIRECTION('center_axis',(-0.16535683118721,0.688760770927084,-0.705879393955974));
#43775=DIRECTION('ref_axis',(-0.164785479532737,0.686375600198312,0.708332041621423));
#43776=DIRECTION('center_axis',(5.15167520928809E-67,-1.18789542670764E-48,
-1.));
#43777=DIRECTION('ref_axis',(-4.33680868994202E-19,1.,-1.18789542670764E-48));
#43778=DIRECTION('center_axis',(-0.110807570905113,0.699611468639715,-0.705879221381313));
#43779=DIRECTION('ref_axis',(-0.110425058151779,0.69718848363325,0.708332213598496));
#43780=DIRECTION('center_axis',(5.15167520928809E-67,-1.18789542670764E-48,
-1.));
#43781=DIRECTION('ref_axis',(-4.33680868994202E-19,1.,-1.18789542670764E-48));
#43782=DIRECTION('center_axis',(-0.0555751238836985,0.706148902304822,-0.705878979272656));
#43783=DIRECTION('ref_axis',(-0.0553838490532064,0.703702893729884,0.708332454868643));
#43784=DIRECTION('center_axis',(5.15167520928809E-67,-1.18789542670764E-48,
-1.));
#43785=DIRECTION('ref_axis',(-4.33680868994202E-19,1.,-1.18789542670764E-48));
#43786=DIRECTION('',(8.69022643068848E-17,-0.707106781186538,-0.707106781186557));
#43787=DIRECTION('center_axis',(5.15167520928809E-67,-1.18789542670764E-48,
-1.));
#43788=DIRECTION('ref_axis',(-4.33680868994202E-19,1.,-1.18789542670764E-48));
#43789=DIRECTION('center_axis',(5.15167520928809E-67,-1.18789542670764E-48,
-1.));
#43790=DIRECTION('ref_axis',(-4.33680868994202E-19,1.,-1.18789542670764E-48));
#43791=DIRECTION('center_axis',(5.15167520928809E-67,-1.18789542670764E-48,
-1.));
#43792=DIRECTION('ref_axis',(0.,1.,0.));
#43793=DIRECTION('center_axis',(5.15167520928809E-67,-1.18789542670764E-48,
-1.));
#43794=DIRECTION('ref_axis',(-4.33680868994202E-19,1.,-1.18789542670764E-48));
#43795=DIRECTION('center_axis',(1.,0.,5.15167520928809E-67));
#43796=DIRECTION('ref_axis',(0.,-1.,0.));
#43797=DIRECTION('center_axis',(5.15167520928809E-67,-1.18789542670764E-48,
-1.));
#43798=DIRECTION('ref_axis',(-4.33680868994202E-19,1.,-1.18789542670764E-48));
#43799=DIRECTION('center_axis',(5.15167520928809E-67,-1.18789542670764E-48,
-1.));
#43800=DIRECTION('ref_axis',(-4.33680868994202E-19,1.,-1.18789542670764E-48));
#43801=DIRECTION('',(-5.15167520928809E-67,1.18789542670764E-48,1.));
#43802=DIRECTION('center_axis',(5.15167520928809E-67,-1.18789542670764E-48,
-1.));
#43803=DIRECTION('ref_axis',(0.,1.,0.));
#43804=DIRECTION('center_axis',(5.15167520928809E-67,-1.18789542670764E-48,
-1.));
#43805=DIRECTION('ref_axis',(-4.33680868994202E-19,1.,-1.18789542670764E-48));
#43806=DIRECTION('center_axis',(-1.,0.,-5.15167520928809E-67));
#43807=DIRECTION('ref_axis',(0.,-1.,0.));
#43808=DIRECTION('center_axis',(5.15167520928809E-67,-1.18789542670764E-48,
-1.));
#43809=DIRECTION('ref_axis',(0.,1.,0.));
#43810=DIRECTION('center_axis',(1.,0.,5.15167520928809E-67));
#43811=DIRECTION('ref_axis',(0.,-1.,0.));
#43812=DIRECTION('center_axis',(5.15167520928809E-67,-1.18789542670764E-48,
-1.));
#43813=DIRECTION('ref_axis',(-4.33680868994202E-19,1.,-1.18789542670764E-48));
#43814=DIRECTION('center_axis',(5.15167520928809E-67,-1.18789542670764E-48,
-1.));
#43815=DIRECTION('ref_axis',(0.,1.,0.));
#43816=DIRECTION('center_axis',(-0.726741019926939,-0.686911553067863,9.06501466507717E-5));
#43817=DIRECTION('ref_axis',(0.686840456252471,-0.726663889286196,0.0144837723800636));
#43818=DIRECTION('center_axis',(5.15167520928809E-67,-1.18789542670764E-48,
-1.));
#43819=DIRECTION('ref_axis',(-4.33680868994202E-19,1.,-1.18789542670764E-48));
#43820=DIRECTION('center_axis',(0.0503838293498797,0.99872992276226,0.000105448247773495));
#43821=DIRECTION('ref_axis',(0.998655285166785,-0.0503813543085061,0.012220496982052));
#43822=DIRECTION('center_axis',(5.15167520928809E-67,-1.18789542670764E-48,
-1.));
#43823=DIRECTION('ref_axis',(0.,1.,0.));
#43824=DIRECTION('center_axis',(-0.0281309337977199,0.999604241409737,0.000105448247664664));
#43825=DIRECTION('ref_axis',(0.999529639708461,0.0281275452111534,0.0122204969076063));
#43826=DIRECTION('center_axis',(-0.670606260601171,-0.741813477246852,9.06501467500846E-5));
#43827=DIRECTION('ref_axis',(0.741736547998884,-0.670534945920291,0.0144837723805249));
#43828=DIRECTION('center_axis',(5.15167520928809E-67,-1.18789542670764E-48,
-1.));
#43829=DIRECTION('ref_axis',(-4.33680868994202E-19,1.,-1.18789542670764E-48));
#43830=DIRECTION('center_axis',(5.15167520928809E-67,-1.18789542670764E-48,
-1.));
#43831=DIRECTION('ref_axis',(0.,1.,0.));
#43832=DIRECTION('center_axis',(-0.106472260383779,0.994315667506771,0.000105448247699395));
#43833=DIRECTION('ref_axis',(0.99424156164256,0.106463029061011,0.0122204969504906));
#43834=DIRECTION('center_axis',(-0.610336990679751,-0.792141874660428,9.06501467512865E-5));
#43835=DIRECTION('ref_axis',(0.792059587274889,-0.610271931637935,0.0144837723275367));
#43836=DIRECTION('center_axis',(5.15167520928809E-67,-1.18789542670764E-48,
-1.));
#43837=DIRECTION('ref_axis',(-4.33680868994202E-19,1.,-1.18789542670764E-48));
#43838=DIRECTION('center_axis',(5.15167520928809E-67,-1.18789542670764E-48,
-1.));
#43839=DIRECTION('ref_axis',(0.,1.,0.));
#43840=DIRECTION('center_axis',(-0.18415715007879,0.982896806870144,0.000105448247763879));
#43841=DIRECTION('ref_axis',(0.982823653730846,0.18414213293402,0.0122204969481005));
#43842=DIRECTION('center_axis',(-0.546304790252955,-0.837586454002944,9.06501468511952E-5));
#43843=DIRECTION('ref_axis',(0.837499315807933,-0.546246387960026,0.0144837723631749));
#43844=DIRECTION('center_axis',(5.15167520928809E-67,-1.18789542670764E-48,
-1.));
#43845=DIRECTION('ref_axis',(-4.33680868994202E-19,1.,-1.18789542670764E-48));
#43846=DIRECTION('center_axis',(5.15167520928809E-67,-1.18789542670764E-48,
-1.));
#43847=DIRECTION('ref_axis',(0.,1.,0.));
#43848=DIRECTION('center_axis',(-0.260706649705391,0.965418060572754,0.000105448247684059));
#43849=DIRECTION('ref_axis',(0.965346311171948,0.260685939324359,0.0122204969329739));
#43850=DIRECTION('center_axis',(-0.478904439129961,-0.877867034330466,9.06501466909999E-5));
#43851=DIRECTION('ref_axis',(0.877775582562065,-0.478853053655646,0.0144837723846339));
#43852=DIRECTION('center_axis',(5.15167520928809E-67,-1.18789542670764E-48,
-1.));
#43853=DIRECTION('ref_axis',(-4.33680868994202E-19,1.,-1.18789542670764E-48));
#43854=DIRECTION('center_axis',(5.15167520928809E-67,-1.18789542670764E-48,
-1.));
#43855=DIRECTION('ref_axis',(0.,1.,0.));
#43856=DIRECTION('center_axis',(-0.33564880614276,0.941987190897842,0.000105448247631265));
#43857=DIRECTION('ref_axis',(0.941917287593993,0.335622530211717,0.0122204969563928));
#43858=DIRECTION('center_axis',(-0.408551482887427,-0.912735272471178,9.06501467675252E-5));
#43859=DIRECTION('ref_axis',(0.91264007095957,-0.408507431040139,0.0144837724331839));
#43860=DIRECTION('center_axis',(5.15167520928809E-67,-1.18789542670764E-48,
-1.));
#43861=DIRECTION('ref_axis',(-4.33680868994202E-19,1.,-1.18789542670764E-48));
#43862=DIRECTION('center_axis',(5.15167520928809E-67,-1.18789542670764E-48,
-1.));
#43863=DIRECTION('ref_axis',(0.,1.,0.));
#43864=DIRECTION('center_axis',(-0.408521576075341,0.912748656948662,0.000105448247753309));
#43865=DIRECTION('ref_axis',(0.912681030719062,0.40848989659417,0.0122204969651243));
#43866=DIRECTION('center_axis',(-0.335679670896088,-0.941976194141681,9.06501466394305E-5));
#43867=DIRECTION('ref_axis',(0.941877829837658,-0.335643224270894,0.0144837723450194));
#43868=DIRECTION('center_axis',(5.15167520928809E-67,-1.18789542670764E-48,
-1.));
#43869=DIRECTION('ref_axis',(-4.33680868994202E-19,1.,-1.18789542670764E-48));
#43870=DIRECTION('center_axis',(5.15167520928809E-67,-1.18789542670764E-48,
-1.));
#43871=DIRECTION('ref_axis',(0.,1.,0.));
#43872=DIRECTION('center_axis',(-0.478875674645407,0.877882724009063,0.000105448247283112));
#43873=DIRECTION('ref_axis',(0.877817791790398,0.478838786927794,0.012220497115417));
#43874=DIRECTION('center_axis',(-0.260738282108194,-0.965409519336649,9.06501468435925E-5));
#43875=DIRECTION('ref_axis',(0.965308598687812,-0.260709665410158,0.0144837723364994));
#43876=DIRECTION('center_axis',(5.15167520928809E-67,-1.18789542670764E-48,
-1.));
#43877=DIRECTION('ref_axis',(-4.33680868994202E-19,1.,-1.18789542670764E-48));
#43878=DIRECTION('center_axis',(5.15167520928809E-67,-1.18789542670764E-48,
-1.));
#43879=DIRECTION('ref_axis',(0.,1.,0.));
#43880=DIRECTION('center_axis',(-0.546277345437336,0.837604352151184,0.000105448247639474));
#43881=DIRECTION('ref_axis',(0.837542514276272,0.546235476910692,0.0122204968773897));
#43882=DIRECTION('center_axis',(-0.184189355107295,-0.982890773813505,9.06501468099581E-5));
#43883=DIRECTION('ref_axis',(0.982787919029019,-0.184168744767822,0.0144837723419927));
#43884=DIRECTION('center_axis',(5.15167520928809E-67,-1.18789542670764E-48,
-1.));
#43885=DIRECTION('ref_axis',(-4.33680868994202E-19,1.,-1.18789542670764E-48));
#43886=DIRECTION('center_axis',(5.15167520928809E-67,-1.18789542670764E-48,
-1.));
#43887=DIRECTION('ref_axis',(0.,1.,0.));
#43888=DIRECTION('center_axis',(-0.610311034740724,0.792161870929404,0.000105448247072483));
#43889=DIRECTION('ref_axis',(0.792103508642798,0.610264443533926,0.0122204972891987));
#43890=DIRECTION('center_axis',(-0.106504839483277,-0.994312179825427,9.06501466463657E-5));
#43891=DIRECTION('ref_axis',(0.994208025037708,-0.106492362571804,0.014483772453865));
#43892=DIRECTION('center_axis',(5.15167520928809E-67,-1.18789542670764E-48,
-1.));
#43893=DIRECTION('ref_axis',(-4.33680868994202E-19,1.,-1.18789542670764E-48));
#43894=DIRECTION('center_axis',(5.15167520928809E-67,-1.18789542670764E-48,
-1.));
#43895=DIRECTION('ref_axis',(0.,1.,0.));
#43896=DIRECTION('center_axis',(-0.670581953563772,0.74183544835446,0.000105448247723866));
#43897=DIRECTION('ref_axis',(0.741780921486778,0.670530926933108,0.012220496898794));
#43898=DIRECTION('center_axis',(-0.0281636861068304,-0.999603320606443,
9.06501467794172E-5));
#43899=DIRECTION('ref_axis',(0.999498507966719,-0.0281594195479949,0.0144837724030356));
#43900=DIRECTION('center_axis',(5.15167520928809E-67,-1.18789542670764E-48,
-1.));
#43901=DIRECTION('ref_axis',(-4.33680868994202E-19,1.,-1.18789542670764E-48));
#43902=DIRECTION('center_axis',(5.15167520928809E-67,-1.18789542670764E-48,
-1.));
#43903=DIRECTION('ref_axis',(0.,1.,0.));
#43904=DIRECTION('center_axis',(-0.726718511653027,0.686935363554299,0.000105448247728815));
#43905=DIRECTION('ref_axis',(0.686885008277766,0.726663364191397,0.0122204969332444));
#43906=DIRECTION('center_axis',(0.050351105759542,-0.998731574514065,9.06501467573609E-5));
#43907=DIRECTION('ref_axis',(0.998626750226961,0.0503471356610921,0.014483772362966));
#43908=DIRECTION('center_axis',(5.15167520928809E-67,-1.18789542670764E-48,
-1.));
#43909=DIRECTION('ref_axis',(-4.33680868994202E-19,1.,-1.18789542670764E-48));
#43910=DIRECTION('center_axis',(5.15167520928809E-67,-1.18789542670764E-48,
-1.));
#43911=DIRECTION('ref_axis',(0.,1.,0.));
#43912=DIRECTION('center_axis',(-0.778374608459537,0.627800093808634,0.000105448247783041));
#43913=DIRECTION('ref_axis',(0.627754220580437,0.778315680169477,0.01222049695274));
#43914=DIRECTION('center_axis',(0.128555466315269,-0.991702316152894,9.06501465984867E-5));
#43915=DIRECTION('ref_axis',(0.99159812649388,0.128543284036463,0.0144837724004731));
#43916=DIRECTION('center_axis',(5.15167520928809E-67,-1.18789542670764E-48,
-1.));
#43917=DIRECTION('ref_axis',(-4.33680868994202E-19,1.,-1.18789542670764E-48));
#43918=DIRECTION('center_axis',(5.15167520928809E-67,-1.18789542670764E-48,
-1.));
#43919=DIRECTION('ref_axis',(0.,1.,0.));
#43920=DIRECTION('center_axis',(-0.825231766969855,0.564794227718802,0.000105448247237627));
#43921=DIRECTION('ref_axis',(0.564753119361559,0.825169421162197,0.0122204971352771));
#43922=DIRECTION('center_axis',(0.205967239672467,-0.97855888323813,9.06501466256469E-5));
#43923=DIRECTION('ref_axis',(0.978455970572454,0.205946920321296,0.0144837723432324));
#43924=DIRECTION('center_axis',(5.15167520928809E-67,-1.18789542670764E-48,
-1.));
#43925=DIRECTION('ref_axis',(-4.33680868994202E-19,1.,-1.18789542670764E-48));
#43926=DIRECTION('center_axis',(5.15167520928809E-67,-1.18789542670764E-48,
-1.));
#43927=DIRECTION('ref_axis',(0.,1.,0.));
#43928=DIRECTION('center_axis',(-0.867001097222074,0.498306217396881,0.00010544824406792));
#43929=DIRECTION('ref_axis',(0.498270127350421,0.866935718266621,0.0122204985059196));
#43930=DIRECTION('center_axis',(0.282109156506117,-0.959382309404316,9.06501467341775E-5));
#43931=DIRECTION('ref_axis',(0.959281308220891,0.282080825357731,0.0144837724201092));
#43932=DIRECTION('center_axis',(5.15167520928809E-67,-1.18789542670764E-48,
-1.));
#43933=DIRECTION('ref_axis',(-4.33680868994202E-19,1.,-1.18789542670764E-48));
#43934=DIRECTION('center_axis',(5.15167520928809E-67,-1.18789542670764E-48,
-1.));
#43935=DIRECTION('ref_axis',(0.,1.,0.));
#43936=DIRECTION('center_axis',(-0.903425077395399,0.428745983554114,0.00010544824771057));
#43937=DIRECTION('ref_axis',(0.42871513434286,0.903357068405985,0.0122204969754959));
#43938=DIRECTION('center_axis',(0.356511776578972,-0.934290824606052,9.06501467185522E-5));
#43939=DIRECTION('ref_axis',(0.934192357612503,0.356475608304786,0.0144837723720686));
#43940=DIRECTION('center_axis',(5.15167520928809E-67,-1.18789542670764E-48,
-1.));
#43941=DIRECTION('ref_axis',(-4.33680868994202E-19,1.,-1.18789542670764E-48));
#43942=DIRECTION('center_axis',(5.15167520928809E-67,-1.18789542670764E-48,
-1.));
#43943=DIRECTION('ref_axis',(0.,1.,0.));
#43944=DIRECTION('center_axis',(-0.934279141551227,0.35654238814336,0.000105448247725771));
#43945=DIRECTION('ref_axis',(0.356516969954114,0.934208921810617,0.0122204968876431));
#43946=DIRECTION('center_axis',(0.428716382996855,-0.903439126190938,9.06501466905075E-5));
#43947=DIRECTION('ref_axis',(0.903343800467886,0.428672600585895,0.0144837724078269));
#43948=DIRECTION('center_axis',(5.15167520928809E-67,-1.18789542670764E-48,
-1.));
#43949=DIRECTION('ref_axis',(-4.33680868994202E-19,1.,-1.18789542670764E-48));
#43950=DIRECTION('center_axis',(5.15167520928809E-67,-1.18789542670764E-48,
-1.));
#43951=DIRECTION('ref_axis',(0.,1.,0.));
#43952=DIRECTION('center_axis',(-0.959373064120116,0.282140590347166,0.000105448247704078));
#43953=DIRECTION('ref_axis',(0.282120759890668,0.959301066553995,0.0122204970062476));
#43954=DIRECTION('center_axis',(0.498277810351468,-0.867017425138559,9.06501469271671E-5));
#43955=DIRECTION('ref_axis',(0.86692582840188,0.498226683737388,0.0144837723593644));
#43956=DIRECTION('center_axis',(5.15167520928809E-67,-1.18789542670764E-48,
-1.));
#43957=DIRECTION('ref_axis',(-4.33680868994202E-19,1.,-1.18789542670764E-48));
#43958=DIRECTION('center_axis',(5.15167520928809E-67,-1.18789542670764E-48,
-1.));
#43959=DIRECTION('ref_axis',(0.,1.,0.));
#43960=DIRECTION('center_axis',(-0.978552132724721,0.205999301990486,0.000105448247790145));
#43961=DIRECTION('ref_axis',(0.205985181528783,0.978478801224291,0.0122204969305395));
#43962=DIRECTION('center_axis',(0.564767189310343,-0.825250273348059,9.06501467424166E-5));
#43963=DIRECTION('ref_axis',(0.825162970321744,0.56470903370561,0.0144837723356968));
#43964=DIRECTION('center_axis',(5.15167520928809E-67,-1.18789542670764E-48,
-1.));
#43965=DIRECTION('ref_axis',(-4.33680868994202E-19,1.,-1.18789542670764E-48));
#43966=DIRECTION('center_axis',(5.15167520928809E-67,-1.18789542670764E-48,
-1.));
#43967=DIRECTION('ref_axis',(0.,1.,0.));
#43968=DIRECTION('center_axis',(-0.991698102029505,0.128587959435343,0.000105448247905715));
#43969=DIRECTION('ref_axis',(0.12857963602553,0.991623888707005,0.0122204969268892));
#43970=DIRECTION('center_axis',(0.627774590743107,-0.778395179198763,9.06501466692162E-5));
#43971=DIRECTION('ref_axis',(0.778312708134479,0.627709764696018,0.0144837723553914));
#43972=DIRECTION('center_axis',(5.15167520928809E-67,-1.18789542670764E-48,
-1.));
#43973=DIRECTION('ref_axis',(-4.33680868994202E-19,1.,-1.18789542670764E-48));
#43974=DIRECTION('center_axis',(5.15167520928809E-67,-1.18789542670764E-48,
-1.));
#43975=DIRECTION('ref_axis',(0.,1.,0.));
#43976=DIRECTION('center_axis',(-0.998729922762266,0.05038382934976,0.000105448247701369));
#43977=DIRECTION('ref_axis',(0.0503813543083786,0.998655285166624,0.0122204969957313));
#43978=DIRECTION('center_axis',(0.686911553067687,-0.726741019927105,9.06501465529425E-5));
#43979=DIRECTION('ref_axis',(0.726663889286156,0.686840456252101,0.0144837723995786));
#43980=DIRECTION('center_axis',(5.15167520928809E-67,-1.18789542670764E-48,
-1.));
#43981=DIRECTION('ref_axis',(-4.33680868994202E-19,1.,-1.18789542670764E-48));
#43982=DIRECTION('center_axis',(5.15167520928809E-67,-1.18789542670764E-48,
-1.));
#43983=DIRECTION('ref_axis',(0.,1.,0.));
#43984=DIRECTION('center_axis',(-0.999604241409733,-0.0281309337978441,
0.000105448247608528));
#43985=DIRECTION('ref_axis',(0.0281275452112647,-0.999529639708088,-0.0122204969378127));
#43986=DIRECTION('center_axis',(0.741813477246663,-0.67060626060138,9.06501466416355E-5));
#43987=DIRECTION('ref_axis',(0.670534945920398,0.741736547998582,0.0144837723910712));
#43988=DIRECTION('center_axis',(5.15167520928809E-67,-1.18789542670764E-48,
-1.));
#43989=DIRECTION('ref_axis',(-4.33680868994202E-19,1.,-1.18789542670764E-48));
#43990=DIRECTION('center_axis',(5.15167520928809E-67,-1.18789542670764E-48,
-1.));
#43991=DIRECTION('ref_axis',(0.,1.,0.));
#43992=DIRECTION('center_axis',(-0.994315667506803,-0.106472260383486,0.000105448247832577));
#43993=DIRECTION('ref_axis',(0.10646302906079,-0.994241561643227,-0.0122204968981425));
#43994=DIRECTION('center_axis',(0.792141874660394,-0.610336990679795,9.06501467163515E-5));
#43995=DIRECTION('ref_axis',(0.610271931637984,0.792059587274861,0.0144837723269713));
#43996=DIRECTION('center_axis',(5.15167520928809E-67,-1.18789542670764E-48,
-1.));
#43997=DIRECTION('ref_axis',(-4.33680868994202E-19,1.,-1.18789542670764E-48));
#43998=DIRECTION('center_axis',(5.15167520928809E-67,-1.18789542670764E-48,
-1.));
#43999=DIRECTION('ref_axis',(0.,1.,0.));
#44000=DIRECTION('center_axis',(-0.982896806870098,-0.184157150079038,0.000105448247610839));
#44001=DIRECTION('ref_axis',(0.184142132934261,-0.982823653730751,-0.0122204969521754));
#44002=DIRECTION('center_axis',(0.837586454002892,-0.546304790253034,9.06501468389122E-5));
#44003=DIRECTION('ref_axis',(0.546246387959946,0.837499315807641,0.014483772383082));
#44004=DIRECTION('center_axis',(5.15167520928809E-67,-1.18789542670764E-48,
-1.));
#44005=DIRECTION('ref_axis',(-4.33680868994202E-19,1.,-1.18789542670764E-48));
#44006=DIRECTION('center_axis',(5.15167520928809E-67,-1.18789542670764E-48,
-1.));
#44007=DIRECTION('ref_axis',(0.,1.,0.));
#44008=DIRECTION('center_axis',(-0.965418060572767,-0.260706649705342,0.000105448247695262));
#44009=DIRECTION('ref_axis',(0.260685939324476,-0.965346311172558,-0.0122204968822783));
#44010=DIRECTION('center_axis',(0.877867034330398,-0.478904439130086,9.06501466177592E-5));
#44011=DIRECTION('ref_axis',(0.478853053655353,0.877775582561241,0.0144837724443041));
#44012=DIRECTION('center_axis',(5.15167520928809E-67,-1.18789542670764E-48,
-1.));
#44013=DIRECTION('ref_axis',(-4.33680868994202E-19,1.,-1.18789542670764E-48));
#44014=DIRECTION('center_axis',(5.15167520928809E-67,-1.18789542670764E-48,
-1.));
#44015=DIRECTION('ref_axis',(0.,1.,0.));
#44016=DIRECTION('center_axis',(-0.941987190897914,-0.335648806142557,0.000105448247712849));
#44017=DIRECTION('ref_axis',(0.335622530211483,-0.941917287593983,-0.0122204969636003));
#44018=DIRECTION('center_axis',(0.912735272471151,-0.408551482887487,9.06501467033935E-5));
#44019=DIRECTION('ref_axis',(0.408507431040848,0.912640070960968,0.0144837723251257));
#44020=DIRECTION('center_axis',(5.15167520928809E-67,-1.18789542670764E-48,
-1.));
#44021=DIRECTION('ref_axis',(-4.33680868994202E-19,1.,-1.18789542670764E-48));
#44022=DIRECTION('center_axis',(5.15167520928809E-67,-1.18789542670764E-48,
-1.));
#44023=DIRECTION('ref_axis',(0.,1.,0.));
#44024=DIRECTION('center_axis',(-0.912748656948201,-0.408521576076371,0.000105448247247158));
#44025=DIRECTION('ref_axis',(0.408489896594259,-0.912681030716532,-0.012220497151094));
#44026=DIRECTION('center_axis',(0.941976194141716,-0.335679670895989,9.06501466623777E-5));
#44027=DIRECTION('ref_axis',(0.335643224270751,0.941877829837572,0.0144837723539316));
#44028=DIRECTION('center_axis',(5.15167520928809E-67,-1.18789542670764E-48,
-1.));
#44029=DIRECTION('ref_axis',(-4.33680868994202E-19,1.,-1.18789542670764E-48));
#44030=DIRECTION('center_axis',(5.15167520928809E-67,-1.18789542670764E-48,
-1.));
#44031=DIRECTION('ref_axis',(0.,1.,0.));
#44032=DIRECTION('center_axis',(-0.877882724009451,-0.478875674644697,0.000105448247674909));
#44033=DIRECTION('ref_axis',(0.478838786928496,-0.877817791793333,-0.0122204968770904));
#44034=DIRECTION('center_axis',(0.965409519336493,-0.26073828210877,9.06501465579451E-5));
#44035=DIRECTION('ref_axis',(0.260709665410522,0.965308598686875,0.0144837723924504));
#44036=DIRECTION('center_axis',(5.15167520928809E-67,-1.18789542670764E-48,
-1.));
#44037=DIRECTION('ref_axis',(-4.33680868994202E-19,1.,-1.18789542670764E-48));
#44038=DIRECTION('center_axis',(5.15167520928809E-67,-1.18789542670764E-48,
-1.));
#44039=DIRECTION('ref_axis',(0.,1.,0.));
#44040=DIRECTION('center_axis',(-0.837604352151306,-0.546277345437149,0.00010544824776483));
#44041=DIRECTION('ref_axis',(0.546235476910197,-0.837542514275933,-0.0122204969227218));
#44042=DIRECTION('center_axis',(0.982890773813463,-0.184189355107518,9.06501466980053E-5));
#44043=DIRECTION('ref_axis',(0.184168744767822,0.982787919027818,0.0144837724235038));
#44044=DIRECTION('center_axis',(5.15167520928809E-67,-1.18789542670764E-48,
-1.));
#44045=DIRECTION('ref_axis',(-4.33680868994202E-19,1.,-1.18789542670764E-48));
#44046=DIRECTION('center_axis',(5.15167520928809E-67,-1.18789542670764E-48,
-1.));
#44047=DIRECTION('ref_axis',(0.,1.,0.));
#44048=DIRECTION('center_axis',(-0.792161870930109,-0.610311034739809,0.000105448247597277));
#44049=DIRECTION('ref_axis',(0.610264443535208,-0.792103508646315,-0.0122204969972532));
#44050=DIRECTION('center_axis',(0.994312179825469,-0.106504839482882,9.06501468290203E-5));
#44051=DIRECTION('ref_axis',(0.106492362571566,0.994208025039157,0.0144837723561435));
#44052=DIRECTION('center_axis',(5.15167520928809E-67,-1.18789542670764E-48,
-1.));
#44053=DIRECTION('ref_axis',(-4.33680868994202E-19,1.,-1.18789542670764E-48));
#44054=DIRECTION('center_axis',(5.15167520928809E-67,-1.18789542670764E-48,
-1.));
#44055=DIRECTION('ref_axis',(0.,1.,0.));
#44056=DIRECTION('center_axis',(-0.741835448354634,-0.670581953563579,0.000105448247853962));
#44057=DIRECTION('ref_axis',(0.67053092693267,-0.741780921486687,-0.0122204969283275));
#44058=DIRECTION('center_axis',(0.99960332060645,-0.0281636861065795,9.06501468718404E-5));
#44059=DIRECTION('ref_axis',(0.0281594195477731,0.999498507967606,0.014483772342229));
#44060=DIRECTION('center_axis',(5.15167520928809E-67,-1.18789542670764E-48,
-1.));
#44061=DIRECTION('ref_axis',(-4.33680868994202E-19,1.,-1.18789542670764E-48));
#44062=DIRECTION('center_axis',(5.15167520928809E-67,-1.18789542670764E-48,
-1.));
#44063=DIRECTION('ref_axis',(0.,1.,0.));
#44064=DIRECTION('center_axis',(-0.686935363552547,-0.726718511654683,0.000105448246665782));
#44065=DIRECTION('ref_axis',(0.726663364188996,-0.686885008272227,-0.0122204973873402));
#44066=DIRECTION('center_axis',(0.998731574514055,0.0503511057597249,9.06501467982717E-5));
#44067=DIRECTION('ref_axis',(0.050347135661256,-0.998626750226507,-0.0144837723936806));
#44068=DIRECTION('center_axis',(5.15167520928809E-67,-1.18789542670764E-48,
-1.));
#44069=DIRECTION('ref_axis',(-4.33680868994202E-19,1.,-1.18789542670764E-48));
#44070=DIRECTION('center_axis',(5.15167520928809E-67,-1.18789542670764E-48,
-1.));
#44071=DIRECTION('ref_axis',(0.,1.,0.));
#44072=DIRECTION('center_axis',(-0.627800093808639,-0.778374608459533,0.000105448247779514));
#44073=DIRECTION('ref_axis',(0.778315680170178,-0.627754220581,-0.0122204968791585));
#44074=DIRECTION('center_axis',(0.991702316152886,0.12855546631533,9.06501466251883E-5));
#44075=DIRECTION('ref_axis',(0.128543284036466,-0.991598126493403,-0.0144837724330683));
#44076=DIRECTION('center_axis',(5.15167520928809E-67,-1.18789542670764E-48,
-1.));
#44077=DIRECTION('ref_axis',(-4.33680868994202E-19,1.,-1.18789542670764E-48));
#44078=DIRECTION('center_axis',(5.15167520928809E-67,-1.18789542670764E-48,
-1.));
#44079=DIRECTION('ref_axis',(0.,1.,0.));
#44080=DIRECTION('center_axis',(-0.564794227719968,-0.825231766969057,0.000105448247863909));
#44081=DIRECTION('ref_axis',(0.825169421163414,-0.564753119364088,-0.0122204969362205));
#44082=DIRECTION('center_axis',(0.978558883238036,0.205967239672914,9.06501468463484E-5));
#44083=DIRECTION('ref_axis',(0.205946920321936,-0.978455970573291,-0.014483772277592));
#44084=DIRECTION('center_axis',(5.15167520928809E-67,-1.18789542670764E-48,
-1.));
#44085=DIRECTION('ref_axis',(-4.33680868994202E-19,1.,-1.18789542670764E-48));
#44086=DIRECTION('center_axis',(5.15167520928809E-67,-1.18789542670764E-48,
-1.));
#44087=DIRECTION('ref_axis',(0.,1.,0.));
#44088=DIRECTION('center_axis',(-0.498306217403848,-0.86700109721807,0.000105448247661773));
#44089=DIRECTION('ref_axis',(0.866935718279092,-0.498270127366718,-0.0122204969566953));
#44090=DIRECTION('center_axis',(0.959382309404258,0.282109156506314,9.06501467982869E-5));
#44091=DIRECTION('ref_axis',(0.282080825358155,-0.959281308221622,-0.014483772363392));
#44092=DIRECTION('center_axis',(5.15167520928809E-67,-1.18789542670764E-48,
-1.));
#44093=DIRECTION('ref_axis',(-4.33680868994202E-19,1.,-1.18789542670764E-48));
#44094=DIRECTION('center_axis',(5.15167520928809E-67,-1.18789542670764E-48,
-1.));
#44095=DIRECTION('ref_axis',(0.,1.,0.));
#44096=DIRECTION('center_axis',(-0.428745983554159,-0.903425077395378,0.000105448247692435));
#44097=DIRECTION('ref_axis',(0.903357068405516,-0.428715134342697,-0.0122204970158381));
#44098=DIRECTION('center_axis',(0.934290824605943,0.356511776579256,9.06501468588022E-5));
#44099=DIRECTION('ref_axis',(0.35647560830508,-0.934192357612417,-0.0144837723703894));
#44100=DIRECTION('center_axis',(5.15167520928809E-67,-1.18789542670764E-48,
-1.));
#44101=DIRECTION('ref_axis',(-4.33680868994202E-19,1.,-1.18789542670764E-48));
#44102=DIRECTION('center_axis',(5.15167520928809E-67,-1.18789542670764E-48,
-1.));
#44103=DIRECTION('ref_axis',(0.,1.,0.));
#44104=DIRECTION('center_axis',(-0.356542388142294,-0.934279141551633,0.000105448247232403));
#44105=DIRECTION('ref_axis',(0.934208921807365,-0.356516969951681,-0.0122204972072322));
#44106=DIRECTION('center_axis',(0.903439126190767,0.428716382997215,9.06501468179925E-5));
#44107=DIRECTION('ref_axis',(0.428672600586429,-0.903343800468082,-0.0144837723797852));
#44108=DIRECTION('center_axis',(5.15167520928809E-67,-1.18789542670764E-48,
-1.));
#44109=DIRECTION('ref_axis',(-4.33680868994202E-19,1.,-1.18789542670764E-48));
#44110=DIRECTION('center_axis',(5.15167520928809E-67,-1.18789542670764E-48,
-1.));
#44111=DIRECTION('ref_axis',(0.,1.,0.));
#44112=DIRECTION('center_axis',(-0.282140590347279,-0.959373064120083,0.000105448247741099));
#44113=DIRECTION('ref_axis',(0.959301066555032,-0.282120759891086,-0.012220496915153));
#44114=DIRECTION('center_axis',(0.867017425138588,0.498277810351419,9.06501468672452E-5));
#44115=DIRECTION('ref_axis',(0.498226683737162,-0.866925828401598,-0.0144837723840689));
#44116=DIRECTION('center_axis',(5.15167520928809E-67,-1.18789542670764E-48,
-1.));
#44117=DIRECTION('ref_axis',(-4.33680868994202E-19,1.,-1.18789542670764E-48));
#44118=DIRECTION('center_axis',(5.15167520928809E-67,-1.18789542670764E-48,
-1.));
#44119=DIRECTION('ref_axis',(0.,1.,0.));
#44120=DIRECTION('center_axis',(-0.20599930198994,-0.978552132724836,0.000105448247552452));
#44121=DIRECTION('ref_axis',(0.97847880122346,-0.205985181528044,-0.0122204970095074));
#44122=DIRECTION('center_axis',(0.825250273348004,0.564767189310424,9.06501467639861E-5));
#44123=DIRECTION('ref_axis',(0.56470903370563,-0.825162970321598,-0.0144837723432248));
#44124=DIRECTION('center_axis',(5.15167520928809E-67,-1.18789542670764E-48,
-1.));
#44125=DIRECTION('ref_axis',(-4.33680868994202E-19,1.,-1.18789542670764E-48));
#44126=DIRECTION('center_axis',(5.15167520928809E-67,-1.18789542670764E-48,
-1.));
#44127=DIRECTION('ref_axis',(0.,1.,0.));
#44128=DIRECTION('center_axis',(-0.128587959431095,-0.991698102030056,0.000105448246015545));
#44129=DIRECTION('ref_axis',(0.991623888697772,-0.128579636020076,-0.0122204977334817));
#44130=DIRECTION('center_axis',(0.778395179198649,0.627774590743249,9.06501467187627E-5));
#44131=DIRECTION('ref_axis',(0.62770976469618,-0.778312708134389,-0.0144837723532511));
#44132=DIRECTION('center_axis',(5.15167520928809E-67,-1.18789542670764E-48,
-1.));
#44133=DIRECTION('ref_axis',(-4.33680868994202E-19,1.,-1.18789542670764E-48));
#44134=DIRECTION('center_axis',(5.15167520928809E-67,-1.18789542670764E-48,
-1.));
#44135=DIRECTION('ref_axis',(0.,1.,0.));
#44136=DIRECTION('center_axis',(-0.0503838293498799,-0.99872992276226,0.000105448247790322));
#44137=DIRECTION('ref_axis',(0.998655285167012,-0.050381354308516,-0.0122204969634886));
#44138=DIRECTION('center_axis',(0.726741019926698,0.686911553068118,9.06501468063716E-5));
#44139=DIRECTION('ref_axis',(0.686840456253071,-0.726663889286322,-0.0144837723452766));
#44140=DIRECTION('center_axis',(5.15167520928809E-67,-1.18789542670764E-48,
-1.));
#44141=DIRECTION('ref_axis',(-4.33680868994202E-19,1.,-1.18789542670764E-48));
#44142=DIRECTION('center_axis',(5.15167520928809E-67,-1.18789542670764E-48,
-1.));
#44143=DIRECTION('ref_axis',(0.,1.,0.));
#44144=DIRECTION('center_axis',(0.0281309337977714,-0.999604241409735,0.000105448247661813));
#44145=DIRECTION('ref_axis',(0.999529639707556,0.0281275452111717,-0.0122204969816086));
#44146=DIRECTION('center_axis',(0.670606260601294,0.741813477246741,9.06501466782892E-5));
#44147=DIRECTION('ref_axis',(0.741736547997904,-0.67053494591962,-0.0144837724617815));
#44148=DIRECTION('center_axis',(5.15167520928809E-67,-1.18789542670764E-48,
-1.));
#44149=DIRECTION('ref_axis',(-4.33680868994202E-19,1.,-1.18789542670764E-48));
#44150=DIRECTION('center_axis',(5.15167520928809E-67,-1.18789542670764E-48,
-1.));
#44151=DIRECTION('ref_axis',(0.,1.,0.));
#44152=DIRECTION('center_axis',(0.106472260384112,-0.994315667506736,0.000105448247531298));
#44153=DIRECTION('ref_axis',(0.994241561642015,0.106463029061287,-0.01222049699245));
#44154=DIRECTION('center_axis',(0.610336990679746,0.792141874660432,9.06501467541659E-5));
#44155=DIRECTION('ref_axis',(0.792059587274579,-0.610271931637685,-0.0144837723550388));
#44156=DIRECTION('center_axis',(5.15167520928809E-67,-1.18789542670764E-48,
-1.));
#44157=DIRECTION('ref_axis',(-4.33680868994202E-19,1.,-1.18789542670764E-48));
#44158=DIRECTION('center_axis',(5.15167520928809E-67,-1.18789542670764E-48,
-1.));
#44159=DIRECTION('ref_axis',(0.,1.,0.));
#44160=DIRECTION('center_axis',(0.184157150078655,-0.982896806870169,0.000105448247826086));
#44161=DIRECTION('ref_axis',(0.982823653731041,0.184142132933918,-0.01222049693405));
#44162=DIRECTION('center_axis',(0.546304790253063,0.837586454002874,9.06501468026834E-5));
#44163=DIRECTION('ref_axis',(0.837499315807096,-0.546246387959628,-0.0144837724265968));
#44164=DIRECTION('center_axis',(5.15167520928809E-67,-1.18789542670764E-48,
-1.));
#44165=DIRECTION('ref_axis',(-4.33680868994202E-19,1.,-1.18789542670764E-48));
#44166=DIRECTION('center_axis',(5.15167520928809E-67,-1.18789542670764E-48,
-1.));
#44167=DIRECTION('ref_axis',(0.,1.,0.));
#44168=DIRECTION('center_axis',(0.260706649723291,-0.965418060567921,0.000105448239312411));
#44169=DIRECTION('ref_axis',(0.965346311124436,0.260685939330442,-0.0122205005564138));
#44170=DIRECTION('center_axis',(0.478904439129984,0.877867034330454,9.06501466836614E-5));
#44171=DIRECTION('ref_axis',(0.877775582561938,-0.478853053655605,-0.0144837723936657));
#44172=DIRECTION('center_axis',(5.15167520928809E-67,-1.18789542670764E-48,
-1.));
#44173=DIRECTION('ref_axis',(-4.33680868994202E-19,1.,-1.18789542670764E-48));
#44174=DIRECTION('center_axis',(5.15167520928809E-67,-1.18789542670764E-48,
-1.));
#44175=DIRECTION('ref_axis',(0.,1.,0.));
#44176=DIRECTION('center_axis',(0.335648806142683,-0.941987190897869,0.000105448247681778));
#44177=DIRECTION('ref_axis',(0.941917287594608,0.335622530211854,-0.012220496905163));
#44178=DIRECTION('center_axis',(0.408551482887321,0.912735272471225,9.06501468104788E-5));
#44179=DIRECTION('ref_axis',(0.912640070960436,-0.408507431040405,-0.014483772371131));
#44180=DIRECTION('center_axis',(5.15167520928809E-67,-1.18789542670764E-48,
-1.));
#44181=DIRECTION('ref_axis',(-4.33680868994202E-19,1.,-1.18789542670764E-48));
#44182=DIRECTION('center_axis',(5.15167520928809E-67,-1.18789542670764E-48,
-1.));
#44183=DIRECTION('ref_axis',(0.,1.,0.));
#44184=DIRECTION('center_axis',(0.408521576076219,-0.912748656948269,0.000105448247344423));
#44185=DIRECTION('ref_axis',(0.912681030717311,0.408489896594431,-0.0122204970871443));
#44186=DIRECTION('center_axis',(0.335679670895796,0.941976194141785,9.06501467685389E-5));
#44187=DIRECTION('ref_axis',(0.941877829836932,-0.335643224270299,-0.0144837724059784));
#44188=DIRECTION('center_axis',(5.15167520928809E-67,-1.18789542670764E-48,
-1.));
#44189=DIRECTION('ref_axis',(-4.33680868994202E-19,1.,-1.18789542670764E-48));
#44190=DIRECTION('center_axis',(5.15167520928809E-67,-1.18789542670764E-48,
-1.));
#44191=DIRECTION('ref_axis',(0.,1.,0.));
#44192=DIRECTION('center_axis',(0.478875674644822,-0.877882724009383,0.000105448247602163));
#44193=DIRECTION('ref_axis',(0.877817791792273,0.47883878692807,-0.0122204969699355));
#44194=DIRECTION('center_axis',(0.260738282108074,0.965409519336681,9.06501468936573E-5));
#44195=DIRECTION('ref_axis',(0.965308598687316,-0.260709665409891,-0.0144837723743816));
#44196=DIRECTION('center_axis',(5.15167520928809E-67,-1.18789542670764E-48,
-1.));
#44197=DIRECTION('ref_axis',(-4.33680868994202E-19,1.,-1.18789542670764E-48));
#44198=DIRECTION('center_axis',(5.15167520928809E-67,-1.18789542670764E-48,
-1.));
#44199=DIRECTION('ref_axis',(0.,1.,0.));
#44200=DIRECTION('center_axis',(0.546277345437349,-0.837604352151176,0.000105448247639465));
#44201=DIRECTION('ref_axis',(0.837542514275712,0.546235476910338,-0.0122204969316073));
#44202=DIRECTION('center_axis',(0.184189355107516,0.982890773813463,9.06501467024073E-5));
#44203=DIRECTION('ref_axis',(0.982787919028468,-0.184168744767946,-0.0144837723778112));
#44204=DIRECTION('center_axis',(5.15167520928809E-67,-1.18789542670764E-48,
-1.));
#44205=DIRECTION('ref_axis',(-4.33680868994202E-19,1.,-1.18789542670764E-48));
#44206=DIRECTION('center_axis',(5.15167520928809E-67,-1.18789542670764E-48,
-1.));
#44207=DIRECTION('ref_axis',(0.,1.,0.));
#44208=DIRECTION('center_axis',(0.610311034750668,-0.792161870921744,0.000105448241406271));
#44209=DIRECTION('ref_axis',(0.79210350861157,0.610264443525473,-0.0122204997355093));
#44210=DIRECTION('center_axis',(0.106504839483129,0.994312179825443,9.06501467375791E-5));
#44211=DIRECTION('ref_axis',(0.994208025038601,-0.106492362571754,-0.0144837723929676));
#44212=DIRECTION('center_axis',(5.15167520928809E-67,-1.18789542670764E-48,
-1.));
#44213=DIRECTION('ref_axis',(-4.33680868994202E-19,1.,-1.18789542670764E-48));
#44214=DIRECTION('center_axis',(5.15167520928809E-67,-1.18789542670764E-48,
-1.));
#44215=DIRECTION('ref_axis',(0.,1.,0.));
#44216=DIRECTION('center_axis',(0.670581953563674,-0.741835448354548,0.000105448247759945));
#44217=DIRECTION('ref_axis',(0.741780921486581,0.670530926932748,-0.0122204969305506));
#44218=DIRECTION('center_axis',(0.0281636861069903,0.999603320606438,9.06501466992701E-5));
#44219=DIRECTION('ref_axis',(0.999498507967367,-0.0281594195481785,-0.0144837723579484));
#44220=DIRECTION('center_axis',(5.15167520928809E-67,-1.18789542670764E-48,
-1.));
#44221=DIRECTION('ref_axis',(-4.33680868994202E-19,1.,-1.18789542670764E-48));
#44222=DIRECTION('center_axis',(5.15167520928809E-67,-1.18789542670764E-48,
-1.));
#44223=DIRECTION('ref_axis',(0.,1.,0.));
#44224=DIRECTION('center_axis',(0.726718511653026,-0.6869353635543,0.000105448247761845));
#44225=DIRECTION('ref_axis',(0.686885008277897,0.726663364191536,-0.0122204969175564));
#44226=DIRECTION('center_axis',(-0.0503511057596336,0.99873157451406,9.06501467774672E-5));
#44227=DIRECTION('ref_axis',(0.998626750226755,0.0503471356611751,-0.0144837723768601));
#44228=DIRECTION('center_axis',(5.15167520928809E-67,-1.18789542670764E-48,
-1.));
#44229=DIRECTION('ref_axis',(-4.33680868994202E-19,1.,-1.18789542670764E-48));
#44230=DIRECTION('center_axis',(5.15167520928809E-67,-1.18789542670764E-48,
-1.));
#44231=DIRECTION('ref_axis',(0.,1.,0.));
#44232=DIRECTION('center_axis',(0.778374608459656,-0.627800093808486,0.000105448247696036));
#44233=DIRECTION('ref_axis',(0.627754220580537,0.778315680169911,-0.0122204969200215));
#44234=DIRECTION('center_axis',(-0.128555466315276,0.991702316152893,9.06501466266556E-5));
#44235=DIRECTION('ref_axis',(0.991598126493641,0.128543284036441,-0.0144837724170315));
#44236=DIRECTION('center_axis',(5.15167520928809E-67,-1.18789542670764E-48,
-1.));
#44237=DIRECTION('ref_axis',(-4.33680868994202E-19,1.,-1.18789542670764E-48));
#44238=DIRECTION('center_axis',(5.15167520928809E-67,-1.18789542670764E-48,
-1.));
#44239=DIRECTION('ref_axis',(0.,1.,0.));
#44240=DIRECTION('center_axis',(0.825231766969182,-0.564794227719785,0.000105448247768853));
#44241=DIRECTION('ref_axis',(0.564753119363901,0.825169421163535,-0.0122204969367096));
#44242=DIRECTION('center_axis',(-0.205967239672835,0.978558883238052,9.06501467925213E-5));
#44243=DIRECTION('ref_axis',(0.978455970572528,0.205946920321698,-0.0144837723325158));
#44244=DIRECTION('center_axis',(5.15167520928809E-67,-1.18789542670764E-48,
-1.));
#44245=DIRECTION('ref_axis',(-4.33680868994202E-19,1.,-1.18789542670764E-48));
#44246=DIRECTION('center_axis',(5.15167520928809E-67,-1.18789542670764E-48,
-1.));
#44247=DIRECTION('ref_axis',(0.,1.,0.));
#44248=DIRECTION('center_axis',(0.867001097218019,-0.498306217403936,0.000105448247742928));
#44249=DIRECTION('ref_axis',(0.498270127367224,0.866935718279781,-0.0122204968872419));
#44250=DIRECTION('center_axis',(-0.282109156506148,0.959382309404307,9.06501467249393E-5));
#44251=DIRECTION('ref_axis',(0.959281308221143,0.282080825357837,-0.0144837724013445));
#44252=DIRECTION('center_axis',(5.15167520928809E-67,-1.18789542670764E-48,
-1.));
#44253=DIRECTION('ref_axis',(-4.33680868994202E-19,1.,-1.18789542670764E-48));
#44254=DIRECTION('center_axis',(5.15167520928809E-67,-1.18789542670764E-48,
-1.));
#44255=DIRECTION('ref_axis',(0.,1.,0.));
#44256=DIRECTION('center_axis',(0.903425077395463,-0.428745983553979,0.000105448247628158));
#44257=DIRECTION('ref_axis',(0.428715134343002,0.903357068406648,-0.0122204969215573));
#44258=DIRECTION('center_axis',(-0.356511776579108,0.934290824606,9.06501467950618E-5));
#44259=DIRECTION('ref_axis',(0.934192357613078,0.356475608305158,-0.0144837723258434));
#44260=DIRECTION('center_axis',(5.15167520928809E-67,-1.18789542670764E-48,
-1.));
#44261=DIRECTION('ref_axis',(-4.33680868994202E-19,1.,-1.18789542670764E-48));
#44262=DIRECTION('center_axis',(5.15167520928809E-67,-1.18789542670764E-48,
-1.));
#44263=DIRECTION('ref_axis',(0.,1.,0.));
#44264=DIRECTION('center_axis',(0.93427914155167,-0.356542388142199,0.000105448247170392));
#44265=DIRECTION('ref_axis',(0.356516969951772,0.934208921807903,-0.012220497163456));
#44266=DIRECTION('center_axis',(-0.428716382997142,0.903439126190801,9.06501468381065E-5));
#44267=DIRECTION('ref_axis',(0.903343800468038,0.42867260058632,-0.0144837723857595));
#44268=DIRECTION('center_axis',(5.15167520928809E-67,-1.18789542670764E-48,
-1.));
#44269=DIRECTION('ref_axis',(-4.33680868994202E-19,1.,-1.18789542670764E-48));
#44270=DIRECTION('center_axis',(5.15167520928809E-67,-1.18789542670764E-48,
-1.));
#44271=DIRECTION('ref_axis',(0.,1.,0.));
#44272=DIRECTION('center_axis',(0.959373064120116,-0.282140590347164,0.000105448247729292));
#44273=DIRECTION('ref_axis',(0.282120759890968,0.959301066555056,-0.0122204969160199));
#44274=DIRECTION('center_axis',(-0.498277810351142,0.867017425138747,9.06501467342992E-5));
#44275=DIRECTION('ref_axis',(0.866925828401964,0.498226683737,-0.0144837723677419));
#44276=DIRECTION('center_axis',(5.15167520928809E-67,-1.18789542670764E-48,
-1.));
#44277=DIRECTION('ref_axis',(-4.33680868994202E-19,1.,-1.18789542670764E-48));
#44278=DIRECTION('center_axis',(5.15167520928809E-67,-1.18789542670764E-48,
-1.));
#44279=DIRECTION('ref_axis',(0.,1.,0.));
#44280=DIRECTION('center_axis',(0.978552132724802,-0.205999301990102,0.000105448247615573));
#44281=DIRECTION('ref_axis',(0.205985181528349,0.978478801224133,-0.0122204969505153));
#44282=DIRECTION('center_axis',(-0.564767189310334,0.825250273348065,9.0650146758551E-5));
#44283=DIRECTION('ref_axis',(0.82516297032109,0.564709033705155,-0.014483772390721));
#44284=DIRECTION('center_axis',(5.15167520928809E-67,-1.18789542670764E-48,
-1.));
#44285=DIRECTION('ref_axis',(-4.33680868994202E-19,1.,-1.18789542670764E-48));
#44286=DIRECTION('center_axis',(5.15167520928809E-67,-1.18789542670764E-48,
-1.));
#44287=DIRECTION('ref_axis',(0.,1.,0.));
#44288=DIRECTION('center_axis',(0.991698102030069,-0.128587959430995,0.000105448245943976));
#44289=DIRECTION('ref_axis',(0.128579636019992,0.99162388869792,-0.0122204977223251));
#44290=DIRECTION('center_axis',(-0.627774590743336,0.778395179198579,9.06501467764949E-5));
#44291=DIRECTION('ref_axis',(0.778312708134504,0.627709764696415,-0.014483772336843));
#44292=DIRECTION('center_axis',(5.15167520928809E-67,-1.18789542670764E-48,
-1.));
#44293=DIRECTION('ref_axis',(-4.33680868994202E-19,1.,-1.18789542670764E-48));
#44294=DIRECTION('center_axis',(5.15167520928809E-67,-1.18789542670764E-48,
-1.));
#44295=DIRECTION('ref_axis',(0.,1.,0.));
#44296=DIRECTION('center_axis',(0.998729922762269,-0.0503838293497056,0.000105448247690158));
#44297=DIRECTION('ref_axis',(0.0503813543083624,0.998655285167543,-0.0122204969206726));
#44298=DIRECTION('center_axis',(-0.686911553068082,0.726741019926732,9.065014676939E-5));
#44299=DIRECTION('ref_axis',(0.726663889285701,0.686840456252424,-0.0144837724071123));
#44300=DIRECTION('center_axis',(5.15167520928809E-67,-1.18789542670764E-48,
-1.));
#44301=DIRECTION('ref_axis',(-4.33680868994202E-19,1.,-1.18789542670764E-48));
#44302=DIRECTION('center_axis',(5.15167520928809E-67,-1.18789542670764E-48,
-1.));
#44303=DIRECTION('ref_axis',(0.,1.,0.));
#44304=DIRECTION('center_axis',(0.999604241409737,0.0281309337977193,0.000105448247673278));
#44305=DIRECTION('ref_axis',(0.0281275452111183,-0.999529639707527,0.0122204969841135));
#44306=DIRECTION('center_axis',(-0.741813477246845,0.670606260601179,9.06501467534462E-5));
#44307=DIRECTION('ref_axis',(0.670534945920493,0.741736547999089,-0.0144837723606804));
#44308=DIRECTION('center_axis',(5.15167520928809E-67,-1.18789542670764E-48,
-1.));
#44309=DIRECTION('ref_axis',(-4.33680868994202E-19,1.,-1.18789542670764E-48));
#44310=DIRECTION('center_axis',(5.15167520928809E-67,-1.18789542670764E-48,
-1.));
#44311=DIRECTION('ref_axis',(0.,1.,0.));
#44312=DIRECTION('center_axis',(0.994315667506773,0.106472260383761,0.000105448247684943));
#44313=DIRECTION('ref_axis',(0.106463029060952,-0.994241561642206,0.0122204969798675));
#44314=DIRECTION('center_axis',(-0.792141874660476,0.610336990679688,9.06501468075157E-5));
#44315=DIRECTION('ref_axis',(0.610271931637649,0.792059587274653,-0.0144837723525293));
#44316=DIRECTION('center_axis',(5.15167520928809E-67,-1.18789542670764E-48,
-1.));
#44317=DIRECTION('ref_axis',(-4.33680868994202E-19,1.,-1.18789542670764E-48));
#44318=DIRECTION('center_axis',(5.15167520928809E-67,-1.18789542670764E-48,
-1.));
#44319=DIRECTION('ref_axis',(0.,1.,0.));
#44320=DIRECTION('center_axis',(0.982896806870138,0.184157150078822,0.000105448247739781));
#44321=DIRECTION('ref_axis',(0.184142132934029,-0.982823653730722,0.0122204969580191));
#44322=DIRECTION('center_axis',(-0.837586454002804,0.546304790253169,9.06501467452083E-5));
#44323=DIRECTION('ref_axis',(0.546246387960594,0.837499315808325,-0.0144837723191043));
#44324=DIRECTION('center_axis',(5.15167520928809E-67,-1.18789542670764E-48,
-1.));
#44325=DIRECTION('ref_axis',(-4.33680868994202E-19,1.,-1.18789542670764E-48));
#44326=DIRECTION('center_axis',(5.15167520928809E-67,-1.18789542670764E-48,
-1.));
#44327=DIRECTION('ref_axis',(0.,1.,0.));
#44328=DIRECTION('center_axis',(-0.778395179198544,-0.62777459074338,9.06501468008605E-5));
#44329=DIRECTION('ref_axis',(0.62770976469586,-0.778312708133716,0.0144837724032618));
#44330=DIRECTION('center_axis',(5.15167520928809E-67,-1.18789542670764E-48,
-1.));
#44331=DIRECTION('ref_axis',(-4.33680868994202E-19,1.,-1.18789542670764E-48));
#44332=DIRECTION('center_axis',(0.128587959434843,0.991698102029569,0.000105448247713068));
#44333=DIRECTION('ref_axis',(0.991623888707174,-0.128579636025041,0.0122204969182792));
#44334=DIRECTION('center_axis',(5.15167520928809E-67,-1.18789542670764E-48,
-1.));
#44335=DIRECTION('ref_axis',(0.,1.,0.));
#44336=DIRECTION('center_axis',(-0.82525027334801,-0.564767189310415,9.06501467887519E-5));
#44337=DIRECTION('ref_axis',(0.56470903370554,-0.825162970321483,0.0144837723533119));
#44338=DIRECTION('center_axis',(5.15167520928809E-67,-1.18789542670764E-48,
-1.));
#44339=DIRECTION('ref_axis',(-4.33680868994202E-19,1.,-1.18789542670764E-48));
#44340=DIRECTION('center_axis',(0.205999301990312,0.978552132724757,0.000105448247717959));
#44341=DIRECTION('ref_axis',(0.978478801224664,-0.205985181528676,0.0122204969024898));
#44342=DIRECTION('center_axis',(5.15167520928809E-67,-1.18789542670764E-48,
-1.));
#44343=DIRECTION('ref_axis',(0.,1.,0.));
#44344=DIRECTION('center_axis',(-0.867017425138643,-0.498277810351323,9.06501468256068E-5));
#44345=DIRECTION('ref_axis',(0.498226683737087,-0.866925828401692,0.014483772381015));
#44346=DIRECTION('center_axis',(5.15167520928809E-67,-1.18789542670764E-48,
-1.));
#44347=DIRECTION('ref_axis',(-4.33680868994202E-19,1.,-1.18789542670764E-48));
#44348=DIRECTION('center_axis',(0.282140590347035,0.959373064120154,0.000105448247634384));
#44349=DIRECTION('ref_axis',(0.959301066555324,-0.282120759890904,0.0122204968965099));
#44350=DIRECTION('center_axis',(5.15167520928809E-67,-1.18789542670764E-48,
-1.));
#44351=DIRECTION('ref_axis',(0.,1.,0.));
#44352=DIRECTION('center_axis',(-0.903439126190879,-0.428716382996979,9.06501467301661E-5));
#44353=DIRECTION('ref_axis',(0.428672600586422,-0.903343800468688,0.0144837723422516));
#44354=DIRECTION('center_axis',(5.15167520928809E-67,-1.18789542670764E-48,
-1.));
#44355=DIRECTION('ref_axis',(-4.33680868994202E-19,1.,-1.18789542670764E-48));
#44356=DIRECTION('center_axis',(0.356542388143256,0.934279141551266,0.000105448247681697));
#44357=DIRECTION('ref_axis',(0.934208921810558,-0.356516969953973,0.0122204968962765));
#44358=DIRECTION('center_axis',(5.15167520928809E-67,-1.18789542670764E-48,
-1.));
#44359=DIRECTION('ref_axis',(0.,1.,0.));
#44360=DIRECTION('center_axis',(-0.934290824606111,-0.356511776578816,9.06501466618288E-5));
#44361=DIRECTION('ref_axis',(0.356475608304419,-0.934192357612002,0.0144837724134131));
#44362=DIRECTION('center_axis',(5.15167520928809E-67,-1.18789542670764E-48,
-1.));
#44363=DIRECTION('ref_axis',(-4.33680868994202E-19,1.,-1.18789542670764E-48));
#44364=DIRECTION('center_axis',(0.428745983554273,0.903425077395324,0.000105448247749283));
#44365=DIRECTION('ref_axis',(0.903357068406257,-0.428715134343181,0.0122204969441668));
#44366=DIRECTION('center_axis',(5.15167520928809E-67,-1.18789542670764E-48,
-1.));
#44367=DIRECTION('ref_axis',(0.,1.,0.));
#44368=DIRECTION('center_axis',(-0.959382309404256,-0.282109156506322,9.06501468215648E-5));
#44369=DIRECTION('ref_axis',(0.282080825358184,-0.959281308221691,0.0144837723582998));
#44370=DIRECTION('center_axis',(5.15167520928809E-67,-1.18789542670764E-48,
-1.));
#44371=DIRECTION('ref_axis',(-4.33680868994202E-19,1.,-1.18789542670764E-48));
#44372=DIRECTION('center_axis',(0.498306217397306,0.86700109722183,0.000105448244261109));
#44373=DIRECTION('ref_axis',(0.866935718266673,-0.498270127351015,0.0122204984779969));
#44374=DIRECTION('center_axis',(5.15167520928809E-67,-1.18789542670764E-48,
-1.));
#44375=DIRECTION('ref_axis',(0.,1.,0.));
#44376=DIRECTION('center_axis',(-0.978558883238081,-0.205967239672699,9.06501467769327E-5));
#44377=DIRECTION('ref_axis',(0.205946920321355,-0.978455970571544,0.0144837724038677));
#44378=DIRECTION('center_axis',(5.15167520928809E-67,-1.18789542670764E-48,
-1.));
#44379=DIRECTION('ref_axis',(-4.33680868994202E-19,1.,-1.18789542670764E-48));
#44380=DIRECTION('center_axis',(0.564794227718686,0.825231766969935,0.000105448247134299));
#44381=DIRECTION('ref_axis',(0.825169421162366,-0.564753119361502,0.0122204971264834));
#44382=DIRECTION('center_axis',(5.15167520928809E-67,-1.18789542670764E-48,
-1.));
#44383=DIRECTION('ref_axis',(0.,1.,0.));
#44384=DIRECTION('center_axis',(-0.991702316152861,-0.128555466315523,9.06501467288715E-5));
#44385=DIRECTION('ref_axis',(0.12854328403675,-0.991598126494102,0.0144837723826971));
#44386=DIRECTION('center_axis',(5.15167520928809E-67,-1.18789542670764E-48,
-1.));
#44387=DIRECTION('ref_axis',(-4.33680868994202E-19,1.,-1.18789542670764E-48));
#44388=DIRECTION('center_axis',(0.627800093808552,0.778374608459603,0.000105448247728723));
#44389=DIRECTION('ref_axis',(0.778315680170199,-0.627754220580874,0.0122204968843025));
#44390=DIRECTION('center_axis',(5.15167520928809E-67,-1.18789542670764E-48,
-1.));
#44391=DIRECTION('ref_axis',(0.,1.,0.));
#44392=DIRECTION('center_axis',(-0.998731574514058,-0.0503511057596628,
9.06501468007229E-5));
#44393=DIRECTION('ref_axis',(0.0503471356611987,-0.998626750226619,0.0144837723861814));
#44394=DIRECTION('center_axis',(5.15167520928809E-67,-1.18789542670764E-48,
-1.));
#44395=DIRECTION('ref_axis',(-4.33680868994202E-19,1.,-1.18789542670764E-48));
#44396=DIRECTION('center_axis',(0.686935363554282,0.726718511653043,0.000105448247718559));
#44397=DIRECTION('ref_axis',(0.726663364191442,-0.686885008277775,0.012220496930023));
#44398=DIRECTION('center_axis',(5.15167520928809E-67,-1.18789542670764E-48,
-1.));
#44399=DIRECTION('ref_axis',(0.,1.,0.));
#44400=DIRECTION('center_axis',(-0.99960332060644,0.0281636861069471,9.06501467308329E-5));
#44401=DIRECTION('ref_axis',(0.0281594195481261,0.999498507967114,-0.0144837723754724));
#44402=DIRECTION('center_axis',(5.15167520928809E-67,-1.18789542670764E-48,
-1.));
#44403=DIRECTION('ref_axis',(-4.33680868994202E-19,1.,-1.18789542670764E-48));
#44404=DIRECTION('center_axis',(0.741835448354451,0.670581953563782,0.00010544824772104));
#44405=DIRECTION('ref_axis',(0.670530926933101,-0.74178092148675,0.0122204969008548));
#44406=DIRECTION('center_axis',(5.15167520928809E-67,-1.18789542670764E-48,
-1.));
#44407=DIRECTION('ref_axis',(0.,1.,0.));
#44408=DIRECTION('center_axis',(-0.994312179825441,0.106504839483146,9.06501467381912E-5));
#44409=DIRECTION('ref_axis',(0.106492362571802,0.99420802503887,-0.0144837723741357));
#44410=DIRECTION('center_axis',(5.15167520928809E-67,-1.18789542670764E-48,
-1.));
#44411=DIRECTION('ref_axis',(-4.33680868994202E-19,1.,-1.18789542670764E-48));
#44412=DIRECTION('center_axis',(0.792161870929241,0.610311034740936,0.000105448246928053));
#44413=DIRECTION('ref_axis',(0.610264443534212,-0.792103508642726,0.0122204972796185));
#44414=DIRECTION('center_axis',(5.15167520928809E-67,-1.18789542670764E-48,
-1.));
#44415=DIRECTION('ref_axis',(0.,1.,0.));
#44416=DIRECTION('center_axis',(-0.982890773813477,0.184189355107443,9.06501467544422E-5));
#44417=DIRECTION('ref_axis',(0.184168744767819,0.982787919028209,-0.0144837723970302));
#44418=DIRECTION('center_axis',(5.15167520928809E-67,-1.18789542670764E-48,
-1.));
#44419=DIRECTION('ref_axis',(-4.33680868994202E-19,1.,-1.18789542670764E-48));
#44420=DIRECTION('center_axis',(0.837604352151223,0.546277345437276,0.000105448247675196));
#44421=DIRECTION('ref_axis',(0.546235476910048,-0.837542514275434,0.0122204969635834));
#44422=DIRECTION('center_axis',(5.15167520928809E-67,-1.18789542670764E-48,
-1.));
#44423=DIRECTION('ref_axis',(0.,1.,0.));
#44424=DIRECTION('center_axis',(-0.96540951933663,0.260738282108263,9.06501468112521E-5));
#44425=DIRECTION('ref_axis',(0.26070966540993,0.965308598686718,-0.0144837724135372));
#44426=DIRECTION('center_axis',(5.15167520928809E-67,-1.18789542670764E-48,
-1.));
#44427=DIRECTION('ref_axis',(-4.33680868994202E-19,1.,-1.18789542670764E-48));
#44428=DIRECTION('center_axis',(0.877882724009476,0.478875674644651,0.000105448247670176));
#44429=DIRECTION('ref_axis',(0.478838786927941,-0.877817791792444,0.0122204969627255));
#44430=DIRECTION('center_axis',(5.15167520928809E-67,-1.18789542670764E-48,
-1.));
#44431=DIRECTION('ref_axis',(0.,1.,0.));
#44432=DIRECTION('center_axis',(-0.941976194141744,0.33567967089591,9.06501467361574E-5));
#44433=DIRECTION('ref_axis',(0.335643224270696,0.941877829837669,-0.0144837723488913));
#44434=DIRECTION('center_axis',(5.15167520928809E-67,-1.18789542670764E-48,
-1.));
#44435=DIRECTION('ref_axis',(-4.33680868994202E-19,1.,-1.18789542670764E-48));
#44436=DIRECTION('center_axis',(0.912748656948457,0.408521576075799,0.000105448247549386));
#44437=DIRECTION('ref_axis',(0.408489896594413,-0.912681030718381,0.0122204970078645));
#44438=DIRECTION('center_axis',(5.15167520928809E-67,-1.18789542670764E-48,
-1.));
#44439=DIRECTION('ref_axis',(0.,1.,0.));
#44440=DIRECTION('center_axis',(0.965418060567994,0.260706649723021,0.000105448239440975));
#44441=DIRECTION('ref_axis',(0.260685939330027,-0.965346311123993,0.0122205006002244));
#44442=DIRECTION('center_axis',(-0.877867034330543,0.478904439129822,9.06501467527618E-5));
#44443=DIRECTION('ref_axis',(0.478853053655558,0.877775582562237,-0.014483772377146));
#44444=DIRECTION('center_axis',(5.15167520928809E-67,-1.18789542670764E-48,
-1.));
#44445=DIRECTION('ref_axis',(-4.33680868994202E-19,1.,-1.18789542670764E-48));
#44446=DIRECTION('center_axis',(5.15167520928809E-67,-1.18789542670764E-48,
-1.));
#44447=DIRECTION('ref_axis',(-4.33680868994202E-19,1.,-1.18789542670764E-48));
#44448=DIRECTION('',(5.15167520928809E-67,-1.18789542670764E-48,-1.));
#44449=DIRECTION('center_axis',(5.15167520928809E-67,-1.18789542670764E-48,
-1.));
#44450=DIRECTION('ref_axis',(-4.33680868994202E-19,1.,-1.18789542670764E-48));
#44451=DIRECTION('',(-5.15167520928809E-67,1.18789542670764E-48,1.));
#44452=DIRECTION('center_axis',(5.15167520928809E-67,-1.18789542670764E-48,
-1.));
#44453=DIRECTION('ref_axis',(-4.33680868994202E-19,1.,-1.18789542670764E-48));
#44454=DIRECTION('',(-5.15167520928809E-67,1.18789542670764E-48,1.));
#44455=DIRECTION('',(5.15167520928809E-67,-1.18789542670764E-48,-1.));
#44456=DIRECTION('center_axis',(5.15167520928809E-67,-1.18789542670764E-48,
-1.));
#44457=DIRECTION('ref_axis',(-4.33680868994202E-19,1.,-1.18789542670764E-48));
#44458=DIRECTION('center_axis',(5.15167520928809E-67,-1.18789542670764E-48,
-1.));
#44459=DIRECTION('ref_axis',(-4.33680868994202E-19,1.,-1.18789542670764E-48));
#44460=DIRECTION('',(-5.15167520928809E-67,1.18789542670764E-48,1.));
#44461=DIRECTION('',(5.15167520928809E-67,-1.18789542670764E-48,-1.));
#44462=DIRECTION('center_axis',(5.15167520928809E-67,-1.18789542670764E-48,
-1.));
#44463=DIRECTION('ref_axis',(-4.33680868994202E-19,1.,-1.18789542670764E-48));
#44464=DIRECTION('center_axis',(5.15167520928809E-67,-1.18789542670764E-48,
-1.));
#44465=DIRECTION('ref_axis',(-4.33680868994202E-19,1.,-1.18789542670764E-48));
#44466=DIRECTION('',(-5.15167520928809E-67,1.18789542670764E-48,1.));
#44467=DIRECTION('',(5.15167520928809E-67,-1.18789542670764E-48,-1.));
#44468=DIRECTION('center_axis',(5.15167520928809E-67,-1.18789542670764E-48,
-1.));
#44469=DIRECTION('ref_axis',(-4.33680868994202E-19,1.,-1.18789542670764E-48));
#44470=DIRECTION('center_axis',(5.15167520928809E-67,-1.18789542670764E-48,
-1.));
#44471=DIRECTION('ref_axis',(-4.33680868994202E-19,1.,-1.18789542670764E-48));
#44472=DIRECTION('',(-5.15167520928809E-67,1.18789542670764E-48,1.));
#44473=DIRECTION('',(5.15167520928809E-67,-1.18789542670764E-48,-1.));
#44474=DIRECTION('center_axis',(5.15167520928809E-67,-1.18789542670764E-48,
-1.));
#44475=DIRECTION('ref_axis',(-4.33680868994202E-19,1.,-1.18789542670764E-48));
#44476=DIRECTION('center_axis',(5.15167520928809E-67,-1.18789542670764E-48,
-1.));
#44477=DIRECTION('ref_axis',(-4.33680868994202E-19,1.,-1.18789542670764E-48));
#44478=DIRECTION('',(-5.15167520928809E-67,1.18789542670764E-48,1.));
#44479=DIRECTION('',(5.15167520928809E-67,-1.18789542670764E-48,-1.));
#44480=DIRECTION('center_axis',(5.15167520928809E-67,-1.18789542670764E-48,
-1.));
#44481=DIRECTION('ref_axis',(-4.33680868994202E-19,1.,-1.18789542670764E-48));
#44482=DIRECTION('center_axis',(5.15167520928809E-67,-1.18789542670764E-48,
-1.));
#44483=DIRECTION('ref_axis',(-4.33680868994202E-19,1.,-1.18789542670764E-48));
#44484=DIRECTION('',(-5.15167520928809E-67,1.18789542670764E-48,1.));
#44485=DIRECTION('',(5.15167520928809E-67,-1.18789542670764E-48,-1.));
#44486=DIRECTION('center_axis',(5.15167520928809E-67,-1.18789542670764E-48,
-1.));
#44487=DIRECTION('ref_axis',(-4.33680868994202E-19,1.,-1.18789542670764E-48));
#44488=DIRECTION('center_axis',(5.15167520928809E-67,-1.18789542670764E-48,
-1.));
#44489=DIRECTION('ref_axis',(-4.33680868994202E-19,1.,-1.18789542670764E-48));
#44490=DIRECTION('',(-5.15167520928809E-67,1.18789542670764E-48,1.));
#44491=DIRECTION('',(5.15167520928809E-67,-1.18789542670764E-48,-1.));
#44492=DIRECTION('center_axis',(5.15167520928809E-67,-1.18789542670764E-48,
-1.));
#44493=DIRECTION('ref_axis',(-4.33680868994202E-19,1.,-1.18789542670764E-48));
#44494=DIRECTION('center_axis',(5.15167520928809E-67,-1.18789542670764E-48,
-1.));
#44495=DIRECTION('ref_axis',(-4.33680868994202E-19,1.,-1.18789542670764E-48));
#44496=DIRECTION('',(-5.15167520928809E-67,1.18789542670764E-48,1.));
#44497=DIRECTION('',(5.15167520928809E-67,-1.18789542670764E-48,-1.));
#44498=DIRECTION('center_axis',(5.15167520928809E-67,-1.18789542670764E-48,
-1.));
#44499=DIRECTION('ref_axis',(-4.33680868994202E-19,1.,-1.18789542670764E-48));
#44500=DIRECTION('center_axis',(5.15167520928809E-67,-1.18789542670764E-48,
-1.));
#44501=DIRECTION('ref_axis',(-4.33680868994202E-19,1.,-1.18789542670764E-48));
#44502=DIRECTION('',(-5.15167520928809E-67,1.18789542670764E-48,1.));
#44503=DIRECTION('',(5.15167520928809E-67,-1.18789542670764E-48,-1.));
#44504=DIRECTION('center_axis',(5.15167520928809E-67,-1.18789542670764E-48,
-1.));
#44505=DIRECTION('ref_axis',(-4.33680868994202E-19,1.,-1.18789542670764E-48));
#44506=DIRECTION('center_axis',(5.15167520928809E-67,-1.18789542670764E-48,
-1.));
#44507=DIRECTION('ref_axis',(-4.33680868994202E-19,1.,-1.18789542670764E-48));
#44508=DIRECTION('',(-5.15167520928809E-67,1.18789542670764E-48,1.));
#44509=DIRECTION('',(5.15167520928809E-67,-1.18789542670764E-48,-1.));
#44510=DIRECTION('center_axis',(5.15167520928809E-67,-1.18789542670764E-48,
-1.));
#44511=DIRECTION('ref_axis',(-4.33680868994202E-19,1.,-1.18789542670764E-48));
#44512=DIRECTION('center_axis',(5.15167520928809E-67,-1.18789542670764E-48,
-1.));
#44513=DIRECTION('ref_axis',(-4.33680868994202E-19,1.,-1.18789542670764E-48));
#44514=DIRECTION('',(-5.15167520928809E-67,1.18789542670764E-48,1.));
#44515=DIRECTION('',(5.15167520928809E-67,-1.18789542670764E-48,-1.));
#44516=DIRECTION('center_axis',(5.15167520928809E-67,-1.18789542670764E-48,
-1.));
#44517=DIRECTION('ref_axis',(-4.33680868994202E-19,1.,-1.18789542670764E-48));
#44518=DIRECTION('center_axis',(5.15167520928809E-67,-1.18789542670764E-48,
-1.));
#44519=DIRECTION('ref_axis',(-4.33680868994202E-19,1.,-1.18789542670764E-48));
#44520=DIRECTION('',(-5.15167520928809E-67,1.18789542670764E-48,1.));
#44521=DIRECTION('',(5.15167520928809E-67,-1.18789542670764E-48,-1.));
#44522=DIRECTION('center_axis',(5.15167520928809E-67,-1.18789542670764E-48,
-1.));
#44523=DIRECTION('ref_axis',(-4.33680868994202E-19,1.,-1.18789542670764E-48));
#44524=DIRECTION('center_axis',(5.15167520928809E-67,-1.18789542670764E-48,
-1.));
#44525=DIRECTION('ref_axis',(-4.33680868994202E-19,1.,-1.18789542670764E-48));
#44526=DIRECTION('',(-5.15167520928809E-67,1.18789542670764E-48,1.));
#44527=DIRECTION('',(5.15167520928809E-67,-1.18789542670764E-48,-1.));
#44528=DIRECTION('center_axis',(5.15167520928809E-67,-1.18789542670764E-48,
-1.));
#44529=DIRECTION('ref_axis',(-4.33680868994202E-19,1.,-1.18789542670764E-48));
#44530=DIRECTION('center_axis',(5.15167520928809E-67,-1.18789542670764E-48,
-1.));
#44531=DIRECTION('ref_axis',(-4.33680868994202E-19,1.,-1.18789542670764E-48));
#44532=DIRECTION('',(-5.15167520928809E-67,1.18789542670764E-48,1.));
#44533=DIRECTION('',(5.15167520928809E-67,-1.18789542670764E-48,-1.));
#44534=DIRECTION('center_axis',(5.15167520928809E-67,-1.18789542670764E-48,
-1.));
#44535=DIRECTION('ref_axis',(-4.33680868994202E-19,1.,-1.18789542670764E-48));
#44536=DIRECTION('center_axis',(5.15167520928809E-67,-1.18789542670764E-48,
-1.));
#44537=DIRECTION('ref_axis',(-4.33680868994202E-19,1.,-1.18789542670764E-48));
#44538=DIRECTION('',(-5.15167520928809E-67,1.18789542670764E-48,1.));
#44539=DIRECTION('',(5.15167520928809E-67,-1.18789542670764E-48,-1.));
#44540=DIRECTION('center_axis',(5.15167520928809E-67,-1.18789542670764E-48,
-1.));
#44541=DIRECTION('ref_axis',(-4.33680868994202E-19,1.,-1.18789542670764E-48));
#44542=DIRECTION('center_axis',(5.15167520928809E-67,-1.18789542670764E-48,
-1.));
#44543=DIRECTION('ref_axis',(-4.33680868994202E-19,1.,-1.18789542670764E-48));
#44544=DIRECTION('',(-5.15167520928809E-67,1.18789542670764E-48,1.));
#44545=DIRECTION('',(5.15167520928809E-67,-1.18789542670764E-48,-1.));
#44546=DIRECTION('center_axis',(5.15167520928809E-67,-1.18789542670764E-48,
-1.));
#44547=DIRECTION('ref_axis',(-4.33680868994202E-19,1.,-1.18789542670764E-48));
#44548=DIRECTION('center_axis',(5.15167520928809E-67,-1.18789542670764E-48,
-1.));
#44549=DIRECTION('ref_axis',(-4.33680868994202E-19,1.,-1.18789542670764E-48));
#44550=DIRECTION('',(-5.15167520928809E-67,1.18789542670764E-48,1.));
#44551=DIRECTION('',(5.15167520928809E-67,-1.18789542670764E-48,-1.));
#44552=DIRECTION('center_axis',(5.15167520928809E-67,-1.18789542670764E-48,
-1.));
#44553=DIRECTION('ref_axis',(-4.33680868994202E-19,1.,-1.18789542670764E-48));
#44554=DIRECTION('center_axis',(5.15167520928809E-67,-1.18789542670764E-48,
-1.));
#44555=DIRECTION('ref_axis',(-4.33680868994202E-19,1.,-1.18789542670764E-48));
#44556=DIRECTION('',(-5.15167520928809E-67,1.18789542670764E-48,1.));
#44557=DIRECTION('',(5.15167520928809E-67,-1.18789542670764E-48,-1.));
#44558=DIRECTION('center_axis',(5.15167520928809E-67,-1.18789542670764E-48,
-1.));
#44559=DIRECTION('ref_axis',(-4.33680868994202E-19,1.,-1.18789542670764E-48));
#44560=DIRECTION('center_axis',(5.15167520928809E-67,-1.18789542670764E-48,
-1.));
#44561=DIRECTION('ref_axis',(-4.33680868994202E-19,1.,-1.18789542670764E-48));
#44562=DIRECTION('',(-5.15167520928809E-67,1.18789542670764E-48,1.));
#44563=DIRECTION('',(5.15167520928809E-67,-1.18789542670764E-48,-1.));
#44564=DIRECTION('center_axis',(5.15167520928809E-67,-1.18789542670764E-48,
-1.));
#44565=DIRECTION('ref_axis',(-4.33680868994202E-19,1.,-1.18789542670764E-48));
#44566=DIRECTION('center_axis',(5.15167520928809E-67,-1.18789542670764E-48,
-1.));
#44567=DIRECTION('ref_axis',(-4.33680868994202E-19,1.,-1.18789542670764E-48));
#44568=DIRECTION('',(-5.15167520928809E-67,1.18789542670764E-48,1.));
#44569=DIRECTION('',(5.15167520928809E-67,-1.18789542670764E-48,-1.));
#44570=DIRECTION('center_axis',(5.15167520928809E-67,-1.18789542670764E-48,
-1.));
#44571=DIRECTION('ref_axis',(-4.33680868994202E-19,1.,-1.18789542670764E-48));
#44572=DIRECTION('center_axis',(5.15167520928809E-67,-1.18789542670764E-48,
-1.));
#44573=DIRECTION('ref_axis',(-4.33680868994202E-19,1.,-1.18789542670764E-48));
#44574=DIRECTION('',(-5.15167520928809E-67,1.18789542670764E-48,1.));
#44575=DIRECTION('',(5.15167520928809E-67,-1.18789542670764E-48,-1.));
#44576=DIRECTION('center_axis',(5.15167520928809E-67,-1.18789542670764E-48,
-1.));
#44577=DIRECTION('ref_axis',(-4.33680868994202E-19,1.,-1.18789542670764E-48));
#44578=DIRECTION('center_axis',(5.15167520928809E-67,-1.18789542670764E-48,
-1.));
#44579=DIRECTION('ref_axis',(-4.33680868994202E-19,1.,-1.18789542670764E-48));
#44580=DIRECTION('',(-5.15167520928809E-67,1.18789542670764E-48,1.));
#44581=DIRECTION('',(5.15167520928809E-67,-1.18789542670764E-48,-1.));
#44582=DIRECTION('center_axis',(5.15167520928809E-67,-1.18789542670764E-48,
-1.));
#44583=DIRECTION('ref_axis',(-4.33680868994202E-19,1.,-1.18789542670764E-48));
#44584=DIRECTION('center_axis',(5.15167520928809E-67,-1.18789542670764E-48,
-1.));
#44585=DIRECTION('ref_axis',(-4.33680868994202E-19,1.,-1.18789542670764E-48));
#44586=DIRECTION('',(-5.15167520928809E-67,1.18789542670764E-48,1.));
#44587=DIRECTION('',(5.15167520928809E-67,-1.18789542670764E-48,-1.));
#44588=DIRECTION('center_axis',(5.15167520928809E-67,-1.18789542670764E-48,
-1.));
#44589=DIRECTION('ref_axis',(-4.33680868994202E-19,1.,-1.18789542670764E-48));
#44590=DIRECTION('center_axis',(5.15167520928809E-67,-1.18789542670764E-48,
-1.));
#44591=DIRECTION('ref_axis',(-4.33680868994202E-19,1.,-1.18789542670764E-48));
#44592=DIRECTION('',(-5.15167520928809E-67,1.18789542670764E-48,1.));
#44593=DIRECTION('',(5.15167520928809E-67,-1.18789542670764E-48,-1.));
#44594=DIRECTION('center_axis',(5.15167520928809E-67,-1.18789542670764E-48,
-1.));
#44595=DIRECTION('ref_axis',(-4.33680868994202E-19,1.,-1.18789542670764E-48));
#44596=DIRECTION('center_axis',(5.15167520928809E-67,-1.18789542670764E-48,
-1.));
#44597=DIRECTION('ref_axis',(-4.33680868994202E-19,1.,-1.18789542670764E-48));
#44598=DIRECTION('',(-5.15167520928809E-67,1.18789542670764E-48,1.));
#44599=DIRECTION('',(5.15167520928809E-67,-1.18789542670764E-48,-1.));
#44600=DIRECTION('center_axis',(5.15167520928809E-67,-1.18789542670764E-48,
-1.));
#44601=DIRECTION('ref_axis',(-4.33680868994202E-19,1.,-1.18789542670764E-48));
#44602=DIRECTION('center_axis',(5.15167520928809E-67,-1.18789542670764E-48,
-1.));
#44603=DIRECTION('ref_axis',(-4.33680868994202E-19,1.,-1.18789542670764E-48));
#44604=DIRECTION('',(-5.15167520928809E-67,1.18789542670764E-48,1.));
#44605=DIRECTION('',(5.15167520928809E-67,-1.18789542670764E-48,-1.));
#44606=DIRECTION('center_axis',(5.15167520928809E-67,-1.18789542670764E-48,
-1.));
#44607=DIRECTION('ref_axis',(-4.33680868994202E-19,1.,-1.18789542670764E-48));
#44608=DIRECTION('center_axis',(5.15167520928809E-67,-1.18789542670764E-48,
-1.));
#44609=DIRECTION('ref_axis',(-4.33680868994202E-19,1.,-1.18789542670764E-48));
#44610=DIRECTION('',(-5.15167520928809E-67,1.18789542670764E-48,1.));
#44611=DIRECTION('',(5.15167520928809E-67,-1.18789542670764E-48,-1.));
#44612=DIRECTION('center_axis',(5.15167520928809E-67,-1.18789542670764E-48,
-1.));
#44613=DIRECTION('ref_axis',(-4.33680868994202E-19,1.,-1.18789542670764E-48));
#44614=DIRECTION('center_axis',(5.15167520928809E-67,-1.18789542670764E-48,
-1.));
#44615=DIRECTION('ref_axis',(-4.33680868994202E-19,1.,-1.18789542670764E-48));
#44616=DIRECTION('',(-5.15167520928809E-67,1.18789542670764E-48,1.));
#44617=DIRECTION('',(5.15167520928809E-67,-1.18789542670764E-48,-1.));
#44618=DIRECTION('center_axis',(5.15167520928809E-67,-1.18789542670764E-48,
-1.));
#44619=DIRECTION('ref_axis',(-4.33680868994202E-19,1.,-1.18789542670764E-48));
#44620=DIRECTION('center_axis',(5.15167520928809E-67,-1.18789542670764E-48,
-1.));
#44621=DIRECTION('ref_axis',(-4.33680868994202E-19,1.,-1.18789542670764E-48));
#44622=DIRECTION('',(-5.15167520928809E-67,1.18789542670764E-48,1.));
#44623=DIRECTION('',(5.15167520928809E-67,-1.18789542670764E-48,-1.));
#44624=DIRECTION('center_axis',(5.15167520928809E-67,-1.18789542670764E-48,
-1.));
#44625=DIRECTION('ref_axis',(-4.33680868994202E-19,1.,-1.18789542670764E-48));
#44626=DIRECTION('center_axis',(5.15167520928809E-67,-1.18789542670764E-48,
-1.));
#44627=DIRECTION('ref_axis',(-4.33680868994202E-19,1.,-1.18789542670764E-48));
#44628=DIRECTION('',(-5.15167520928809E-67,1.18789542670764E-48,1.));
#44629=DIRECTION('',(5.15167520928809E-67,-1.18789542670764E-48,-1.));
#44630=DIRECTION('center_axis',(5.15167520928809E-67,-1.18789542670764E-48,
-1.));
#44631=DIRECTION('ref_axis',(-4.33680868994202E-19,1.,-1.18789542670764E-48));
#44632=DIRECTION('center_axis',(5.15167520928809E-67,-1.18789542670764E-48,
-1.));
#44633=DIRECTION('ref_axis',(-4.33680868994202E-19,1.,-1.18789542670764E-48));
#44634=DIRECTION('',(-5.15167520928809E-67,1.18789542670764E-48,1.));
#44635=DIRECTION('',(5.15167520928809E-67,-1.18789542670764E-48,-1.));
#44636=DIRECTION('center_axis',(5.15167520928809E-67,-1.18789542670764E-48,
-1.));
#44637=DIRECTION('ref_axis',(-4.33680868994202E-19,1.,-1.18789542670764E-48));
#44638=DIRECTION('center_axis',(5.15167520928809E-67,-1.18789542670764E-48,
-1.));
#44639=DIRECTION('ref_axis',(-4.33680868994202E-19,1.,-1.18789542670764E-48));
#44640=DIRECTION('',(-5.15167520928809E-67,1.18789542670764E-48,1.));
#44641=DIRECTION('',(5.15167520928809E-67,-1.18789542670764E-48,-1.));
#44642=DIRECTION('center_axis',(5.15167520928809E-67,-1.18789542670764E-48,
-1.));
#44643=DIRECTION('ref_axis',(-4.33680868994202E-19,1.,-1.18789542670764E-48));
#44644=DIRECTION('center_axis',(5.15167520928809E-67,-1.18789542670764E-48,
-1.));
#44645=DIRECTION('ref_axis',(-4.33680868994202E-19,1.,-1.18789542670764E-48));
#44646=DIRECTION('',(-5.15167520928809E-67,1.18789542670764E-48,1.));
#44647=DIRECTION('',(5.15167520928809E-67,-1.18789542670764E-48,-1.));
#44648=DIRECTION('center_axis',(5.15167520928809E-67,-1.18789542670764E-48,
-1.));
#44649=DIRECTION('ref_axis',(-4.33680868994202E-19,1.,-1.18789542670764E-48));
#44650=DIRECTION('center_axis',(5.15167520928809E-67,-1.18789542670764E-48,
-1.));
#44651=DIRECTION('ref_axis',(-4.33680868994202E-19,1.,-1.18789542670764E-48));
#44652=DIRECTION('',(-5.15167520928809E-67,1.18789542670764E-48,1.));
#44653=DIRECTION('',(5.15167520928809E-67,-1.18789542670764E-48,-1.));
#44654=DIRECTION('center_axis',(5.15167520928809E-67,-1.18789542670764E-48,
-1.));
#44655=DIRECTION('ref_axis',(-4.33680868994202E-19,1.,-1.18789542670764E-48));
#44656=DIRECTION('center_axis',(5.15167520928809E-67,-1.18789542670764E-48,
-1.));
#44657=DIRECTION('ref_axis',(-4.33680868994202E-19,1.,-1.18789542670764E-48));
#44658=DIRECTION('',(-5.15167520928809E-67,1.18789542670764E-48,1.));
#44659=DIRECTION('',(5.15167520928809E-67,-1.18789542670764E-48,-1.));
#44660=DIRECTION('center_axis',(5.15167520928809E-67,-1.18789542670764E-48,
-1.));
#44661=DIRECTION('ref_axis',(-4.33680868994202E-19,1.,-1.18789542670764E-48));
#44662=DIRECTION('center_axis',(5.15167520928809E-67,-1.18789542670764E-48,
-1.));
#44663=DIRECTION('ref_axis',(-4.33680868994202E-19,1.,-1.18789542670764E-48));
#44664=DIRECTION('',(-5.15167520928809E-67,1.18789542670764E-48,1.));
#44665=DIRECTION('',(5.15167520928809E-67,-1.18789542670764E-48,-1.));
#44666=DIRECTION('center_axis',(5.15167520928809E-67,-1.18789542670764E-48,
-1.));
#44667=DIRECTION('ref_axis',(-4.33680868994202E-19,1.,-1.18789542670764E-48));
#44668=DIRECTION('center_axis',(5.15167520928809E-67,-1.18789542670764E-48,
-1.));
#44669=DIRECTION('ref_axis',(-4.33680868994202E-19,1.,-1.18789542670764E-48));
#44670=DIRECTION('',(-5.15167520928809E-67,1.18789542670764E-48,1.));
#44671=DIRECTION('',(5.15167520928809E-67,-1.18789542670764E-48,-1.));
#44672=DIRECTION('center_axis',(5.15167520928809E-67,-1.18789542670764E-48,
-1.));
#44673=DIRECTION('ref_axis',(-4.33680868994202E-19,1.,-1.18789542670764E-48));
#44674=DIRECTION('center_axis',(5.15167520928809E-67,-1.18789542670764E-48,
-1.));
#44675=DIRECTION('ref_axis',(-4.33680868994202E-19,1.,-1.18789542670764E-48));
#44676=DIRECTION('',(-5.15167520928809E-67,1.18789542670764E-48,1.));
#44677=DIRECTION('',(5.15167520928809E-67,-1.18789542670764E-48,-1.));
#44678=DIRECTION('center_axis',(5.15167520928809E-67,-1.18789542670764E-48,
-1.));
#44679=DIRECTION('ref_axis',(-4.33680868994202E-19,1.,-1.18789542670764E-48));
#44680=DIRECTION('center_axis',(5.15167520928809E-67,-1.18789542670764E-48,
-1.));
#44681=DIRECTION('ref_axis',(-4.33680868994202E-19,1.,-1.18789542670764E-48));
#44682=DIRECTION('',(-5.15167520928809E-67,1.18789542670764E-48,1.));
#44683=DIRECTION('',(5.15167520928809E-67,-1.18789542670764E-48,-1.));
#44684=DIRECTION('center_axis',(5.15167520928809E-67,-1.18789542670764E-48,
-1.));
#44685=DIRECTION('ref_axis',(-4.33680868994202E-19,1.,-1.18789542670764E-48));
#44686=DIRECTION('center_axis',(5.15167520928809E-67,-1.18789542670764E-48,
-1.));
#44687=DIRECTION('ref_axis',(-4.33680868994202E-19,1.,-1.18789542670764E-48));
#44688=DIRECTION('',(-5.15167520928809E-67,1.18789542670764E-48,1.));
#44689=DIRECTION('',(5.15167520928809E-67,-1.18789542670764E-48,-1.));
#44690=DIRECTION('center_axis',(5.15167520928809E-67,-1.18789542670764E-48,
-1.));
#44691=DIRECTION('ref_axis',(-4.33680868994202E-19,1.,-1.18789542670764E-48));
#44692=DIRECTION('center_axis',(5.15167520928809E-67,-1.18789542670764E-48,
-1.));
#44693=DIRECTION('ref_axis',(-4.33680868994202E-19,1.,-1.18789542670764E-48));
#44694=DIRECTION('',(-5.15167520928809E-67,1.18789542670764E-48,1.));
#44695=DIRECTION('',(5.15167520928809E-67,-1.18789542670764E-48,-1.));
#44696=DIRECTION('center_axis',(5.15167520928809E-67,-1.18789542670764E-48,
-1.));
#44697=DIRECTION('ref_axis',(-4.33680868994202E-19,1.,-1.18789542670764E-48));
#44698=DIRECTION('center_axis',(5.15167520928809E-67,-1.18789542670764E-48,
-1.));
#44699=DIRECTION('ref_axis',(-4.33680868994202E-19,1.,-1.18789542670764E-48));
#44700=DIRECTION('',(-5.15167520928809E-67,1.18789542670764E-48,1.));
#44701=DIRECTION('',(5.15167520928809E-67,-1.18789542670764E-48,-1.));
#44702=DIRECTION('center_axis',(5.15167520928809E-67,-1.18789542670764E-48,
-1.));
#44703=DIRECTION('ref_axis',(-4.33680868994202E-19,1.,-1.18789542670764E-48));
#44704=DIRECTION('center_axis',(5.15167520928809E-67,-1.18789542670764E-48,
-1.));
#44705=DIRECTION('ref_axis',(-4.33680868994202E-19,1.,-1.18789542670764E-48));
#44706=DIRECTION('',(-5.15167520928809E-67,1.18789542670764E-48,1.));
#44707=DIRECTION('',(5.15167520928809E-67,-1.18789542670764E-48,-1.));
#44708=DIRECTION('center_axis',(5.15167520928809E-67,-1.18789542670764E-48,
-1.));
#44709=DIRECTION('ref_axis',(-4.33680868994202E-19,1.,-1.18789542670764E-48));
#44710=DIRECTION('center_axis',(5.15167520928809E-67,-1.18789542670764E-48,
-1.));
#44711=DIRECTION('ref_axis',(-4.33680868994202E-19,1.,-1.18789542670764E-48));
#44712=DIRECTION('',(-5.15167520928809E-67,1.18789542670764E-48,1.));
#44713=DIRECTION('',(5.15167520928809E-67,-1.18789542670764E-48,-1.));
#44714=DIRECTION('center_axis',(5.15167520928809E-67,-1.18789542670764E-48,
-1.));
#44715=DIRECTION('ref_axis',(-4.33680868994202E-19,1.,-1.18789542670764E-48));
#44716=DIRECTION('center_axis',(5.15167520928809E-67,-1.18789542670764E-48,
-1.));
#44717=DIRECTION('ref_axis',(-4.33680868994202E-19,1.,-1.18789542670764E-48));
#44718=DIRECTION('',(-5.15167520928809E-67,1.18789542670764E-48,1.));
#44719=DIRECTION('',(5.15167520928809E-67,-1.18789542670764E-48,-1.));
#44720=DIRECTION('center_axis',(5.15167520928809E-67,-1.18789542670764E-48,
-1.));
#44721=DIRECTION('ref_axis',(-4.33680868994202E-19,1.,-1.18789542670764E-48));
#44722=DIRECTION('center_axis',(5.15167520928809E-67,-1.18789542670764E-48,
-1.));
#44723=DIRECTION('ref_axis',(-4.33680868994202E-19,1.,-1.18789542670764E-48));
#44724=DIRECTION('',(-5.15167520928809E-67,1.18789542670764E-48,1.));
#44725=DIRECTION('',(5.15167520928809E-67,-1.18789542670764E-48,-1.));
#44726=DIRECTION('center_axis',(5.15167520928809E-67,-1.18789542670764E-48,
-1.));
#44727=DIRECTION('ref_axis',(-4.33680868994202E-19,1.,-1.18789542670764E-48));
#44728=DIRECTION('center_axis',(5.15167520928809E-67,-1.18789542670764E-48,
-1.));
#44729=DIRECTION('ref_axis',(-4.33680868994202E-19,1.,-1.18789542670764E-48));
#44730=DIRECTION('',(-5.15167520928809E-67,1.18789542670764E-48,1.));
#44731=DIRECTION('',(5.15167520928809E-67,-1.18789542670764E-48,-1.));
#44732=DIRECTION('center_axis',(5.15167520928809E-67,-1.18789542670764E-48,
-1.));
#44733=DIRECTION('ref_axis',(-4.33680868994202E-19,1.,-1.18789542670764E-48));
#44734=DIRECTION('center_axis',(5.15167520928809E-67,-1.18789542670764E-48,
-1.));
#44735=DIRECTION('ref_axis',(-4.33680868994202E-19,1.,-1.18789542670764E-48));
#44736=DIRECTION('',(-5.15167520928809E-67,1.18789542670764E-48,1.));
#44737=DIRECTION('',(5.15167520928809E-67,-1.18789542670764E-48,-1.));
#44738=DIRECTION('center_axis',(5.15167520928809E-67,-1.18789542670764E-48,
-1.));
#44739=DIRECTION('ref_axis',(-4.33680868994202E-19,1.,-1.18789542670764E-48));
#44740=DIRECTION('center_axis',(5.15167520928809E-67,-1.18789542670764E-48,
-1.));
#44741=DIRECTION('ref_axis',(-4.33680868994202E-19,1.,-1.18789542670764E-48));
#44742=DIRECTION('',(-5.15167520928809E-67,1.18789542670764E-48,1.));
#44743=DIRECTION('',(5.15167520928809E-67,-1.18789542670764E-48,-1.));
#44744=DIRECTION('center_axis',(5.15167520928809E-67,-1.18789542670764E-48,
-1.));
#44745=DIRECTION('ref_axis',(-4.33680868994202E-19,1.,-1.18789542670764E-48));
#44746=DIRECTION('center_axis',(5.15167520928809E-67,-1.18789542670764E-48,
-1.));
#44747=DIRECTION('ref_axis',(-4.33680868994202E-19,1.,-1.18789542670764E-48));
#44748=DIRECTION('',(-5.15167520928809E-67,1.18789542670764E-48,1.));
#44749=DIRECTION('',(5.15167520928809E-67,-1.18789542670764E-48,-1.));
#44750=DIRECTION('center_axis',(5.15167520928809E-67,-1.18789542670764E-48,
-1.));
#44751=DIRECTION('ref_axis',(-4.33680868994202E-19,1.,-1.18789542670764E-48));
#44752=DIRECTION('center_axis',(5.15167520928809E-67,-1.18789542670764E-48,
-1.));
#44753=DIRECTION('ref_axis',(-4.33680868994202E-19,1.,-1.18789542670764E-48));
#44754=DIRECTION('',(-5.15167520928809E-67,1.18789542670764E-48,1.));
#44755=DIRECTION('',(5.15167520928809E-67,-1.18789542670764E-48,-1.));
#44756=DIRECTION('center_axis',(5.15167520928809E-67,-1.18789542670764E-48,
-1.));
#44757=DIRECTION('ref_axis',(-4.33680868994202E-19,1.,-1.18789542670764E-48));
#44758=DIRECTION('center_axis',(5.15167520928809E-67,-1.18789542670764E-48,
-1.));
#44759=DIRECTION('ref_axis',(-4.33680868994202E-19,1.,-1.18789542670764E-48));
#44760=DIRECTION('',(-5.15167520928809E-67,1.18789542670764E-48,1.));
#44761=DIRECTION('',(5.15167520928809E-67,-1.18789542670764E-48,-1.));
#44762=DIRECTION('center_axis',(5.15167520928809E-67,-1.18789542670764E-48,
-1.));
#44763=DIRECTION('ref_axis',(-4.33680868994202E-19,1.,-1.18789542670764E-48));
#44764=DIRECTION('center_axis',(5.15167520928809E-67,-1.18789542670764E-48,
-1.));
#44765=DIRECTION('ref_axis',(-4.33680868994202E-19,1.,-1.18789542670764E-48));
#44766=DIRECTION('',(-5.15167520928809E-67,1.18789542670764E-48,1.));
#44767=DIRECTION('',(5.15167520928809E-67,-1.18789542670764E-48,-1.));
#44768=DIRECTION('center_axis',(5.15167520928809E-67,-1.18789542670764E-48,
-1.));
#44769=DIRECTION('ref_axis',(-4.33680868994202E-19,1.,-1.18789542670764E-48));
#44770=DIRECTION('center_axis',(5.15167520928809E-67,-1.18789542670764E-48,
-1.));
#44771=DIRECTION('ref_axis',(-4.33680868994202E-19,1.,-1.18789542670764E-48));
#44772=DIRECTION('',(-5.15167520928809E-67,1.18789542670764E-48,1.));
#44773=DIRECTION('',(5.15167520928809E-67,-1.18789542670764E-48,-1.));
#44774=DIRECTION('center_axis',(5.15167520928809E-67,-1.18789542670764E-48,
-1.));
#44775=DIRECTION('ref_axis',(-4.33680868994202E-19,1.,-1.18789542670764E-48));
#44776=DIRECTION('center_axis',(5.15167520928809E-67,-1.18789542670764E-48,
-1.));
#44777=DIRECTION('ref_axis',(-4.33680868994202E-19,1.,-1.18789542670764E-48));
#44778=DIRECTION('',(-5.15167520928809E-67,1.18789542670764E-48,1.));
#44779=DIRECTION('',(5.15167520928809E-67,-1.18789542670764E-48,-1.));
#44780=DIRECTION('center_axis',(5.15167520928809E-67,-1.18789542670764E-48,
-1.));
#44781=DIRECTION('ref_axis',(-4.33680868994202E-19,1.,-1.18789542670764E-48));
#44782=DIRECTION('center_axis',(5.15167520928809E-67,-1.18789542670764E-48,
-1.));
#44783=DIRECTION('ref_axis',(-4.33680868994202E-19,1.,-1.18789542670764E-48));
#44784=DIRECTION('',(-5.15167520928809E-67,1.18789542670764E-48,1.));
#44785=DIRECTION('',(5.15167520928809E-67,-1.18789542670764E-48,-1.));
#44786=DIRECTION('center_axis',(5.15167520928809E-67,-1.18789542670764E-48,
-1.));
#44787=DIRECTION('ref_axis',(-4.33680868994202E-19,1.,-1.18789542670764E-48));
#44788=DIRECTION('center_axis',(5.15167520928809E-67,-1.18789542670764E-48,
-1.));
#44789=DIRECTION('ref_axis',(-4.33680868994202E-19,1.,-1.18789542670764E-48));
#44790=DIRECTION('',(-5.15167520928809E-67,1.18789542670764E-48,1.));
#44791=DIRECTION('',(5.15167520928809E-67,-1.18789542670764E-48,-1.));
#44792=DIRECTION('center_axis',(5.15167520928809E-67,-1.18789542670764E-48,
-1.));
#44793=DIRECTION('ref_axis',(-4.33680868994202E-19,1.,-1.18789542670764E-48));
#44794=DIRECTION('center_axis',(5.15167520928809E-67,-1.18789542670764E-48,
-1.));
#44795=DIRECTION('ref_axis',(-4.33680868994202E-19,1.,-1.18789542670764E-48));
#44796=DIRECTION('',(-5.15167520928809E-67,1.18789542670764E-48,1.));
#44797=DIRECTION('',(5.15167520928809E-67,-1.18789542670764E-48,-1.));
#44798=DIRECTION('center_axis',(5.15167520928809E-67,-1.18789542670764E-48,
-1.));
#44799=DIRECTION('ref_axis',(-4.33680868994202E-19,1.,-1.18789542670764E-48));
#44800=DIRECTION('center_axis',(5.15167520928809E-67,-1.18789542670764E-48,
-1.));
#44801=DIRECTION('ref_axis',(-4.33680868994202E-19,1.,-1.18789542670764E-48));
#44802=DIRECTION('',(-5.15167520928809E-67,1.18789542670764E-48,1.));
#44803=DIRECTION('',(5.15167520928809E-67,-1.18789542670764E-48,-1.));
#44804=DIRECTION('center_axis',(5.15167520928809E-67,-1.18789542670764E-48,
-1.));
#44805=DIRECTION('ref_axis',(-4.33680868994202E-19,1.,-1.18789542670764E-48));
#44806=DIRECTION('center_axis',(5.15167520928809E-67,-1.18789542670764E-48,
-1.));
#44807=DIRECTION('ref_axis',(-4.33680868994202E-19,1.,-1.18789542670764E-48));
#44808=DIRECTION('',(-5.15167520928809E-67,1.18789542670764E-48,1.));
#44809=DIRECTION('',(5.15167520928809E-67,-1.18789542670764E-48,-1.));
#44810=DIRECTION('center_axis',(5.15167520928809E-67,-1.18789542670764E-48,
-1.));
#44811=DIRECTION('ref_axis',(-4.33680868994202E-19,1.,-1.18789542670764E-48));
#44812=DIRECTION('center_axis',(5.15167520928809E-67,-1.18789542670764E-48,
-1.));
#44813=DIRECTION('ref_axis',(-4.33680868994202E-19,1.,-1.18789542670764E-48));
#44814=DIRECTION('',(-5.15167520928809E-67,1.18789542670764E-48,1.));
#44815=DIRECTION('',(5.15167520928809E-67,-1.18789542670764E-48,-1.));
#44816=DIRECTION('center_axis',(5.15167520928809E-67,-1.18789542670764E-48,
-1.));
#44817=DIRECTION('ref_axis',(-4.33680868994202E-19,1.,-1.18789542670764E-48));
#44818=DIRECTION('center_axis',(5.15167520928809E-67,-1.18789542670764E-48,
-1.));
#44819=DIRECTION('ref_axis',(-4.33680868994202E-19,1.,-1.18789542670764E-48));
#44820=DIRECTION('',(-5.15167520928809E-67,1.18789542670764E-48,1.));
#44821=DIRECTION('',(5.15167520928809E-67,-1.18789542670764E-48,-1.));
#44822=DIRECTION('center_axis',(5.15167520928809E-67,-1.18789542670764E-48,
-1.));
#44823=DIRECTION('ref_axis',(-4.33680868994202E-19,1.,-1.18789542670764E-48));
#44824=DIRECTION('center_axis',(5.15167520928809E-67,-1.18789542670764E-48,
-1.));
#44825=DIRECTION('ref_axis',(-4.33680868994202E-19,1.,-1.18789542670764E-48));
#44826=DIRECTION('',(-5.15167520928809E-67,1.18789542670764E-48,1.));
#44827=DIRECTION('',(5.15167520928809E-67,-1.18789542670764E-48,-1.));
#44828=DIRECTION('center_axis',(5.15167520928809E-67,-1.18789542670764E-48,
-1.));
#44829=DIRECTION('ref_axis',(-4.33680868994202E-19,1.,-1.18789542670764E-48));
#44830=DIRECTION('center_axis',(5.15167520928809E-67,-1.18789542670764E-48,
-1.));
#44831=DIRECTION('ref_axis',(-4.33680868994202E-19,1.,-1.18789542670764E-48));
#44832=DIRECTION('',(5.15167520928809E-67,-1.18789542670764E-48,-1.));
#44833=DIRECTION('center_axis',(5.15167520928809E-67,-1.18789542670764E-48,
-1.));
#44834=DIRECTION('ref_axis',(-4.33680868994202E-19,1.,-1.18789542670764E-48));
#44835=DIRECTION('',(-5.15167520928809E-67,1.18789542670764E-48,1.));
#44836=DIRECTION('center_axis',(5.15167520928809E-67,-1.18789542670764E-48,
-1.));
#44837=DIRECTION('ref_axis',(-4.33680868994202E-19,1.,-1.18789542670764E-48));
#44838=DIRECTION('',(5.15167520928809E-67,-1.18789542670764E-48,-1.));
#44839=DIRECTION('center_axis',(5.15167520928809E-67,-1.18789542670764E-48,
-1.));
#44840=DIRECTION('ref_axis',(-4.33680868994202E-19,1.,-1.18789542670764E-48));
#44841=DIRECTION('',(-5.15167520928809E-67,1.18789542670764E-48,1.));
#44842=DIRECTION('center_axis',(5.15167520928809E-67,-1.18789542670764E-48,
-1.));
#44843=DIRECTION('ref_axis',(-4.33680868994202E-19,1.,-1.18789542670764E-48));
#44844=DIRECTION('',(5.15167520928809E-67,-1.18789542670764E-48,-1.));
#44845=DIRECTION('center_axis',(5.15167520928809E-67,-1.18789542670764E-48,
-1.));
#44846=DIRECTION('ref_axis',(-4.33680868994202E-19,1.,-1.18789542670764E-48));
#44847=DIRECTION('',(-5.15167520928809E-67,1.18789542670764E-48,1.));
#44848=DIRECTION('center_axis',(5.15167520928809E-67,-1.18789542670764E-48,
-1.));
#44849=DIRECTION('ref_axis',(-4.33680868994202E-19,1.,-1.18789542670764E-48));
#44850=DIRECTION('',(5.15167520928809E-67,-1.18789542670764E-48,-1.));
#44851=DIRECTION('center_axis',(5.15167520928809E-67,-1.18789542670764E-48,
-1.));
#44852=DIRECTION('ref_axis',(-4.33680868994202E-19,1.,-1.18789542670764E-48));
#44853=DIRECTION('',(-5.15167520928809E-67,1.18789542670764E-48,1.));
#44854=DIRECTION('center_axis',(5.15167520928809E-67,-1.18789542670764E-48,
-1.));
#44855=DIRECTION('ref_axis',(-4.33680868994202E-19,1.,-1.18789542670764E-48));
#44856=DIRECTION('',(5.15167520928809E-67,-1.18789542670764E-48,-1.));
#44857=DIRECTION('center_axis',(5.15167520928809E-67,-1.18789542670764E-48,
-1.));
#44858=DIRECTION('ref_axis',(-4.33680868994202E-19,1.,-1.18789542670764E-48));
#44859=DIRECTION('',(-5.15167520928809E-67,1.18789542670764E-48,1.));
#44860=DIRECTION('center_axis',(5.15167520928809E-67,-1.18789542670764E-48,
-1.));
#44861=DIRECTION('ref_axis',(-4.33680868994202E-19,1.,-1.18789542670764E-48));
#44862=DIRECTION('',(5.15167520928809E-67,-1.18789542670764E-48,-1.));
#44863=DIRECTION('center_axis',(5.15167520928809E-67,-1.18789542670764E-48,
-1.));
#44864=DIRECTION('ref_axis',(-4.33680868994202E-19,1.,-1.18789542670764E-48));
#44865=DIRECTION('',(-5.15167520928809E-67,1.18789542670764E-48,1.));
#44866=DIRECTION('center_axis',(5.15167520928809E-67,-1.18789542670764E-48,
-1.));
#44867=DIRECTION('ref_axis',(-4.33680868994202E-19,1.,-1.18789542670764E-48));
#44868=DIRECTION('',(5.15167520928809E-67,-1.18789542670764E-48,-1.));
#44869=DIRECTION('center_axis',(5.15167520928809E-67,-1.18789542670764E-48,
-1.));
#44870=DIRECTION('ref_axis',(-4.33680868994202E-19,1.,-1.18789542670764E-48));
#44871=DIRECTION('',(-5.15167520928809E-67,1.18789542670764E-48,1.));
#44872=DIRECTION('center_axis',(5.15167520928809E-67,-1.18789542670764E-48,
-1.));
#44873=DIRECTION('ref_axis',(-4.33680868994202E-19,1.,-1.18789542670764E-48));
#44874=DIRECTION('',(5.15167520928809E-67,-1.18789542670764E-48,-1.));
#44875=DIRECTION('center_axis',(5.15167520928809E-67,-1.18789542670764E-48,
-1.));
#44876=DIRECTION('ref_axis',(-4.33680868994202E-19,1.,-1.18789542670764E-48));
#44877=DIRECTION('',(-5.15167520928809E-67,1.18789542670764E-48,1.));
#44878=DIRECTION('center_axis',(5.15167520928809E-67,-1.18789542670764E-48,
-1.));
#44879=DIRECTION('ref_axis',(-4.33680868994202E-19,1.,-1.18789542670764E-48));
#44880=DIRECTION('',(5.15167520928809E-67,-1.18789542670764E-48,-1.));
#44881=DIRECTION('center_axis',(5.15167520928809E-67,-1.18789542670764E-48,
-1.));
#44882=DIRECTION('ref_axis',(-4.33680868994202E-19,1.,-1.18789542670764E-48));
#44883=DIRECTION('',(-5.15167520928809E-67,1.18789542670764E-48,1.));
#44884=DIRECTION('center_axis',(5.15167520928809E-67,-1.18789542670764E-48,
-1.));
#44885=DIRECTION('ref_axis',(-4.33680868994202E-19,1.,-1.18789542670764E-48));
#44886=DIRECTION('',(5.15167520928809E-67,-1.18789542670764E-48,-1.));
#44887=DIRECTION('center_axis',(5.15167520928809E-67,-1.18789542670764E-48,
-1.));
#44888=DIRECTION('ref_axis',(-4.33680868994202E-19,1.,-1.18789542670764E-48));
#44889=DIRECTION('',(-5.15167520928809E-67,1.18789542670764E-48,1.));
#44890=DIRECTION('center_axis',(5.15167520928809E-67,-1.18789542670764E-48,
-1.));
#44891=DIRECTION('ref_axis',(-4.33680868994202E-19,1.,-1.18789542670764E-48));
#44892=DIRECTION('',(5.15167520928809E-67,-1.18789542670764E-48,-1.));
#44893=DIRECTION('center_axis',(5.15167520928809E-67,-1.18789542670764E-48,
-1.));
#44894=DIRECTION('ref_axis',(-4.33680868994202E-19,1.,-1.18789542670764E-48));
#44895=DIRECTION('',(-5.15167520928809E-67,1.18789542670764E-48,1.));
#44896=DIRECTION('center_axis',(5.15167520928809E-67,-1.18789542670764E-48,
-1.));
#44897=DIRECTION('ref_axis',(-4.33680868994202E-19,1.,-1.18789542670764E-48));
#44898=DIRECTION('',(5.15167520928809E-67,-1.18789542670764E-48,-1.));
#44899=DIRECTION('center_axis',(5.15167520928809E-67,-1.18789542670764E-48,
-1.));
#44900=DIRECTION('ref_axis',(-4.33680868994202E-19,1.,-1.18789542670764E-48));
#44901=DIRECTION('',(-5.15167520928809E-67,1.18789542670764E-48,1.));
#44902=DIRECTION('center_axis',(5.15167520928809E-67,-1.18789542670764E-48,
-1.));
#44903=DIRECTION('ref_axis',(-4.33680868994202E-19,1.,-1.18789542670764E-48));
#44904=DIRECTION('',(5.15167520928809E-67,-1.18789542670764E-48,-1.));
#44905=DIRECTION('center_axis',(5.15167520928809E-67,-1.18789542670764E-48,
-1.));
#44906=DIRECTION('ref_axis',(-4.33680868994202E-19,1.,-1.18789542670764E-48));
#44907=DIRECTION('',(-5.15167520928809E-67,1.18789542670764E-48,1.));
#44908=DIRECTION('center_axis',(5.15167520928809E-67,-1.18789542670764E-48,
-1.));
#44909=DIRECTION('ref_axis',(-4.33680868994202E-19,1.,-1.18789542670764E-48));
#44910=DIRECTION('',(5.15167520928809E-67,-1.18789542670764E-48,-1.));
#44911=DIRECTION('center_axis',(5.15167520928809E-67,-1.18789542670764E-48,
-1.));
#44912=DIRECTION('ref_axis',(-4.33680868994202E-19,1.,-1.18789542670764E-48));
#44913=DIRECTION('',(-5.15167520928809E-67,1.18789542670764E-48,1.));
#44914=DIRECTION('center_axis',(5.15167520928809E-67,-1.18789542670764E-48,
-1.));
#44915=DIRECTION('ref_axis',(-4.33680868994202E-19,1.,-1.18789542670764E-48));
#44916=DIRECTION('',(-5.15167520928809E-67,1.18789542670764E-48,1.));
#44917=DIRECTION('',(5.15167520928809E-67,-1.18789542670764E-48,-1.));
#44918=DIRECTION('center_axis',(5.15167520928809E-67,-1.18789542670764E-48,
-1.));
#44919=DIRECTION('ref_axis',(-4.33680868994202E-19,1.,-1.18789542670764E-48));
#44920=DIRECTION('center_axis',(5.15167520928809E-67,-1.18789542670764E-48,
-1.));
#44921=DIRECTION('ref_axis',(0.,1.,0.));
#44922=DIRECTION('center_axis',(-0.726718511656259,-0.686935363550879,-0.000105448246390915));
#44923=DIRECTION('ref_axis',(0.686885008270217,-0.726663364190208,-0.0122204974282148));
#44924=DIRECTION('center_axis',(0.0503511057571476,0.998731574514185,-9.06501463958382E-5));
#44925=DIRECTION('ref_axis',(0.998626750226923,-0.0503471356586858,-0.0144837723739379));
#44926=DIRECTION('center_axis',(5.15167520928809E-67,-1.18789542670764E-48,
-1.));
#44927=DIRECTION('ref_axis',(0.,1.,0.));
#44928=DIRECTION('center_axis',(-0.0281636861094737,0.999603320606368,-9.06501463234301E-5));
#44929=DIRECTION('ref_axis',(0.999498507968587,0.0281594195507115,-0.0144837722688343));
#44930=DIRECTION('center_axis',(-0.670581953565459,-0.741835448352935,-0.000105448247414229));
#44931=DIRECTION('ref_axis',(0.741780921484837,-0.670530926934418,-0.0122204969447688));
#44932=DIRECTION('center_axis',(5.15167520928809E-67,-1.18789542670764E-48,
-1.));
#44933=DIRECTION('ref_axis',(0.,1.,0.));
#44934=DIRECTION('center_axis',(-0.106504839485416,0.994312179825198,-9.06501464431132E-5));
#44935=DIRECTION('ref_axis',(0.994208025038947,0.106492362574112,-0.014483772351861));
#44936=DIRECTION('center_axis',(-0.610311034741592,-0.792161870928735,-0.000105448247339917));
#44937=DIRECTION('ref_axis',(0.792103508645573,-0.610264443537491,-0.0122204969313235));
#44938=DIRECTION('center_axis',(5.15167520928809E-67,-1.18789542670764E-48,
-1.));
#44939=DIRECTION('ref_axis',(0.,1.,0.));
#44940=DIRECTION('center_axis',(-0.184189355109993,0.982890773812999,-9.06501463311491E-5));
#44941=DIRECTION('ref_axis',(0.982787919029266,0.184168744770673,-0.0144837722890199));
#44942=DIRECTION('center_axis',(-0.546277345439217,-0.837604352149957,-0.000105448247410497));
#44943=DIRECTION('ref_axis',(0.837542514274823,-0.546235476912428,-0.0122204968991007));
#44944=DIRECTION('center_axis',(5.15167520928809E-67,-1.18789542670764E-48,
-1.));
#44945=DIRECTION('ref_axis',(0.,1.,0.));
#44946=DIRECTION('center_axis',(-0.260738282110594,0.965409519336,-9.0650146457266E-5));
#44947=DIRECTION('ref_axis',(0.965308598686112,0.260709665412272,-0.0144837724117514));
#44948=DIRECTION('center_axis',(-0.478875674647023,-0.877882724008182,-0.000105448247224529));
#44949=DIRECTION('ref_axis',(0.877817791791478,-0.478838786930502,-0.0122204969317693));
#44950=DIRECTION('center_axis',(5.15167520928809E-67,-1.18789542670764E-48,
-1.));
#44951=DIRECTION('ref_axis',(0.,1.,0.));
#44952=DIRECTION('center_axis',(-0.335679670898074,0.941976194140973,-9.06501464082373E-5));
#44953=DIRECTION('ref_axis',(0.941877829837014,0.335643224272907,-0.014483772340284));
#44954=DIRECTION('center_axis',(-0.40852157607848,-0.912748656947257,-0.000105448246964389));
#44955=DIRECTION('ref_axis',(0.912681030716442,-0.408489896596762,-0.0122204970741974));
#44956=DIRECTION('center_axis',(5.15167520928809E-67,-1.18789542670764E-48,
-1.));
#44957=DIRECTION('ref_axis',(0.,1.,0.));
#44958=DIRECTION('center_axis',(-0.408551482889657,0.91273527247018,-9.06501463992171E-5));
#44959=DIRECTION('ref_axis',(0.91264007096006,0.408507431043052,-0.014483772320157));
#44960=DIRECTION('center_axis',(-0.335648806144879,-0.941987190897087,-0.000105448247367288));
#44961=DIRECTION('ref_axis',(0.941917287594001,-0.335622530214118,-0.0122204968897907));
#44962=DIRECTION('center_axis',(5.15167520928809E-67,-1.18789542670764E-48,
-1.));
#44963=DIRECTION('ref_axis',(0.,1.,0.));
#44964=DIRECTION('center_axis',(-0.478904439132113,0.877867034329292,-9.06501463430316E-5));
#44965=DIRECTION('ref_axis',(0.877775582560928,0.478853053657823,-0.0144837723815965));
#44966=DIRECTION('center_axis',(-0.260706649707894,-0.965418060572078,-0.000105448247265905));
#44967=DIRECTION('ref_axis',(0.965346311170054,-0.260685939326527,-0.0122204970363453));
#44968=DIRECTION('center_axis',(5.15167520928809E-67,-1.18789542670764E-48,
-1.));
#44969=DIRECTION('ref_axis',(0.,1.,0.));
#44970=DIRECTION('center_axis',(-0.546304790255147,0.837586454001514,-9.06501464163507E-5));
#44971=DIRECTION('ref_axis',(0.837499315806636,0.546246387962313,-0.0144837723519214));
#44972=DIRECTION('center_axis',(-0.184157150081311,-0.982896806869672,-0.00010544824733539));
#44973=DIRECTION('ref_axis',(0.982823653730718,-0.184142132936614,-0.012220496919376));
#44974=DIRECTION('center_axis',(5.15167520928809E-67,-1.18789542670764E-48,
-1.));
#44975=DIRECTION('ref_axis',(0.,1.,0.));
#44976=DIRECTION('center_axis',(-0.610336990681852,0.792141874658809,-9.06501463120476E-5));
#44977=DIRECTION('ref_axis',(0.792059587273495,0.610271931640219,-0.0144837723075503));
#44978=DIRECTION('center_axis',(-0.106472260385922,-0.994315667506542,-0.000105448247451369));
#44979=DIRECTION('ref_axis',(0.994241561642557,-0.106463029063183,-0.0122204969318448));
#44980=DIRECTION('center_axis',(5.15167520928809E-67,-1.18789542670764E-48,
-1.));
#44981=DIRECTION('ref_axis',(0.,1.,0.));
#44982=DIRECTION('center_axis',(-0.670606260603123,0.741813477245087,-9.06501463072396E-5));
#44983=DIRECTION('ref_axis',(0.741736547997548,0.670534945922644,-0.0144837723400245));
#44984=DIRECTION('center_axis',(-0.0281309338001256,-0.999604241409669,
-0.000105448247349234));
#44985=DIRECTION('ref_axis',(0.999529639708615,-0.0281275452135709,-0.012220496889411));
#44986=DIRECTION('center_axis',(5.15167520928809E-67,-1.18789542670764E-48,
-1.));
#44987=DIRECTION('ref_axis',(0.,1.,0.));
#44988=DIRECTION('center_axis',(-0.726741019928497,0.686911553066215,-9.0650146372247E-5));
#44989=DIRECTION('ref_axis',(0.686840456250864,0.726663889287803,-0.014483772375632));
#44990=DIRECTION('center_axis',(0.0503838293471008,-0.9987299227624,-0.000105448247268434));
#44991=DIRECTION('ref_axis',(0.998655285167451,0.0503813543057433,-0.0122204969390446));
#44992=DIRECTION('center_axis',(5.15167520928809E-67,-1.18789542670764E-48,
-1.));
#44993=DIRECTION('ref_axis',(0.,1.,0.));
#44994=DIRECTION('center_axis',(-0.77839517919999,0.627774590741587,-9.06501465192481E-5));
#44995=DIRECTION('ref_axis',(0.62770976469511,0.778312708136478,-0.0144837722873138));
#44996=DIRECTION('center_axis',(0.128587959432554,-0.991698102029866,-0.000105448247403937));
#44997=DIRECTION('ref_axis',(0.991623888707038,0.128579636022696,-0.0122204969540051));
#44998=DIRECTION('center_axis',(5.15167520928809E-67,-1.18789542670764E-48,
-1.));
#44999=DIRECTION('ref_axis',(0.,1.,0.));
#45000=DIRECTION('center_axis',(-0.825250273349494,0.564767189308247,-9.06501463546308E-5));
#45001=DIRECTION('ref_axis',(0.564709033703414,0.82516297032304,-0.0144837723475052));
#45002=DIRECTION('center_axis',(0.205999301987418,-0.978552132725367,-0.000105448247113811));
#45003=DIRECTION('ref_axis',(0.978478801224233,0.205985181525565,-0.0122204969893998));
#45004=DIRECTION('center_axis',(5.15167520928809E-67,-1.18789542670764E-48,
-1.));
#45005=DIRECTION('ref_axis',(0.,1.,0.));
#45006=DIRECTION('center_axis',(-0.867017425140065,0.498277810348848,-9.06501462870057E-5));
#45007=DIRECTION('ref_axis',(0.498226683734515,0.866925828402957,-0.0144837723937473));
#45008=DIRECTION('center_axis',(0.282140590344591,-0.959373064120873,-0.000105448247263863));
#45009=DIRECTION('ref_axis',(0.959301066555575,0.282120759888322,-0.0122204969363817));
#45010=DIRECTION('center_axis',(5.15167520928809E-67,-1.18789542670764E-48,
-1.));
#45011=DIRECTION('ref_axis',(0.,1.,0.));
#45012=DIRECTION('center_axis',(-0.903439126191882,0.428716382994866,-9.06501464245823E-5));
#45013=DIRECTION('ref_axis',(0.42867260058449,0.903343800470088,-0.0144837723120868));
#45014=DIRECTION('center_axis',(0.356542388140961,-0.934279141552142,-0.000105448247299974));
#45015=DIRECTION('ref_axis',(0.934208921811354,0.356516969951643,-0.0122204969034503));
#45016=DIRECTION('center_axis',(5.15167520928809E-67,-1.18789542670764E-48,
-1.));
#45017=DIRECTION('ref_axis',(0.,1.,0.));
#45018=DIRECTION('center_axis',(-0.934290824606917,0.356511776576704,-9.06501463905499E-5));
#45019=DIRECTION('ref_axis',(0.356475608302988,0.934192357614636,-0.0144837722787681));
#45020=DIRECTION('center_axis',(0.428745983551553,-0.903425077396614,-0.000105448247174382));
#45021=DIRECTION('ref_axis',(0.903357068407879,0.428715134340607,-0.0122204969145006));
#45022=DIRECTION('center_axis',(5.15167520928809E-67,-1.18789542670764E-48,
-1.));
#45023=DIRECTION('ref_axis',(0.,1.,0.));
#45024=DIRECTION('center_axis',(-0.959382309405018,0.282109156503729,-9.06501463332588E-5));
#45025=DIRECTION('ref_axis',(0.282080825355611,0.959281308222547,-0.0144837723517365));
#45026=DIRECTION('center_axis',(0.498306217395032,-0.867001097223137,-0.000105448243846677));
#45027=DIRECTION('ref_axis',(0.866935718268405,0.498270127348975,-0.0122204984383232));
#45028=DIRECTION('center_axis',(5.15167520928809E-67,-1.18789542670764E-48,
-1.));
#45029=DIRECTION('ref_axis',(0.,1.,0.));
#45030=DIRECTION('center_axis',(-0.978558883238511,0.205967239670656,-9.06501465473592E-5));
#45031=DIRECTION('ref_axis',(0.205946920319669,0.978455970573743,-0.0144837722792749));
#45032=DIRECTION('center_axis',(0.564794227716619,-0.825231766971349,-0.000105448246777006));
#45033=DIRECTION('ref_axis',(0.825169421163283,0.564753119359096,-0.01222049717581));
#45034=DIRECTION('center_axis',(5.15167520928809E-67,-1.18789542670764E-48,
-1.));
#45035=DIRECTION('ref_axis',(0.,1.,0.));
#45036=DIRECTION('center_axis',(-0.991702316153162,0.128555466313202,-9.0650146420716E-5));
#45037=DIRECTION('ref_axis',(0.128543284034494,0.991598126494967,-0.0144837723435229));
#45038=DIRECTION('center_axis',(0.627800093806525,-0.778374608461238,-0.000105448247294656));
#45039=DIRECTION('ref_axis',(0.778315680171741,0.627754220578766,-0.012220496894383));
#45040=DIRECTION('center_axis',(5.15167520928809E-67,-1.18789542670764E-48,
-1.));
#45041=DIRECTION('ref_axis',(0.,1.,0.));
#45042=DIRECTION('center_axis',(-0.998731574514195,0.0503511057569474,-9.06501463044587E-5));
#45043=DIRECTION('ref_axis',(0.0503471356585215,0.998626750227776,-0.0144837723156803));
#45044=DIRECTION('center_axis',(0.686935363552588,-0.726718511654644,-0.000105448247440854));
#45045=DIRECTION('ref_axis',(0.726663364192637,0.6868850082757,-0.0122204969756106));
#45046=DIRECTION('center_axis',(5.15167520928809E-67,-1.18789542670764E-48,
-1.));
#45047=DIRECTION('ref_axis',(0.,1.,0.));
#45048=DIRECTION('center_axis',(-0.99960332060638,-0.0281636861090561,-9.06501465204533E-5));
#45049=DIRECTION('ref_axis',(0.0281594195503036,-0.999498507968962,0.0144837722437162));
#45050=DIRECTION('center_axis',(0.741835448352776,-0.670581953565635,-0.000105448247295083));
#45051=DIRECTION('ref_axis',(0.67053092693442,0.741780921484487,-0.0122204969658991));
#45052=DIRECTION('center_axis',(5.15167520928809E-67,-1.18789542670764E-48,
-1.));
#45053=DIRECTION('ref_axis',(0.,1.,0.));
#45054=DIRECTION('center_axis',(-0.994312179825187,-0.106504839485521,-9.0650146389517E-5));
#45055=DIRECTION('ref_axis',(0.106492362574174,-0.994208025038546,0.0144837723789195));
#45056=DIRECTION('center_axis',(0.792161870927703,-0.610311034742932,-0.000105448246562834));
#45057=DIRECTION('ref_axis',(0.610264443536631,0.792103508641721,-0.0122204972240042));
#45058=DIRECTION('center_axis',(5.15167520928809E-67,-1.18789542670764E-48,
-1.));
#45059=DIRECTION('ref_axis',(0.,1.,0.));
#45060=DIRECTION('center_axis',(-0.982890773812962,-0.18418935511019,-9.06501462458389E-5));
#45061=DIRECTION('ref_axis',(0.184168744770736,-0.982787919028534,0.0144837723378535));
#45062=DIRECTION('center_axis',(0.837604352149828,-0.546277345439416,-0.000105448247288724));
#45063=DIRECTION('ref_axis',(0.546235476912052,0.837542514273825,-0.0122204969843265));
#45064=DIRECTION('center_axis',(5.15167520928809E-67,-1.18789542670764E-48,
-1.));
#45065=DIRECTION('ref_axis',(0.,1.,0.));
#45066=DIRECTION('center_axis',(-0.965409519335916,-0.260738282110905,-9.06501463158079E-5));
#45067=DIRECTION('ref_axis',(0.260709665413015,-0.965308598687581,0.0144837723005081));
#45068=DIRECTION('center_axis',(0.877882724007609,-0.478875674648073,-0.000105448246644854));
#45069=DIRECTION('ref_axis',(0.47883878693024,0.877817791788535,-0.012220497153411));
#45070=DIRECTION('center_axis',(5.15167520928809E-67,-1.18789542670764E-48,
-1.));
#45071=DIRECTION('ref_axis',(0.,1.,0.));
#45072=DIRECTION('center_axis',(-0.941976194141077,-0.335679670897783,-9.06501465752214E-5));
#45073=DIRECTION('ref_axis',(0.335643224272825,-0.941877829837701,0.0144837722974511));
#45074=DIRECTION('center_axis',(0.912748656947635,-0.408521576077636,-0.000105448247395522));
#45075=DIRECTION('ref_axis',(0.408489896596716,0.912681030718573,-0.0122204969165703));
#45076=DIRECTION('center_axis',(5.15167520928809E-67,-1.18789542670764E-48,
-1.));
#45077=DIRECTION('ref_axis',(0.,1.,0.));
#45078=DIRECTION('center_axis',(-0.912735272470059,-0.408551482889927,-9.0650146236208E-5));
#45079=DIRECTION('ref_axis',(0.408507431042893,-0.912640070958992,0.0144837723919199));
#45080=DIRECTION('center_axis',(0.941987190897161,-0.335648806144671,-0.000105448247475279));
#45081=DIRECTION('ref_axis',(0.335622530214028,0.941917287594399,-0.0122204968616106));
#45082=DIRECTION('center_axis',(5.15167520928809E-67,-1.18789542670764E-48,
-1.));
#45083=DIRECTION('ref_axis',(0.,1.,0.));
#45084=DIRECTION('center_axis',(-0.877867034329361,-0.478904439131988,-9.06501463610722E-5));
#45085=DIRECTION('ref_axis',(0.478853053657853,-0.877775582561276,0.0144837723595397));
#45086=DIRECTION('center_axis',(0.965418060572122,-0.260706649707733,-0.000105448247352975));
#45087=DIRECTION('ref_axis',(0.260685939326823,0.965346311171741,-0.012220496896787));
#45088=DIRECTION('center_axis',(5.15167520928809E-67,-1.18789542670764E-48,
-1.));
#45089=DIRECTION('ref_axis',(0.,1.,0.));
#45090=DIRECTION('center_axis',(-0.837586454001461,-0.546304790255229,-9.06501463408637E-5));
#45091=DIRECTION('ref_axis',(0.54624638796239,-0.837499315806573,0.0144837723526967));
#45092=DIRECTION('center_axis',(0.982896806869685,-0.184157150081241,-0.000105448247384682));
#45093=DIRECTION('ref_axis',(0.184142132936524,0.982823653730634,-0.0122204969274716));
#45094=DIRECTION('center_axis',(5.15167520928809E-67,-1.18789542670764E-48,
-1.));
#45095=DIRECTION('ref_axis',(0.,1.,0.));
#45096=DIRECTION('center_axis',(-0.792141874658961,-0.610336990681655,-9.06501464140886E-5));
#45097=DIRECTION('ref_axis',(0.610271931639049,-0.792059587272402,0.0144837724166105));
#45098=DIRECTION('center_axis',(0.994315667506523,-0.1064722603861,-0.000105448247372999));
#45099=DIRECTION('ref_axis',(0.106463029063429,0.994241561643113,-0.0122204968844733));
#45100=DIRECTION('center_axis',(5.15167520928809E-67,-1.18789542670764E-48,
-1.));
#45101=DIRECTION('ref_axis',(0.,1.,0.));
#45102=DIRECTION('center_axis',(-0.741813477245026,-0.670606260603191,-9.06501462657205E-5));
#45103=DIRECTION('ref_axis',(0.670534945922615,-0.741736547997381,0.0144837723499451));
#45104=DIRECTION('center_axis',(0.999604241409683,-0.0281309337996267,-0.000105448247542078));
#45105=DIRECTION('ref_axis',(0.0281275452130772,0.999529639708833,-0.0122204968727785));
#45106=DIRECTION('center_axis',(5.15167520928809E-67,-1.18789542670764E-48,
-1.));
#45107=DIRECTION('ref_axis',(0.,1.,0.));
#45108=DIRECTION('center_axis',(-0.686911553066313,-0.726741019928404,-9.0650146445407E-5));
#45109=DIRECTION('ref_axis',(0.726663889287897,-0.686840456251137,0.0144837723579623));
#45110=DIRECTION('center_axis',(0.998729922762429,0.0503838293465177,-0.00010544824700806));
#45111=DIRECTION('ref_axis',(0.0503813543051317,-0.998655285166875,0.0122204969886123));
#45112=DIRECTION('center_axis',(5.15167520928809E-67,-1.18789542670764E-48,
-1.));
#45113=DIRECTION('ref_axis',(0.,1.,0.));
#45114=DIRECTION('center_axis',(-0.627774590741284,-0.778395179200234,-9.06501463091932E-5));
#45115=DIRECTION('ref_axis',(0.778312708136324,-0.627709764694486,0.014483772322638));
#45116=DIRECTION('center_axis',(0.991698102029894,0.128587959432343,-0.000105448247307732));
#45117=DIRECTION('ref_axis',(0.128579636022594,-0.991623888707978,0.0122204968787672));
#45118=DIRECTION('center_axis',(5.15167520928809E-67,-1.18789542670764E-48,
-1.));
#45119=DIRECTION('ref_axis',(0.,1.,0.));
#45120=DIRECTION('center_axis',(-0.564767189308512,-0.825250273349312,-9.06501464604225E-5));
#45121=DIRECTION('ref_axis',(0.825162970323365,-0.564709033704023,0.014483772305219));
#45122=DIRECTION('center_axis',(0.978552132725239,0.205999301988023,-0.000105448247439453));
#45123=DIRECTION('ref_axis',(0.205985181526365,-0.978478801225051,0.0122204969104439));
#45124=DIRECTION('center_axis',(5.15167520928809E-67,-1.18789542670764E-48,
-1.));
#45125=DIRECTION('ref_axis',(0.,1.,0.));
#45126=DIRECTION('center_axis',(-0.498277810349565,-0.867017425139653,-9.06501466563663E-5));
#45127=DIRECTION('ref_axis',(0.86692582840462,-0.498226683736414,0.0144837722289047));
#45128=DIRECTION('center_axis',(0.959373064120893,0.282140590344525,-0.00010544824722367));
#45129=DIRECTION('ref_axis',(0.282120759888269,-0.959301066555644,0.0122204969322086));
#45130=DIRECTION('center_axis',(5.15167520928809E-67,-1.18789542670764E-48,
-1.));
#45131=DIRECTION('ref_axis',(0.,1.,0.));
#45132=DIRECTION('center_axis',(-0.428716382994794,-0.903439126191916,-9.06501464376821E-5));
#45133=DIRECTION('ref_axis',(0.903343800470677,-0.428672600584677,0.0144837722698243));
#45134=DIRECTION('center_axis',(0.934279141552165,0.356542388140901,-0.000105448247303552));
#45135=DIRECTION('ref_axis',(0.356516969951467,-0.934208921811066,0.0122204969306124));
#45136=DIRECTION('center_axis',(5.15167520928809E-67,-1.18789542670764E-48,
-1.));
#45137=DIRECTION('ref_axis',(0.,1.,0.));
#45138=DIRECTION('center_axis',(-0.356511776576584,-0.934290824606963,-9.06501462973138E-5));
#45139=DIRECTION('ref_axis',(0.9341923576135,-0.356475608302424,0.0144837723659048));
#45140=DIRECTION('center_axis',(0.903425077396469,0.42874598355186,-0.000105448247323971));
#45141=DIRECTION('ref_axis',(0.428715134340782,-0.903357068407445,0.0122204969404582));
#45142=DIRECTION('center_axis',(5.15167520928809E-67,-1.18789542670764E-48,
-1.));
#45143=DIRECTION('ref_axis',(0.,1.,0.));
#45144=DIRECTION('center_axis',(-0.282109156503611,-0.959382309405053,-9.06501462853803E-5));
#45145=DIRECTION('ref_axis',(0.959281308222382,-0.282080825355435,0.0144837723660616));
#45146=DIRECTION('center_axis',(0.867001097223284,0.498306217394775,-0.000105448243705777));
#45147=DIRECTION('ref_axis',(0.498270127348596,-0.86693571826834,0.0122204984583659));
#45148=DIRECTION('center_axis',(5.15167520928809E-67,-1.18789542670764E-48,
-1.));
#45149=DIRECTION('ref_axis',(0.,1.,0.));
#45150=DIRECTION('center_axis',(-0.205967239670074,-0.978558883238633,-9.06501462899978E-5));
#45151=DIRECTION('ref_axis',(0.978455970573443,-0.205946920318997,0.0144837723091262));
#45152=DIRECTION('center_axis',(0.825231766971361,0.564794227716602,-0.000105448246768021));
#45153=DIRECTION('ref_axis',(0.56475311935916,-0.825169421163415,0.0122204971638891));
#45154=DIRECTION('center_axis',(5.15167520928809E-67,-1.18789542670764E-48,
-1.));
#45155=DIRECTION('ref_axis',(0.,1.,0.));
#45156=DIRECTION('center_axis',(-0.128555466313085,-0.991702316153177,-9.06501463759606E-5));
#45157=DIRECTION('ref_axis',(0.991598126495219,-0.128543284034406,0.014483772327091));
#45158=DIRECTION('center_axis',(0.778374608461285,0.627800093806467,-0.000105448247278628));
#45159=DIRECTION('ref_axis',(0.627754220578617,-0.778315680171672,0.0122204969064386));
#45160=DIRECTION('center_axis',(5.15167520928809E-67,-1.18789542670764E-48,
-1.));
#45161=DIRECTION('ref_axis',(0.,1.,0.));
#45162=DIRECTION('center_axis',(-0.0503511057568215,-0.998731574514202,
-9.06501462140748E-5));
#45163=DIRECTION('ref_axis',(0.998626750226433,-0.0503471356583347,0.0144837724089729));
#45164=DIRECTION('center_axis',(0.72671851165485,0.686935363552371,-0.000105448247305609));
#45165=DIRECTION('ref_axis',(0.68688500827568,-0.726663364193057,0.0122204969517677));
#45166=DIRECTION('center_axis',(5.15167520928809E-67,-1.18789542670764E-48,
-1.));
#45167=DIRECTION('ref_axis',(0.,1.,0.));
#45168=DIRECTION('center_axis',(0.028163686109212,-0.999603320606376,-9.06501464412085E-5));
#45169=DIRECTION('ref_axis',(0.999498507967367,0.0281594195504058,0.0144837723535955));
#45170=DIRECTION('center_axis',(0.670581953565646,0.741835448352765,-0.000105448247317749));
#45171=DIRECTION('ref_axis',(0.741780921484837,-0.670530926934763,0.0122204969257884));
#45172=DIRECTION('center_axis',(5.15167520928809E-67,-1.18789542670764E-48,
-1.));
#45173=DIRECTION('ref_axis',(0.,1.,0.));
#45174=DIRECTION('center_axis',(0.106504839485654,-0.994312179825173,-9.06501463242885E-5));
#45175=DIRECTION('ref_axis',(0.994208025039066,0.106492362574368,0.0144837723417732));
#45176=DIRECTION('center_axis',(0.610311034742769,0.792161870927829,-0.000105448246632335));
#45177=DIRECTION('ref_axis',(0.792103508641049,-0.610264443535841,0.012220497306985));
#45178=DIRECTION('center_axis',(5.15167520928809E-67,-1.18789542670764E-48,
-1.));
#45179=DIRECTION('ref_axis',(0.,1.,0.));
#45180=DIRECTION('center_axis',(0.184189355110076,-0.982890773812984,-9.06501463014399E-5));
#45181=DIRECTION('ref_axis',(0.982787919027527,0.184168744770422,0.0144837724102069));
#45182=DIRECTION('center_axis',(0.546277345439608,0.837604352149702,-0.000105448247164003));
#45183=DIRECTION('ref_axis',(0.837542514274121,-0.546235476912526,0.0122204969428009));
#45184=DIRECTION('center_axis',(5.15167520928809E-67,-1.18789542670764E-48,
-1.));
#45185=DIRECTION('ref_axis',(0.,1.,0.));
#45186=DIRECTION('center_axis',(0.260738282110494,-0.965409519336027,-9.06501465102787E-5));
#45187=DIRECTION('ref_axis',(0.965308598687087,0.260709665412434,0.0144837723438797));
#45188=DIRECTION('center_axis',(0.47887567464682,0.877882724008293,-0.000105448247318393));
#45189=DIRECTION('ref_axis',(0.877817791791359,-0.47883878693017,0.0122204969532827));
#45190=DIRECTION('center_axis',(5.15167520928809E-67,-1.18789542670764E-48,
-1.));
#45191=DIRECTION('ref_axis',(0.,1.,0.));
#45192=DIRECTION('center_axis',(0.335679670898317,-0.941976194140886,-9.06501463025926E-5));
#45193=DIRECTION('ref_axis',(0.941877829837149,0.335643224273232,0.0144837723239312));
#45194=DIRECTION('center_axis',(0.408521576078182,0.912748656947391,-0.000105448247109452));
#45195=DIRECTION('ref_axis',(0.912681030717227,-0.408489896596761,0.0122204970155898));
#45196=DIRECTION('center_axis',(5.15167520928809E-67,-1.18789542670764E-48,
-1.));
#45197=DIRECTION('ref_axis',(0.,1.,0.));
#45198=DIRECTION('center_axis',(0.40855148288974,-0.912735272470143,-9.06501463607514E-5));
#45199=DIRECTION('ref_axis',(0.912640070959719,0.408507431042997,0.0144837723432182));
#45200=DIRECTION('center_axis',(0.33564880614496,0.941987190897058,-0.00010544824731253));
#45201=DIRECTION('ref_axis',(0.941917287593217,-0.335622530213924,0.0122204969555834));
#45202=DIRECTION('center_axis',(5.15167520928809E-67,-1.18789542670764E-48,
-1.));
#45203=DIRECTION('ref_axis',(0.,1.,0.));
#45204=DIRECTION('center_axis',(0.47890443913187,-0.877867034329425,-9.06501464476592E-5));
#45205=DIRECTION('ref_axis',(0.877775582561568,0.47885305365786,0.0144837723415746));
#45206=DIRECTION('center_axis',(0.260706649725499,0.965418060567325,-0.000105448239035086));
#45207=DIRECTION('ref_axis',(0.965346311123191,-0.260685939332472,0.0122205006114622));
#45208=DIRECTION('center_axis',(5.15167520928809E-67,-1.18789542670764E-48,
-1.));
#45209=DIRECTION('ref_axis',(0.,1.,0.));
#45210=DIRECTION('center_axis',(0.546304790255255,-0.837586454001444,-9.0650146342598E-5));
#45211=DIRECTION('ref_axis',(0.837499315807156,0.546246387962813,0.0144837723030219));
#45212=DIRECTION('center_axis',(0.184157150081292,0.982896806869675,-0.000105448247335927));
#45213=DIRECTION('ref_axis',(0.982823653730575,-0.184142132936566,0.0122204969315608));
#45214=DIRECTION('center_axis',(5.15167520928809E-67,-1.18789542670764E-48,
-1.));
#45215=DIRECTION('ref_axis',(0.,1.,0.));
#45216=DIRECTION('center_axis',(0.610336990681674,-0.792141874658946,-9.06501464101343E-5));
#45217=DIRECTION('ref_axis',(0.792059587273886,0.610271931640238,0.0144837722853376));
#45218=DIRECTION('center_axis',(0.106472260386401,0.99431566750649,-0.000105448247238185));
#45219=DIRECTION('ref_axis',(0.994241561642249,-0.106463029063635,0.0122204969529716));
#45220=DIRECTION('center_axis',(5.15167520928809E-67,-1.18789542670764E-48,
-1.));
#45221=DIRECTION('ref_axis',(0.,1.,0.));
#45222=DIRECTION('center_axis',(0.670606260602894,-0.741813477245294,-9.06501464627064E-5));
#45223=DIRECTION('ref_axis',(0.741736547997723,0.670534945922382,0.0144837723432088));
#45224=DIRECTION('center_axis',(0.0281309337999561,0.999604241409674,-0.000105448247417899));
#45225=DIRECTION('ref_axis',(0.999529639708026,-0.0281275452133787,0.0122204969380853));
#45226=DIRECTION('center_axis',(5.15167520928809E-67,-1.18789542670764E-48,
-1.));
#45227=DIRECTION('ref_axis',(0.,1.,0.));
#45228=DIRECTION('center_axis',(0.726741019928368,-0.686911553066351,-9.0650146471134E-5));
#45229=DIRECTION('ref_axis',(0.686840456251459,0.726663889288164,0.0144837723292476));
#45230=DIRECTION('center_axis',(-0.050383829347144,0.998729922762398,-0.000105448247269544));
#45231=DIRECTION('ref_axis',(0.998655285167744,0.0503813543057988,0.0122204969148411));
#45232=DIRECTION('center_axis',(5.15167520928809E-67,-1.18789542670764E-48,
-1.));
#45233=DIRECTION('ref_axis',(0.,1.,0.));
#45234=DIRECTION('center_axis',(0.778395179200218,-0.627774590741304,-9.06501463631465E-5));
#45235=DIRECTION('ref_axis',(0.627709764694807,0.778312708136684,0.0144837722894029));
#45236=DIRECTION('center_axis',(-0.12858795942834,0.991698102030413,-0.000105448245500489));
#45237=DIRECTION('ref_axis',(0.991623888698102,0.128579636017312,0.0122204977357358));
#45238=DIRECTION('center_axis',(5.15167520928809E-67,-1.18789542670764E-48,
-1.));
#45239=DIRECTION('ref_axis',(0.,1.,0.));
#45240=DIRECTION('center_axis',(0.825250273349428,-0.564767189308343,-9.06501464028957E-5));
#45241=DIRECTION('ref_axis',(0.564709033703531,0.825162970323003,0.0144837723450398));
#45242=DIRECTION('center_axis',(-0.205999301987628,0.978552132725322,-0.000105448247257059));
#45243=DIRECTION('ref_axis',(0.978478801225208,0.205985181525983,0.0122204969042825));
#45244=DIRECTION('center_axis',(5.15167520928809E-67,-1.18789542670764E-48,
-1.));
#45245=DIRECTION('ref_axis',(0.,1.,0.));
#45246=DIRECTION('center_axis',(0.867017425139937,-0.498277810349071,-9.06501464136658E-5));
#45247=DIRECTION('ref_axis',(0.498226683735389,0.866925828403975,0.0144837723027363));
#45248=DIRECTION('center_axis',(-0.282140590344626,0.959373064120863,-0.000105448247277017));
#45249=DIRECTION('ref_axis',(0.959301066555094,0.282120759888223,0.0122204969764503));
#45250=DIRECTION('center_axis',(5.15167520928809E-67,-1.18789542670764E-48,
-1.));
#45251=DIRECTION('ref_axis',(0.,1.,0.));
#45252=DIRECTION('center_axis',(0.90343912619187,-0.42871638299489,-9.06501464260602E-5));
#45253=DIRECTION('ref_axis',(0.428672600584421,0.903343800469878,0.0144837723272369));
#45254=DIRECTION('center_axis',(-0.356542388139781,0.934279141552593,-0.000105448246761887));
#45255=DIRECTION('ref_axis',(0.934208921809314,0.35651696994953,0.012220497120973));
#45256=DIRECTION('center_axis',(5.15167520928809E-67,-1.18789542670764E-48,
-1.));
#45257=DIRECTION('ref_axis',(0.,1.,0.));
#45258=DIRECTION('center_axis',(0.934290824606888,-0.35651177657678,-9.06501464134324E-5));
#45259=DIRECTION('ref_axis',(0.356475608302711,0.934192357613664,0.0144837723482609));
#45260=DIRECTION('center_axis',(-0.428745983551679,0.903425077396555,-0.000105448247222545));
#45261=DIRECTION('ref_axis',(0.903357068407448,0.428715134340562,0.0122204969479439));
#45262=DIRECTION('center_axis',(5.15167520928809E-67,-1.18789542670764E-48,
-1.));
#45263=DIRECTION('ref_axis',(0.,1.,0.));
#45264=DIRECTION('center_axis',(0.959382309405034,-0.282109156503675,-9.06501462956451E-5));
#45265=DIRECTION('ref_axis',(0.282080825355574,0.959281308222623,0.0144837723473633));
#45266=DIRECTION('center_axis',(-0.498306217401744,0.867001097219279,-0.000105448247347347));
#45267=DIRECTION('ref_axis',(0.866935718280794,0.498270127364887,0.0122204969106369));
#45268=DIRECTION('center_axis',(5.15167520928809E-67,-1.18789542670764E-48,
-1.));
#45269=DIRECTION('ref_axis',(0.,1.,0.));
#45270=DIRECTION('center_axis',(0.978558883238587,-0.205967239670296,-9.06501464061553E-5));
#45271=DIRECTION('ref_axis',(0.205946920319019,0.978455970572407,0.0144837723787919));
#45272=DIRECTION('center_axis',(-0.564794227717559,0.825231766970706,-0.000105448247271081));
#45273=DIRECTION('ref_axis',(0.825169421165301,0.564753119361831,0.0122204969131223));
#45274=DIRECTION('center_axis',(5.15167520928809E-67,-1.18789542670764E-48,
-1.));
#45275=DIRECTION('ref_axis',(0.,1.,0.));
#45276=DIRECTION('center_axis',(0.99170231615319,-0.128555466312983,-9.06501463191467E-5));
#45277=DIRECTION('ref_axis',(0.128543284034309,0.991598126495285,0.014483772323378));
#45278=DIRECTION('center_axis',(-0.627800093806562,0.778374608461208,-0.000105448247350595));
#45279=DIRECTION('ref_axis',(0.778315680171392,0.627754220578551,0.0122204969276863));
#45280=DIRECTION('center_axis',(5.15167520928809E-67,-1.18789542670764E-48,
-1.));
#45281=DIRECTION('ref_axis',(0.,1.,0.));
#45282=DIRECTION('center_axis',(0.998731574514188,-0.0503511057570843,-9.06501463742907E-5));
#45283=DIRECTION('ref_axis',(0.0503471356586318,0.998626750227146,0.0144837723587898));
#45284=DIRECTION('center_axis',(-0.686935363552425,0.726718511654798,-0.000105448247333776));
#45285=DIRECTION('ref_axis',(0.726663364192883,0.686885008275621,0.0122204969654078));
#45286=DIRECTION('center_axis',(5.15167520928809E-67,-1.18789542670764E-48,
-1.));
#45287=DIRECTION('ref_axis',(0.,1.,0.));
#45288=DIRECTION('center_axis',(0.999603320606373,0.0281636861093081,-9.0650146390368E-5));
#45289=DIRECTION('ref_axis',(0.0281594195505035,-0.99949850796739,-0.0144837723518616));
#45290=DIRECTION('center_axis',(-0.741835448352795,0.670581953565614,-0.000105448247334273));
#45291=DIRECTION('ref_axis',(0.670530926935027,0.741780921485189,0.0122204968899333));
#45292=DIRECTION('center_axis',(5.15167520928809E-67,-1.18789542670764E-48,
-1.));
#45293=DIRECTION('ref_axis',(0.,1.,0.));
#45294=DIRECTION('center_axis',(0.994312179825183,0.106504839485559,-9.06501463756277E-5));
#45295=DIRECTION('ref_axis',(0.106492362574294,-0.994208025039266,-0.0144837723286163));
#45296=DIRECTION('center_axis',(-0.792161870920044,0.610311034752874,-0.00010544824088436));
#45297=DIRECTION('ref_axis',(0.610264443527485,0.792103508609612,0.0122204997619462));
#45298=DIRECTION('center_axis',(5.15167520928809E-67,-1.18789542670764E-48,
-1.));
#45299=DIRECTION('ref_axis',(0.,1.,0.));
#45300=DIRECTION('center_axis',(0.982890773813025,0.184189355109853,-9.06501463812825E-5));
#45301=DIRECTION('ref_axis',(0.184168744770323,-0.982787919028214,-0.0144837723648623));
#45302=DIRECTION('center_axis',(-0.837604352149864,0.54627734543936,-0.00010544824728987));
#45303=DIRECTION('ref_axis',(0.546235476912709,0.837542514274935,0.0122204968788532));
#45304=DIRECTION('center_axis',(5.15167520928809E-67,-1.18789542670764E-48,
-1.));
#45305=DIRECTION('ref_axis',(0.,1.,0.));
#45306=DIRECTION('center_axis',(-0.778374608461274,-0.62780009380648,-0.000105448247267533));
#45307=DIRECTION('ref_axis',(0.627754220578446,-0.77831568017143,-0.0122204969306265));
#45308=DIRECTION('center_axis',(0.128555466313028,0.991702316153185,-9.06501463500336E-5));
#45309=DIRECTION('ref_axis',(0.991598126495177,-0.128543284034342,-0.0144837723304925));
#45310=DIRECTION('center_axis',(5.15167520928809E-67,-1.18789542670764E-48,
-1.));
#45311=DIRECTION('ref_axis',(0.,1.,0.));
#45312=DIRECTION('center_axis',(-0.825231766970672,-0.564794227717608,-0.000105448247309068));
#45313=DIRECTION('ref_axis',(0.564753119361638,-0.825169421164907,-0.012220496948613));
#45314=DIRECTION('center_axis',(0.205967239670274,0.978558883238591,-9.0650146374353E-5));
#45315=DIRECTION('ref_axis',(0.978455970572943,-0.205946920319105,-0.0144837723413512));
#45316=DIRECTION('center_axis',(5.15167520928809E-67,-1.18789542670764E-48,
-1.));
#45317=DIRECTION('ref_axis',(0.,1.,0.));
#45318=DIRECTION('center_axis',(-0.86700109721932,-0.498306217401672,-0.00010544824729092));
#45319=DIRECTION('ref_axis',(0.498270127364739,-0.8669357182807,-0.0122204969233888));
#45320=DIRECTION('center_axis',(0.282109156504052,0.959382309404923,-9.06501464701313E-5));
#45321=DIRECTION('ref_axis',(0.959281308222407,-0.282080825355923,-0.0144837723548786));
#45322=DIRECTION('center_axis',(5.15167520928809E-67,-1.18789542670764E-48,
-1.));
#45323=DIRECTION('ref_axis',(0.,1.,0.));
#45324=DIRECTION('center_axis',(-0.903425077396529,-0.428745983551733,-0.000105448247249315));
#45325=DIRECTION('ref_axis',(0.428715134340504,-0.903357068407182,-0.0122204969696425));
#45326=DIRECTION('center_axis',(0.356511776576785,0.934290824606886,-9.06501464239672E-5));
#45327=DIRECTION('ref_axis',(0.934192357613866,-0.356475608302793,-0.0144837723332318));
#45328=DIRECTION('center_axis',(5.15167520928809E-67,-1.18789542670764E-48,
-1.));
#45329=DIRECTION('ref_axis',(0.,1.,0.));
#45330=DIRECTION('center_axis',(-0.934279141552621,-0.356542388139705,-0.000105448246733279));
#45331=DIRECTION('ref_axis',(0.356516969949183,-0.934208921808614,-0.0122204971846563));
#45332=DIRECTION('center_axis',(0.428716382994808,0.903439126191909,-9.06501463770139E-5));
#45333=DIRECTION('ref_axis',(0.903343800469329,-0.428672600584064,-0.0144837723720362));
#45334=DIRECTION('center_axis',(5.15167520928809E-67,-1.18789542670764E-48,
-1.));
#45335=DIRECTION('ref_axis',(0.,1.,0.));
#45336=DIRECTION('center_axis',(-0.959373064120865,-0.282140590344618,-0.000105448247270857));
#45337=DIRECTION('ref_axis',(0.282120759888191,-0.959301066555013,-0.0122204969835453));
#45338=DIRECTION('center_axis',(0.498277810349034,0.867017425139958,-9.06501463569771E-5));
#45339=DIRECTION('ref_axis',(0.866925828403698,-0.498226683735182,-0.0144837723264648));
#45340=DIRECTION('center_axis',(5.15167520928809E-67,-1.18789542670764E-48,
-1.));
#45341=DIRECTION('ref_axis',(0.,1.,0.));
#45342=DIRECTION('center_axis',(-0.978552132725285,-0.205999301987804,-0.000105448247338301));
#45343=DIRECTION('ref_axis',(0.205985181526041,-0.978478801224581,-0.0122204969535068));
#45344=DIRECTION('center_axis',(0.564767189308271,0.825250273349477,-9.06501463565956E-5));
#45345=DIRECTION('ref_axis',(0.825162970322881,-0.564709033703342,-0.0144837723594094));
#45346=DIRECTION('center_axis',(5.15167520928809E-67,-1.18789542670764E-48,
-1.));
#45347=DIRECTION('ref_axis',(0.,1.,0.));
#45348=DIRECTION('center_axis',(-0.991698102030424,-0.128587959428258,-0.000105448245434831));
#45349=DIRECTION('ref_axis',(0.128579636017166,-0.991623888697594,-0.0122204977785004));
#45350=DIRECTION('center_axis',(0.627774590741263,0.778395179200251,-9.06501463298504E-5));
#45351=DIRECTION('ref_axis',(0.778312708136619,-0.627709764694687,-0.0144837722981268));
#45352=DIRECTION('center_axis',(5.15167520928809E-67,-1.18789542670764E-48,
-1.));
#45353=DIRECTION('ref_axis',(0.,1.,0.));
#45354=DIRECTION('center_axis',(-0.998729922762387,-0.0503838293473624,
-0.000105448247373321));
#45355=DIRECTION('ref_axis',(0.0503813543060242,-0.998655285167869,-0.0122204969036645));
#45356=DIRECTION('center_axis',(0.686911553066443,0.726741019928282,-9.06501464895761E-5));
#45357=DIRECTION('ref_axis',(0.726663889287984,-0.686840456251464,-0.0144837723380814));
#45358=DIRECTION('center_axis',(5.15167520928809E-67,-1.18789542670764E-48,
-1.));
#45359=DIRECTION('ref_axis',(0.,1.,0.));
#45360=DIRECTION('center_axis',(-0.999604241409666,0.0281309338002504,-0.00010544824728445));
#45361=DIRECTION('ref_axis',(0.0281275452136831,0.999529639708247,0.0122204969192793));
#45362=DIRECTION('center_axis',(0.741813477245179,0.670606260603021,-9.06501463486941E-5));
#45363=DIRECTION('ref_axis',(0.670534945922386,-0.741736547997471,-0.0144837723559454));
#45364=DIRECTION('center_axis',(5.15167520928809E-67,-1.18789542670764E-48,
-1.));
#45365=DIRECTION('ref_axis',(0.,1.,0.));
#45366=DIRECTION('center_axis',(-0.994315667506492,0.106472260386385,-0.000105448247246095));
#45367=DIRECTION('ref_axis',(0.106463029063669,0.99424156164268,0.0122204969176238));
#45368=DIRECTION('center_axis',(0.792141874658893,0.610336990681743,-9.06501463537118E-5));
#45369=DIRECTION('ref_axis',(0.610271931639807,-0.792059587273192,-0.0144837723414781));
#45370=DIRECTION('center_axis',(5.15167520928809E-67,-1.18789542670764E-48,
-1.));
#45371=DIRECTION('ref_axis',(0.,1.,0.));
#45372=DIRECTION('center_axis',(-0.98289680686965,0.184157150081429,-0.000105448247288298));
#45373=DIRECTION('ref_axis',(0.184142132936832,0.982823653731204,0.0122204968770007));
#45374=DIRECTION('center_axis',(0.837586454001503,0.546304790255165,-9.06501464022278E-5));
#45375=DIRECTION('ref_axis',(0.546246387962582,-0.837499315807004,-0.0144837723204838));
#45376=DIRECTION('center_axis',(5.15167520928809E-67,-1.18789542670764E-48,
-1.));
#45377=DIRECTION('ref_axis',(0.,1.,0.));
#45378=DIRECTION('center_axis',(-0.965418060567323,0.260706649725506,-0.000105448239021929));
#45379=DIRECTION('ref_axis',(0.260685939332638,0.965346311123758,0.0122205005631217));
#45380=DIRECTION('center_axis',(0.877867034329392,0.478904439131931,-9.06501464072983E-5));
#45381=DIRECTION('ref_axis',(0.478853053658107,-0.87777558256187,-0.0144837723150808));
#45382=DIRECTION('center_axis',(5.15167520928809E-67,-1.18789542670764E-48,
-1.));
#45383=DIRECTION('ref_axis',(0.,1.,0.));
#45384=DIRECTION('center_axis',(-0.94198719089703,0.335648806145038,-0.000105448247300868));
#45385=DIRECTION('ref_axis',(0.335622530213848,0.941917287592769,0.0122204969921728));
#45386=DIRECTION('center_axis',(0.912735272470196,0.40855148288962,-9.06501464040206E-5));
#45387=DIRECTION('ref_axis',(0.408507431043198,-0.912640070960478,-0.01448377228974));
#45388=DIRECTION('center_axis',(5.15167520928809E-67,-1.18789542670764E-48,
-1.));
#45389=DIRECTION('ref_axis',(0.,1.,0.));
#45390=DIRECTION('center_axis',(0.965409519335958,0.260738282110751,-9.06501464007405E-5));
#45391=DIRECTION('ref_axis',(0.260709665412327,-0.965308598685698,-0.0144837724383535));
#45392=DIRECTION('center_axis',(-0.87788272400828,0.478875674646843,-0.000105448247307507));
#45393=DIRECTION('ref_axis',(0.478838786930294,0.877817791791527,0.0122204969363654));
#45394=DIRECTION('center_axis',(5.15167520928809E-67,-1.18789542670764E-48,
-1.));
#45395=DIRECTION('ref_axis',(-4.33680868994202E-19,1.,-1.18789542670764E-48));
#45396=DIRECTION('center_axis',(5.15167520928809E-67,-1.18789542670764E-48,
-1.));
#45397=DIRECTION('ref_axis',(-4.33680868994202E-19,1.,-1.18789542670764E-48));
#45398=DIRECTION('center_axis',(5.15167520928809E-67,-1.18789542670764E-48,
-1.));
#45399=DIRECTION('ref_axis',(0.,1.,0.));
#45400=DIRECTION('center_axis',(0.941987190897879,0.335648806142656,0.000105448247691596));
#45401=DIRECTION('ref_axis',(0.335622530211987,-0.941917287595053,0.0122204968672344));
#45402=DIRECTION('center_axis',(-0.912735272471169,0.408551482887447,9.06501467246596E-5));
#45403=DIRECTION('ref_axis',(0.408507431040732,0.912640070960819,-0.0144837723377799));
#45404=DIRECTION('center_axis',(5.15167520928809E-67,-1.18789542670764E-48,
-1.));
#45405=DIRECTION('ref_axis',(-4.33680868994202E-19,1.,-1.18789542670764E-48));
#45406=DIRECTION('center_axis',(5.15167520928809E-67,-1.18789542670764E-48,
-1.));
#45407=DIRECTION('ref_axis',(-4.33680868994202E-19,1.,-1.18789542670764E-48));
#45408=DIRECTION('',(-5.15167520928809E-67,1.18789542670764E-48,1.));
#45409=DIRECTION('',(5.15167520928809E-67,-1.18789542670764E-48,-1.));
#45410=DIRECTION('center_axis',(5.15167520928809E-67,-1.18789542670764E-48,
-1.));
#45411=DIRECTION('ref_axis',(-4.33680868994202E-19,1.,-1.18789542670764E-48));
#45412=DIRECTION('center_axis',(5.15167520928809E-67,-1.18789542670764E-48,
-1.));
#45413=DIRECTION('ref_axis',(0.,1.,0.));
#45414=DIRECTION('center_axis',(0.941976194140935,0.33567967089818,-9.06501463865783E-5));
#45415=DIRECTION('ref_axis',(0.335643224273153,-0.94187782983736,-0.014483772312066));
#45416=DIRECTION('center_axis',(-0.912748656947277,0.408521576078436,-0.000105448246989675));
#45417=DIRECTION('ref_axis',(0.408489896596946,0.91268103071696,0.012220497029356));
#45418=DIRECTION('center_axis',(-5.15167520928809E-67,1.18789542670764E-48,
1.));
#45419=DIRECTION('ref_axis',(4.33680868994202E-19,-1.,1.18789542670764E-48));
#45420=DIRECTION('center_axis',(0.,0.,1.));
#45421=DIRECTION('ref_axis',(1.,4.33680868994202E-19,0.));
#45422=DIRECTION('',(0.866025403784438,0.5,0.));
#45423=DIRECTION('',(-4.33680868994202E-19,1.,0.));
#45424=DIRECTION('',(-0.866025403784439,0.499999999999999,0.));
#45425=DIRECTION('',(-0.866025403784439,-0.5,0.));
#45426=DIRECTION('',(6.01359520363859E-16,-1.,0.));
#45427=DIRECTION('',(0.866025403784439,-0.5,0.));
#45428=DIRECTION('center_axis',(1.,4.33680868994202E-19,0.));
#45429=DIRECTION('ref_axis',(0.,0.,-1.));
#45430=DIRECTION('',(0.,0.,1.));
#45431=DIRECTION('',(0.,0.,1.));
#45432=DIRECTION('center_axis',(0.499999999999999,0.866025403784439,0.));
#45433=DIRECTION('ref_axis',(-0.866025403784439,0.499999999999999,0.));
#45434=DIRECTION('',(0.,0.,1.));
#45435=DIRECTION('center_axis',(-0.5,0.866025403784439,0.));
#45436=DIRECTION('ref_axis',(-0.866025403784439,-0.5,0.));
#45437=DIRECTION('',(0.,0.,1.));
#45438=DIRECTION('center_axis',(-1.,-6.01359520363859E-16,0.));
#45439=DIRECTION('ref_axis',(6.01359520363859E-16,-1.,0.));
#45440=DIRECTION('',(0.,0.,1.));
#45441=DIRECTION('center_axis',(-0.5,-0.866025403784439,0.));
#45442=DIRECTION('ref_axis',(0.866025403784439,-0.5,0.));
#45443=DIRECTION('',(0.,0.,1.));
#45444=DIRECTION('center_axis',(0.5,-0.866025403784439,0.));
#45445=DIRECTION('ref_axis',(0.866025403784439,0.5,0.));
#45446=DIRECTION('',(1.0568194522281E-16,0.866025403784468,-0.499999999999949));
#45447=DIRECTION('center_axis',(4.70261923768679E-35,-1.08435016942139E-16,
1.));
#45448=DIRECTION('ref_axis',(0.378466979033695,0.925614793410903,1.00369055805406E-16));
#45449=DIRECTION('center_axis',(0.912653256146669,-0.408734674385332,0.));
#45450=DIRECTION('ref_axis',(0.408734674385332,0.912653256146669,0.));
#45451=DIRECTION('',(0.,0.,1.));
#45452=DIRECTION('center_axis',(0.,0.,1.));
#45453=DIRECTION('ref_axis',(1.,4.33680868994202E-19,0.));
#45454=DIRECTION('',(0.,0.,1.));
#45455=DIRECTION('center_axis',(-0.912653256146668,-0.408734674385334,0.));
#45456=DIRECTION('ref_axis',(0.408734674385334,-0.912653256146668,0.));
#45457=DIRECTION('center_axis',(0.877770897795706,-0.479080630982844,8.35636401295593E-50));
#45458=DIRECTION('ref_axis',(0.479080630982844,0.877770897795706,2.97282767021015E-66));
#45459=DIRECTION('',(-9.32012009987243E-50,3.66188516048321E-51,1.));
#45460=DIRECTION('center_axis',(-9.32012009987243E-50,3.66188516048321E-51,
1.));
#45461=DIRECTION('ref_axis',(1.,4.33680868994202E-19,9.32012009987243E-50));
#45462=DIRECTION('',(-9.32012009987243E-50,3.66188516048321E-51,1.));
#45463=DIRECTION('center_axis',(-0.941908803685482,-0.335868732602165,-8.65571190069724E-50));
#45464=DIRECTION('ref_axis',(0.335868732602165,-0.941908803685482,-2.86613947502886E-66));
#45465=DIRECTION('center_axis',(0.941908803685478,-0.335868732602176,-8.65571190069562E-50));
#45466=DIRECTION('ref_axis',(0.335868732602176,0.941908803685478,5.69318196416785E-66));
#45467=DIRECTION('',(9.32012009987071E-50,3.66188516048189E-51,1.));
#45468=DIRECTION('center_axis',(9.32012009987071E-50,3.66188516048189E-51,
1.));
#45469=DIRECTION('ref_axis',(1.,4.33680868994202E-19,-9.32012009987071E-50));
#45470=DIRECTION('',(9.32012009987071E-50,3.66188516048189E-51,1.));
#45471=DIRECTION('center_axis',(-0.877770897795712,-0.479080630982834,8.35636401295441E-50));
#45472=DIRECTION('ref_axis',(0.479080630982834,-0.877770897795712,-1.78392693329902E-66));
#45473=DIRECTION('center_axis',(0.965357170233111,-0.260932048394827,-1.75574063469501E-49));
#45474=DIRECTION('ref_axis',(0.260932048394827,0.965357170233111,-8.03239509524584E-66));
#45475=DIRECTION('',(1.85827785600731E-49,1.46249639022155E-50,1.));
#45476=DIRECTION('center_axis',(1.8582778560073E-49,1.46249639022155E-50,
1.));
#45477=DIRECTION('ref_axis',(1.,4.33680868994202E-19,-1.8582778560073E-49));
#45478=DIRECTION('',(1.85827785600731E-49,1.46249639022155E-50,1.));
#45479=DIRECTION('center_axis',(-0.837476789971396,-0.546472896179862,1.63618603752562E-49));
#45480=DIRECTION('ref_axis',(0.546472896179862,-0.837476789971396,1.23627039651628E-65));
#45481=DIRECTION('center_axis',(0.982853788812423,-0.184386631340412,-2.66502014323869E-49));
#45482=DIRECTION('ref_axis',(0.184386631340412,0.982853788812423,-4.59929189808117E-66));
#45483=DIRECTION('',(2.77308680110516E-49,3.28216451991643E-50,1.));
#45484=DIRECTION('center_axis',(2.77308680110516E-49,3.28216451991643E-50,
1.));
#45485=DIRECTION('ref_axis',(1.,4.33680868994202E-19,-2.77308680110516E-49));
#45486=DIRECTION('',(2.77308680110516E-49,3.28216451991643E-50,1.));
#45487=DIRECTION('center_axis',(-0.792019359247614,-0.610495974251263,2.39671325397326E-49));
#45488=DIRECTION('ref_axis',(0.610495974251263,-0.792019359247614,-2.26955332198497E-65));
#45489=DIRECTION('center_axis',(0.994290786951656,-0.106704409389008,-3.5878037051643E-49));
#45490=DIRECTION('ref_axis',(0.106704409389008,0.994290786951656,1.37166247450949E-66));
#45491=DIRECTION('',(3.67079874392927E-49,5.81397404601223E-50,1.));
#45492=DIRECTION('center_axis',(3.67079874392927E-49,5.81397404601223E-50,
1.));
#45493=DIRECTION('ref_axis',(1.,4.33680868994202E-19,-3.67079874392927E-49));
#45494=DIRECTION('',(3.67079874392927E-49,5.81397404601223E-50,1.));
#45495=DIRECTION('center_axis',(-0.741678865800908,-0.670755141630892,3.11252914744798E-49));
#45496=DIRECTION('ref_axis',(0.670755141630892,-0.741678865800908,-3.59898235302298E-65));
#45497=DIRECTION('center_axis',(0.999597651754094,-0.028364319270904,-4.5184020529559E-49));
#45498=DIRECTION('ref_axis',(0.028364319270904,0.999597651754094,-3.26521667006146E-66));
#45499=DIRECTION('',(4.54587899183259E-49,9.04231552086841E-50,1.));
#45500=DIRECTION('center_axis',(4.54587899183259E-49,9.04231552086841E-50,
1.));
#45501=DIRECTION('ref_axis',(1.,4.33680868994202E-19,-4.54587899183259E-49));
#45502=DIRECTION('',(4.54587899183259E-49,9.04231552086841E-50,1.));
#45503=DIRECTION('center_axis',(-0.68676567551329,-0.726878880513649,3.77922047493358E-49));
#45504=DIRECTION('ref_axis',(0.726878880513649,-0.68676567551329,8.44347396578498E-67));
#45505=DIRECTION('center_axis',(0.998741664633518,0.0501506463075991,-5.45107773834402E-49));
#45506=DIRECTION('ref_axis',(-0.0501506463075991,0.998741664633518,-5.68155672720376E-65));
#45507=DIRECTION('center_axis',(-0.62761834646337,-0.778521169386283,4.39267686269876E-49));
#45508=DIRECTION('ref_axis',(0.778521169386283,-0.62761834646337,2.86838711888421E-65));
#45509=DIRECTION('center_axis',(0.991728103035171,0.128356416474834,-6.38008050558209E-49));
#45510=DIRECTION('ref_axis',(-0.128356416474834,0.991728103035171,2.64164793875071E-66));
#45511=DIRECTION('center_axis',(-0.564601541603225,-0.825363616365092,4.94911614811798E-49));
#45512=DIRECTION('ref_axis',(0.825363616365092,-0.564601541603225,-1.21982614064914E-65));
#45513=DIRECTION('center_axis',(0.978600207898554,0.20577082665166,-7.29968274368531E-49));
#45514=DIRECTION('ref_axis',(-0.20577082665166,0.978600207898554,7.99368498149713E-66));
#45515=DIRECTION('center_axis',(-0.498103780490032,-0.867117422187756,5.44510769796179E-49));
#45516=DIRECTION('ref_axis',(0.867117422187756,-0.498103780490032,-1.67935322369464E-65));
#45517=DIRECTION('center_axis',(0.95943891706265,0.281916591256437,-8.20421479905702E-49));
#45518=DIRECTION('ref_axis',(-0.281916591256437,0.95943891706265,1.24589067679861E-65));
#45519=DIRECTION('center_axis',(-0.428535043933802,-0.903525160756829,5.87759355939149E-49));
#45520=DIRECTION('ref_axis',(0.903525160756829,-0.428535043933802,-8.86364012879408E-65));
#45521=DIRECTION('center_axis',(0.93436236625724,0.356324246329338,-9.08809993078841E-49));
#45522=DIRECTION('ref_axis',(-0.356324246329338,0.93436236625724,-2.69950222050985E-65));
#45523=DIRECTION('center_axis',(-0.356324246329358,-0.934362366257233,6.24390731325522E-49));
#45524=DIRECTION('ref_axis',(0.934362366257233,-0.356324246329358,4.50754916861586E-65));
#45525=DIRECTION('center_axis',(0.903525160756839,0.428535043933782,-9.94588869312071E-49));
#45526=DIRECTION('ref_axis',(-0.428535043933782,0.903525160756839,-3.06876799885187E-65));
#45527=DIRECTION('center_axis',(-0.281916591256458,-0.959438917062644,6.54179051344872E-49));
#45528=DIRECTION('ref_axis',(0.959438917062644,-0.281916591256458,5.46345068117847E-65));
#45529=DIRECTION('center_axis',(0.867117422187767,0.498103780490012,-1.07722925330905E-48));
#45530=DIRECTION('ref_axis',(-0.498103780490012,0.867117422187767,2.63677046246647E-65));
#45531=DIRECTION('center_axis',(-0.205770826651682,-0.978600207898549,6.76940661098659E-49));
#45532=DIRECTION('ref_axis',(0.978600207898549,-0.205770826651682,1.20007194121145E-65));
#45533=DIRECTION('center_axis',(0.825363616365104,0.564601541603207,-1.15622163962171E-48));
#45534=DIRECTION('ref_axis',(-0.564601541603207,0.825363616365104,5.34857418276646E-65));
#45535=DIRECTION('center_axis',(-0.128356416474855,-0.991728103035168,6.92535227693746E-49));
#45536=DIRECTION('ref_axis',(0.991728103035168,-0.128356416474855,1.05782428992148E-64));
#45537=DIRECTION('center_axis',(0.778521169386297,0.627618346463353,-1.2310790139208E-48));
#45538=DIRECTION('ref_axis',(-0.627618346463353,0.778521169386297,-3.24299836420865E-65));
#45539=DIRECTION('center_axis',(-0.0501506463076206,-0.998741664633517,
7.00866605441356E-49));
#45540=DIRECTION('ref_axis',(0.998741664633517,-0.0501506463076206,5.61717615944791E-66));
#45541=DIRECTION('center_axis',(0.83747678997139,-0.546472896179871,1.63618603752577E-49));
#45542=DIRECTION('ref_axis',(0.546472896179871,0.83747678997139,8.18221406165844E-66));
#45543=DIRECTION('',(-1.85827785600747E-49,1.46249639022181E-50,1.));
#45544=DIRECTION('center_axis',(-1.85827785600747E-49,1.46249639022181E-50,
1.));
#45545=DIRECTION('ref_axis',(1.,4.33680868994202E-19,1.85827785600747E-49));
#45546=DIRECTION('',(-1.85827785600747E-49,1.46249639022181E-50,1.));
#45547=DIRECTION('center_axis',(-0.965357170233114,-0.260932048394816,-1.75574063469517E-49));
#45548=DIRECTION('ref_axis',(0.260932048394816,-0.965357170233114,4.85072620126884E-66));
#45549=DIRECTION('center_axis',(0.792019359247608,-0.610495974251272,2.39671325397339E-49));
#45550=DIRECTION('ref_axis',(0.610495974251272,0.792019359247608,6.86514884131891E-66));
#45551=DIRECTION('',(-2.77308680110532E-49,3.28216451991683E-50,1.));
#45552=DIRECTION('center_axis',(-2.77308680110532E-49,3.28216451991683E-50,
1.));
#45553=DIRECTION('ref_axis',(1.,4.33680868994202E-19,2.77308680110532E-49));
#45554=DIRECTION('',(-2.77308680110532E-49,3.28216451991683E-50,1.));
#45555=DIRECTION('center_axis',(-0.982853788812425,-0.184386631340402,-2.66502014323885E-49));
#45556=DIRECTION('ref_axis',(0.184386631340402,-0.982853788812425,5.0100483719309E-66));
#45557=DIRECTION('center_axis',(0.741678865800901,-0.6707551416309,3.11252914744811E-49));
#45558=DIRECTION('ref_axis',(0.6707551416309,0.741678865800901,2.48321099822104E-65));
#45559=DIRECTION('',(-3.67079874392942E-49,5.81397404601274E-50,1.));
#45560=DIRECTION('center_axis',(-3.67079874392942E-49,5.81397404601274E-50,
1.));
#45561=DIRECTION('ref_axis',(1.,4.33680868994202E-19,3.67079874392942E-49));
#45562=DIRECTION('',(-3.67079874392942E-49,5.81397404601274E-50,1.));
#45563=DIRECTION('center_axis',(-0.994290786951657,-0.106704409388997,-3.58780370516446E-49));
#45564=DIRECTION('ref_axis',(0.106704409388997,-0.994290786951657,8.97464790050996E-66));
#45565=DIRECTION('center_axis',(0.686765675513281,-0.726878880513656,3.77922047493371E-49));
#45566=DIRECTION('ref_axis',(0.726878880513657,0.686765675513281,3.1589153081368E-66));
#45567=DIRECTION('',(-4.54587899183275E-49,9.04231552086907E-50,1.));
#45568=DIRECTION('center_axis',(-4.54587899183275E-49,9.04231552086907E-50,
1.));
#45569=DIRECTION('ref_axis',(1.,4.33680868994202E-19,4.54587899183275E-49));
#45570=DIRECTION('',(-4.54587899183275E-49,9.04231552086907E-50,1.));
#45571=DIRECTION('center_axis',(-0.999597651754094,-0.0283643192708926,
-4.51840205295607E-49));
#45572=DIRECTION('ref_axis',(0.0283643192708926,-0.999597651754094,-3.99287521021606E-67));
#45573=DIRECTION('center_axis',(0.627618346463361,-0.77852116938629,4.39267686269887E-49));
#45574=DIRECTION('ref_axis',(0.77852116938629,0.627618346463361,3.8324092947301E-66));
#45575=DIRECTION('',(-5.39293238409326E-49,1.29472851457609E-49,1.));
#45576=DIRECTION('center_axis',(-5.39293238409326E-49,1.29472851457609E-49,
1.));
#45577=DIRECTION('ref_axis',(-0.453990499739606,-0.891006524188338,-1.29472851457643E-49));
#45578=DIRECTION('',(-5.39293238409326E-49,1.29472851457609E-49,1.));
#45579=DIRECTION('center_axis',(-0.998741664633517,0.0501506463076103,-5.45107773834419E-49));
#45580=DIRECTION('ref_axis',(-0.0501506463076103,-0.998741664633517,1.75141110323522E-67));
#45581=DIRECTION('center_axis',(0.564601541603216,-0.825363616365098,4.94911614811808E-49));
#45582=DIRECTION('ref_axis',(0.825363616365098,0.564601541603216,-2.63676715352381E-65));
#45583=DIRECTION('',(-6.20673655487384E-49,1.75048074844164E-49,1.));
#45584=DIRECTION('center_axis',(-6.20673655487384E-49,1.75048074844164E-49,
1.));
#45585=DIRECTION('ref_axis',(-0.52249856471585,-0.852640164354153,-1.75048074844092E-49));
#45586=DIRECTION('',(-6.20673655487384E-49,1.75048074844164E-49,1.));
#45587=DIRECTION('center_axis',(-0.99172810303517,0.128356416474844,-6.38008050558225E-49));
#45588=DIRECTION('ref_axis',(-0.128356416474844,-0.99172810303517,-6.45104663994926E-66));
#45589=DIRECTION('center_axis',(0.498103780490022,-0.867117422187761,5.44510769796189E-49));
#45590=DIRECTION('ref_axis',(0.867117422187761,0.498103780490022,4.62928424055004E-65));
#45591=DIRECTION('',(-6.98227413084428E-49,2.26867838960881E-49,1.));
#45592=DIRECTION('center_axis',(-6.98227413084428E-49,2.26867838960881E-49,
1.));
#45593=DIRECTION('ref_axis',(-0.587785252292493,-0.809016994374933,-2.26867838960897E-49));
#45594=DIRECTION('',(-6.98227413084428E-49,2.26867838960881E-49,1.));
#45595=DIRECTION('center_axis',(-0.978600207898551,0.205770826651671,-7.29968274368548E-49));
#45596=DIRECTION('ref_axis',(-0.205770826651671,-0.978600207898551,-8.37640359713844E-66));
#45597=DIRECTION('center_axis',(0.428535043933792,-0.903525160756834,5.87759355939158E-49));
#45598=DIRECTION('ref_axis',(0.903525160756834,0.428535043933792,-6.0990810847752E-65));
#45599=DIRECTION('',(-7.71476366495631E-49,2.84612657730158E-49,1.));
#45600=DIRECTION('center_axis',(-7.71476366495631E-49,2.84612657730158E-49,
1.));
#45601=DIRECTION('ref_axis',(-0.649448048330161,-0.76040596560005,-2.84612657730134E-49));
#45602=DIRECTION('',(-7.71476366495631E-49,2.84612657730158E-49,1.));
#45603=DIRECTION('center_axis',(-0.959438917062647,0.281916591256448,-8.20421479905718E-49));
#45604=DIRECTION('ref_axis',(-0.281916591256448,-0.959438917062647,-3.25299225253391E-65));
#45605=DIRECTION('center_axis',(0.356324246329348,-0.934362366257237,6.2439073132553E-49));
#45606=DIRECTION('ref_axis',(0.934362366257237,0.356324246329348,-6.3916346242107E-66));
#45607=DIRECTION('',(-8.39968911565463E-49,3.47926515142182E-49,1.));
#45608=DIRECTION('center_axis',(-8.39968911565463E-49,3.47926515142182E-49,
1.));
#45609=DIRECTION('ref_axis',(-0.707106781186566,-0.707106781186529,-3.47926515142204E-49));
#45610=DIRECTION('',(-8.39968911565463E-49,3.47926515142182E-49,1.));
#45611=DIRECTION('center_axis',(-0.934362366257236,0.356324246329348,-9.08809993078856E-49));
#45612=DIRECTION('ref_axis',(-0.356324246329348,-0.934362366257236,-6.41640199023417E-65));
#45613=DIRECTION('center_axis',(0.281916591256447,-0.959438917062647,6.54179051344879E-49));
#45614=DIRECTION('ref_axis',(0.959438917062647,0.281916591256447,-1.09781434718078E-65));
#45615=DIRECTION('',(-9.03282768977487E-49,4.16419060212015E-49,1.));
#45616=DIRECTION('center_axis',(-9.03282768977487E-49,4.16419060212015E-49,
1.));
#45617=DIRECTION('ref_axis',(-0.760405965599942,-0.649448048330288,-4.16419060211889E-49));
#45618=DIRECTION('',(-9.03282768977487E-49,4.16419060212015E-49,1.));
#45619=DIRECTION('center_axis',(-0.903525160756834,0.428535043933793,-9.94588869312087E-49));
#45620=DIRECTION('ref_axis',(-0.428535043933793,-0.903525160756834,3.14193955482054E-65));
#45621=DIRECTION('center_axis',(0.205770826651671,-0.978600207898551,6.76940661098664E-49));
#45622=DIRECTION('ref_axis',(0.978600207898551,0.205770826651671,1.21103353553181E-65));
#45623=DIRECTION('',(-9.61027587746764E-49,4.89668013623218E-49,1.));
#45624=DIRECTION('center_axis',(-9.61027587746764E-49,4.89668013623218E-49,
1.));
#45625=DIRECTION('ref_axis',(-0.809016994374948,-0.587785252292472,-4.89668013623217E-49));
#45626=DIRECTION('',(-9.61027587746764E-49,4.89668013623218E-49,1.));
#45627=DIRECTION('center_axis',(-0.867117422187761,0.498103780490022,-1.07722925330906E-48));
#45628=DIRECTION('ref_axis',(-0.498103780490022,-0.867117422187761,1.20400755006059E-65));
#45629=DIRECTION('center_axis',(0.128356416474844,-0.99172810303517,6.92535227693751E-49));
#45630=DIRECTION('ref_axis',(0.99172810303517,0.128356416474844,1.37955244398014E-65));
#45631=DIRECTION('',(-1.01284735186348E-48,5.67221771220262E-49,1.));
#45632=DIRECTION('center_axis',(-1.01284735186348E-48,5.67221771220262E-49,
1.));
#45633=DIRECTION('ref_axis',(-0.852640164354111,-0.522498564715917,-5.67221771220297E-49));
#45634=DIRECTION('',(-1.01284735186348E-48,5.67221771220262E-49,1.));
#45635=DIRECTION('center_axis',(-0.825363616365097,0.564601541603216,-1.15622163962172E-48));
#45636=DIRECTION('ref_axis',(-0.564601541603216,-0.825363616365097,3.75089637720347E-65));
#45637=DIRECTION('center_axis',(0.0501506463076098,-0.998741664633517,7.0086660544136E-49));
#45638=DIRECTION('ref_axis',(0.998741664633517,0.0501506463076098,-1.39822384050416E-65));
#45639=DIRECTION('',(-1.05842257525004E-48,6.4860218829832E-49,1.));
#45640=DIRECTION('center_axis',(-1.05842257525004E-48,6.4860218829832E-49,
1.));
#45641=DIRECTION('ref_axis',(-0.891006524188326,-0.453990499739629,-6.48602188298224E-49));
#45642=DIRECTION('',(-1.05842257525004E-48,6.4860218829832E-49,1.));
#45643=DIRECTION('center_axis',(-0.77852116938629,0.627618346463361,-1.23107901392082E-48));
#45644=DIRECTION('ref_axis',(-0.627618346463361,-0.77852116938629,-1.0235164758246E-65));
#45645=DIRECTION('center_axis',(-0.0283643192708931,-0.999597651754094,
7.01883428627214E-49));
#45646=DIRECTION('ref_axis',(0.999597651754094,-0.0283643192708931,-4.40612052675408E-66));
#45647=DIRECTION('',(-1.09747227149895E-48,7.33307527524372E-49,1.));
#45648=DIRECTION('center_axis',(-1.09747227149895E-48,7.33307527524372E-49,
1.));
#45649=DIRECTION('ref_axis',(-0.923879532511259,-0.382683432365157,-7.33307527524286E-49));
#45650=DIRECTION('',(-1.09747227149895E-48,7.33307527524372E-49,1.));
#45651=DIRECTION('center_axis',(-0.726878880513656,0.686765675513282,-1.30133985560119E-48));
#45652=DIRECTION('ref_axis',(-0.686765675513282,-0.726878880513656,-1.0460740182702E-64));
#45653=DIRECTION('center_axis',(-0.106704409388998,-0.994290786951657,6.95579428198243E-49));
#45654=DIRECTION('ref_axis',(0.994290786951657,-0.106704409388998,-7.09717408543387E-66));
#45655=DIRECTION('',(-1.12975568624752E-48,8.20815552314704E-49,1.));
#45656=DIRECTION('center_axis',(-1.12975568624752E-48,8.20815552314704E-49,
1.));
#45657=DIRECTION('ref_axis',(-0.951056516295187,-0.309016994374844,-8.20815552314827E-49));
#45658=DIRECTION('',(-1.12975568624752E-48,8.20815552314704E-49,1.));
#45659=DIRECTION('center_axis',(-0.6707551416309,0.741678865800901,-1.36657098320978E-48));
#45660=DIRECTION('ref_axis',(-0.741678865800901,-0.6707551416309,3.57211103088032E-65));
#45661=DIRECTION('center_axis',(-0.184386631340402,-0.982853788812425,6.81993470413386E-49));
#45662=DIRECTION('ref_axis',(0.982853788812425,-0.184386631340402,2.71684956354986E-65));
#45663=DIRECTION('',(-1.15507378150848E-48,9.10586746597114E-49,1.));
#45664=DIRECTION('center_axis',(-1.15507378150848E-48,9.10586746597114E-49,
1.));
#45665=DIRECTION('ref_axis',(-0.972369920397692,-0.233445363855843,-9.1058674659719E-49));
#45666=DIRECTION('',(-1.15507378150848E-48,9.10586746597114E-49,1.));
#45667=DIRECTION('center_axis',(-0.610495974251271,0.792019359247608,-1.42637022515333E-48));
#45668=DIRECTION('ref_axis',(-0.792019359247608,-0.610495974251271,3.09249712984754E-64));
#45669=DIRECTION('center_axis',(-0.260932048394816,-0.965357170233114,6.61209317220174E-49));
#45670=DIRECTION('ref_axis',(0.965357170233114,-0.260932048394816,1.42679734120621E-65));
#45671=DIRECTION('',(-1.17327046280543E-48,1.0020676411069E-48,1.));
#45672=DIRECTION('center_axis',(-1.17327046280543E-48,1.0020676411069E-48,
1.));
#45673=DIRECTION('ref_axis',(-0.987688340595155,-0.156434465040119,-1.00206764110703E-48));
#45674=DIRECTION('',(-1.17327046280543E-48,1.0020676411069E-48,1.));
#45675=DIRECTION('center_axis',(-0.546472896179871,0.83747678997139,-1.48036889921999E-48));
#45676=DIRECTION('ref_axis',(-0.83747678997139,-0.546472896179871,5.98336102584152E-65));
#45677=DIRECTION('center_axis',(-0.335868732602165,-0.941908803685482,6.33355109834478E-49));
#45678=DIRECTION('ref_axis',(0.941908803685482,-0.335868732602165,5.83703495410428E-65));
#45679=DIRECTION('',(-1.18423354154716E-48,1.09469422570892E-48,1.));
#45680=DIRECTION('center_axis',(-1.18423354154716E-48,1.09469422570892E-48,
1.));
#45681=DIRECTION('ref_axis',(-0.996917333733132,-0.0784590957277897,-1.09469422570898E-48));
#45682=DIRECTION('',(-1.18423354154716E-48,1.09469422570892E-48,1.));
#45683=DIRECTION('center_axis',(-0.479080630982844,0.877770897795706,-1.52823408562776E-48));
#45684=DIRECTION('ref_axis',(-0.877770897795706,-0.479080630982844,-1.85065299173653E-65));
#45685=DIRECTION('center_axis',(-0.408734674385335,-0.912653256146667,5.98602578707292E-49));
#45686=DIRECTION('ref_axis',(0.912653256146667,-0.408734674385335,-4.742731066544E-66));
#45687=DIRECTION('',(-1.18789542670764E-48,1.18789542670765E-48,1.));
#45688=DIRECTION('center_axis',(-1.18789542670764E-48,1.18789542670765E-48,
1.));
#45689=DIRECTION('ref_axis',(4.33680868994202E-19,-1.,1.18789542670765E-48));
#45690=DIRECTION('',(-1.18789542670764E-48,1.18789542670765E-48,1.));
#45691=DIRECTION('center_axis',(-0.408734674385331,0.912653256146669,-1.56967067958564E-48));
#45692=DIRECTION('ref_axis',(-0.912653256146669,-0.408734674385331,-1.44539080722799E-64));
#45693=DIRECTION('center_axis',(-0.479080630982847,-0.877770897795704,5.57165984749406E-49));
#45694=DIRECTION('ref_axis',(0.877770897795704,-0.479080630982847,-3.32989513528092E-65));
#45695=DIRECTION('',(-1.18423354154716E-48,1.28109662770637E-48,1.));
#45696=DIRECTION('center_axis',(-1.18423354154716E-48,1.28109662770637E-48,
1.));
#45697=DIRECTION('ref_axis',(4.33680868994202E-19,-1.,1.28109662770637E-48));
#45698=DIRECTION('',(-1.18423354154716E-48,1.28109662770637E-48,1.));
#45699=DIRECTION('center_axis',(-0.335868732602161,0.941908803685483,-1.60442321071283E-48));
#45700=DIRECTION('ref_axis',(-0.941908803685483,-0.335868732602161,-1.10077185323049E-64));
#45701=DIRECTION('center_axis',(-0.546472896179874,-0.837476789971388,5.09300798341636E-49));
#45702=DIRECTION('ref_axis',(0.837476789971388,-0.546472896179874,-4.24396990687181E-65));
#45703=DIRECTION('',(-1.17327046280542E-48,1.37372321230839E-48,1.));
#45704=DIRECTION('center_axis',(-1.17327046280542E-48,1.37372321230839E-48,
1.));
#45705=DIRECTION('ref_axis',(4.33680868994202E-19,-1.,1.37372321230839E-48));
#45706=DIRECTION('',(-1.17327046280542E-48,1.37372321230839E-48,1.));
#45707=DIRECTION('center_axis',(-0.260932048394812,0.965357170233115,-1.63227741809852E-48));
#45708=DIRECTION('ref_axis',(-0.965357170233115,-0.260932048394812,1.79840374663787E-65));
#45709=DIRECTION('center_axis',(-0.610495974251274,-0.792019359247605,4.55302124274975E-49));
#45710=DIRECTION('ref_axis',(0.792019359247605,-0.610495974251274,-1.92107929694605E-65));
#45711=DIRECTION('',(-1.15507378150847E-48,1.46520410681818E-48,1.));
#45712=DIRECTION('center_axis',(-1.15507378150847E-48,1.46520410681818E-48,
1.));
#45713=DIRECTION('ref_axis',(4.33680868994202E-19,-1.,1.46520410681818E-48));
#45714=DIRECTION('',(-1.15507378150847E-48,1.46520410681818E-48,1.));
#45715=DIRECTION('center_axis',(-0.184386631340398,0.982853788812426,-1.65306157129174E-48));
#45716=DIRECTION('ref_axis',(-0.982853788812426,-0.184386631340398,3.00112067034686E-65));
#45717=DIRECTION('center_axis',(-0.670755141630903,-0.741678865800898,3.95502882331426E-49));
#45718=DIRECTION('ref_axis',(0.741678865800898,-0.670755141630903,1.84878394507284E-65));
#45719=DIRECTION('',(-1.12975568624751E-48,1.55497530110059E-48,1.));
#45720=DIRECTION('center_axis',(-1.12975568624751E-48,1.55497530110059E-48,
1.));
#45721=DIRECTION('ref_axis',(4.33680868994202E-19,-1.,1.55497530110059E-48));
#45722=DIRECTION('',(-1.12975568624751E-48,1.55497530110059E-48,1.));
#45723=DIRECTION('center_axis',(-0.106704409388993,0.994290786951657,-1.66664752907659E-48));
#45724=DIRECTION('ref_axis',(-0.994290786951658,-0.106704409388993,-2.84767254643969E-65));
#45725=DIRECTION('center_axis',(-0.726878880513659,-0.686765675513279,3.30271754722836E-49));
#45726=DIRECTION('ref_axis',(0.686765675513279,-0.726878880513659,1.35737227185702E-66));
#45727=DIRECTION('',(-1.09747227149895E-48,1.64248332589092E-48,1.));
#45728=DIRECTION('center_axis',(-1.09747227149895E-48,1.64248332589092E-48,
1.));
#45729=DIRECTION('ref_axis',(4.33680868994202E-19,-1.,1.64248332589092E-48));
#45730=DIRECTION('',(-1.09747227149895E-48,1.64248332589092E-48,1.));
#45731=DIRECTION('center_axis',(-0.0283643192708891,0.999597651754094,-1.67295152950556E-48));
#45732=DIRECTION('ref_axis',(-0.999597651754094,-0.0283643192708891,-1.01926051780483E-65));
#45733=DIRECTION('center_axis',(-0.778521169386292,-0.627618346463358,2.60010913042463E-49));
#45734=DIRECTION('ref_axis',(0.627618346463358,-0.778521169386292,-1.77736454987801E-64));
#45735=DIRECTION('',(-1.05842257525003E-48,1.72718866511697E-48,1.));
#45736=DIRECTION('center_axis',(-1.05842257525003E-48,1.72718866511697E-48,
1.));
#45737=DIRECTION('ref_axis',(-0.891006524188322,0.453990499739636,-1.72718866511707E-48));
#45738=DIRECTION('',(-1.05842257525003E-48,1.72718866511697E-48,1.));
#45739=DIRECTION('center_axis',(0.050150646307614,0.998741664633517,-1.67193470631971E-48));
#45740=DIRECTION('ref_axis',(-0.998741664633517,0.050150646307614,1.52017605534737E-65));
#45741=DIRECTION('center_axis',(-0.8253636163651,-0.564601541603213,1.85153538743368E-49));
#45742=DIRECTION('ref_axis',(0.564601541603213,-0.8253636163651,-7.9609822926636E-66));
#45743=DIRECTION('',(-1.01284735186348E-48,1.80856908219503E-48,1.));
#45744=DIRECTION('center_axis',(-1.01284735186348E-48,1.80856908219503E-48,
1.));
#45745=DIRECTION('ref_axis',(-0.852640164354107,0.522498564715924,-1.808569082195E-48));
#45746=DIRECTION('',(-1.01284735186348E-48,1.80856908219503E-48,1.));
#45747=DIRECTION('center_axis',(0.128356416474848,0.991728103035169,-1.6636033285721E-48));
#45748=DIRECTION('ref_axis',(-0.991728103035169,0.128356416474848,-6.99057875847398E-66));
#45749=DIRECTION('center_axis',(-0.867117422187763,-0.498103780490019,1.06161152430708E-49));
#45750=DIRECTION('ref_axis',(0.498103780490019,-0.867117422187763,1.00088346227585E-65));
#45751=DIRECTION('',(-9.61027587746759E-49,1.88612283979207E-48,1.));
#45752=DIRECTION('center_axis',(-9.61027587746759E-49,1.88612283979207E-48,
1.));
#45753=DIRECTION('ref_axis',(-0.809016994374894,0.587785252292546,-1.88612283979215E-48));
#45754=DIRECTION('',(-9.61027587746759E-49,1.88612283979207E-48,1.));
#45755=DIRECTION('center_axis',(0.205770826651675,0.978600207898551,-1.64800876197701E-48));
#45756=DIRECTION('ref_axis',(-0.978600207898551,0.205770826651675,2.0991990898783E-65));
#45757=DIRECTION('center_axis',(-0.903525160756836,-0.428535043933789,2.35207684337335E-50));
#45758=DIRECTION('ref_axis',(0.428535043933789,-0.903525160756836,-9.18347163738211E-68));
#45759=DIRECTION('',(-9.03282768977482E-49,1.95937179320328E-48,1.));
#45760=DIRECTION('center_axis',(-9.03282768977482E-49,1.95937179320328E-48,
1.));
#45761=DIRECTION('ref_axis',(-0.760405965599999,0.649448048330221,-1.95937179320332E-48));
#45762=DIRECTION('',(-9.03282768977482E-49,1.95937179320328E-48,1.));
#45763=DIRECTION('center_axis',(0.281916591256451,0.959438917062646,-1.62524715222323E-48));
#45764=DIRECTION('ref_axis',(-0.959438917062646,0.281916591256451,8.99283719863503E-66));
#45765=DIRECTION('center_axis',(-0.934362366257238,-0.356324246329344,-6.22581077994971E-50));
#45766=DIRECTION('ref_axis',(0.356324246329344,-0.934362366257238,-2.14283631075808E-67));
#45767=DIRECTION('',(-8.39968911565457E-49,2.02786433827311E-48,1.));
#45768=DIRECTION('center_axis',(-8.39968911565457E-49,2.02786433827311E-48,
1.));
#45769=DIRECTION('ref_axis',(-0.707106781186559,0.707106781186536,-2.02786433827309E-48));
#45770=DIRECTION('',(-8.39968911565457E-49,2.02786433827311E-48,1.));
#45771=DIRECTION('center_axis',(0.356324246329351,0.934362366257235,-1.59545883220388E-48));
#45772=DIRECTION('ref_axis',(-0.934362366257235,0.356324246329351,6.60900149289003E-65));
#45773=DIRECTION('center_axis',(-0.959438917062648,-0.281916591256444,-1.50646620972636E-49));
#45774=DIRECTION('ref_axis',(0.281916591256444,-0.959438917062648,3.84808191287826E-66));
#45775=DIRECTION('',(-7.71476366495624E-49,2.09117819568513E-48,1.));
#45776=DIRECTION('center_axis',(-7.71476366495624E-49,2.09117819568513E-48,
1.));
#45777=DIRECTION('ref_axis',(-0.649448048330135,0.760405965600073,-2.09117819568518E-48));
#45778=DIRECTION('',(-7.71476366495624E-49,2.09117819568513E-48,1.));
#45779=DIRECTION('center_axis',(0.428535043933796,0.903525160756832,-1.5588274568175E-48));
#45780=DIRECTION('ref_axis',(-0.903525160756832,0.428535043933796,-3.10862492143316E-66));
#45781=DIRECTION('center_axis',(-0.978600207898552,-0.205770826651667,-2.41099826509806E-49));
#45782=DIRECTION('ref_axis',(0.205770826651667,-0.978600207898552,1.22158844253494E-66));
#45783=DIRECTION('',(-6.98227413084421E-49,2.14892301445441E-48,1.));
#45784=DIRECTION('center_axis',(-6.98227413084421E-49,2.14892301445441E-48,
1.));
#45785=DIRECTION('ref_axis',(-0.587785252292501,0.809016994374927,-2.14892301445438E-48));
#45786=DIRECTION('',(-6.98227413084421E-49,2.14892301445441E-48,1.));
#45787=DIRECTION('center_axis',(0.498103780490025,0.867117422187759,-1.51557887067454E-48));
#45788=DIRECTION('ref_axis',(-0.867117422187759,0.498103780490025,2.99504754920617E-65));
#45789=DIRECTION('center_axis',(-0.99172810303517,-0.128356416474841,-3.33060050320128E-49));
#45790=DIRECTION('ref_axis',(0.128356416474841,-0.99172810303517,-3.10963647347836E-66));
#45791=DIRECTION('',(-6.20673655487377E-49,2.20074277857113E-48,1.));
#45792=DIRECTION('center_axis',(-6.20673655487377E-49,2.20074277857113E-48,
1.));
#45793=DIRECTION('ref_axis',(-0.522498564715884,0.852640164354132,-2.20074277857117E-48));
#45794=DIRECTION('',(-6.20673655487377E-49,2.20074277857113E-48,1.));
#45795=DIRECTION('center_axis',(0.564601541603219,0.825363616365096,-1.46597971569015E-48));
#45796=DIRECTION('ref_axis',(-0.825363616365096,0.564601541603219,-1.28895308917342E-64));
#45797=DIRECTION('center_axis',(-0.998741664633517,-0.0501506463076061,
-4.25960327043935E-49));
#45798=DIRECTION('ref_axis',(0.0501506463076061,-0.998741664633517,-2.80568036684895E-66));
#45799=DIRECTION('',(-5.39293238409318E-49,2.24631800195768E-48,1.));
#45800=DIRECTION('center_axis',(-5.39293238409318E-49,2.24631800195768E-48,
1.));
#45801=DIRECTION('ref_axis',(-0.453990499739489,0.891006524188397,-2.24631800195771E-48));
#45802=DIRECTION('',(-5.39293238409318E-49,2.24631800195768E-48,1.));
#45803=DIRECTION('center_axis',(0.627618346463364,0.778521169386287,-1.41033578714823E-48));
#45804=DIRECTION('ref_axis',(-0.778521169386288,0.627618346463364,5.07659402759256E-65));
#45805=DIRECTION('center_axis',(-0.999597651754094,0.0283643192708965,-5.19227895582746E-49));
#45806=DIRECTION('ref_axis',(-0.0283643192708965,-0.999597651754094,2.50391620144835E-67));
#45807=DIRECTION('',(-4.54587899183267E-49,2.2853676982066E-48,1.));
#45808=DIRECTION('center_axis',(-4.54587899183267E-49,2.2853676982066E-48,
1.));
#45809=DIRECTION('ref_axis',(-0.382683432365006,0.923879532511321,-2.28536769820664E-48));
#45810=DIRECTION('',(-4.54587899183267E-49,2.2853676982066E-48,1.));
#45811=DIRECTION('center_axis',(0.686765675513284,0.726878880513654,-1.34899014837172E-48));
#45812=DIRECTION('ref_axis',(-0.726878880513654,0.686765675513284,4.51664321804638E-65));
#45813=DIRECTION('center_axis',(-0.994290786951657,0.106704409389001,-6.12287730361908E-49));
#45814=DIRECTION('ref_axis',(-0.106704409389001,-0.994290786951657,-3.36897451344462E-66));
#45815=DIRECTION('',(-3.67079874392934E-49,2.31765111295516E-48,1.));
#45816=DIRECTION('center_axis',(-3.67079874392934E-49,2.31765111295516E-48,
1.));
#45817=DIRECTION('ref_axis',(-0.309016994374936,0.951056516295157,-2.31765111295516E-48));
#45818=DIRECTION('',(-3.67079874392934E-49,2.31765111295516E-48,1.));
#45819=DIRECTION('center_axis',(0.741678865800904,0.670755141630897,-1.28232101562316E-48));
#45820=DIRECTION('ref_axis',(-0.670755141630897,0.741678865800904,-7.13448931820408E-65));
#45821=DIRECTION('center_axis',(-0.982853788812424,0.184386631340406,-7.04566086554469E-49));
#45822=DIRECTION('ref_axis',(-0.184386631340406,-0.982853788812424,1.03257498418151E-65));
#45823=DIRECTION('',(-2.77308680110524E-49,2.34296920821612E-48,1.));
#45824=DIRECTION('center_axis',(-2.77308680110524E-49,2.34296920821612E-48,
1.));
#45825=DIRECTION('ref_axis',(-0.233445363855831,0.972369920397695,-2.34296920821614E-48));
#45826=DIRECTION('',(-2.77308680110524E-49,2.34296920821612E-48,1.));
#45827=DIRECTION('center_axis',(0.79201935924761,0.610495974251268,-1.21073942627568E-48));
#45828=DIRECTION('ref_axis',(-0.610495974251268,0.79201935924761,-4.36775682720849E-65));
#45829=DIRECTION('center_axis',(-0.965357170233113,0.260932048394819,-7.95494037408836E-49));
#45830=DIRECTION('ref_axis',(-0.260932048394819,-0.965357170233113,-3.47978634051958E-65));
#45831=DIRECTION('',(-1.85827785600739E-49,2.36116588951307E-48,1.));
#45832=DIRECTION('center_axis',(-1.85827785600739E-49,2.36116588951307E-48,
1.));
#45833=DIRECTION('ref_axis',(-0.156434465040246,0.987688340595135,-2.36116588951307E-48));
#45834=DIRECTION('',(-1.85827785600739E-49,2.36116588951307E-48,1.));
#45835=DIRECTION('center_axis',(0.837476789971392,0.546472896179868,-1.13468670463092E-48));
#45836=DIRECTION('ref_axis',(-0.546472896179868,0.837476789971392,7.35185048458512E-65));
#45837=DIRECTION('center_axis',(-0.94190880368548,0.335868732602169,-8.84510981871381E-49));
#45838=DIRECTION('ref_axis',(-0.335868732602169,-0.94190880368548,-2.80378683690505E-64));
#45839=DIRECTION('',(-9.32012009987159E-50,2.3721289682548E-48,1.));
#45840=DIRECTION('center_axis',(-9.32012009987159E-50,2.3721289682548E-48,
1.));
#45841=DIRECTION('ref_axis',(-0.0784590957277844,0.996917333733133,-2.3721289682548E-48));
#45842=DIRECTION('',(-9.32012009987159E-50,2.3721289682548E-48,1.));
#45843=DIRECTION('center_axis',(0.877770897795708,0.47908063098284,-1.0546317410079E-48));
#45844=DIRECTION('ref_axis',(-0.47908063098284,0.877770897795708,-1.46432166581228E-64));
#45845=DIRECTION('center_axis',(-0.912653256146669,0.408734674385332,-9.71068100878346E-49));
#45846=DIRECTION('ref_axis',(-0.408734674385332,-0.912653256146669,4.78015562106795E-65));
#45847=DIRECTION('',(-1.03033504185762E-66,2.37579085341529E-48,1.));
#45848=DIRECTION('center_axis',(-1.03033504185762E-66,2.37579085341529E-48,
1.));
#45849=DIRECTION('ref_axis',(-5.51899603821915E-14,1.,-2.37579085341529E-48));
#45850=DIRECTION('',(-1.03033504185762E-66,2.37579085341529E-48,1.));
#45851=DIRECTION('center_axis',(0.912653256146668,0.408734674385334,-9.71068100878352E-49));
#45852=DIRECTION('ref_axis',(-0.408734674385334,0.912653256146668,-3.97320112854764E-64));
#45853=DIRECTION('center_axis',(-0.877770897795703,0.47908063098285,-1.05463174100791E-48));
#45854=DIRECTION('ref_axis',(-0.47908063098285,-0.877770897795703,8.5181126283276E-66));
#45855=DIRECTION('',(9.32012009987329E-50,2.3721289682548E-48,1.));
#45856=DIRECTION('center_axis',(9.32012009987329E-50,2.3721289682548E-48,
1.));
#45857=DIRECTION('ref_axis',(0.078459095727909,0.996917333733123,-2.37212896825479E-48));
#45858=DIRECTION('',(9.32012009987329E-50,2.3721289682548E-48,1.));
#45859=DIRECTION('center_axis',(0.941908803685484,0.335868732602158,-8.84510981871371E-49));
#45860=DIRECTION('ref_axis',(-0.335868732602158,0.941908803685484,-1.44601818635795E-65));
#45861=DIRECTION('center_axis',(-0.837476789971386,0.546472896179877,-1.13468670463093E-48));
#45862=DIRECTION('ref_axis',(-0.546472896179877,-0.837476789971386,1.1507371701338E-64));
#45863=DIRECTION('',(1.85827785600756E-49,2.36116588951307E-48,1.));
#45864=DIRECTION('center_axis',(1.85827785600756E-49,2.36116588951307E-48,
1.));
#45865=DIRECTION('ref_axis',(0.156434465040226,0.987688340595138,-2.36116588951307E-48));
#45866=DIRECTION('',(1.85827785600756E-49,2.36116588951307E-48,1.));
#45867=DIRECTION('center_axis',(0.965357170233116,0.260932048394809,-7.95494037408827E-49));
#45868=DIRECTION('ref_axis',(-0.260932048394809,0.965357170233116,-4.20694512990981E-65));
#45869=DIRECTION('center_axis',(-0.792019359247603,0.610495974251277,-1.21073942627569E-48));
#45870=DIRECTION('ref_axis',(-0.610495974251277,-0.792019359247603,-2.13945998802071E-65));
#45871=DIRECTION('',(2.7730868011054E-49,2.34296920821612E-48,1.));
#45872=DIRECTION('center_axis',(2.7730868011054E-49,2.34296920821612E-48,
1.));
#45873=DIRECTION('ref_axis',(0.233445363855898,0.972369920397678,-2.34296920821612E-48));
#45874=DIRECTION('',(2.7730868011054E-49,2.34296920821612E-48,1.));
#45875=DIRECTION('center_axis',(0.982853788812426,0.184386631340395,-7.04566086554459E-49));
#45876=DIRECTION('ref_axis',(-0.184386631340395,0.982853788812426,-1.76256118611904E-65));
#45877=DIRECTION('center_axis',(-0.741678865800896,0.670755141630906,-1.28232101562316E-48));
#45878=DIRECTION('ref_axis',(-0.670755141630906,-0.741678865800896,1.75561258236883E-65));
#45879=DIRECTION('',(3.6707987439295E-49,2.31765111295516E-48,1.));
#45880=DIRECTION('center_axis',(3.6707987439295E-49,2.31765111295516E-48,
1.));
#45881=DIRECTION('ref_axis',(0.309016994374949,0.951056516295153,-2.31765111295516E-48));
#45882=DIRECTION('',(3.6707987439295E-49,2.31765111295516E-48,1.));
#45883=DIRECTION('center_axis',(0.994290786951658,0.10670440938899,-6.12287730361897E-49));
#45884=DIRECTION('ref_axis',(-0.10670440938899,0.994290786951658,-7.83421067979577E-66));
#45885=DIRECTION('center_axis',(-0.686765675513276,0.726878880513661,-1.34899014837172E-48));
#45886=DIRECTION('ref_axis',(-0.726878880513661,-0.686765675513276,5.3563970103269E-65));
#45887=DIRECTION('',(4.54587899183282E-49,2.28536769820659E-48,1.));
#45888=DIRECTION('center_axis',(4.54587899183282E-49,2.28536769820659E-48,
1.));
#45889=DIRECTION('ref_axis',(0.382683432365024,0.923879532511314,-2.28536769820663E-48));
#45890=DIRECTION('',(4.54587899183282E-49,2.28536769820659E-48,1.));
#45891=DIRECTION('center_axis',(0.999597651754094,0.0283643192708856,-5.19227895582736E-49));
#45892=DIRECTION('ref_axis',(-0.0283643192708856,0.999597651754094,1.94568536261846E-66));
#45893=DIRECTION('center_axis',(-0.627618346463355,0.778521169386295,-1.41033578714824E-48));
#45894=DIRECTION('ref_axis',(-0.778521169386295,-0.627618346463355,-4.32781502974933E-65));
#45895=DIRECTION('',(5.39293238409334E-49,2.24631800195767E-48,1.));
#45896=DIRECTION('center_axis',(5.39293238409334E-49,2.24631800195767E-48,
1.));
#45897=DIRECTION('ref_axis',(0.45399049973962,0.89100652418833,-2.24631800195763E-48));
#45898=DIRECTION('',(5.39293238409334E-49,2.24631800195767E-48,1.));
#45899=DIRECTION('center_axis',(0.998741664633517,-0.0501506463076175,-4.25960327043925E-49));
#45900=DIRECTION('ref_axis',(0.0501506463076175,0.998741664633517,-4.14088422014228E-66));
#45901=DIRECTION('center_axis',(-0.56460154160321,0.825363616365102,-1.46597971569016E-48));
#45902=DIRECTION('ref_axis',(-0.825363616365102,-0.56460154160321,7.97777118454868E-65));
#45903=DIRECTION('',(6.20673655487391E-49,2.20074277857112E-48,1.));
#45904=DIRECTION('center_axis',(6.20673655487391E-49,2.20074277857112E-48,
1.));
#45905=DIRECTION('ref_axis',(0.522498564715976,0.852640164354076,-2.20074277857111E-48));
#45906=DIRECTION('',(6.20673655487391E-49,2.20074277857112E-48,1.));
#45907=DIRECTION('center_axis',(0.991728103035169,-0.128356416474851,-3.33060050320119E-49));
#45908=DIRECTION('ref_axis',(0.128356416474851,0.991728103035169,2.08257490756294E-67));
#45909=DIRECTION('center_axis',(-0.498103780490015,0.867117422187765,-1.51557887067454E-48));
#45910=DIRECTION('ref_axis',(-0.867117422187765,-0.498103780490015,2.18779707200991E-65));
#45911=DIRECTION('',(6.98227413084436E-49,2.1489230144544E-48,1.));
#45912=DIRECTION('center_axis',(6.98227413084435E-49,2.1489230144544E-48,
1.));
#45913=DIRECTION('ref_axis',(0.587785252292489,0.809016994374936,-2.14892301445439E-48));
#45914=DIRECTION('',(6.98227413084436E-49,2.1489230144544E-48,1.));
#45915=DIRECTION('center_axis',(0.97860020789855,-0.205770826651679,-2.41099826509796E-49));
#45916=DIRECTION('ref_axis',(0.205770826651679,0.97860020789855,-2.74077973100627E-66));
#45917=DIRECTION('center_axis',(-0.428535043933785,0.903525160756837,-1.55882745681751E-48));
#45918=DIRECTION('ref_axis',(-0.903525160756837,-0.428535043933785,-8.73188639847288E-65));
#45919=DIRECTION('',(7.71476366495637E-49,2.09117819568512E-48,1.));
#45920=DIRECTION('center_axis',(7.71476366495637E-49,2.09117819568512E-48,
1.));
#45921=DIRECTION('ref_axis',(0.649448048330186,0.760405965600029,-2.09117819568512E-48));
#45922=DIRECTION('',(7.71476366495637E-49,2.09117819568512E-48,1.));
#45923=DIRECTION('center_axis',(0.959438917062645,-0.281916591256455,-1.50646620972626E-49));
#45924=DIRECTION('ref_axis',(0.281916591256455,0.959438917062645,-2.91844467010393E-67));
#45925=DIRECTION('center_axis',(-0.356324246329341,0.934362366257239,-1.59545883220388E-48));
#45926=DIRECTION('ref_axis',(-0.934362366257239,-0.356324246329341,1.49301625507406E-64));
#45927=DIRECTION('',(8.39968911565469E-49,2.0278643382731E-48,1.));
#45928=DIRECTION('center_axis',(8.39968911565469E-49,2.0278643382731E-48,
1.));
#45929=DIRECTION('ref_axis',(0.707106781186573,0.707106781186522,-2.02786433827308E-48));
#45930=DIRECTION('',(8.39968911565469E-49,2.0278643382731E-48,1.));
#45931=DIRECTION('center_axis',(0.934362366257234,-0.356324246329355,-6.22581077994883E-50));
#45932=DIRECTION('ref_axis',(0.356324246329355,0.934362366257234,-4.97582464336991E-66));
#45933=DIRECTION('center_axis',(-0.28191659125644,0.959438917062649,-1.62524715222323E-48));
#45934=DIRECTION('ref_axis',(-0.959438917062649,-0.28191659125644,-5.29515836320384E-66));
#45935=DIRECTION('',(9.03282768977493E-49,1.95937179320326E-48,1.));
#45936=DIRECTION('center_axis',(9.03282768977493E-49,1.95937179320326E-48,
1.));
#45937=DIRECTION('ref_axis',(0.760405965600079,0.649448048330127,-1.9593717932032E-48));
#45938=DIRECTION('',(9.03282768977493E-49,1.95937179320326E-48,1.));
#45939=DIRECTION('center_axis',(0.903525160756831,-0.428535043933799,2.35207684337425E-50));
#45940=DIRECTION('ref_axis',(0.428535043933799,0.903525160756831,3.46790681006673E-67));
#45941=DIRECTION('center_axis',(-0.205770826651664,0.978600207898553,-1.64800876197701E-48));
#45942=DIRECTION('ref_axis',(-0.978600207898553,-0.205770826651664,-5.70930081633759E-65));
#45943=DIRECTION('',(9.61027587746769E-49,1.88612283979206E-48,1.));
#45944=DIRECTION('center_axis',(9.61027587746769E-49,1.88612283979206E-48,
1.));
#45945=DIRECTION('ref_axis',(0.809016994374978,0.587785252292432,-1.88612283979202E-48));
#45946=DIRECTION('',(9.61027587746769E-49,1.88612283979206E-48,1.));
#45947=DIRECTION('center_axis',(0.867117422187757,-0.498103780490029,1.06161152430717E-49));
#45948=DIRECTION('ref_axis',(0.498103780490029,0.867117422187757,8.6756046158998E-66));
#45949=DIRECTION('center_axis',(-0.128356416474837,0.991728103035171,-1.6636033285721E-48));
#45950=DIRECTION('ref_axis',(-0.991728103035171,-0.128356416474837,3.98742758462882E-65));
#45951=DIRECTION('',(1.01284735186348E-48,1.80856908219502E-48,1.));
#45952=DIRECTION('center_axis',(1.01284735186348E-48,1.80856908219502E-48,
1.));
#45953=DIRECTION('ref_axis',(0.852640164354111,0.522498564715918,-1.80856908219499E-48));
#45954=DIRECTION('',(1.01284735186348E-48,1.80856908219502E-48,1.));
#45955=DIRECTION('center_axis',(0.825363616365094,-0.564601541603222,1.85153538743376E-49));
#45956=DIRECTION('ref_axis',(0.564601541603222,0.825363616365094,-1.20460226317478E-65));
#45957=DIRECTION('center_axis',(-0.0501506463076026,0.998741664633518,-1.67193470631971E-48));
#45958=DIRECTION('ref_axis',(-0.998741664633518,-0.0501506463076026,9.17993822873344E-66));
#45959=DIRECTION('',(1.05842257525004E-48,1.72718866511696E-48,1.));
#45960=DIRECTION('center_axis',(1.05842257525004E-48,1.72718866511696E-48,
1.));
#45961=DIRECTION('ref_axis',(0.891006524188331,0.453990499739619,-1.72718866511705E-48));
#45962=DIRECTION('',(1.05842257525004E-48,1.72718866511696E-48,1.));
#45963=DIRECTION('center_axis',(0.778521169386285,-0.627618346463367,2.6001091304247E-49));
#45964=DIRECTION('ref_axis',(0.627618346463367,0.778521169386285,-2.38387219843189E-65));
#45965=DIRECTION('center_axis',(0.0283643192709005,0.999597651754094,-1.67295152950556E-48));
#45966=DIRECTION('ref_axis',(-0.999597651754094,0.0283643192709005,5.71503284305285E-66));
#45967=DIRECTION('',(1.09747227149896E-48,1.6424833258909E-48,1.));
#45968=DIRECTION('center_axis',(1.09747227149896E-48,1.6424833258909E-48,
1.));
#45969=DIRECTION('ref_axis',(4.33680868994202E-19,-1.,1.6424833258909E-48));
#45970=DIRECTION('',(1.09747227149896E-48,1.6424833258909E-48,1.));
#45971=DIRECTION('center_axis',(0.726878880513651,-0.686765675513287,3.30271754722842E-49));
#45972=DIRECTION('ref_axis',(0.686765675513287,0.726878880513651,-2.02185804836064E-65));
#45973=DIRECTION('center_axis',(0.106704409389004,0.994290786951656,-1.66664752907659E-48));
#45974=DIRECTION('ref_axis',(-0.994290786951656,0.106704409389004,-7.60908949083185E-66));
#45975=DIRECTION('',(1.12975568624752E-48,1.55497530110057E-48,1.));
#45976=DIRECTION('center_axis',(1.12975568624752E-48,1.55497530110057E-48,
1.));
#45977=DIRECTION('ref_axis',(4.33680868994202E-19,-1.,1.55497530110057E-48));
#45978=DIRECTION('',(1.12975568624752E-48,1.55497530110057E-48,1.));
#45979=DIRECTION('center_axis',(0.670755141630895,-0.741678865800906,3.95502882331431E-49));
#45980=DIRECTION('ref_axis',(0.741678865800906,0.670755141630895,-5.99583083400171E-67));
#45981=DIRECTION('center_axis',(0.184386631340409,0.982853788812424,-1.65306157129173E-48));
#45982=DIRECTION('ref_axis',(-0.982853788812424,0.184386631340409,2.90870213757036E-65));
#45983=DIRECTION('',(1.15507378150848E-48,1.46520410681816E-48,1.));
#45984=DIRECTION('center_axis',(1.15507378150848E-48,1.46520410681816E-48,
1.));
#45985=DIRECTION('ref_axis',(4.33680868994202E-19,-1.,1.46520410681816E-48));
#45986=DIRECTION('',(1.15507378150848E-48,1.46520410681816E-48,1.));
#45987=DIRECTION('center_axis',(0.610495974251266,-0.792019359247612,4.5530212427498E-49));
#45988=DIRECTION('ref_axis',(0.792019359247612,0.610495974251266,2.91962028883906E-65));
#45989=DIRECTION('center_axis',(0.260932048394823,0.965357170233112,-1.63227741809852E-48));
#45990=DIRECTION('ref_axis',(-0.965357170233112,0.260932048394823,3.06323067308603E-65));
#45991=DIRECTION('',(1.17327046280543E-48,1.37372321230838E-48,1.));
#45992=DIRECTION('center_axis',(1.17327046280543E-48,1.37372321230838E-48,
1.));
#45993=DIRECTION('ref_axis',(4.33680868994202E-19,-1.,1.37372321230838E-48));
#45994=DIRECTION('',(1.17327046280543E-48,1.37372321230838E-48,1.));
#45995=DIRECTION('center_axis',(0.546472896179865,-0.837476789971394,5.0930079834164E-49));
#45996=DIRECTION('ref_axis',(0.837476789971394,0.546472896179865,-4.56422939014991E-65));
#45997=DIRECTION('center_axis',(0.335868732602171,0.94190880368548,-1.60442321071282E-48));
#45998=DIRECTION('ref_axis',(-0.94190880368548,0.335868732602171,4.87630450545203E-65));
#45999=DIRECTION('',(1.18423354154716E-48,1.28109662770635E-48,1.));
#46000=DIRECTION('center_axis',(1.18423354154716E-48,1.28109662770635E-48,
1.));
#46001=DIRECTION('ref_axis',(4.33680868994202E-19,-1.,1.28109662770635E-48));
#46002=DIRECTION('',(1.18423354154716E-48,1.28109662770635E-48,1.));
#46003=DIRECTION('center_axis',(0.479080630982838,-0.87777089779571,5.57165984749409E-49));
#46004=DIRECTION('ref_axis',(0.87777089779571,0.479080630982838,-3.73128804317402E-67));
#46005=DIRECTION('center_axis',(0.408734674385341,0.912653256146664,-1.56967067958563E-48));
#46006=DIRECTION('ref_axis',(-0.912653256146664,0.408734674385341,1.45818743306131E-64));
#46007=DIRECTION('center_axis',(0.408734674385325,-0.912653256146672,5.98602578707294E-49));
#46008=DIRECTION('ref_axis',(0.912653256146672,0.408734674385325,1.90174553100142E-65));
#46009=DIRECTION('center_axis',(0.479080630982853,0.877770897795701,-1.52823408562775E-48));
#46010=DIRECTION('ref_axis',(-0.877770897795701,0.479080630982853,5.61428358120402E-65));
#46011=DIRECTION('center_axis',(0.335868732602155,-0.941908803685485,6.33355109834479E-49));
#46012=DIRECTION('ref_axis',(0.941908803685485,0.335868732602155,-2.18452554190007E-64));
#46013=DIRECTION('center_axis',(0.54647289617988,0.837476789971384,-1.48036889921998E-48));
#46014=DIRECTION('ref_axis',(-0.837476789971384,0.54647289617988,1.0038841655118E-64));
#46015=DIRECTION('center_axis',(0.260932048394805,-0.965357170233117,6.61209317220175E-49));
#46016=DIRECTION('ref_axis',(0.965357170233117,0.260932048394805,-1.34731391844263E-65));
#46017=DIRECTION('center_axis',(0.61049597425128,0.792019359247601,-1.42637022515332E-48));
#46018=DIRECTION('ref_axis',(-0.792019359247601,0.61049597425128,4.68595517840464E-65));
#46019=DIRECTION('center_axis',(0.184386631340391,-0.982853788812427,6.81993470413385E-49));
#46020=DIRECTION('ref_axis',(0.982853788812427,0.184386631340391,-4.82159387328582E-66));
#46021=DIRECTION('center_axis',(0.670755141630908,0.741678865800894,-1.36657098320977E-48));
#46022=DIRECTION('ref_axis',(-0.741678865800894,0.670755141630908,-1.20021806126158E-65));
#46023=DIRECTION('center_axis',(0.106704409388986,-0.994290786951658,6.95579428198241E-49));
#46024=DIRECTION('ref_axis',(0.994290786951658,0.106704409388986,-5.2899598259714E-66));
#46025=DIRECTION('center_axis',(0.726878880513664,0.686765675513273,-1.30133985560118E-48));
#46026=DIRECTION('ref_axis',(-0.686765675513273,0.726878880513664,8.56568901676031E-65));
#46027=DIRECTION('center_axis',(0.0283643192708817,-0.999597651754094,7.01883428627211E-49));
#46028=DIRECTION('ref_axis',(0.999597651754094,0.0283643192708817,4.29698701010715E-68));
#65620=CARTESIAN_POINT('',(0.,0.,0.));
#65621=CARTESIAN_POINT('Origin',(30.,-1.32966554433622E-14,16.));
#65622=CARTESIAN_POINT('',(29.9999999999999,-1.50000000000001,30.25));
#65623=CARTESIAN_POINT('',(30.,-1.50000000000001,30.3125));
#65624=CARTESIAN_POINT('',(30.,-1.50000000000001,16.));
#65625=CARTESIAN_POINT('',(30.,-1.50000000000002,30.75));
#65626=CARTESIAN_POINT('Ctrl Pts',(29.9999999999999,-1.50000000000001,30.25));
#65627=CARTESIAN_POINT('Ctrl Pts',(30.1658036138247,-1.50000000000003,30.2579772300895));
#65628=CARTESIAN_POINT('Ctrl Pts',(30.3306771390814,-1.47251502213024,30.2666731828795));
#65629=CARTESIAN_POINT('Ctrl Pts',(30.6740051197163,-1.35441705513551,30.2864720571327));
#65630=CARTESIAN_POINT('Ctrl Pts',(30.8456956760641,-1.25440329321601,30.2975106829297));
#65631=CARTESIAN_POINT('Ctrl Pts',(31.1355371924707,-0.998320157723232,
30.31856910982));
#65632=CARTESIAN_POINT('Ctrl Pts',(31.2526807741055,-0.846671576374736,
30.3279626902015));
#65633=CARTESIAN_POINT('Ctrl Pts',(31.4282014939959,-0.499786966349004,
30.3472340574251));
#65634=CARTESIAN_POINT('Ctrl Pts',(31.4817951924464,-0.306278304449559,
30.3579845386417));
#65635=CARTESIAN_POINT('Ctrl Pts',(31.5101111597472,0.0860175204635018,
30.3797787511369));
#65636=CARTESIAN_POINT('Ctrl Pts',(31.4862462216493,0.280921846793951,30.3906067692664));
#65637=CARTESIAN_POINT('Ctrl Pts',(31.3664146176937,0.647698903970874,30.4109832724428));
#65638=CARTESIAN_POINT('Ctrl Pts',(31.2727727808063,0.816486916731949,30.4197772164968));
#65639=CARTESIAN_POINT('Ctrl Pts',(31.0215777110749,1.11639419547156,30.440193602667));
#65640=CARTESIAN_POINT('Ctrl Pts',(30.8638920671928,1.2424306705166,30.4512812699412));
#65641=CARTESIAN_POINT('Ctrl Pts',(30.51519869364,1.4218077371841,30.4730404839947));
#65642=CARTESIAN_POINT('Ctrl Pts',(30.3288784064271,1.47608428096084,30.4835125047644));
#65643=CARTESIAN_POINT('Ctrl Pts',(29.9417076474062,1.51169090841865,30.5031293395779));
#65644=CARTESIAN_POINT('Ctrl Pts',(29.7444133180912,1.49107258678014,30.5125449036674));
#65645=CARTESIAN_POINT('Ctrl Pts',(29.3680874803138,1.37464650826943,30.5338849467157));
#65646=CARTESIAN_POINT('Ctrl Pts',(29.192868275455,1.27964935682832,30.5449539944024));
#65647=CARTESIAN_POINT('Ctrl Pts',(28.8948089362382,1.03185947909864,30.5661774332058));
#65648=CARTESIAN_POINT('Ctrl Pts',(28.7730426891403,0.883581363472215,30.5759121464738));
#65649=CARTESIAN_POINT('Ctrl Pts',(28.5872420086988,0.541893735862482,30.5948947924521));
#65650=CARTESIAN_POINT('Ctrl Pts',(28.5279457886126,0.350092848014275,30.6055503973326));
#65651=CARTESIAN_POINT('Ctrl Pts',(28.4879441501424,-0.0417086531130522,
30.6273171473952));
#65652=CARTESIAN_POINT('Ctrl Pts',(28.5061747163527,-0.237794814766365,
30.6382108230426));
#65653=CARTESIAN_POINT('Ctrl Pts',(28.6154381406337,-0.60772707143957,30.65876261508));
#65654=CARTESIAN_POINT('Ctrl Pts',(28.7037802077497,-0.77855877037785,30.6675955620118));
#65655=CARTESIAN_POINT('Ctrl Pts',(28.9458348287961,-1.08578773838532,30.687775558397));
#65656=CARTESIAN_POINT('Ctrl Pts',(29.1002278810903,-1.21679626071423,30.6988429232091));
#65657=CARTESIAN_POINT('Ctrl Pts',(29.3881527190005,-1.37554036843891,30.7171052719799));
#65658=CARTESIAN_POINT('Ctrl Pts',(29.5080276522,-1.42282651307167,30.7241862614101));
#65659=CARTESIAN_POINT('Ctrl Pts',(29.7526687702711,-1.48465507368766,30.7376740227083));
#65660=CARTESIAN_POINT('Ctrl Pts',(29.8761199631302,-1.50000000000009,30.7440398189472));
#65661=CARTESIAN_POINT('Ctrl Pts',(30.0000000000009,-1.50000000000001,30.75));
#65662=CARTESIAN_POINT('',(30.,-1.50000000000001,30.85));
#65663=CARTESIAN_POINT('',(30.,-1.50000000000001,16.));
#65664=CARTESIAN_POINT('Origin',(30.,-1.32966554433622E-14,30.85));
#65665=CARTESIAN_POINT('',(28.9490560961666,-1.07028823734334,30.75));
#65666=CARTESIAN_POINT('Origin',(30.,-1.5916987375435E-14,30.75));
#65667=CARTESIAN_POINT('Ctrl Pts',(28.9490560961666,-1.07028823734332,30.75));
#65668=CARTESIAN_POINT('Ctrl Pts',(28.8761609488349,-0.998710593084209,
30.7445045626927));
#65669=CARTESIAN_POINT('Ctrl Pts',(28.8107674297946,-0.919873442584925,
30.7391683946938));
#65670=CARTESIAN_POINT('Ctrl Pts',(28.6983154051604,-0.752052754529888,
30.7290963583567));
#65671=CARTESIAN_POINT('Ctrl Pts',(28.6511686993163,-0.663795554008335,
30.7243775307781));
#65672=CARTESIAN_POINT('Ctrl Pts',(28.5395598759442,-0.392939439769756,
30.709329968876));
#65673=CARTESIAN_POINT('Ctrl Pts',(28.5011631241701,-0.201888114570883,
30.6987160063649));
#65674=CARTESIAN_POINT('Ctrl Pts',(28.4988436150777,0.191908857459164,30.6768383968077));
#65675=CARTESIAN_POINT('Ctrl Pts',(28.5379718270057,0.390884408078152,30.6657841995511));
#65676=CARTESIAN_POINT('Ctrl Pts',(28.6882496652404,0.752033457565058,30.6457203634686));
#65677=CARTESIAN_POINT('Ctrl Pts',(28.7941652988744,0.912256576314666,30.6368419553212));
#65678=CARTESIAN_POINT('Ctrl Pts',(29.0637866570552,1.18813740110581,30.6162064354332));
#65679=CARTESIAN_POINT('Ctrl Pts',(29.2263162356668,1.29983562680085,30.6052839989448));
#65680=CARTESIAN_POINT('Ctrl Pts',(29.5881540142218,1.45598200117754,30.5835376714189));
#65681=CARTESIAN_POINT('Ctrl Pts',(29.7845106480132,1.49769538170803,30.5729317534561));
#65682=CARTESIAN_POINT('Ctrl Pts',(30.1735918421599,1.5020241460186,30.5540918323215));
#65683=CARTESIAN_POINT('Ctrl Pts',(30.3626153088868,1.46791385953203,30.544162381137));
#65684=CARTESIAN_POINT('Ctrl Pts',(30.7246797057952,1.32812661690519,30.5228595707569));
#65685=CARTESIAN_POINT('Ctrl Pts',(30.8932233177541,1.2211620663456,30.5117792749302));
#65686=CARTESIAN_POINT('Ctrl Pts',(31.1776737025205,0.949411483501645,30.4905450221109));
#65687=CARTESIAN_POINT('Ctrl Pts',(31.2913339229655,0.787872571372875,30.4812706984095));
#65688=CARTESIAN_POINT('Ctrl Pts',(31.4489779041399,0.433069950768308,30.4615594417092));
#65689=CARTESIAN_POINT('Ctrl Pts',(31.4925441992832,0.243681023738972,30.451037834652));
#65690=CARTESIAN_POINT('Ctrl Pts',(31.5059639907605,-0.148777135728896,
30.4292346035705));
#65691=CARTESIAN_POINT('Ctrl Pts',(31.4726973264507,-0.348194823891665,
30.418155843117));
#65692=CARTESIAN_POINT('Ctrl Pts',(31.3331360295961,-0.713588890875335,
30.3978561727291));
#65693=CARTESIAN_POINT('Ctrl Pts',(31.2315888806866,-0.877298264710928,
30.3890521180742));
#65694=CARTESIAN_POINT('Ctrl Pts',(30.969887909143,-1.16071911064266,30.3685882229343));
#65695=CARTESIAN_POINT('Ctrl Pts',(30.8111118646049,-1.27673016594729,30.3577265776157));
#65696=CARTESIAN_POINT('Ctrl Pts',(30.4544959445291,-1.44324278722566,30.3359435355702));
#65697=CARTESIAN_POINT('Ctrl Pts',(30.2594138454525,-1.49071962728781,30.3252388425894));
#65698=CARTESIAN_POINT('Ctrl Pts',(30.0404799678322,-1.49959063127059,30.3144589647139));
#65699=CARTESIAN_POINT('Ctrl Pts',(30.0202329450965,-1.50000000000001,30.3134734580248));
#65700=CARTESIAN_POINT('Ctrl Pts',(30.,-1.50000000000001,30.3125));
#65701=CARTESIAN_POINT('Origin',(30.,-1.32966554433622E-14,16.));
#65702=CARTESIAN_POINT('',(30.0000000422953,-1.50000000000001,29.7500000040699));
#65703=CARTESIAN_POINT('',(30.0000000000001,-1.50000000000001,29.8125));
#65704=CARTESIAN_POINT('',(30.,-1.50000000000001,16.));
#65705=CARTESIAN_POINT('Ctrl Pts',(30.0000000423936,-1.50000000000001,29.7500000020397));
#65706=CARTESIAN_POINT('Ctrl Pts',(30.195284159332,-1.49999999448081,29.7593956136499));
#65707=CARTESIAN_POINT('Ctrl Pts',(30.3888046451199,-1.46186371850976,29.7697657133627));
#65708=CARTESIAN_POINT('Ctrl Pts',(30.7506676874449,-1.3133124636612,29.7913022808498));
#65709=CARTESIAN_POINT('Ctrl Pts',(30.9154176613495,-1.20428706546983,29.8022573009481));
#65710=CARTESIAN_POINT('Ctrl Pts',(31.18981388205,-0.933008136594988,29.8229947210741));
#65711=CARTESIAN_POINT('Ctrl Pts',(31.2983679232815,-0.774850228387389,
29.8319527650896));
#65712=CARTESIAN_POINT('Ctrl Pts',(31.4541476549185,-0.418353419581691,
29.8517581433566));
#65713=CARTESIAN_POINT('Ctrl Pts',(31.4967395542031,-0.22207441884915,29.8626625322862));
#65714=CARTESIAN_POINT('Ctrl Pts',(31.5028167108854,0.170195075492689,29.8844552819718));
#65715=CARTESIAN_POINT('Ctrl Pts',(31.4683656451658,0.362410265994727,29.8951339036664));
#65716=CARTESIAN_POINT('Ctrl Pts',(31.3284167977355,0.722950513431523,29.9151639174129));
#65717=CARTESIAN_POINT('Ctrl Pts',(31.2243440361084,0.887881539566768,29.9240904295301));
#65718=CARTESIAN_POINT('Ctrl Pts',(30.9555499935672,1.17320843290826,29.9449485359688));
#65719=CARTESIAN_POINT('Ctrl Pts',(30.7918896841479,1.28933944326239,29.9560485076758));
#65720=CARTESIAN_POINT('Ctrl Pts',(30.4356884609645,1.44801470954154,29.9775938933022));
#65721=CARTESIAN_POINT('Ctrl Pts',(30.24769400318,1.49172420709908,29.9878529335795));
#65722=CARTESIAN_POINT('Ctrl Pts',(29.8564383086953,1.50648133745832,30.007087152245));
#65723=CARTESIAN_POINT('Ctrl Pts',(29.6568006042803,1.4738887523207,30.0172375010609));
#65724=CARTESIAN_POINT('Ctrl Pts',(29.2858871639067,1.33362042993594,30.0389794245699));
#65725=CARTESIAN_POINT('Ctrl Pts',(29.1177424716204,1.22887149382963,30.049978982519));
#65726=CARTESIAN_POINT('Ctrl Pts',(28.8358984689122,0.964859074366596,30.0708728867402));
#65727=CARTESIAN_POINT('Ctrl Pts',(28.7232154667205,0.809870978335536,30.0800071678703));
#65728=CARTESIAN_POINT('Ctrl Pts',(28.5578456280088,0.457982195266601,30.0995565447074));
#65729=CARTESIAN_POINT('Ctrl Pts',(28.5099042682065,0.262965364708001,30.1103908130718));
#65730=CARTESIAN_POINT('Ctrl Pts',(28.4930631778567,-0.129475272168894,
30.1321930706761));
#65731=CARTESIAN_POINT('Ctrl Pts',(28.5224126203679,-0.323064053208287,
30.142948002956));
#65732=CARTESIAN_POINT('Ctrl Pts',(28.6526173206986,-0.686662322858743,
30.1631479068255));
#65733=CARTESIAN_POINT('Ctrl Pts',(28.7515795011674,-0.85345907766542,30.1719758706799));
#65734=CARTESIAN_POINT('Ctrl Pts',(29.0118186458561,-1.14595641051804,30.1926215582791));
#65735=CARTESIAN_POINT('Ctrl Pts',(29.172636650331,-1.26695599442051,30.2037200176798));
#65736=CARTESIAN_POINT('Ctrl Pts',(29.5253217759949,-1.43577307549295,30.2253779520631));
#65737=CARTESIAN_POINT('Ctrl Pts',(29.7125728326969,-1.48464476779679,30.2357446197376));
#65738=CARTESIAN_POINT('Ctrl Pts',(29.9359811243456,-1.49897644179293,30.2468914582366));
#65739=CARTESIAN_POINT('Ctrl Pts',(29.9680065223165,-1.50000000000001,30.2484607130873));
#65740=CARTESIAN_POINT('Ctrl Pts',(29.9999999999999,-1.50000000000001,30.25));
#65741=CARTESIAN_POINT('Ctrl Pts',(30.,-1.50000000000001,30.3125));
#65742=CARTESIAN_POINT('Ctrl Pts',(29.8305649734084,-1.50000000000001,30.3043480534823));
#65743=CARTESIAN_POINT('Ctrl Pts',(29.6621927434306,-1.471296371185,30.2954499177677));
#65744=CARTESIAN_POINT('Ctrl Pts',(29.3161242189391,-1.34950305066004,30.2754165403276));
#65745=CARTESIAN_POINT('Ctrl Pts',(29.1449154106261,-1.2480688680691,30.264361636514));
#65746=CARTESIAN_POINT('Ctrl Pts',(28.8512754656375,-0.984586302069753,
30.242914917907));
#65747=CARTESIAN_POINT('Ctrl Pts',(28.7318299827785,-0.825047829175388,
30.2333359905097));
#65748=CARTESIAN_POINT('Ctrl Pts',(28.5638630976012,-0.47370253085421,30.2138168072696));
#65749=CARTESIAN_POINT('Ctrl Pts',(28.5150825240157,-0.286153024679847,
30.2033973902599));
#65750=CARTESIAN_POINT('Ctrl Pts',(28.4904050702493,0.104624550291977,30.1816875249837));
#65751=CARTESIAN_POINT('Ctrl Pts',(28.5176966903753,0.304322584656878,30.1705931897412));
#65752=CARTESIAN_POINT('Ctrl Pts',(28.6462704703314,0.673930577459572,30.1500594123633));
#65753=CARTESIAN_POINT('Ctrl Pts',(28.7433931121189,0.841252262459088,30.141257075347));
#65754=CARTESIAN_POINT('Ctrl Pts',(28.9970706151381,1.13219704351489,30.1209702113185));
#65755=CARTESIAN_POINT('Ctrl Pts',(29.1519620886259,1.25242080149054,30.1101784429931));
#65756=CARTESIAN_POINT('Ctrl Pts',(29.5030294160994,1.42917820121841,30.0883777805545));
#65757=CARTESIAN_POINT('Ctrl Pts',(29.696654967539,1.48240812812318,30.0775833577866));
#65758=CARTESIAN_POINT('Ctrl Pts',(30.0844620336651,1.50960977413546,30.0581693803401));
#65759=CARTESIAN_POINT('Ctrl Pts',(30.2746950762916,1.48681483093204,30.0489174722834));
#65760=CARTESIAN_POINT('Ctrl Pts',(30.642872277816,1.3694262764412,30.0279427452356));
#65761=CARTESIAN_POINT('Ctrl Pts',(30.8165454300566,1.27352463490858,30.0169229573155));
#65762=CARTESIAN_POINT('Ctrl Pts',(31.1192034235311,1.01839257572982,29.9952743161713));
#65763=CARTESIAN_POINT('Ctrl Pts',(31.2444516003803,0.860842115189833,29.9853245619549));
#65764=CARTESIAN_POINT('Ctrl Pts',(31.4225185229473,0.51295924874081,29.9659977360411));
#65765=CARTESIAN_POINT('Ctrl Pts',(31.476317491186,0.327339595503408,29.9556855330835));
#65766=CARTESIAN_POINT('Ctrl Pts',(31.5118899575654,-0.0614966036299657,
29.9340835220205));
#65767=CARTESIAN_POINT('Ctrl Pts',(31.49041063713,-0.261302093346022,29.9229832170363));
#65768=CARTESIAN_POINT('Ctrl Pts',(31.3726040951777,-0.63490434793495,29.9022275362258));
#65769=CARTESIAN_POINT('Ctrl Pts',(31.2797800327084,-0.805795593106099,
29.8933569012793));
#65770=CARTESIAN_POINT('Ctrl Pts',(31.0338687856651,-1.10392432463312,29.873244137236));
#65771=CARTESIAN_POINT('Ctrl Pts',(30.8828092373533,-1.22807490132932,29.8625276541988));
#65772=CARTESIAN_POINT('Ctrl Pts',(30.5373473005298,-1.41449618106684,29.8407282401322));
#65773=CARTESIAN_POINT('Ctrl Pts',(30.3452845785499,-1.47320733373471,29.8298567527606));
#65774=CARTESIAN_POINT('Ctrl Pts',(30.0982962322989,-1.49758712755237,29.8172963039161));
#65775=CARTESIAN_POINT('Ctrl Pts',(30.0491225084885,-1.50000000000001,29.8148634077916));
#65776=CARTESIAN_POINT('Ctrl Pts',(30.0000000000002,-1.50000000000001,29.8125));
#65777=CARTESIAN_POINT('Origin',(30.,-1.32966554433622E-14,16.));
#65778=CARTESIAN_POINT('',(30.,-1.50000000000001,29.25));
#65779=CARTESIAN_POINT('',(30.,-1.50000000000001,29.3125));
#65780=CARTESIAN_POINT('',(30.,-1.50000000000001,16.));
#65781=CARTESIAN_POINT('Ctrl Pts',(30.0000000000001,-1.50000000000001,29.25));
#65782=CARTESIAN_POINT('Ctrl Pts',(30.0257058009192,-1.50000000000001,29.2512367709234));
#65783=CARTESIAN_POINT('Ctrl Pts',(30.0514327409082,-1.49933922123128,29.2524929138666));
#65784=CARTESIAN_POINT('Ctrl Pts',(30.2757518694164,-1.4877855903611,29.2636064071598));
#65785=CARTESIAN_POINT('Ctrl Pts',(30.4703136581261,-1.43816783024051,29.2743455366981));
#65786=CARTESIAN_POINT('Ctrl Pts',(30.8249043497727,-1.26783071251083,29.2961373759079));
#65787=CARTESIAN_POINT('Ctrl Pts',(30.9822510518058,-1.15024113589767,29.3069740997672));
#65788=CARTESIAN_POINT('Ctrl Pts',(31.2409808029183,-0.864020908483806,
29.3273728025942));
#65789=CARTESIAN_POINT('Ctrl Pts',(31.3408899715229,-0.698983488656709,
29.3361675839636));
#65790=CARTESIAN_POINT('Ctrl Pts',(31.4763980403227,-0.332018378933428,
29.3565545345038));
#65791=CARTESIAN_POINT('Ctrl Pts',(31.5074559153656,-0.132477013527386,
29.3676401659153));
#65792=CARTESIAN_POINT('Ctrl Pts',(31.4898677318573,0.259397054955175,29.3894109474976));
#65793=CARTESIAN_POINT('Ctrl Pts',(31.444367356687,0.448123046557066,29.3998957248088));
#65794=CARTESIAN_POINT('Ctrl Pts',(31.2829132867175,0.801659109129801,29.419536617174));
#65795=CARTESIAN_POINT('Ctrl Pts',(31.1671346623852,0.962462537199801,29.4289146111855));
#65796=CARTESIAN_POINT('Ctrl Pts',(30.8792964511142,1.23119218867364,29.4502279461232));
#65797=CARTESIAN_POINT('Ctrl Pts',(30.7097525390342,1.33613064071083,29.4613000883974));
#65798=CARTESIAN_POINT('Ctrl Pts',(30.346523773562,1.47177468007876,29.4825438305068));
#65799=CARTESIAN_POINT('Ctrl Pts',(30.1572989096959,1.50379960302192,29.4923264081504));
#65800=CARTESIAN_POINT('Ctrl Pts',(29.7684168962525,1.49529312487305,29.5112727938055));
#65801=CARTESIAN_POINT('Ctrl Pts',(29.5725063077327,1.45146676708809,29.5219159452176));
#65802=CARTESIAN_POINT('Ctrl Pts',(29.2125442219205,1.29150806105852,29.5436779265358));
#65803=CARTESIAN_POINT('Ctrl Pts',(29.051374885103,1.17821798386326,29.5545791364576));
#65804=CARTESIAN_POINT('Ctrl Pts',(28.784644635234,0.899571593555892,29.5751523790963));
#65805=CARTESIAN_POINT('Ctrl Pts',(28.6803243600253,0.738084850822973,29.5839952860653));
#65806=CARTESIAN_POINT('Ctrl Pts',(28.5339435846744,0.375376943196454,29.6041457253779));
#65807=CARTESIAN_POINT('Ctrl Pts',(28.4969501646145,0.176221200716502,29.6152099332935));
#65808=CARTESIAN_POINT('Ctrl Pts',(28.5033188891713,-0.217123692718195,
29.6370624273732));
#65809=CARTESIAN_POINT('Ctrl Pts',(28.5436046203998,-0.407585858885439,
29.6476436588269));
#65810=CARTESIAN_POINT('Ctrl Pts',(28.6948329707667,-0.764496194056087,
29.6674720107808));
#65811=CARTESIAN_POINT('Ctrl Pts',(28.8049699824855,-0.927268122072015,
29.6765948726435));
#65812=CARTESIAN_POINT('Ctrl Pts',(29.0837280295094,-1.20402609540407,29.6976943469156));
#65813=CARTESIAN_POINT('Ctrl Pts',(29.2505451199729,-1.31436112105669,29.7087851997463));
#65814=CARTESIAN_POINT('Ctrl Pts',(29.6105129505334,-1.46104267840857,29.7301786477734));
#65815=CARTESIAN_POINT('Ctrl Pts',(29.799201008928,-1.49868271487424,29.7403024627842));
#65816=CARTESIAN_POINT('Ctrl Pts',(29.9932712661576,-1.49998868274459,29.7496759492739));
#65817=CARTESIAN_POINT('Ctrl Pts',(29.9966359009771,-1.50000000009509,29.7498381447076));
#65818=CARTESIAN_POINT('Ctrl Pts',(30.0000000423936,-1.50000000000001,29.7500000020397));
#65819=CARTESIAN_POINT('Ctrl Pts',(30.0000000000002,-1.50000000000001,29.8125));
#65820=CARTESIAN_POINT('Ctrl Pts',(29.8597537134085,-1.50000000000001,29.8057523973903));
#65821=CARTESIAN_POINT('Ctrl Pts',(29.7199776172616,-1.48033650865739,29.798481208736));
#65822=CARTESIAN_POINT('Ctrl Pts',(29.396444095828,-1.38712528602054,29.7803259942996));
#65823=CARTESIAN_POINT('Ctrl Pts',(29.2206000446906,-1.29650603057681,29.7693484919046));
#65824=CARTESIAN_POINT('Ctrl Pts',(28.911420128637,-1.05097346611518,29.747652717245));
#65825=CARTESIAN_POINT('Ctrl Pts',(28.7818724475201,-0.897590413872414,
29.737366134104));
#65826=CARTESIAN_POINT('Ctrl Pts',(28.5939020851709,-0.556198210295242,
29.7183999005719));
#65827=CARTESIAN_POINT('Ctrl Pts',(28.5345980064858,-0.372882477899534,
29.7082156932166));
#65828=CARTESIAN_POINT('Ctrl Pts',(28.4870031451474,0.0134445146485481,
29.6867530825195));
#65829=CARTESIAN_POINT('Ctrl Pts',(28.502033993864,0.213177772539474,29.6756567904145));
#65830=CARTESIAN_POINT('Ctrl Pts',(28.6077791980133,0.591085049341038,29.6546619417033));
#65831=CARTESIAN_POINT('Ctrl Pts',(28.6958240597398,0.766015662165753,29.6456356480104));
#65832=CARTESIAN_POINT('Ctrl Pts',(28.9331445661562,1.07197536298372,29.6257186792435));
#65833=CARTESIAN_POINT('Ctrl Pts',(29.079894739921,1.20029258347643,29.6150937909803));
#65834=CARTESIAN_POINT('Ctrl Pts',(29.4205899711736,1.39807482372058,29.5932081329061));
#65835=CARTESIAN_POINT('Ctrl Pts',(29.6127784235583,1.46301280498413,29.5821576288666));
#65836=CARTESIAN_POINT('Ctrl Pts',(30.000882127086,1.51202551870596,29.5621235164545));
#65837=CARTESIAN_POINT('Ctrl Pts',(30.1924980276144,1.49972435337029,29.5532307774773));
#65838=CARTESIAN_POINT('Ctrl Pts',(30.565900986819,1.40283604422102,29.5325740773055));
#65839=CARTESIAN_POINT('Ctrl Pts',(30.7436552900603,1.31725598082702,29.5216446454201));
#65840=CARTESIAN_POINT('Ctrl Pts',(31.0589827795059,1.08076551025951,29.4999042647726));
#65841=CARTESIAN_POINT('Ctrl Pts',(31.1927323157941,0.931082658468895,29.4893113802134));
#65842=CARTESIAN_POINT('Ctrl Pts',(31.3898152208091,0.595521362119493,29.470508077404));
#65843=CARTESIAN_POINT('Ctrl Pts',(31.454132752542,0.414466978649508,29.4605259432583));
#65844=CARTESIAN_POINT('Ctrl Pts',(31.5126702779257,0.0306540870738048,
29.4392030048374));
#65845=CARTESIAN_POINT('Ctrl Pts',(31.5035323460368,-0.168835937693657,
29.4281202256837));
#65846=CARTESIAN_POINT('Ctrl Pts',(31.4089367798935,-0.550558804938134,
29.4069133997257));
#65847=CARTESIAN_POINT('Ctrl Pts',(31.3252882833553,-0.729258932876967,
29.3976724363492));
#65848=CARTESIAN_POINT('Ctrl Pts',(31.095809753143,-1.04226364925314,29.3779370699617));
#65849=CARTESIAN_POINT('Ctrl Pts',(30.9530486497371,-1.17422022183269,29.3674030128222));
#65850=CARTESIAN_POINT('Ctrl Pts',(30.6189939852,-1.38091973480463,29.3455891471428));
#65851=CARTESIAN_POINT('Ctrl Pts',(30.429320489981,-1.45113472826307,29.3345130603643));
#65852=CARTESIAN_POINT('Ctrl Pts',(30.1547092959792,-1.49402062264703,29.3201095482887));
#65853=CARTESIAN_POINT('Ctrl Pts',(30.0773321028638,-1.50000000000001,29.3162206425338));
#65854=CARTESIAN_POINT('Ctrl Pts',(30.,-1.50000000000001,29.3125));
#65855=CARTESIAN_POINT('Origin',(30.,-1.32966554433622E-14,16.));
#65856=CARTESIAN_POINT('',(30.0000000000001,-1.50000000000001,28.75));
#65857=CARTESIAN_POINT('',(30.,-1.50000000000001,28.8125));
#65858=CARTESIAN_POINT('',(30.,-1.50000000000001,16.));
#65859=CARTESIAN_POINT('Ctrl Pts',(30.0000000000002,-1.50000000000001,28.75));
#65860=CARTESIAN_POINT('Ctrl Pts',(30.0540853804301,-1.50000000000001,28.7526021840792));
#65861=CARTESIAN_POINT('Ctrl Pts',(30.1082259230801,-1.49707499170992,28.7552882723823));
#65862=CARTESIAN_POINT('Ctrl Pts',(30.3599293953789,-1.46969892581938,28.7681588076143));
#65863=CARTESIAN_POINT('Ctrl Pts',(30.551406195325,-1.40907643365525,28.7790551975627));
#65864=CARTESIAN_POINT('Ctrl Pts',(30.8948389562126,-1.21930777033508,28.8008499657338));
#65865=CARTESIAN_POINT('Ctrl Pts',(31.0445316684251,-1.09380802186036,28.8115381638324));
#65866=CARTESIAN_POINT('Ctrl Pts',(31.2877030940359,-0.793168713090864,
28.8315888464123));
#65867=CARTESIAN_POINT('Ctrl Pts',(31.379006293082,-0.620999590881335,28.8405000227289));
#65868=CARTESIAN_POINT('Ctrl Pts',(31.4929834420294,-0.246010850263539,
28.861332730541));
#65869=CARTESIAN_POINT('Ctrl Pts',(31.5124077516471,-0.0462064671363202,
28.872432974048));
#65870=CARTESIAN_POINT('Ctrl Pts',(31.472996504913,0.34187077296362,28.8939928207202));
#65871=CARTESIAN_POINT('Ctrl Pts',(31.4174359900152,0.526774847879437,28.9042652693267));
#65872=CARTESIAN_POINT('Ctrl Pts',(31.2357811865968,0.873408443354475,28.9235226912975));
#65873=CARTESIAN_POINT('Ctrl Pts',(31.1084372252019,1.03024288184359,28.9336214802999));
#65874=CARTESIAN_POINT('Ctrl Pts',(30.8025714917792,1.28234443647017,28.9553402732223));
#65875=CARTESIAN_POINT('Ctrl Pts',(30.6280587815183,1.37625325113107,28.9663450980946));
#65876=CARTESIAN_POINT('Ctrl Pts',(30.2588396849677,1.48965870484553,28.9872593116519));
#65877=CARTESIAN_POINT('Ctrl Pts',(30.068359262301,1.51042753130005,28.996421409812));
#65878=CARTESIAN_POINT('Ctrl Pts',(29.6808324457,1.4790834395187,29.015936971685));
#65879=CARTESIAN_POINT('Ctrl Pts',(29.4877765738488,1.42378431516532,29.0267614634377));
#65880=CARTESIAN_POINT('Ctrl Pts',(29.1387883585853,1.24336756773843,29.0485637430906));
#65881=CARTESIAN_POINT('Ctrl Pts',(28.9853282851658,1.12165139698337,29.0593280990587));
#65882=CARTESIAN_POINT('Ctrl Pts',(28.7345675292747,0.827996981331758,29.0795498986531));
#65883=CARTESIAN_POINT('Ctrl Pts',(28.6390572969471,0.659343561113025,29.0883698021604));
#65884=CARTESIAN_POINT('Ctrl Pts',(28.5145121329283,0.288224890453508,29.108987506086));
#65885=CARTESIAN_POINT('Ctrl Pts',(28.4894007489509,0.0884674237606763,
29.1200851431244));
#65886=CARTESIAN_POINT('Ctrl Pts',(28.5181714945435,-0.301617414497863,
29.1417565230277));
#65887=CARTESIAN_POINT('Ctrl Pts',(28.5688407456957,-0.488459284239858,
29.1521366269022));
#65888=CARTESIAN_POINT('Ctrl Pts',(28.7405885892344,-0.838517734954907,
29.1715843186086));
#65889=CARTESIAN_POINT('Ctrl Pts',(28.8621896492638,-0.99731625641509,29.1812936366545));
#65890=CARTESIAN_POINT('Ctrl Pts',(29.1592029920166,-1.25770358504828,29.2028166791214));
#65891=CARTESIAN_POINT('Ctrl Pts',(29.3313514615525,-1.35708034159287,29.2138596416832));
#65892=CARTESIAN_POINT('Ctrl Pts',(29.6732716198879,-1.47316539526991,29.2335348677957));
#65893=CARTESIAN_POINT('Ctrl Pts',(29.836171069295,-1.50000000000001,29.2421177768964));
#65894=CARTESIAN_POINT('Ctrl Pts',(30.0000000000001,-1.50000000000001,29.25));
#65895=CARTESIAN_POINT('Ctrl Pts',(30.,-1.50000000000001,29.3125));
#65896=CARTESIAN_POINT('Ctrl Pts',(29.8873008443269,-1.50000000000001,29.3070777593446));
#65897=CARTESIAN_POINT('Ctrl Pts',(29.7747317592542,-1.48730209620256,29.3013090571639));
#65898=CARTESIAN_POINT('Ctrl Pts',(29.4744632015876,-1.41837586794508,29.2849477619958));
#65899=CARTESIAN_POINT('Ctrl Pts',(29.294837753903,-1.33817655775596,29.2740777699983));
#65900=CARTESIAN_POINT('Ctrl Pts',(28.9731315511867,-1.11133054751215,29.2522983950411));
#65901=CARTESIAN_POINT('Ctrl Pts',(28.8350302040853,-0.965600487241644,
29.241605933651));
#65902=CARTESIAN_POINT('Ctrl Pts',(28.6283822605559,-0.636211572057215,
29.2225138877439));
#65903=CARTESIAN_POINT('Ctrl Pts',(28.5588803689078,-0.457503373167084,
29.2129168540649));
#65904=CARTESIAN_POINT('Ctrl Pts',(28.4890373687744,-0.0765943370343735,
29.1917552409464));
#65905=CARTESIAN_POINT('Ctrl Pts',(28.4920613555339,0.122462822378066,29.1806965098678));
#65906=CARTESIAN_POINT('Ctrl Pts',(28.5749385187676,0.508021327520356,29.1592765929154));
#65907=CARTESIAN_POINT('Ctrl Pts',(28.6539760022703,0.690715131611738,29.1497407450183));
#65908=CARTESIAN_POINT('Ctrl Pts',(28.8753117279029,1.01093295253508,29.1301967854836));
#65909=CARTESIAN_POINT('Ctrl Pts',(29.0138845897616,1.14650161502305,29.1197638993787));
#65910=CARTESIAN_POINT('Ctrl Pts',(29.3408853293963,1.36213850199283,29.0980411554306));
#65911=CARTESIAN_POINT('Ctrl Pts',(29.5278326261113,1.43768005817386,29.0869482728631));
#65912=CARTESIAN_POINT('Ctrl Pts',(29.9124519842907,1.50965487695232,29.0664439648431));
#65913=CARTESIAN_POINT('Ctrl Pts',(30.1057978761999,1.50848592114141,29.0576455173396));
#65914=CARTESIAN_POINT('Ctrl Pts',(30.4842893221004,1.43290905070853,29.0373359816462));
#65915=CARTESIAN_POINT('Ctrl Pts',(30.6656448486515,1.3581864320247,29.02653488151));
#65916=CARTESIAN_POINT('Ctrl Pts',(30.9934995933557,1.14126552935963,29.0047353821212));
#65917=CARTESIAN_POINT('Ctrl Pts',(31.1358790692293,0.999664672511309,28.9939517892597));
#65918=CARTESIAN_POINT('Ctrl Pts',(31.3521306759684,0.67660748989115,28.974573568351));
#65919=CARTESIAN_POINT('Ctrl Pts',(31.426848104494,0.500181082019829,28.9652878378899));
#65920=CARTESIAN_POINT('Ctrl Pts',(31.5078778462889,0.122255781263764,28.9442919878479));
#65921=CARTESIAN_POINT('Ctrl Pts',(31.5109056485428,-0.0761896933508503,
28.9332672392582));
#65922=CARTESIAN_POINT('Ctrl Pts',(31.4398008862795,-0.46541654048851,28.9116435255283));
#65923=CARTESIAN_POINT('Ctrl Pts',(31.3653977766762,-0.65214948337147,28.9017441343992));
#65924=CARTESIAN_POINT('Ctrl Pts',(31.1521444486118,-0.979425287841449,
28.8823929843003));
#65925=CARTESIAN_POINT('Ctrl Pts',(31.0177656624447,-1.1184106596764,28.8720669771632));
#65926=CARTESIAN_POINT('Ctrl Pts',(30.6979072153004,-1.34258973369453,28.8504505839492));
#65927=CARTESIAN_POINT('Ctrl Pts',(30.5137720633169,-1.42326028628083,28.8393505286358));
#65928=CARTESIAN_POINT('Ctrl Pts',(30.2141280739392,-1.48853135114915,28.8231208153399));
#65929=CARTESIAN_POINT('Ctrl Pts',(30.107104215103,-1.50000000000001,28.8176530539518));
#65930=CARTESIAN_POINT('Ctrl Pts',(30.,-1.50000000000001,28.8125));
#65931=CARTESIAN_POINT('Origin',(30.,-1.32966554433622E-14,16.));
#65932=CARTESIAN_POINT('',(30.,-1.50000000000001,28.25));
#65933=CARTESIAN_POINT('',(29.9999999999999,-1.50000000000001,28.3125));
#65934=CARTESIAN_POINT('',(30.,-1.50000000000001,16.));
#65935=CARTESIAN_POINT('Ctrl Pts',(30.,-1.50000000000001,28.25));
#65936=CARTESIAN_POINT('Ctrl Pts',(30.0829658981124,-1.50000000000001,28.2539916986341));
#65937=CARTESIAN_POINT('Ctrl Pts',(30.1659646402018,-1.49311778203419,28.258176150196));
#65938=CARTESIAN_POINT('Ctrl Pts',(30.4454386189069,-1.44623695759697,28.272924593389));
#65939=CARTESIAN_POINT('Ctrl Pts',(30.6341065114148,-1.37401296366571,28.2840081036532));
#65940=CARTESIAN_POINT('Ctrl Pts',(30.9655430066945,-1.16393488515826,28.305789851648));
#65941=CARTESIAN_POINT('Ctrl Pts',(31.1067439460802,-1.03060853555517,28.3162868947229));
#65942=CARTESIAN_POINT('Ctrl Pts',(31.3331794991128,-0.714896180931114,
28.3359510679762));
#65943=CARTESIAN_POINT('Ctrl Pts',(31.4151109522262,-0.5347128589249,28.3452937300598));
#65944=CARTESIAN_POINT('Ctrl Pts',(31.5053441166005,-0.151540941191815,
28.3665810588227));
#65945=CARTESIAN_POINT('Ctrl Pts',(31.5121960357138,0.047808853319833,28.3776560474067));
#65946=CARTESIAN_POINT('Ctrl Pts',(31.4494295470438,0.430548940590616,28.3989193855884));
#65947=CARTESIAN_POINT('Ctrl Pts',(31.3831821322801,0.610720967506089,28.4087494232854));
#65948=CARTESIAN_POINT('Ctrl Pts',(31.1825379493516,0.943999251999173,28.4276606511623));
#65949=CARTESIAN_POINT('Ctrl Pts',(31.047158086339,1.09222920702457,28.4382916166091));
#65950=CARTESIAN_POINT('Ctrl Pts',(30.7294268326579,1.32515752881874,28.4600486998403));
#65951=CARTESIAN_POINT('Ctrl Pts',(30.550958922042,1.4087432384851,28.4709570664618));
#65952=CARTESIAN_POINT('Ctrl Pts',(30.1765920486677,1.5017020595339,28.4915509905286));
#65953=CARTESIAN_POINT('Ctrl Pts',(29.9846796160604,1.51197023290498,28.5004045958464));
#65954=CARTESIAN_POINT('Ctrl Pts',(29.5971747277955,1.45876321333926,28.5205264062414));
#65955=CARTESIAN_POINT('Ctrl Pts',(29.4058997547266,1.39186434368365,28.5315874296089));
#65956=CARTESIAN_POINT('Ctrl Pts',(29.0676327101079,1.19076140439435,28.5534485031393));
#65957=CARTESIAN_POINT('Ctrl Pts',(28.9223466869136,1.06108495094317,28.5640407038963));
#65958=CARTESIAN_POINT('Ctrl Pts',(28.6879155980949,0.752518131365587,28.5838910754598));
#65959=CARTESIAN_POINT('Ctrl Pts',(28.6014862328755,0.576207606788701,28.5929884662895));
#65960=CARTESIAN_POINT('Ctrl Pts',(28.499833643426,0.196881228217823,28.6140621539879));
#65961=CARTESIAN_POINT('Ctrl Pts',(28.4869739372834,-0.00278217893022192,
28.6251545654961));
#65962=CARTESIAN_POINT('Ctrl Pts',(28.5386011115484,-0.388179803466622,
28.646565544637));
#65963=CARTESIAN_POINT('Ctrl Pts',(28.5997438056181,-0.57068109411198,28.6567045052284));
#65964=CARTESIAN_POINT('Ctrl Pts',(28.7910752661536,-0.909939730661663,
28.6755522072589));
#65965=CARTESIAN_POINT('Ctrl Pts',(28.9221594106395,-1.06198129449833,28.6859751842018));
#65966=CARTESIAN_POINT('Ctrl Pts',(29.2336502066539,-1.30423330232361,28.7076910145522));
#65967=CARTESIAN_POINT('Ctrl Pts',(29.4102115046891,-1.39300789458955,28.7186517848609));
#65968=CARTESIAN_POINT('Ctrl Pts',(29.7297304238973,-1.48169043732429,28.7364880499937));
#65969=CARTESIAN_POINT('Ctrl Pts',(29.8646679236608,-1.50000000000001,28.7434888324413));
#65970=CARTESIAN_POINT('Ctrl Pts',(30.0000000000002,-1.50000000000001,28.75));
#65971=CARTESIAN_POINT('Ctrl Pts',(30.,-1.50000000000001,28.8125));
#65972=CARTESIAN_POINT('Ctrl Pts',(29.915383015882,-1.50000000000001,28.8084288634535));
#65973=CARTESIAN_POINT('Ctrl Pts',(29.8307352254749,-1.4928411598692,28.8041573880682));
#65974=CARTESIAN_POINT('Ctrl Pts',(29.5559284168413,-1.44580747389306,28.7896292480462));
#65975=CARTESIAN_POINT('Ctrl Pts',(29.3730572440495,-1.37640415455312,28.7789029846613));
#65976=CARTESIAN_POINT('Ctrl Pts',(29.0395563050654,-1.16922544646275,28.7571024491396));
#65977=CARTESIAN_POINT('Ctrl Pts',(28.8931654598463,-1.03173520870096,28.7462400430439));
#65978=CARTESIAN_POINT('Ctrl Pts',(28.6676984257239,-0.714888535897263,
28.7265909588401));
#65979=CARTESIAN_POINT('Ctrl Pts',(28.5879546245725,-0.540586509645268,
28.7175325838691));
#65980=CARTESIAN_POINT('Ctrl Pts',(28.4963360655409,-0.165582907317607,
28.6966990504065));
#65981=CARTESIAN_POINT('Ctrl Pts',(28.4875887561367,0.032114568158461,28.6857158573245));
#65982=CARTESIAN_POINT('Ctrl Pts',(28.5470557852483,0.422500942588754,28.6640277254117));
#65983=CARTESIAN_POINT('Ctrl Pts',(28.6157998677826,0.611145026803925,28.6537877758344));
#65984=CARTESIAN_POINT('Ctrl Pts',(28.8187186237447,0.943964110383672,28.6347798680923));
#65985=CARTESIAN_POINT('Ctrl Pts',(28.9483973542157,1.08655537048085,28.6245798289275));
#65986=CARTESIAN_POINT('Ctrl Pts',(29.2601643471919,1.31985362966521,28.6030994252846));
#65987=CARTESIAN_POINT('Ctrl Pts',(29.4410566887989,1.40604402433623,28.5920020608114));
#65988=CARTESIAN_POINT('Ctrl Pts',(29.8214920682634,1.50190823479761,28.5710354603478));
#65989=CARTESIAN_POINT('Ctrl Pts',(30.0168727428654,1.5123834847247,28.5620321954671));
#65990=CARTESIAN_POINT('Ctrl Pts',(30.4002098002625,1.45848214178997,28.5420916231679));
#65991=CARTESIAN_POINT('Ctrl Pts',(30.5845472296663,1.39485738401663,28.531455330078));
#65992=CARTESIAN_POINT('Ctrl Pts',(30.9255768985555,1.19735876148644,28.5095614596354));
#65993=CARTESIAN_POINT('Ctrl Pts',(31.0774615143075,1.06275841541511,28.4985150091509));
#65994=CARTESIAN_POINT('Ctrl Pts',(31.3127681711381,0.750226996476014,28.4785123840417));
#65995=CARTESIAN_POINT('Ctrl Pts',(31.3972426471779,0.57785906771898,28.4696032815399));
#65996=CARTESIAN_POINT('Ctrl Pts',(31.4986444188222,0.205636520695856,28.4489242511497));
#65997=CARTESIAN_POINT('Ctrl Pts',(31.5126593744967,0.00877624847217685,
28.4379875693595));
#65998=CARTESIAN_POINT('Ctrl Pts',(31.4639817400215,-0.38243148199871,28.4162538065556));
#65999=CARTESIAN_POINT('Ctrl Pts',(31.4004868863224,-0.572852347631721,
28.405674869576));
#66000=CARTESIAN_POINT('Ctrl Pts',(31.2070793636249,-0.910612756316215,
28.3869104024268));
#66001=CARTESIAN_POINT('Ctrl Pts',(31.0818178721223,-1.05640050494828,28.3768711948362));
#66002=CARTESIAN_POINT('Ctrl Pts',(30.7776023551779,-1.29787423387296,28.3555270153716));
#66003=CARTESIAN_POINT('Ctrl Pts',(30.5998203088742,-1.38901510440857,28.3444417818325));
#66004=CARTESIAN_POINT('Ctrl Pts',(30.2759956104928,-1.48090471471267,28.3263092695923));
#66005=CARTESIAN_POINT('Ctrl Pts',(30.1382050521625,-1.50000000000003,28.3191493936725));
#66006=CARTESIAN_POINT('Ctrl Pts',(29.9999999999998,-1.50000000000001,28.3125));
#66007=CARTESIAN_POINT('Origin',(30.,-1.32966554433622E-14,16.));
#66008=CARTESIAN_POINT('',(30.,-1.50000000000001,27.75));
#66009=CARTESIAN_POINT('',(29.9999999999999,-1.50000000000001,27.8125));
#66010=CARTESIAN_POINT('',(30.,-1.50000000000001,16.));
#66011=CARTESIAN_POINT('Ctrl Pts',(30.,-1.50000000000001,27.75));
#66012=CARTESIAN_POINT('Ctrl Pts',(30.1124415068704,-1.50000000000002,27.7554098445216));
#66013=CARTESIAN_POINT('Ctrl Pts',(30.2247618661566,-1.48736003703784,27.7611649704098));
#66014=CARTESIAN_POINT('Ctrl Pts',(30.5287085515254,-1.41774990238772,27.7777222269793));
#66015=CARTESIAN_POINT('Ctrl Pts',(30.7117935692984,-1.3352484713228,27.7888226154224));
#66016=CARTESIAN_POINT('Ctrl Pts',(31.0290158327245,-1.10803593258209,27.810396438097));
#66017=CARTESIAN_POINT('Ctrl Pts',(31.1618575965723,-0.967846133863366,
27.8206819515156));
#66018=CARTESIAN_POINT('Ctrl Pts',(31.3721629460689,-0.6380210664967,27.8399620797878));
#66019=CARTESIAN_POINT('Ctrl Pts',(31.4448593309443,-0.449797513993593,
27.8500112492227));
#66020=CARTESIAN_POINT('Ctrl Pts',(31.5116357099559,-0.0592694964018678,
27.8717072502));
#66021=CARTESIAN_POINT('Ctrl Pts',(31.5064070816201,0.138907825669745,27.8827171014262));
#66022=CARTESIAN_POINT('Ctrl Pts',(31.4213057895144,0.515720730899333,27.9036511517167));
#66023=CARTESIAN_POINT('Ctrl Pts',(31.3446665574137,0.691326301909506,27.9128415418121));
#66024=CARTESIAN_POINT('Ctrl Pts',(31.1248857141117,1.01202109760975,27.9323239413351));
#66025=CARTESIAN_POINT('Ctrl Pts',(30.9809587395189,1.15206471718701,27.9431387316727));
#66026=CARTESIAN_POINT('Ctrl Pts',(30.6509116511972,1.36527940308072,27.964940759777));
#66027=CARTESIAN_POINT('Ctrl Pts',(30.4689587309927,1.43797198007731,27.9757142119819));
#66028=CARTESIAN_POINT('Ctrl Pts',(30.0895559298121,1.50958056680736,27.9959573651739));
#66029=CARTESIAN_POINT('Ctrl Pts',(29.8958570870542,1.50864454830606,28.0047704518936));
#66030=CARTESIAN_POINT('Ctrl Pts',(29.5119529197823,1.43233602869983,28.0253607308535));
#66031=CARTESIAN_POINT('Ctrl Pts',(29.326059536573,1.35483178794297,28.0364574259998));
#66032=CARTESIAN_POINT('Ctrl Pts',(29.0017503691465,1.13591853977073,28.058141681653));
#66033=CARTESIAN_POINT('Ctrl Pts',(28.8647633102306,0.999035130825837,28.0685347915132));
#66034=CARTESIAN_POINT('Ctrl Pts',(28.6464909172802,0.676130375169667,28.0880060034614));
#66035=CARTESIAN_POINT('Ctrl Pts',(28.5692025798653,0.491914163630282,28.097671435354));
#66036=CARTESIAN_POINT('Ctrl Pts',(28.4907708909632,0.10494838810591,28.1191695339942));
#66037=CARTESIAN_POINT('Ctrl Pts',(28.4900432259905,-0.0938982867387415,
28.1302165714856));
#66038=CARTESIAN_POINT('Ctrl Pts',(28.5641302538219,-0.473688030944453,
28.1513160017192));
#66039=CARTESIAN_POINT('Ctrl Pts',(28.6356001259049,-0.65152593371875,28.1607865563875));
#66040=CARTESIAN_POINT('Ctrl Pts',(28.845875335272,-0.978539657712538,28.1799871416705));
#66041=CARTESIAN_POINT('Ctrl Pts',(28.9856037255401,-1.12272886979256,28.1907150828729));
#66042=CARTESIAN_POINT('Ctrl Pts',(29.3096631032409,-1.34585412683097,28.2125043207586));
#66043=CARTESIAN_POINT('Ctrl Pts',(29.4899597666947,-1.42399330666579,28.2233493807965));
#66044=CARTESIAN_POINT('Ctrl Pts',(29.7854687062271,-1.48848755634025,28.2393585682142));
#66045=CARTESIAN_POINT('Ctrl Pts',(29.8926913234913,-1.50000000000001,28.2448371088943));
#66046=CARTESIAN_POINT('Ctrl Pts',(30.,-1.50000000000001,28.25));
#66047=CARTESIAN_POINT('Ctrl Pts',(29.9999999999998,-1.50000000000001,28.3125));
#66048=CARTESIAN_POINT('Ctrl Pts',(29.9436942937174,-1.50000000000001,28.3097909904434));
#66049=CARTESIAN_POINT('Ctrl Pts',(29.8873283119117,-1.49682992210333,28.3069910231599));
#66050=CARTESIAN_POINT('Ctrl Pts',(29.6396724584349,-1.46877643215582,28.2942964117443));
#66051=CARTESIAN_POINT('Ctrl Pts',(29.4541661443778,-1.41038581308707,28.2837492734071));
#66052=CARTESIAN_POINT('Ctrl Pts',(29.1087260311914,-1.22301113475657,28.2619244260365));
#66053=CARTESIAN_POINT('Ctrl Pts',(28.9535330490943,-1.09318251992373,28.250851349792));
#66054=CARTESIAN_POINT('Ctrl Pts',(28.7092889328235,-0.787692454984111,
28.2306143141317));
#66055=CARTESIAN_POINT('Ctrl Pts',(28.6196840987504,-0.61735395437333,28.2217974419096));
#66056=CARTESIAN_POINT('Ctrl Pts',(28.5078809954767,-0.248171981043882,
28.2012873322802));
#66057=CARTESIAN_POINT('Ctrl Pts',(28.4882926923279,-0.0523550997824531,
28.1904086166545));
#66058=CARTESIAN_POINT('Ctrl Pts',(28.5254878247544,0.339597077669009,28.168633495685));
#66059=CARTESIAN_POINT('Ctrl Pts',(28.5834194437059,0.531823926835376,28.1579542262869));
#66060=CARTESIAN_POINT('Ctrl Pts',(28.7667554264755,0.874769226053054,28.1389017096637));
#66061=CARTESIAN_POINT('Ctrl Pts',(28.8874031082008,1.02385470321529,28.129256101159));
#66062=CARTESIAN_POINT('Ctrl Pts',(29.1834814070674,1.27365788399194,28.1080720501192));
#66063=CARTESIAN_POINT('Ctrl Pts',(29.3578610118793,1.36987818467188,28.0970094213409));
#66064=CARTESIAN_POINT('Ctrl Pts',(29.7335617480327,1.48922788034193,28.0756182419206));
#66065=CARTESIAN_POINT('Ctrl Pts',(29.9311376367095,1.51130087803589,28.0661270552772));
#66066=CARTESIAN_POINT('Ctrl Pts',(30.3188296259211,1.47827076732948,28.0465567126743));
#66067=CARTESIAN_POINT('Ctrl Pts',(30.5053902810264,1.4253063260919,28.0361095744917));
#66068=CARTESIAN_POINT('Ctrl Pts',(30.8550820522802,1.24848731142734,28.0143733820065));
#66069=CARTESIAN_POINT('Ctrl Pts',(31.0135429189334,1.12366789185429,28.0032822239058));
#66070=CARTESIAN_POINT('Ctrl Pts',(31.2669421658592,0.825551327222966,27.9828095312695));
#66071=CARTESIAN_POINT('Ctrl Pts',(31.3618736710286,0.657250577679458,27.9740139209821));
#66072=CARTESIAN_POINT('Ctrl Pts',(31.4842407851538,0.291243414392501,27.9536801896884));
#66073=CARTESIAN_POINT('Ctrl Pts',(31.509450941646,0.0966465287303217,27.9428692515961));
#66074=CARTESIAN_POINT('Ctrl Pts',(31.4839402912682,-0.295715862316101,
27.9210713409824));
#66075=CARTESIAN_POINT('Ctrl Pts',(31.4317236332783,-0.489608696036187,
27.9102995168868));
#66076=CARTESIAN_POINT('Ctrl Pts',(31.2586786377253,-0.837725609348495,
27.8909596883695));
#66077=CARTESIAN_POINT('Ctrl Pts',(31.1426320784322,-0.99018742000189,27.8816363720611));
#66078=CARTESIAN_POINT('Ctrl Pts',(30.8547518896528,-1.24822771259633,27.8606179441152));
#66079=CARTESIAN_POINT('Ctrl Pts',(30.683921012954,-1.3494162779034,27.8495880462471));
#66080=CARTESIAN_POINT('Ctrl Pts',(30.3380948295812,-1.47125624803439,27.8295650326271));
#66081=CARTESIAN_POINT('Ctrl Pts',(30.1695563642114,-1.50000000000003,27.8206577843767));
#66082=CARTESIAN_POINT('Ctrl Pts',(29.9999999999999,-1.50000000000001,27.8125));
#66083=CARTESIAN_POINT('Origin',(30.,-1.32966554433622E-14,16.));
#66084=CARTESIAN_POINT('',(29.9999999999999,-1.50000000000001,27.25));
#66085=CARTESIAN_POINT('',(30.0000000001561,-1.50000000000001,27.312500000015));
#66086=CARTESIAN_POINT('',(30.,-1.50000000000001,16.));
#66087=CARTESIAN_POINT('Ctrl Pts',(29.9999999999998,-1.50000000000001,27.25));
#66088=CARTESIAN_POINT('Ctrl Pts',(30.1442714687728,-1.50000000000004,27.2569412642777));
#66089=CARTESIAN_POINT('Ctrl Pts',(30.2880340149987,-1.4791914741294,27.2644360576155));
#66090=CARTESIAN_POINT('Ctrl Pts',(30.6163114314673,-1.38174334274362,27.2829372047179));
#66091=CARTESIAN_POINT('Ctrl Pts',(30.7927900386128,-1.28861749288707,27.2940148648257));
#66092=CARTESIAN_POINT('Ctrl Pts',(31.0938533402203,-1.04389816914467,27.3152975386708));
#66093=CARTESIAN_POINT('Ctrl Pts',(31.2173213404585,-0.896838599044721,
27.3251756333865));
#66094=CARTESIAN_POINT('Ctrl Pts',(31.4068435879888,-0.557063752560209,
27.3440520137467));
#66095=CARTESIAN_POINT('Ctrl Pts',(31.4681965573585,-0.365925712559008,
27.3546707937468));
#66096=CARTESIAN_POINT('Ctrl Pts',(31.5124404667227,0.0256096349450533,
27.376422757497));
#66097=CARTESIAN_POINT('Ctrl Pts',(31.4962677243898,0.222085336897189,27.3873380742721));
#66098=CARTESIAN_POINT('Ctrl Pts',(31.3908461160845,0.593142920619804,27.4079523844789));
#66099=CARTESIAN_POINT('Ctrl Pts',(31.304401721973,0.764723471695272,27.4168175948822));
#66100=CARTESIAN_POINT('Ctrl Pts',(31.0656503667188,1.07455866625052,27.4369110579998));
#66101=CARTESIAN_POINT('Ctrl Pts',(30.9124772117446,1.20733392111332,27.4479688063785));
#66102=CARTESIAN_POINT('Ctrl Pts',(30.5697179509117,1.40095220523075,27.4698381046742));
#66103=CARTESIAN_POINT('Ctrl Pts',(30.3849139570494,1.46256729268532,27.4804410211816));
#66104=CARTESIAN_POINT('Ctrl Pts',(30.0007344874447,1.51254230178002,27.5003130592281));
#66105=CARTESIAN_POINT('Ctrl Pts',(29.8049569216954,1.49991645600797,27.5093863351468));
#66106=CARTESIAN_POINT('Ctrl Pts',(29.4253565109394,1.3996692288739,27.5304345136228));
#66107=CARTESIAN_POINT('Ctrl Pts',(29.245638701995,1.31157237616612,27.5415283255346));
#66108=CARTESIAN_POINT('Ctrl Pts',(28.9367683949736,1.07514318986943,27.562956332507));
#66109=CARTESIAN_POINT('Ctrl Pts',(28.8087599369318,0.93132448347984,27.5731101063824));
#66110=CARTESIAN_POINT('Ctrl Pts',(28.6094708234815,0.596592375009914,27.591996522448));
#66111=CARTESIAN_POINT('Ctrl Pts',(28.5427132787644,0.407261741609369,27.6023743476884));
#66112=CARTESIAN_POINT('Ctrl Pts',(28.4873635075659,0.0164898797776363,
27.624083895568));
#66113=CARTESIAN_POINT('Ctrl Pts',(28.4981279946982,-0.180903932406258,
27.6350502184671));
#66114=CARTESIAN_POINT('Ctrl Pts',(28.5934885065557,-0.554852956622451,
27.6558251642568));
#66115=CARTESIAN_POINT('Ctrl Pts',(28.6750314181996,-0.72841210507679,27.6648194223046));
#66116=CARTESIAN_POINT('Ctrl Pts',(28.9037835277885,-1.04301134033857,27.6845641309549));
#66117=CARTESIAN_POINT('Ctrl Pts',(29.0515807305306,-1.17900166318454,27.6954525361552));
#66118=CARTESIAN_POINT('Ctrl Pts',(29.3870321030576,-1.38265756586298,27.7172490562487));
#66119=CARTESIAN_POINT('Ctrl Pts',(29.570408592882,-1.45015060314336,27.7279465683201));
#66120=CARTESIAN_POINT('Ctrl Pts',(29.8405845073873,-1.49365112485936,27.7421537608929));
#66121=CARTESIAN_POINT('Ctrl Pts',(29.920314098353,-1.50000000000001,27.7461661102695));
#66122=CARTESIAN_POINT('Ctrl Pts',(30.,-1.50000000000001,27.75));
#66123=CARTESIAN_POINT('Ctrl Pts',(29.9999999999999,-1.50000000000001,27.8125));
#66124=CARTESIAN_POINT('Ctrl Pts',(29.9712572824709,-1.50000000000001,27.8111171153581));
#66125=CARTESIAN_POINT('Ctrl Pts',(29.9424874969812,-1.49917387170699,27.8097099804002));
#66126=CARTESIAN_POINT('Ctrl Pts',(29.7223735770152,-1.48649276547853,27.7987674915373));
#66127=CARTESIAN_POINT('Ctrl Pts',(29.5349257292356,-1.43889608772887,27.7884267728186));
#66128=CARTESIAN_POINT('Ctrl Pts',(29.1813453265204,-1.27257887490163,27.7667952051828));
#66129=CARTESIAN_POINT('Ctrl Pts',(29.0198117779222,-1.15277654761383,27.7556955762776));
#66130=CARTESIAN_POINT('Ctrl Pts',(28.7574522908629,-0.862041024530384,
27.7349968128188));
#66131=CARTESIAN_POINT('Ctrl Pts',(28.6572312223829,-0.695708343276581,
27.7261504635153));
#66132=CARTESIAN_POINT('Ctrl Pts',(28.524605736016,-0.332863036208749,27.7059923909005));
#66133=CARTESIAN_POINT('Ctrl Pts',(28.4939840388333,-0.139603136099824,
27.6952557297833));
#66134=CARTESIAN_POINT('Ctrl Pts',(28.508148989394,0.25282273238934,27.673454292645));
#66135=CARTESIAN_POINT('Ctrl Pts',(28.5547646373704,0.44816718663467,27.6626018229647));
#66136=CARTESIAN_POINT('Ctrl Pts',(28.7177569938957,0.801209312950165,27.6429883715028));
#66137=CARTESIAN_POINT('Ctrl Pts',(28.8294090431484,0.956981758536969,27.6339039237114));
#66138=CARTESIAN_POINT('Ctrl Pts',(29.1093968787388,1.22281551664853,27.6130487316321));
#66139=CARTESIAN_POINT('Ctrl Pts',(29.2767036270498,1.32864238149993,27.6020595468161));
#66140=CARTESIAN_POINT('Ctrl Pts',(29.6469534397504,1.47162694755714,27.5802741008953));
#66141=CARTESIAN_POINT('Ctrl Pts',(29.8468632228895,1.50560128622732,27.570023387908));
#66142=CARTESIAN_POINT('Ctrl Pts',(30.2385607914922,1.49319741260661,27.5508332778069));
#66143=CARTESIAN_POINT('Ctrl Pts',(30.4267058309758,1.45067195878526,27.540599882768));
#66144=CARTESIAN_POINT('Ctrl Pts',(30.7836729511717,1.29433057010809,27.5190824778378));
#66145=CARTESIAN_POINT('Ctrl Pts',(30.9479647504538,1.17932417828325,27.5079833629642));
#66146=CARTESIAN_POINT('Ctrl Pts',(31.2187102492265,0.89565657574078,27.4870774584548));
#66147=CARTESIAN_POINT('Ctrl Pts',(31.3239608540741,0.731149127851972,27.4781193959917));
#66148=CARTESIAN_POINT('Ctrl Pts',(31.4661242989034,0.37131396030254,27.4581285533501));
#66149=CARTESIAN_POINT('Ctrl Pts',(31.5017272578984,0.179429293592902,27.4474682940885));
#66150=CARTESIAN_POINT('Ctrl Pts',(31.4980926781097,-0.21275991516766,27.4256800047129));
#66151=CARTESIAN_POINT('Ctrl Pts',(31.4567210643059,-0.409304691427262,
27.4147608504762));
#66152=CARTESIAN_POINT('Ctrl Pts',(31.3031284414201,-0.766835781066652,
27.394898012163));
#66153=CARTESIAN_POINT('Ctrl Pts',(31.1955054411838,-0.925718941221814,
27.3859710339898));
#66154=CARTESIAN_POINT('Ctrl Pts',(30.9227930606553,-1.19862566676885,27.3652694110877));
#66155=CARTESIAN_POINT('Ctrl Pts',(30.75882230211,-1.30859982122977,27.354325526665));
#66156=CARTESIAN_POINT('Ctrl Pts',(30.3950972752779,-1.46060207029247,27.3326035134561));
#66157=CARTESIAN_POINT('Ctrl Pts',(30.198484714314,-1.4999999999587,27.3220496002711));
#66158=CARTESIAN_POINT('Ctrl Pts',(30.0000000003122,-1.50000000000001,27.312500000015));
#66159=CARTESIAN_POINT('Origin',(30.,-1.32966554433622E-14,16.));
#66160=CARTESIAN_POINT('',(30.,-1.50000000000001,26.75));
#66161=CARTESIAN_POINT('',(30.0000000000001,-1.50000000000001,26.8125));
#66162=CARTESIAN_POINT('',(30.,-1.50000000000001,16.));
#66163=CARTESIAN_POINT('Ctrl Pts',(29.9999999999999,-1.50000000000002,26.75));
#66164=CARTESIAN_POINT('Ctrl Pts',(30.1755630845093,-1.50000000000003,26.7584467828418));
#66165=CARTESIAN_POINT('Ctrl Pts',(30.3499584064833,-1.46918259215549,26.7676934207892));
#66166=CARTESIAN_POINT('Ctrl Pts',(30.6997034276012,-1.3412672085792,26.7880737410627));
#66167=CARTESIAN_POINT('Ctrl Pts',(30.8691431470038,-1.23821435243508,26.7990884927007));
#66168=CARTESIAN_POINT('Ctrl Pts',(31.1538803669515,-0.977054933639417,
26.8200423468827));
#66169=CARTESIAN_POINT('Ctrl Pts',(31.2681733329846,-0.823282264050392,
26.8292620964417));
#66170=CARTESIAN_POINT('Ctrl Pts',(31.4372326110993,-0.473197410553428,
26.8487112549693));
#66171=CARTESIAN_POINT('Ctrl Pts',(31.4872301101415,-0.278708237309613,
26.8595162090384));
#66172=CARTESIAN_POINT('Ctrl Pts',(31.5082331683214,0.113718878171538,26.881317715454));
#66173=CARTESIAN_POINT('Ctrl Pts',(31.4808674747884,0.307802550913579,26.8921001417175));
#66174=CARTESIAN_POINT('Ctrl Pts',(31.3544261384598,0.67256246632588,26.9123645814626));
#66175=CARTESIAN_POINT('Ctrl Pts',(31.2574072539999,0.840081862517357,26.9211719059107));
#66176=CARTESIAN_POINT('Ctrl Pts',(31.0004574791989,1.1352928844589,26.9417347138799));
#66177=CARTESIAN_POINT('Ctrl Pts',(30.8407636896231,1.25813738072432,26.9528303320317));
#66178=CARTESIAN_POINT('Ctrl Pts',(30.4894980147219,1.43081423936239,26.9745271891017));
#66179=CARTESIAN_POINT('Ctrl Pts',(30.302568408204,1.48165789304525,26.984933167702));
#66180=CARTESIAN_POINT('Ctrl Pts',(29.9140424353861,1.51051713966446,27.0044277780243));
#66181=CARTESIAN_POINT('Ctrl Pts',(29.7160053760103,1.48607476032932,27.0140505099305));
#66182=CARTESIAN_POINT('Ctrl Pts',(29.3413420123945,1.36197834203437,27.0355236321475));
#66183=CARTESIAN_POINT('Ctrl Pts',(29.1683424827117,1.26378814603618,27.0465745813446));
#66184=CARTESIAN_POINT('Ctrl Pts',(28.87548492057,1.01073104588063,27.0676940612658));
#66185=CARTESIAN_POINT('Ctrl Pts',(28.7566499301147,0.860326156686485,27.0772041024063));
#66186=CARTESIAN_POINT('Ctrl Pts',(28.5773390955292,0.515342682333064,27.0963698509815));
#66187=CARTESIAN_POINT('Ctrl Pts',(28.5216397715234,0.322442560698391,27.1070865244057));
#66188=CARTESIAN_POINT('Ctrl Pts',(28.4890218615652,-0.0697120082430973,
27.1288728893469));
#66189=CARTESIAN_POINT('Ctrl Pts',(28.510818362855,-0.265069960572926,27.1397261089208));
#66190=CARTESIAN_POINT('Ctrl Pts',(28.6267610927498,-0.633018179794785,
27.1601676766553));
#66191=CARTESIAN_POINT('Ctrl Pts',(28.7184387624141,-0.802555681667626,
27.1689674029211));
#66192=CARTESIAN_POINT('Ctrl Pts',(28.9662614123549,-1.10518359683465,27.1892971067025));
#66193=CARTESIAN_POINT('Ctrl Pts',(29.1227466839353,-1.23306866661795,27.2003783708913));
#66194=CARTESIAN_POINT('Ctrl Pts',(29.4698813680168,-1.416339226716,27.2221707450579));
#66195=CARTESIAN_POINT('Ctrl Pts',(29.6558172836666,-1.47261637710131,27.232679845148));
#66196=CARTESIAN_POINT('Ctrl Pts',(29.8981460836565,-1.49740948534734,27.2450275924248));
#66197=CARTESIAN_POINT('Ctrl Pts',(29.9491012405249,-1.5,27.247551132293));
#66198=CARTESIAN_POINT('Ctrl Pts',(29.9999999999998,-1.50000000000001,27.25));
#66199=CARTESIAN_POINT('Ctrl Pts',(30.0000000003122,-1.50000000000001,27.312500000015));
#66200=CARTESIAN_POINT('Ctrl Pts',(29.9998020603292,-1.50000000000005,27.3124904766232));
#66201=CARTESIAN_POINT('Ctrl Pts',(29.9996041185888,-1.49999996081992,27.3124809520584));
#66202=CARTESIAN_POINT('Ctrl Pts',(29.8088160951652,-1.49992443102837,27.3032995609518));
#66203=CARTESIAN_POINT('Ctrl Pts',(29.6200100906951,-1.46352575850992,27.2932045535897));
#66204=CARTESIAN_POINT('Ctrl Pts',(29.2593205849108,-1.31930644298838,27.2718447795537));
#66205=CARTESIAN_POINT('Ctrl Pts',(29.0918823606668,-1.21016636340677,27.2607572353565));
#66206=CARTESIAN_POINT('Ctrl Pts',(28.8110979291704,-0.935181294724627,
27.2396095139674));
#66207=CARTESIAN_POINT('Ctrl Pts',(28.6997118002275,-0.772848068745042,
27.2304360038192));
#66208=CARTESIAN_POINT('Ctrl Pts',(28.5461974612702,-0.416685157506792,
27.210649175417));
#66209=CARTESIAN_POINT('Ctrl Pts',(28.5047394765833,-0.226599155889903,
27.2000888419939));
#66210=CARTESIAN_POINT('Ctrl Pts',(28.4958539389935,0.166443777601294,27.1782531234666));
#66211=CARTESIAN_POINT('Ctrl Pts',(28.5315184967694,0.365700597221805,27.1671833001544));
#66212=CARTESIAN_POINT('Ctrl Pts',(28.6754701753172,0.729371435414476,27.1469793646992));
#66213=CARTESIAN_POINT('Ctrl Pts',(28.7788000491734,0.891648198610453,27.1381536711784));
#66214=CARTESIAN_POINT('Ctrl Pts',(29.0437345128306,1.17200464814443,27.1176193266989));
#66215=CARTESIAN_POINT('Ctrl Pts',(29.2040531543845,1.2862733419873,27.1067318620762));
#66216=CARTESIAN_POINT('Ctrl Pts',(29.5628324377282,1.44858368838945,27.0849614650246));
#66217=CARTESIAN_POINT('Ctrl Pts',(29.7584548095726,1.49371725552991,27.0742958690726));
#66218=CARTESIAN_POINT('Ctrl Pts',(30.1472060622831,1.50481186242553,27.055283882181));
#66219=CARTESIAN_POINT('Ctrl Pts',(30.3365600149074,1.47407427722924,27.045587089767));
#66220=CARTESIAN_POINT('Ctrl Pts',(30.7004989886168,1.34098519143669,27.0243801486806));
#66221=CARTESIAN_POINT('Ctrl Pts',(30.8706482413977,1.23730103012925,27.0133137233474));
#66222=CARTESIAN_POINT('Ctrl Pts',(31.1605713571455,0.970446090199086,26.991952153717));
#66223=CARTESIAN_POINT('Ctrl Pts',(31.2776619344983,0.810096307036669,26.9825053503909));
#66224=CARTESIAN_POINT('Ctrl Pts',(31.4414580755822,0.457344311316898,26.9629080172954));
#66225=CARTESIAN_POINT('Ctrl Pts',(31.4881418689773,0.269035150966863,26.9524463972759));
#66226=CARTESIAN_POINT('Ctrl Pts',(31.508284818313,-0.122458793694974,26.9306967336836));
#66227=CARTESIAN_POINT('Ctrl Pts',(31.478582774639,-0.322064434897177,26.9196075313946));
#66228=CARTESIAN_POINT('Ctrl Pts',(31.3455674834561,-0.689986184900448,
26.8991674341722));
#66229=CARTESIAN_POINT('Ctrl Pts',(31.246662212612,-0.855842984261559,26.8903733141072));
#66230=CARTESIAN_POINT('Ctrl Pts',(30.9897531567272,-1.14377092738595,26.8700147729728));
#66231=CARTESIAN_POINT('Ctrl Pts',(30.8332877383797,-1.26231706455743,26.8591938787678));
#66232=CARTESIAN_POINT('Ctrl Pts',(30.4799553603842,-1.43498001100993,26.8373979738484));
#66233=CARTESIAN_POINT('Ctrl Pts',(30.2857235516143,-1.48590367409306,26.8266384453951));
#66234=CARTESIAN_POINT('Ctrl Pts',(30.0581276265954,-1.49915605873645,26.8153201095514));
#66235=CARTESIAN_POINT('Ctrl Pts',(30.0290509426437,-1.50000000000001,26.8138977141296));
#66236=CARTESIAN_POINT('Ctrl Pts',(30.0000000000001,-1.50000000000001,26.8125));
#66237=CARTESIAN_POINT('Origin',(30.,-1.32966554433622E-14,16.));
#66238=CARTESIAN_POINT('',(30.,-1.50000000000001,26.25));
#66239=CARTESIAN_POINT('',(30.0000000000001,-1.50000000000001,26.3125));
#66240=CARTESIAN_POINT('',(30.,-1.50000000000001,16.));
#66241=CARTESIAN_POINT('Ctrl Pts',(30.,-1.50000000000001,26.25));
#66242=CARTESIAN_POINT('Ctrl Pts',(30.0056194401817,-1.50000000000001,26.2502703654418));
#66243=CARTESIAN_POINT('Ctrl Pts',(30.0112401600052,-1.49996842190559,26.2505416696197));
#66244=CARTESIAN_POINT('Ctrl Pts',(30.2156637559459,-1.49767029707552,26.2604408412659));
#66245=CARTESIAN_POINT('Ctrl Pts',(30.4120156853044,-1.45593401100177,26.2710471691517));
#66246=CARTESIAN_POINT('Ctrl Pts',(30.7738333695248,-1.29974623576057,26.2927936799124));
#66247=CARTESIAN_POINT('Ctrl Pts',(30.9363483004055,-1.18803068750778,26.3037158928437));
#66248=CARTESIAN_POINT('Ctrl Pts',(31.2059383925193,-0.91211987124096,26.3243507415389));
#66249=CARTESIAN_POINT('Ctrl Pts',(31.3118367658411,-0.751883140819906,
26.3332287143989));
#66250=CARTESIAN_POINT('Ctrl Pts',(31.4620725484111,-0.390717177178761,
26.3532934901568));
#66251=CARTESIAN_POINT('Ctrl Pts',(31.5011777050095,-0.191739563198423,
26.3643478020445));
#66252=CARTESIAN_POINT('Ctrl Pts',(31.4988144256802,0.202052743889533,26.3862251524383));
#66253=CARTESIAN_POINT('Ctrl Pts',(31.4603972352794,0.393097806012914,26.3968387670007));
#66254=CARTESIAN_POINT('Ctrl Pts',(31.3127984325509,0.751186708707084,26.4167325949282));
#66255=CARTESIAN_POINT('Ctrl Pts',(31.2046306350456,0.914654115967526,26.4257825736587));
#66256=CARTESIAN_POINT('Ctrl Pts',(30.929085340333,1.1942016269637,26.4468049614706));
#66257=CARTESIAN_POINT('Ctrl Pts',(30.763267624326,1.30642002708729,26.4579000478329));
#66258=CARTESIAN_POINT('Ctrl Pts',(30.4044749371868,1.4569895622401,26.479344956129));
#66259=CARTESIAN_POINT('Ctrl Pts',(30.2159899848526,1.49659297949806,26.4895135375502));
#66260=CARTESIAN_POINT('Ctrl Pts',(29.8264040657205,1.50311771775866,26.5084387415533));
#66261=CARTESIAN_POINT('Ctrl Pts',(29.6289313228251,1.46692091172634,26.5187719136178));
#66262=CARTESIAN_POINT('Ctrl Pts',(29.2622864534942,1.32066065000658,26.5404749081659));
#66263=CARTESIAN_POINT('Ctrl Pts',(29.0963152488665,1.21314636529189,26.5514467093804));
#66264=CARTESIAN_POINT('Ctrl Pts',(28.8192613253014,0.944447852152411,26.5722403200802));
#66265=CARTESIAN_POINT('Ctrl Pts',(28.7092361098565,0.787428080615722,26.5812539955214));
#66266=CARTESIAN_POINT('Ctrl Pts',(28.5500186537103,0.4325695152731,26.6009683602626));
#66267=CARTESIAN_POINT('Ctrl Pts',(28.5055087117716,0.236724815037938,26.6118486213868));
#66268=CARTESIAN_POINT('Ctrl Pts',(28.4955827399852,-0.155640049113208,
26.6336466693952));
#66269=CARTESIAN_POINT('Ctrl Pts',(28.5282144121142,-0.348361913823613,
26.6443534396569));
#66270=CARTESIAN_POINT('Ctrl Pts',(28.6646766132005,-0.710004687419899,
26.6644447048566));
#66271=CARTESIAN_POINT('Ctrl Pts',(28.7669073789545,-0.875602741749661,
26.6733284353239));
#66272=CARTESIAN_POINT('Ctrl Pts',(29.0326342692594,-1.16351957915387,26.6941109162225));
#66273=CARTESIAN_POINT('Ctrl Pts',(29.1952892767769,-1.28140768888904,26.7052113286353));
#66274=CARTESIAN_POINT('Ctrl Pts',(29.5502593863542,-1.44373597574174,26.7267989550745));
#66275=CARTESIAN_POINT('Ctrl Pts',(29.7380028348229,-1.48930167419739,26.7370974797965));
#66276=CARTESIAN_POINT('Ctrl Pts',(29.9528487018704,-1.49944465692866,26.7477160059146));
#66277=CARTESIAN_POINT('Ctrl Pts',(29.9764341399413,-1.50000000000001,26.7488661870293));
#66278=CARTESIAN_POINT('Ctrl Pts',(29.9999999999999,-1.50000000000001,26.75));
#66279=CARTESIAN_POINT('Ctrl Pts',(30.0000000000001,-1.50000000000001,26.8125));
#66280=CARTESIAN_POINT('Ctrl Pts',(29.8395800016776,-1.50000000000002,26.8047817892321));
#66281=CARTESIAN_POINT('Ctrl Pts',(29.6800130120943,-1.4742710204936,26.7963899249912));
#66282=CARTESIAN_POINT('Ctrl Pts',(29.3406580591605,-1.36160698346738,26.7769331456215));
#66283=CARTESIAN_POINT('Ctrl Pts',(29.1679496395237,-1.26348603655748,26.7658981260489));
#66284=CARTESIAN_POINT('Ctrl Pts',(28.8688888773426,-1.00499369846698,26.744329215695));
#66285=CARTESIAN_POINT('Ctrl Pts',(28.7459708502921,-0.846646295408431,
26.7345359053005));
#66286=CARTESIAN_POINT('Ctrl Pts',(28.5719299961441,-0.497373685523865,
26.7151318714181));
#66287=CARTESIAN_POINT('Ctrl Pts',(28.5201211210885,-0.310969647956289,
26.7047760915532));
#66288=CARTESIAN_POINT('Ctrl Pts',(28.4888763927518,0.078675171393689,26.6831291571448));
#66289=CARTESIAN_POINT('Ctrl Pts',(28.5126680280148,0.27845746343119,26.6720301409206));
#66290=CARTESIAN_POINT('Ctrl Pts',(28.6347687943924,0.650483449918004,26.6513620305602));
#66291=CARTESIAN_POINT('Ctrl Pts',(28.7293030467267,0.819946999855557,26.6425267967844));
#66292=CARTESIAN_POINT('Ctrl Pts',(28.9783004894773,1.11523286685495,26.62234451654));
#66293=CARTESIAN_POINT('Ctrl Pts',(29.1308905878018,1.23784103842587,26.6115972394678));
#66294=CARTESIAN_POINT('Ctrl Pts',(29.4786064716065,1.42045274911996,26.5897952036888));
#66295=CARTESIAN_POINT('Ctrl Pts',(29.671307799161,1.47699671076135,26.5789531911429));
#66296=CARTESIAN_POINT('Ctrl Pts',(30.058657983757,1.51083891985875,26.5593767353335));
#66297=CARTESIAN_POINT('Ctrl Pts',(30.2492918070221,1.49128918840572,26.5502639753537));
#66298=CARTESIAN_POINT('Ctrl Pts',(30.6191301716824,1.38027512961514,26.5293863948823));
#66299=CARTESIAN_POINT('Ctrl Pts',(30.7941362196709,1.2875659668366,26.518391157951));
#66300=CARTESIAN_POINT('Ctrl Pts',(31.1019229551517,1.03729505553015,26.4966307919773));
#66301=CARTESIAN_POINT('Ctrl Pts',(31.2305302882388,0.880892156398053,26.4864384531331));
#66302=CARTESIAN_POINT('Ctrl Pts',(31.4143329938993,0.535011347738905,26.467222852652));
#66303=CARTESIAN_POINT('Ctrl Pts',(31.4709425533457,0.350543024469619,26.4569746124704));
#66304=CARTESIAN_POINT('Ctrl Pts',(31.5126435249117,-0.0370627264893054,
26.4354409596394));
#66305=CARTESIAN_POINT('Ctrl Pts',(31.4944467514533,-0.236856679751601,
26.4243412955692));
#66306=CARTESIAN_POINT('Ctrl Pts',(31.382763240843,-0.612667143007661,26.4034629364995));
#66307=CARTESIAN_POINT('Ctrl Pts',(31.2923692914564,-0.785603738087747,
26.3945234871348));
#66308=CARTESIAN_POINT('Ctrl Pts',(31.0508333839059,-1.08773585408316,26.3745100265869));
#66309=CARTESIAN_POINT('Ctrl Pts',(30.9019600520426,-1.21403192877114,26.3638391307711));
#66310=CARTESIAN_POINT('Ctrl Pts',(30.559750929656,-1.4057831061822,26.3420481650989));
#66311=CARTESIAN_POINT('Ctrl Pts',(30.3686322762759,-1.46754077280931,26.3311374738613));
#66312=CARTESIAN_POINT('Ctrl Pts',(30.1141378164167,-1.49674664949133,26.3180818291001));
#66313=CARTESIAN_POINT('Ctrl Pts',(30.0570405412872,-1.50000000000001,26.3152443643222));
#66314=CARTESIAN_POINT('Ctrl Pts',(30.0000000000002,-1.50000000000001,26.3125));
#66315=CARTESIAN_POINT('Origin',(30.,-1.32966554433622E-14,16.));
#66316=CARTESIAN_POINT('',(30.0000000000001,-1.50000000000001,25.75));
#66317=CARTESIAN_POINT('',(30.,-1.50000000000001,25.8125));
#66318=CARTESIAN_POINT('',(30.,-1.50000000000001,16.));
#66319=CARTESIAN_POINT('Ctrl Pts',(30.0000000000002,-1.50000000000001,25.75));
#66320=CARTESIAN_POINT('Ctrl Pts',(30.0350308469701,-1.50000000000001,25.7516854224107));
#66321=CARTESIAN_POINT('Ctrl Pts',(30.0700958017757,-1.49877287551864,25.7534065726266));
#66322=CARTESIAN_POINT('Ctrl Pts',(30.3035194655511,-1.48237243734734,25.7650927416133));
#66323=CARTESIAN_POINT('Ctrl Pts',(30.4971388675202,-1.42911969045028,25.7758875024032));
#66324=CARTESIAN_POINT('Ctrl Pts',(30.848183508266,-1.2523218603483,25.7976881963921));
#66325=CARTESIAN_POINT('Ctrl Pts',(31.0030592952475,-1.13208157746957,25.8084796690252));
#66326=CARTESIAN_POINT('Ctrl Pts',(31.2567047166631,-0.841106936698577,
25.8287658189633));
#66327=CARTESIAN_POINT('Ctrl Pts',(31.3538096540821,-0.673770640691784,
25.8375682977395));
#66328=CARTESIAN_POINT('Ctrl Pts',(31.4823392304013,-0.304145984064151,
25.8581030008855));
#66329=CARTESIAN_POINT('Ctrl Pts',(31.5096068971125,-0.104447172132542,
25.8691973793261));
#66330=CARTESIAN_POINT('Ctrl Pts',(31.4848844296652,0.286323023183646,25.8909068346215));
#66331=CARTESIAN_POINT('Ctrl Pts',(31.4360830652788,0.473864860798067,25.9013258256));
#66332=CARTESIAN_POINT('Ctrl Pts',(31.2680746858178,0.825196096656156,25.9208442275921));
#66333=CARTESIAN_POINT('Ctrl Pts',(31.1486056539627,0.984726473310249,25.9304245311885));
#66334=CARTESIAN_POINT('Ctrl Pts',(30.8549287066094,1.24817526789042,25.9518720919776));
#66335=CARTESIAN_POINT('Ctrl Pts',(30.6837094772403,1.34958696185865,25.9629268724906));
#66336=CARTESIAN_POINT('Ctrl Pts',(30.3185036845909,1.47806545582453,25.9840666914365));
#66337=CARTESIAN_POINT('Ctrl Pts',(30.1289070957048,1.50647679352315,25.993618043535));
#66338=CARTESIAN_POINT('Ctrl Pts',(29.7404075656125,1.49068855536224,26.0127482980627));
#66339=CARTESIAN_POINT('Ctrl Pts',(29.545331017818,1.44318830470102,26.0234533742517));
#66340=CARTESIAN_POINT('Ctrl Pts',(29.188736991222,1.27663378618483,26.0452365267588));
#66341=CARTESIAN_POINT('Ctrl Pts',(29.0299764729631,1.16060540084053,26.056097906459));
#66342=CARTESIAN_POINT('Ctrl Pts',(28.7683079019703,0.877153943717209,26.0765610930375));
#66343=CARTESIAN_POINT('Ctrl Pts',(28.6667786145465,0.713430148276809,26.0853649917623));
#66344=CARTESIAN_POINT('Ctrl Pts',(28.5272614190292,0.348018884480366,26.1056656175288));
#66345=CARTESIAN_POINT('Ctrl Pts',(28.4940188142116,0.14859972255689,26.1167444598579));
#66346=CARTESIAN_POINT('Ctrl Pts',(28.5074840531687,-0.243852309362615,
26.1385473505201));
#66347=CARTESIAN_POINT('Ctrl Pts',(28.5510714566589,-0.433234122923729,
26.1490685623846));
#66348=CARTESIAN_POINT('Ctrl Pts',(28.7087569062828,-0.788023018123922,
26.1687790565624));
#66349=CARTESIAN_POINT('Ctrl Pts',(28.8224400778707,-0.949553940205162,
26.1780544535033));
#66350=CARTESIAN_POINT('Ctrl Pts',(29.1069273076436,-1.22127183449108,26.1992895710132));
#66351=CARTESIAN_POINT('Ctrl Pts',(29.2754819087647,-1.32821443027861,26.2103697857015));
#66352=CARTESIAN_POINT('Ctrl Pts',(29.6323103908041,-1.46593097223903,26.2313631635471));
#66353=CARTESIAN_POINT('Ctrl Pts',(29.8154198943914,-1.50000000000001,26.2411193855283));
#66354=CARTESIAN_POINT('Ctrl Pts',(30.,-1.50000000000001,26.25));
#66355=CARTESIAN_POINT('Ctrl Pts',(30.0000000000002,-1.50000000000001,26.3125));
#66356=CARTESIAN_POINT('Ctrl Pts',(29.867580258195,-1.50000000000001,26.3061289522019));
#66357=CARTESIAN_POINT('Ctrl Pts',(29.7355134428156,-1.48246999719879,26.299287940062));
#66358=CARTESIAN_POINT('Ctrl Pts',(29.4184023489971,-1.39643165750255,26.2816409715667));
#66359=CARTESIAN_POINT('Ctrl Pts',(29.2414246745114,-1.30875331188796,26.2706906196325));
#66360=CARTESIAN_POINT('Ctrl Pts',(28.9285790709285,-1.068455989113,26.2489639028796));
#66361=CARTESIAN_POINT('Ctrl Pts',(28.7965902868422,-0.917216536990246,
26.2384564742772));
#66362=CARTESIAN_POINT('Ctrl Pts',(28.6032774267936,-0.57923818308581,26.2196798990602));
#66363=CARTESIAN_POINT('Ctrl Pts',(28.5410496718181,-0.397228347537677,
26.2095682415298));
#66364=CARTESIAN_POINT('Ctrl Pts',(28.4870387262231,-0.0124011503103316,
26.1881889527949));
#66365=CARTESIAN_POINT('Ctrl Pts',(28.4986129287161,0.187210043596071,26.1770994420224));
#66366=CARTESIAN_POINT('Ctrl Pts',(28.5978341126594,0.567369358609899,26.1559794800772));
#66367=CARTESIAN_POINT('Ctrl Pts',(28.6833047820777,0.744501773375072,26.1468355900596));
#66368=CARTESIAN_POINT('Ctrl Pts',(28.9160253075989,1.05460577600707,26.1270248184819));
#66369=CARTESIAN_POINT('Ctrl Pts',(29.060441358732,1.18507685788338,26.1164524012633));
#66370=CARTESIAN_POINT('Ctrl Pts',(29.3972605323865,1.3881264388998,26.0946069150758));
#66371=CARTESIAN_POINT('Ctrl Pts',(29.5879874006837,1.45617711323181,26.0835402678372));
#66372=CARTESIAN_POINT('Ctrl Pts',(29.9751313819113,1.51185807000195,26.0633671011121));
#66373=CARTESIAN_POINT('Ctrl Pts',(30.1672228871666,1.50278877622694,26.0545319510962));
#66374=CARTESIAN_POINT('Ctrl Pts',(30.5421508905102,1.41213985662164,26.0339751935801));
#66375=CARTESIAN_POINT('Ctrl Pts',(30.7210278648892,1.32972839399854,26.0230797638426));
#66376=CARTESIAN_POINT('Ctrl Pts',(31.0401525812529,1.09890434445495,26.0013140896138));
#66377=CARTESIAN_POINT('Ctrl Pts',(31.1764827770535,0.951536572108244,25.9906613507783));
#66378=CARTESIAN_POINT('Ctrl Pts',(31.3792148041551,0.619604996410003,25.9716870800294));
#66379=CARTESIAN_POINT('Ctrl Pts',(31.4465937278795,0.439945368358781,25.9619414093531));
#66380=CARTESIAN_POINT('Ctrl Pts',(31.5118285637272,0.0578389075257285,
25.9407132726402));
#66381=CARTESIAN_POINT('Ctrl Pts',(31.5063115855957,-0.141417075009879,
25.9296434958327));
#66382=CARTESIAN_POINT('Ctrl Pts',(31.4186362556573,-0.525426994647723,
25.9083096114084));
#66383=CARTESIAN_POINT('Ctrl Pts',(31.3377111820022,-0.706481965554299,
25.8989028268757));
#66384=CARTESIAN_POINT('Ctrl Pts',(31.1130533652913,-1.0237694591265,25.8792804311414));
#66385=CARTESIAN_POINT('Ctrl Pts',(30.972766729538,-1.15788504149396,25.8688054543882));
#66386=CARTESIAN_POINT('Ctrl Pts',(30.6428698469895,-1.36991560346518,25.8470435453937));
#66387=CARTESIAN_POINT('Ctrl Pts',(30.4547968017865,-1.44330311864552,25.835956334699));
#66388=CARTESIAN_POINT('Ctrl Pts',(30.1725168697432,-1.4925627888959,25.8210068109627));
#66389=CARTESIAN_POINT('Ctrl Pts',(30.0862466800351,-1.50000000000001,25.8166495453279));
#66390=CARTESIAN_POINT('Ctrl Pts',(30.,-1.50000000000001,25.8125));
#66391=CARTESIAN_POINT('Origin',(30.,-1.32966554433622E-14,16.));
#66392=CARTESIAN_POINT('',(30.0000000000001,-1.50000000000001,25.25));
#66393=CARTESIAN_POINT('',(30.,-1.50000000000001,25.3125));
#66394=CARTESIAN_POINT('',(30.,-1.50000000000001,16.));
#66395=CARTESIAN_POINT('Ctrl Pts',(30.0000000000001,-1.50000000000001,25.25));
#66396=CARTESIAN_POINT('Ctrl Pts',(30.0627700539087,-1.50000000000001,25.2530200256268));
#66397=CARTESIAN_POINT('Ctrl Pts',(30.1255978857231,-1.49606031931736,25.2561522666689));
#66398=CARTESIAN_POINT('Ctrl Pts',(30.387395972516,-1.46296629655124,25.2696673114027));
#66399=CARTESIAN_POINT('Ctrl Pts',(30.5795743359629,-1.39800636679879,25.2807179397182));
#66400=CARTESIAN_POINT('Ctrl Pts',(30.9202426421314,-1.20018691165606,25.3026033361058));
#66401=CARTESIAN_POINT('Ctrl Pts',(31.0669765445057,-1.07185443274338,25.3132278653563));
#66402=CARTESIAN_POINT('Ctrl Pts',(31.3042648643842,-0.765865616588927,
25.3331440943071));
#66403=CARTESIAN_POINT('Ctrl Pts',(31.3922917557281,-0.59091969078094,25.3421711282901));
#66404=CARTESIAN_POINT('Ctrl Pts',(31.4979914701149,-0.212996523390812,
25.3631668598117));
#66405=CARTESIAN_POINT('Ctrl Pts',(31.5129981369395,-0.0132639168507718,
25.3742631157306));
#66406=CARTESIAN_POINT('Ctrl Pts',(31.4653583210385,0.373052959697002,25.3957251644277));
#66407=CARTESIAN_POINT('Ctrl Pts',(31.4060337226141,0.556359728684241,25.4059088738159));
#66408=CARTESIAN_POINT('Ctrl Pts',(31.2180258231604,0.89772836856045,25.4248737982534));
#66409=CARTESIAN_POINT('Ctrl Pts',(31.088460968798,1.05109657163312,25.4351618575451));
#66410=CARTESIAN_POINT('Ctrl Pts',(30.7792551558925,1.29659274113508,25.4568578671965));
#66411=CARTESIAN_POINT('Ctrl Pts',(30.6034030192283,1.3871914976091,25.4678351891908));
#66412=CARTESIAN_POINT('Ctrl Pts',(30.2324892526205,1.49400946706811,25.4886479519256));
#66413=CARTESIAN_POINT('Ctrl Pts',(30.0415773273281,1.51141487828139,25.4976825299541));
#66414=CARTESIAN_POINT('Ctrl Pts',(29.6545526771042,1.47316919187237,25.5173656422979));
#66415=CARTESIAN_POINT('Ctrl Pts',(29.4624963512885,1.41443679130397,25.5282374121534));
#66416=CARTESIAN_POINT('Ctrl Pts',(29.1170567587378,1.22797823527613,25.5500367866331));
#66417=CARTESIAN_POINT('Ctrl Pts',(28.9660123174462,1.10381260264269,25.560752961054));
#66418=CARTESIAN_POINT('Ctrl Pts',(28.7201314342041,0.805655980053721,25.5808650389699));
#66419=CARTESIAN_POINT('Ctrl Pts',(28.627324212077,0.634750626561539,25.5897360763022));
#66420=CARTESIAN_POINT('Ctrl Pts',(28.5095600205757,0.261132939276874,25.6104926144847));
#66421=CARTESIAN_POINT('Ctrl Pts',(28.4881034640454,0.0613273497745445,
25.6215929250126));
#66422=CARTESIAN_POINT('Ctrl Pts',(28.5237184917358,-0.327500650137204,
25.6431944805633));
#66423=CARTESIAN_POINT('Ctrl Pts',(28.57753700972,-0.513112472024964,25.6535062484459));
#66424=CARTESIAN_POINT('Ctrl Pts',(28.7556436240904,-0.860981573894074,
25.6728323096608));
#66425=CARTESIAN_POINT('Ctrl Pts',(28.8809148866478,-1.0185241445112,25.6827836630609));
#66426=CARTESIAN_POINT('Ctrl Pts',(29.1836083572217,-1.27362286430434,25.7044330850039));
#66427=CARTESIAN_POINT('Ctrl Pts',(29.357290902101,-1.3695025366285,25.7154527145718));
#66428=CARTESIAN_POINT('Ctrl Pts',(29.6920067607584,-1.47617903100382,25.7345199747848));
#66429=CARTESIAN_POINT('Ctrl Pts',(29.8456406050883,-1.50000000000001,25.7425733801496));
#66430=CARTESIAN_POINT('Ctrl Pts',(30.0000000000002,-1.50000000000001,25.75));
#66431=CARTESIAN_POINT('Ctrl Pts',(30.,-1.50000000000001,25.8125));
#66432=CARTESIAN_POINT('Ctrl Pts',(29.8958136711151,-1.50000000000001,25.8074873329144));
#66433=CARTESIAN_POINT('Ctrl Pts',(29.7916909834384,-1.4891476478018,25.80217627354));
#66434=CARTESIAN_POINT('Ctrl Pts',(29.4989680289332,-1.42717135574301,25.7863710701566));
#66435=CARTESIAN_POINT('Ctrl Pts',(29.3182929815531,-1.3502283271827,25.7755410315376));
#66436=CARTESIAN_POINT('Ctrl Pts',(28.9928896773701,-1.12927046795383,25.7537473394536));
#66437=CARTESIAN_POINT('Ctrl Pts',(28.8522264483536,-0.985982788210688,
25.7429994633659));
#66438=CARTESIAN_POINT('Ctrl Pts',(28.639853465626,-0.660351661724937,25.7237363544014));
#66439=CARTESIAN_POINT('Ctrl Pts',(28.5672444995779,-0.483012345456745,
25.714334019192));
#66440=CARTESIAN_POINT('Ctrl Pts',(28.4907135279836,-0.103874220197911,
25.6932707900109));
#66441=CARTESIAN_POINT('Ctrl Pts',(28.4901189594842,0.0948392876888842,
25.6822311506839));
#66442=CARTESIAN_POINT('Ctrl Pts',(28.5659791907661,0.482606924381713,25.660688504201));
#66443=CARTESIAN_POINT('Ctrl Pts',(28.6422553573453,0.667705397375409,25.6509438140946));
#66444=CARTESIAN_POINT('Ctrl Pts',(28.8587620723286,0.992152292410515,25.6315147161622));
#66445=CARTESIAN_POINT('Ctrl Pts',(28.9948328944551,1.12978254443193,25.6211449431241));
#66446=CARTESIAN_POINT('Ctrl Pts',(29.3175819275344,1.35056278988812,25.599483888434));
#66447=CARTESIAN_POINT('Ctrl Pts',(29.5028611462505,1.42918794783786,25.5883856057019));
#66448=CARTESIAN_POINT('Ctrl Pts',(29.8863465577115,1.507984767606,25.5677463546914));
#66449=CARTESIAN_POINT('Ctrl Pts',(30.0802506039983,1.51013051078303,25.5589203440921));
#66450=CARTESIAN_POINT('Ctrl Pts',(30.4601704571654,1.44079280620514,25.5387153942847));
#66451=CARTESIAN_POINT('Ctrl Pts',(30.6424548754516,1.36926262641685,25.5279582816823));
#66452=CARTESIAN_POINT('Ctrl Pts',(30.9737363815272,1.15817666999724,25.5061559940003));
#66453=CARTESIAN_POINT('Ctrl Pts',(31.118540202541,1.01903114337744,25.4953239633962));
#66454=CARTESIAN_POINT('Ctrl Pts',(31.3403349350297,0.699693252907024,25.4757823623965));
#66455=CARTESIAN_POINT('Ctrl Pts',(31.418072458882,0.524551989157358,25.4666417771753));
#66456=CARTESIAN_POINT('Ctrl Pts',(31.5054879258866,0.148377517280613,25.4457431954044));
#66457=CARTESIAN_POINT('Ctrl Pts',(31.5119666548414,-0.0496365545101339,
25.4347424136382));
#66458=CARTESIAN_POINT('Ctrl Pts',(31.4476607795272,-0.440895614279282,
25.4130057992066));
#66459=CARTESIAN_POINT('Ctrl Pts',(31.3759395541655,-0.629971074835861,
25.4028673928089));
#66460=CARTESIAN_POINT('Ctrl Pts',(31.1673112734267,-0.961240411187918,
25.383627833962));
#66461=CARTESIAN_POINT('Ctrl Pts',(31.0353453440586,-1.10210544227651,25.3733657026948));
#66462=CARTESIAN_POINT('Ctrl Pts',(30.7196295943324,-1.33102399282861,25.3518169729773));
#66463=CARTESIAN_POINT('Ctrl Pts',(30.5371475111052,-1.41455738295539,25.3407169277066));
#66464=CARTESIAN_POINT('Ctrl Pts',(30.2307882933611,-1.48667060842925,25.3239740678184));
#66465=CARTESIAN_POINT('Ctrl Pts',(30.1154677152456,-1.50000000000002,25.31805544304));
#66466=CARTESIAN_POINT('Ctrl Pts',(29.9999999999999,-1.50000000000001,25.3125));
#66467=CARTESIAN_POINT('Origin',(30.,-1.32966554433622E-14,16.));
#66468=CARTESIAN_POINT('',(30.,-1.50000000000001,24.75));
#66469=CARTESIAN_POINT('',(29.9999999999999,-1.50000000000001,24.8125));
#66470=CARTESIAN_POINT('',(30.,-1.50000000000001,16.));
#66471=CARTESIAN_POINT('Ctrl Pts',(30.,-1.50000000000001,24.75));
#66472=CARTESIAN_POINT('Ctrl Pts',(30.0924202028298,-1.50000000000002,24.7544465690819));
#66473=CARTESIAN_POINT('Ctrl Pts',(30.1848415762481,-1.49146009950343,24.759130413942));
#66474=CARTESIAN_POINT('Ctrl Pts',(30.4723479931102,-1.43762037173554,24.7744586208663));
#66475=CARTESIAN_POINT('Ctrl Pts',(30.6592834359903,-1.36205645668747,24.7855515541955));
#66476=CARTESIAN_POINT('Ctrl Pts',(30.9862537983022,-1.14638219357722,24.80727387484));
#66477=CARTESIAN_POINT('Ctrl Pts',(31.1248087259681,-1.01079850350159,24.8177063155187));
#66478=CARTESIAN_POINT('Ctrl Pts',(31.346109752526,-0.69055016576277,24.8372494532827));
#66479=CARTESIAN_POINT('Ctrl Pts',(31.4251274703691,-0.50783917665878,24.8467867124079));
#66480=CARTESIAN_POINT('Ctrl Pts',(31.5079543915197,-0.122264618516638,
24.8682075211936));
#66481=CARTESIAN_POINT('Ctrl Pts',(31.5109523526148,0.0767903025210503,
24.8792661279179));
#66482=CARTESIAN_POINT('Ctrl Pts',(31.441061251381,0.457686740875712,24.9004270411598));
#66483=CARTESIAN_POINT('Ctrl Pts',(31.3715371249325,0.636385044039808,24.9100225849775));
#66484=CARTESIAN_POINT('Ctrl Pts',(31.1648481820269,0.965747220324715,24.9291158607209));
#66485=CARTESIAN_POINT('Ctrl Pts',(31.0267283705006,1.11145999209774,24.939808730245));
#66486=CARTESIAN_POINT('Ctrl Pts',(30.7049953637051,1.33826413832451,24.9615882319247));
#66487=CARTESIAN_POINT('Ctrl Pts',(30.525362209954,1.41844022126688,24.9724579494792));
#66488=CARTESIAN_POINT('Ctrl Pts',(30.1493787440764,1.50469862427576,24.9929435291658));
#66489=CARTESIAN_POINT('Ctrl Pts',(29.9569371691124,1.5114809139774,25.00175294714));
#66490=CARTESIAN_POINT('Ctrl Pts',(29.5704977811955,1.45108059660786,25.0220233074535));
#66491=CARTESIAN_POINT('Ctrl Pts',(29.3808354910635,1.38084291684638,25.0330994853021));
#66492=CARTESIAN_POINT('Ctrl Pts',(29.0468101101847,1.17410520091496,25.0549130032641));
#66493=CARTESIAN_POINT('Ctrl Pts',(28.9040664949486,1.04213311105638,25.0654466500392));
#66494=CARTESIAN_POINT('Ctrl Pts',(28.6746221434491,0.72909790198446,25.0851812190219));
#66495=CARTESIAN_POINT('Ctrl Pts',(28.5909928953227,0.55038117737188,25.0944232679238));
#66496=CARTESIAN_POINT('Ctrl Pts',(28.496446216206,0.168641933616187,25.115631003688));
#66497=CARTESIAN_POINT('Ctrl Pts',(28.4873339658181,-0.0308466586561953,
25.1267137032587));
#66498=CARTESIAN_POINT('Ctrl Pts',(28.5459190178277,-0.414647584032544,
25.1480359768907));
#66499=CARTESIAN_POINT('Ctrl Pts',(28.6102581790788,-0.595692019972521,
25.1580163493537));
#66500=CARTESIAN_POINT('Ctrl Pts',(28.8073809961852,-0.931227827424643,
25.1768208644096));
#66501=CARTESIAN_POINT('Ctrl Pts',(28.9411488677475,-1.08089452062442,25.1874141822753));
#66502=CARTESIAN_POINT('Ctrl Pts',(29.2565034825196,-1.31734526046784,25.2091547643595));
#66503=CARTESIAN_POINT('Ctrl Pts',(29.4342658933141,-1.40290303357365,25.220083967145));
#66504=CARTESIAN_POINT('Ctrl Pts',(29.7466738861071,-1.48392560477994,25.2373653306843));
#66505=CARTESIAN_POINT('Ctrl Pts',(29.8731973879732,-1.50000000000001,25.2438992064844));
#66506=CARTESIAN_POINT('Ctrl Pts',(30.0000000000001,-1.50000000000001,25.25));
#66507=CARTESIAN_POINT('Ctrl Pts',(29.9999999999999,-1.50000000000001,25.3125));
#66508=CARTESIAN_POINT('Ctrl Pts',(29.9230963675565,-1.50000000000001,25.3087999722589));
#66509=CARTESIAN_POINT('Ctrl Pts',(29.8461434428577,-1.49408668250554,25.3049333141238));
#66510=CARTESIAN_POINT('Ctrl Pts',(29.5785997947569,-1.4525378268213,25.2909069794727));
#66511=CARTESIAN_POINT('Ctrl Pts',(29.394946779968,-1.38612426885289,25.2802261486243));
#66512=CARTESIAN_POINT('Ctrl Pts',(29.0584111434883,-1.1844646483524,25.2584329141398));
#66513=CARTESIAN_POINT('Ctrl Pts',(28.9098271705268,-1.04932739740415,25.2475303518813));
#66514=CARTESIAN_POINT('Ctrl Pts',(28.679224033866,-0.736002543967933,25.2277319851447));
#66515=CARTESIAN_POINT('Ctrl Pts',(28.5966653608253,-0.562858820299269,
25.218769934461));
#66516=CARTESIAN_POINT('Ctrl Pts',(28.4992036771274,-0.189506940379824,
25.1980281633544));
#66517=CARTESIAN_POINT('Ctrl Pts',(28.4873077258157,0.00770736323463039,
25.1870718131536));
#66518=CARTESIAN_POINT('Ctrl Pts',(28.5403428741226,0.398677937032776,25.1653512257204));
#66519=CARTESIAN_POINT('Ctrl Pts',(28.6059812891417,0.588385613614782,25.1548923783415));
#66520=CARTESIAN_POINT('Ctrl Pts',(28.8032229731553,0.924175534219124,25.1360750856002));
#66521=CARTESIAN_POINT('Ctrl Pts',(28.9302878616598,1.06867554049118,25.1259477842385));
#66522=CARTESIAN_POINT('Ctrl Pts',(29.2375170160562,1.30684882772379,25.1045502900104));
#66523=CARTESIAN_POINT('Ctrl Pts',(29.416566346389,1.39601031268743,25.0934590671725));
#66524=CARTESIAN_POINT('Ctrl Pts',(29.7956879290814,1.49872079338579,25.0723655026123));
#66525=CARTESIAN_POINT('Ctrl Pts',(29.9916913791595,1.51255777708596,25.0632485758478));
#66526=CARTESIAN_POINT('Ctrl Pts',(30.376338186137,1.46478286918679,25.0434151669436));
#66527=CARTESIAN_POINT('Ctrl Pts',(30.5613937867408,1.40429329778983,25.0328314093361));
#66528=CARTESIAN_POINT('Ctrl Pts',(30.9051019650582,1.2128519030953,25.0109769253773));
#66529=CARTESIAN_POINT('Ctrl Pts',(31.0589867932662,1.08110262857348,24.9999134360581));
#66530=CARTESIAN_POINT('Ctrl Pts',(31.2996601001576,0.7727813254929,24.9797695555402));
#66531=CARTESIAN_POINT('Ctrl Pts',(31.3872075591177,0.601637196257516,24.9709242886809));
#66532=CARTESIAN_POINT('Ctrl Pts',(31.4948659823167,0.231233394936456,24.9503462997187));
#66533=CARTESIAN_POINT('Ctrl Pts',(31.5122374051454,0.0349818838105959,
24.9394434379894));
#66534=CARTESIAN_POINT('Ctrl Pts',(31.4704629549247,-0.356714017311379,
24.9176825545938));
#66535=CARTESIAN_POINT('Ctrl Pts',(31.410306361987,-0.548240683911054,24.9070421842271));
#66536=CARTESIAN_POINT('Ctrl Pts',(31.2229499202263,-0.889130700933294,
24.8881038499482));
#66537=CARTESIAN_POINT('Ctrl Pts',(31.1004741653132,-1.03689935475768,24.8783104947773));
#66538=CARTESIAN_POINT('Ctrl Pts',(30.8011609016804,-1.28341012707365,24.8570622572132));
#66539=CARTESIAN_POINT('Ctrl Pts',(30.6254139659021,-1.37762857486559,24.8459894497178));
#66540=CARTESIAN_POINT('Ctrl Pts',(30.2947063232275,-1.4782094919839,24.8272843564766));
#66541=CARTESIAN_POINT('Ctrl Pts',(30.1476360382517,-1.50000000000004,24.8196031422022));
#66542=CARTESIAN_POINT('Ctrl Pts',(29.9999999999998,-1.50000000000001,24.8125));
#66543=CARTESIAN_POINT('Origin',(30.,-1.32966554433622E-14,16.));
#66544=CARTESIAN_POINT('',(30.,-1.50000000000001,24.25));
#66545=CARTESIAN_POINT('',(30.,-1.50000000000001,24.3125));
#66546=CARTESIAN_POINT('',(30.,-1.50000000000001,16.));
#66547=CARTESIAN_POINT('Ctrl Pts',(29.9999999999999,-1.50000000000001,24.25));
#66548=CARTESIAN_POINT('Ctrl Pts',(30.1233865336442,-1.50000000000002,24.2559364373678));
#66549=CARTESIAN_POINT('Ctrl Pts',(30.2465476489323,-1.48477988594364,24.2622848102359));
#66550=CARTESIAN_POINT('Ctrl Pts',(30.5591244259704,-1.40597165010196,24.2795127850953));
#66551=CARTESIAN_POINT('Ctrl Pts',(30.7400033595231,-1.31975922707827,24.2906101163719));
#66552=CARTESIAN_POINT('Ctrl Pts',(31.0517371878966,-1.08642473531537,24.3120899308425));
#66553=CARTESIAN_POINT('Ctrl Pts',(31.181396759577,-0.943819238764671,24.3222894436867));
#66554=CARTESIAN_POINT('Ctrl Pts',(31.3842738432636,-0.610977913754327,
24.341295964288));
#66555=CARTESIAN_POINT('Ctrl Pts',(31.4529950991553,-0.422325812949031,
24.3515374548362));
#66556=CARTESIAN_POINT('Ctrl Pts',(31.5124147536636,-0.0319347678693356,
24.3732258462295));
#66557=CARTESIAN_POINT('Ctrl Pts',(31.5036442008573,0.165759327603677,24.3842088515336));
#66558=CARTESIAN_POINT('Ctrl Pts',(31.4119825510711,0.540750850840327,24.4050417139356));
#66559=CARTESIAN_POINT('Ctrl Pts',(31.3322181025457,0.715044299742208,24.4140993016492));
#66560=CARTESIAN_POINT('Ctrl Pts',(31.106713322535,1.03186525150623,24.4337494874295));
#66561=CARTESIAN_POINT('Ctrl Pts',(30.9603062459911,1.1693383575936,24.4446121985753));
#66562=CARTESIAN_POINT('Ctrl Pts',(30.6267827077052,1.37647673516795,24.4664127011144));
#66563=CARTESIAN_POINT('Ctrl Pts',(30.4439056234701,1.4458581458551,24.47713864034));
#66564=CARTESIAN_POINT('Ctrl Pts',(30.0630400763872,1.51099956140736,24.4972725262831));
#66565=CARTESIAN_POINT('Ctrl Pts',(29.8687484810349,1.50660828894347,24.5061312780688));
#66566=CARTESIAN_POINT('Ctrl Pts',(29.4860566158504,1.4231980920111,24.526860498932));
#66567=CARTESIAN_POINT('Ctrl Pts',(29.3019333862064,1.34250650777999,24.5379605648438));
#66568=CARTESIAN_POINT('Ctrl Pts',(28.9821049580114,1.11829253966791,24.5595764830508));
#66569=CARTESIAN_POINT('Ctrl Pts',(28.8477437066725,0.979293286040407,24.5699020321484));
#66570=CARTESIAN_POINT('Ctrl Pts',(28.6345240475922,0.651988290747904,24.5892523732038));
#66571=CARTESIAN_POINT('Ctrl Pts',(28.5601403785395,0.465238374198666,24.5991534236556));
#66572=CARTESIAN_POINT('Ctrl Pts',(28.489084947481,0.0759965520384366,24.6207779693312));
#66573=CARTESIAN_POINT('Ctrl Pts',(28.4921379080883,-0.122445995567395,
24.6318025553093));
#66574=CARTESIAN_POINT('Ctrl Pts',(28.5732141775453,-0.500358663169468,
24.6527977035094));
#66575=CARTESIAN_POINT('Ctrl Pts',(28.6479534934179,-0.676775662247645,
24.662082289407));
#66576=CARTESIAN_POINT('Ctrl Pts',(28.8642453292122,-0.999806026462223,
24.6814617008812));
#66577=CARTESIAN_POINT('Ctrl Pts',(29.0066425215227,-1.1413892524153,24.6922456563782));
#66578=CARTESIAN_POINT('Ctrl Pts',(29.3345224631394,-1.35826808429126,24.7140451994209));
#66579=CARTESIAN_POINT('Ctrl Pts',(29.515884916708,-1.43296761407463,24.7248459914751));
#66580=CARTESIAN_POINT('Ctrl Pts',(29.8033393621129,-1.4903304156034,24.7402695610815));
#66581=CARTESIAN_POINT('Ctrl Pts',(29.901655948172,-1.50000000000001,24.7452684196003));
#66582=CARTESIAN_POINT('Ctrl Pts',(30.,-1.50000000000001,24.75));
#66583=CARTESIAN_POINT('Ctrl Pts',(29.9999999999998,-1.50000000000001,24.8125));
#66584=CARTESIAN_POINT('Ctrl Pts',(29.9520844763832,-1.50000000000001,24.8101946632951));
#66585=CARTESIAN_POINT('Ctrl Pts',(29.9041155058213,-1.49770423456202,24.8078229838607));
#66586=CARTESIAN_POINT('Ctrl Pts',(29.6647429412583,-1.47465918202179,24.7956660256301));
#66587=CARTESIAN_POINT('Ctrl Pts',(29.4785801635781,-1.4195491435244,24.7851784304102));
#66588=CARTESIAN_POINT('Ctrl Pts',(29.1305308217309,-1.23854895841351,24.7634051157232));
#66589=CARTESIAN_POINT('Ctrl Pts',(28.9733425780824,-1.11174127780071,24.752319957252));
#66590=CARTESIAN_POINT('Ctrl Pts',(28.7235507953419,-0.81069913235786,24.7319395626836));
#66591=CARTESIAN_POINT('Ctrl Pts',(28.6307275649839,-0.641599855569549,
24.7231444364205));
#66592=CARTESIAN_POINT('Ctrl Pts',(28.5125127288929,-0.274334472746556,
24.7027408040415));
#66593=CARTESIAN_POINT('Ctrl Pts',(28.4895069858667,-0.0792389156648355,
24.6919021619814));
#66594=CARTESIAN_POINT('Ctrl Pts',(28.5196116095794,0.313003938746328,24.6701108922919));
#66595=CARTESIAN_POINT('Ctrl Pts',(28.5740816740222,0.506262436197778,24.6593743091001));
#66596=CARTESIAN_POINT('Ctrl Pts',(28.7511791399573,0.852358280491469,24.640146762195));
#66597=CARTESIAN_POINT('Ctrl Pts',(28.8690245914396,1.00348928998653,24.630706043882));
#66598=CARTESIAN_POINT('Ctrl Pts',(29.1601188576535,1.25831795738381,24.6096221903744));
#66599=CARTESIAN_POINT('Ctrl Pts',(29.3323550489326,1.35757677634782,24.5985782833421));
#66600=CARTESIAN_POINT('Ctrl Pts',(29.7064392762191,1.4842685830248,24.577060930713));
#66601=CARTESIAN_POINT('Ctrl Pts',(29.9047304118308,1.51001063736079,24.5673617334579));
#66602=CARTESIAN_POINT('Ctrl Pts',(30.2937060245362,1.48342562743484,24.547908663068));
#66603=CARTESIAN_POINT('Ctrl Pts',(30.4808263548115,1.43373651283452,24.5375255787967));
#66604=CARTESIAN_POINT('Ctrl Pts',(30.8329282215013,1.26331849859809,24.5158512361083));
#66605=CARTESIAN_POINT('Ctrl Pts',(30.9932828024692,1.14155315563778,24.5047538020966));
#66606=CARTESIAN_POINT('Ctrl Pts',(31.2521599269974,0.847929325410954,24.4841423531291));
#66607=CARTESIAN_POINT('Ctrl Pts',(31.3503160471837,0.680833771104865,24.4753240983947));
#66608=CARTESIAN_POINT('Ctrl Pts',(31.4789636487266,0.316753550496772,24.455097419472));
#66609=CARTESIAN_POINT('Ctrl Pts',(31.5074931621648,0.122957581810777,24.4443309767673));
#66610=CARTESIAN_POINT('Ctrl Pts',(31.4889302469637,-0.269482846800126,
24.4225287307333));
#66611=CARTESIAN_POINT('Ctrl Pts',(31.4401374224707,-0.464284058469581,
24.4117064411961));
#66612=CARTESIAN_POINT('Ctrl Pts',(31.2732400969951,-0.815428064678723,
24.3921984408512));
#66613=CARTESIAN_POINT('Ctrl Pts',(31.1598920572171,-0.96991270557316,24.3830299796895));
#66614=CARTESIAN_POINT('Ctrl Pts',(30.8768520990815,-1.23274788918355,24.3621112360319));
#66615=CARTESIAN_POINT('Ctrl Pts',(30.7081704356177,-1.33679806788068,24.351105252973));
#66616=CARTESIAN_POINT('Ctrl Pts',(30.3563528915165,-1.46803396077468,24.330532982021));
#66617=CARTESIAN_POINT('Ctrl Pts',(30.1788031709794,-1.50000000000002,24.3211026715747));
#66618=CARTESIAN_POINT('Ctrl Pts',(29.9999999999999,-1.50000000000001,24.3125));
#66619=CARTESIAN_POINT('Origin',(30.,-1.32966554433622E-14,16.));
#66620=CARTESIAN_POINT('',(29.9999999999999,-1.50000000000001,23.75));
#66621=CARTESIAN_POINT('',(30.,-1.50000000000001,23.8125));
#66622=CARTESIAN_POINT('',(30.,-1.50000000000001,16.));
#66623=CARTESIAN_POINT('Ctrl Pts',(29.9999999999998,-1.50000000000001,23.75));
#66624=CARTESIAN_POINT('Ctrl Pts',(30.1539214445734,-1.50000000000004,23.7574055489549));
#66625=CARTESIAN_POINT('Ctrl Pts',(30.3071622224275,-1.47631426128188,23.7654362865035));
#66626=CARTESIAN_POINT('Ctrl Pts',(30.6423330661034,-1.36978679250727,23.7845212975935));
#66627=CARTESIAN_POINT('Ctrl Pts',(30.8166966283757,-1.27354330571266,23.7955837985834));
#66628=CARTESIAN_POINT('Ctrl Pts',(31.1127372375018,-1.02370190976136,23.8167670978074));
#66629=CARTESIAN_POINT('Ctrl Pts',(31.2333636655921,-0.874601042154043,
23.8264110532137));
#66630=CARTESIAN_POINT('Ctrl Pts',(31.4166526755054,-0.531631844802988,
23.8454648975109));
#66631=CARTESIAN_POINT('Ctrl Pts',(31.4745582697856,-0.339396978512901,
23.8561446123048));
#66632=CARTESIAN_POINT('Ctrl Pts',(31.511699941184,0.0525578729813968,23.8779198818323));
#66633=CARTESIAN_POINT('Ctrl Pts',(31.4920858025539,0.248369535334408,23.8887983075186));
#66634=CARTESIAN_POINT('Ctrl Pts',(31.3802343334373,0.617537171179423,23.909307620621));
#66635=CARTESIAN_POINT('Ctrl Pts',(31.2906053859832,0.78786629286171,23.9181242275504));
#66636=CARTESIAN_POINT('Ctrl Pts',(31.0463195284336,1.0933231170364,23.9383623481344));
#66637=CARTESIAN_POINT('Ctrl Pts',(30.8911113639651,1.22312916938911,23.9494355281055));
#66638=CARTESIAN_POINT('Ctrl Pts',(30.5456512461468,1.41045613992281,23.9712600127329));
#66639=CARTESIAN_POINT('Ctrl Pts',(30.3601397930707,1.4688221637187,23.9818067151192));
#66640=CARTESIAN_POINT('Ctrl Pts',(29.9746198000426,1.51244309002935,24.0015667468295));
#66641=CARTESIAN_POINT('Ctrl Pts',(29.7781833324316,1.4963071428617,24.0107747387592));
#66642=CARTESIAN_POINT('Ctrl Pts',(29.3999877237922,1.38893180194388,24.0319533318226));
#66643=CARTESIAN_POINT('Ctrl Pts',(29.222220687541,1.29776778429998,24.0430384861654));
#66644=CARTESIAN_POINT('Ctrl Pts',(28.9180417312452,1.05625627096343,24.0643819561719));
#66645=CARTESIAN_POINT('Ctrl Pts',(28.7928010889864,0.910453809129913,24.0744192328261));
#66646=CARTESIAN_POINT('Ctrl Pts',(28.5994385143727,0.572669994103534,24.0931850003275));
#66647=CARTESIAN_POINT('Ctrl Pts',(28.5359684061524,0.382240685005912,24.1037644063885));
#66648=CARTESIAN_POINT('Ctrl Pts',(28.4873420883061,-0.00897112678811804,
24.1254983959326));
#66649=CARTESIAN_POINT('Ctrl Pts',(28.5013820601517,-0.205827079960202,
24.1364348377755));
#66650=CARTESIAN_POINT('Ctrl Pts',(28.6028303892674,-0.578036208077185,
24.1571131226709));
#66651=CARTESIAN_POINT('Ctrl Pts',(28.6873275910153,-0.750394994115161,
24.1660216580016));
#66652=CARTESIAN_POINT('Ctrl Pts',(28.922674074919,-1.0628953635868,24.1860253368065));
#66653=CARTESIAN_POINT('Ctrl Pts',(29.0745736829203,-1.19747470970914,24.197071925274));
#66654=CARTESIAN_POINT('Ctrl Pts',(29.4156235588556,-1.39492862582615,24.2189655260838));
#66655=CARTESIAN_POINT('Ctrl Pts',(29.5999664963488,-1.45853020454807,24.2296014403193));
#66656=CARTESIAN_POINT('Ctrl Pts',(29.8606029709014,-1.49514680076604,24.2431584462207));
#66657=CARTESIAN_POINT('Ctrl Pts',(29.9303308703141,-1.50000000000001,24.2466480424351));
#66658=CARTESIAN_POINT('Ctrl Pts',(29.9999999999999,-1.50000000000001,24.25));
#66659=CARTESIAN_POINT('Ctrl Pts',(29.9999999999999,-1.50000000000001,24.3125));
#66660=CARTESIAN_POINT('Ctrl Pts',(29.9792133017942,-1.50000000000001,24.3114998995163));
#66661=CARTESIAN_POINT('Ctrl Pts',(29.9584107993835,-1.49956791710601,24.3104870363498));
#66662=CARTESIAN_POINT('Ctrl Pts',(29.7464034347025,-1.4907415866322,24.3000416514142));
#66663=CARTESIAN_POINT('Ctrl Pts',(29.5585103106211,-1.44626636462019,24.2897662164333));
#66664=CARTESIAN_POINT('Ctrl Pts',(29.2028124426411,-1.28608329400307,24.2682031650416));
#66665=CARTESIAN_POINT('Ctrl Pts',(29.0395645726164,-1.16922656097766,24.2571028778712));
#66666=CARTESIAN_POINT('Ctrl Pts',(28.7720346147835,-0.882829614311603,
24.2362758660328));
#66667=CARTESIAN_POINT('Ctrl Pts',(28.6687223598358,-0.717623891574991,
24.2273679939764));
#66668=CARTESIAN_POINT('Ctrl Pts',(28.5302095932634,-0.356628416668571,
24.2073126898149));
#66669=CARTESIAN_POINT('Ctrl Pts',(28.4965070465723,-0.164202501526158,
24.1966223611959));
#66670=CARTESIAN_POINT('Ctrl Pts',(28.504169008249,0.22811087427228,24.1748271736516));
#66671=CARTESIAN_POINT('Ctrl Pts',(28.547551398078,0.424213342298486,24.1639325920946));
#66672=CARTESIAN_POINT('Ctrl Pts',(28.7047478969298,0.780036844220854,24.1441646197656));
#66673=CARTESIAN_POINT('Ctrl Pts',(28.8139070776359,0.937725434330763,24.1351846602695));
#66674=CARTESIAN_POINT('Ctrl Pts',(29.089396967151,1.20794416549895,24.1144240709145));
#66675=CARTESIAN_POINT('Ctrl Pts',(29.2546507832928,1.31634974323744,24.10346202693));
#66676=CARTESIAN_POINT('Ctrl Pts',(29.6203184116569,1.46471395475137,24.0817476068599));
#66677=CARTESIAN_POINT('Ctrl Pts',(29.817562104219,1.50206749812624,24.0713349778568));
#66678=CARTESIAN_POINT('Ctrl Pts',(30.2070481745296,1.49784204922514,24.0524784469813));
#66679=CARTESIAN_POINT('Ctrl Pts',(30.3956551706626,1.45939464529562,24.0423361052064));
#66680=CARTESIAN_POINT('Ctrl Pts',(30.7551447714595,1.31111335433136,24.0209212289748));
#66681=CARTESIAN_POINT('Ctrl Pts',(30.9215534250012,1.20000288285394,24.0098284869129));
#66682=CARTESIAN_POINT('Ctrl Pts',(31.1989915137811,0.922095691461922,23.9887605964375));
#66683=CARTESIAN_POINT('Ctrl Pts',(31.3083178283937,0.759038041694919,23.9796687800942));
#66684=CARTESIAN_POINT('Ctrl Pts',(31.4580557742773,0.401642541393168,23.9598134745218));
#66685=CARTESIAN_POINT('Ctrl Pts',(31.4975752946798,0.210938880716583,23.9492188267065));
#66686=CARTESIAN_POINT('Ctrl Pts',(31.5023006219625,-0.182594498957542,
23.927355861169));
#66687=CARTESIAN_POINT('Ctrl Pts',(31.4644403140633,-0.381679718202,23.916295571211));
#66688=CARTESIAN_POINT('Ctrl Pts',(31.3164762945118,-0.74375638752885,23.8961802006929));
#66689=CARTESIAN_POINT('Ctrl Pts',(31.2115088567194,-0.904729197971778,
23.8873240471024));
#66690=CARTESIAN_POINT('Ctrl Pts',(30.9436055459159,-1.18225533242814,23.8667254837612));
#66691=CARTESIAN_POINT('Ctrl Pts',(30.7818828902994,-1.29490194314203,23.8558155263452));
#66692=CARTESIAN_POINT('Ctrl Pts',(30.4211554702292,-1.45331769745592,23.8340595826352));
#66693=CARTESIAN_POINT('Ctrl Pts',(30.225061216149,-1.49628795964726,23.8234313750427));
#66694=CARTESIAN_POINT('Ctrl Pts',(30.01751075903,-1.49992336974507,23.8133446154048));
#66695=CARTESIAN_POINT('Ctrl Pts',(30.0087538759465,-1.50000000000001,23.8129211710528));
#66696=CARTESIAN_POINT('Ctrl Pts',(30.,-1.50000000000001,23.8125));
#66697=CARTESIAN_POINT('Origin',(30.,-1.32966554433622E-14,16.));
#66698=CARTESIAN_POINT('',(30.,-1.50000000000001,23.25));
#66699=CARTESIAN_POINT('',(30.0000000000001,-1.50000000000001,23.3125));
#66700=CARTESIAN_POINT('',(30.,-1.50000000000001,16.));
#66701=CARTESIAN_POINT('Ctrl Pts',(30.,-1.50000000000001,23.25));
#66702=CARTESIAN_POINT('Ctrl Pts',(30.1848807806478,-1.50000000000001,23.2588950807062));
#66703=CARTESIAN_POINT('Ctrl Pts',(30.3682821495602,-1.46581977714696,23.268668433817));
#66704=CARTESIAN_POINT('Ctrl Pts',(30.7253175152828,-1.32777981441322,23.2896807492688));
#66705=CARTESIAN_POINT('Ctrl Pts',(30.8938177244611,-1.22072861570022,23.3007613637715));
#66706=CARTESIAN_POINT('Ctrl Pts',(31.17812266521,-0.948849031570725,23.3219922022812));
#66707=CARTESIAN_POINT('Ctrl Pts',(31.2916923057403,-0.787278580688064,
23.3312623010729));
#66708=CARTESIAN_POINT('Ctrl Pts',(31.4491725851422,-0.432421790169133,
23.3509765672128));
#66709=CARTESIAN_POINT('Ctrl Pts',(31.4926555401856,-0.243004803835009,
23.3614997331203));
#66710=CARTESIAN_POINT('Ctrl Pts',(31.5058959055076,0.149477495401521,23.3833043053001));
#66711=CARTESIAN_POINT('Ctrl Pts',(31.4725342594551,0.348889338242185,23.3943827410135));
#66712=CARTESIAN_POINT('Ctrl Pts',(31.3327988700423,0.714215497781599,23.4146786387656));
#66713=CARTESIAN_POINT('Ctrl Pts',(31.2311812032015,0.877867947558743,23.4234833208414));
#66714=CARTESIAN_POINT('Ctrl Pts',(30.9693523131294,1.16116792111582,23.4439500128983));
#66715=CARTESIAN_POINT('Ctrl Pts',(30.8105149834806,1.27711053175663,23.4548127055575));
#66716=CARTESIAN_POINT('Ctrl Pts',(30.4538126686857,1.44345770015622,23.4765953083576));
#66717=CARTESIAN_POINT('Ctrl Pts',(30.2587086794859,1.49084210066152,23.487298486762));
#66718=CARTESIAN_POINT('Ctrl Pts',(29.8701963712835,1.50640033026212,23.5064229669502));
#66719=CARTESIAN_POINT('Ctrl Pts',(29.6806119299331,1.47787523708767,23.5159811423084));
#66720=CARTESIAN_POINT('Ctrl Pts',(29.3158918902727,1.34932104216597,23.5370996932649));
#66721=CARTESIAN_POINT('Ctrl Pts',(29.1450773397405,1.24811033609704,23.5481294207781));
#66722=CARTESIAN_POINT('Ctrl Pts',(28.8572342555358,0.990033097118328,23.5691470898178));
#66723=CARTESIAN_POINT('Ctrl Pts',(28.741208429162,0.837555866674711,23.578469118518));
#66724=CARTESIAN_POINT('Ctrl Pts',(28.5682103547001,0.489415671302002,23.5978102404832));
#66725=CARTESIAN_POINT('Ctrl Pts',(28.5160198061383,0.295515658346084,23.6085824634252));
#66726=CARTESIAN_POINT('Ctrl Pts',(28.4905622848027,-0.0968477988030621,
23.6303804332668));
#66727=CARTESIAN_POINT('Ctrl Pts',(28.5157978904665,-0.291438773395986,
23.6411910429664));
#66728=CARTESIAN_POINT('Ctrl Pts',(28.6382130227664,-0.657431308298791,
23.6615239615721));
#66729=CARTESIAN_POINT('Ctrl Pts',(28.733169022031,-0.825722839750627,23.6703196450362));
#66730=CARTESIAN_POINT('Ctrl Pts',(28.9866100524997,-1.12380536152502,23.6907934023492));
#66731=CARTESIAN_POINT('Ctrl Pts',(29.1450855427347,-1.24860164286396,23.7018846212987));
#66732=CARTESIAN_POINT('Ctrl Pts',(29.4947960835532,-1.42537206508902,23.723620367045));
#66733=CARTESIAN_POINT('Ctrl Pts',(29.6813612118254,-1.47831159941945,23.7340670285844));
#66734=CARTESIAN_POINT('Ctrl Pts',(29.9152096611065,-1.49820471212254,23.7458706538102));
#66735=CARTESIAN_POINT('Ctrl Pts',(29.957628226374,-1.50000000000001,23.7479613870909));
#66736=CARTESIAN_POINT('Ctrl Pts',(29.9999999999998,-1.50000000000001,23.75));
#66737=CARTESIAN_POINT('Ctrl Pts',(30.,-1.50000000000001,23.8125));
#66738=CARTESIAN_POINT('Ctrl Pts',(29.8186899108673,-1.50000000000001,23.8037767142694));
#66739=CARTESIAN_POINT('Ctrl Pts',(29.6387564217711,-1.46712852254306,23.7942065636429));
#66740=CARTESIAN_POINT('Ctrl Pts',(29.284195027604,-1.33291119731626,23.7734194615783));
#66741=CARTESIAN_POINT('Ctrl Pts',(29.1150531352934,-1.22715164870581,23.762343853251));
#66742=CARTESIAN_POINT('Ctrl Pts',(28.8285848658366,-0.957196675383623,
23.7410623929517));
#66743=CARTESIAN_POINT('Ctrl Pts',(28.713664846415,-0.796095622176884,23.7317275345654));
#66744=CARTESIAN_POINT('Ctrl Pts',(28.5537507892143,-0.442046290271719,
23.7120581272374));
#66745=CARTESIAN_POINT('Ctrl Pts',(28.50903084701,-0.253050072432249,23.7015583373574));
#66746=CARTESIAN_POINT('Ctrl Pts',(28.493125704307,0.139065210502765,23.6797741549721));
#66747=CARTESIAN_POINT('Ctrl Pts',(28.5250759127101,0.338559440554235,23.6686911421915));
#66748=CARTESIAN_POINT('Ctrl Pts',(28.6622225705316,0.704891738980156,23.6483393478345));
#66749=CARTESIAN_POINT('Ctrl Pts',(28.7627930544851,0.869391639366899,23.6395420458263));
#66750=CARTESIAN_POINT('Ctrl Pts',(29.0227223626785,1.15448356589741,23.6191169709735));
#66751=CARTESIAN_POINT('Ctrl Pts',(29.1806474642266,1.27143845898823,23.6082700489523));
#66752=CARTESIAN_POINT('Ctrl Pts',(29.5360600403599,1.4402358268239,23.5864814376371));
#66753=CARTESIAN_POINT('Ctrl Pts',(29.7308346201,1.48899068833401,23.5757560395914));
#66754=CARTESIAN_POINT('Ctrl Pts',(30.1191927262396,1.50727161649964,23.5565633479378));
#66755=CARTESIAN_POINT('Ctrl Pts',(30.3089226794933,1.48009155403507,23.5470839383266));
#66756=CARTESIAN_POINT('Ctrl Pts',(30.6746275130695,1.35410584970156,23.5259893534154));
#66757=CARTESIAN_POINT('Ctrl Pts',(30.8462644331352,1.25401826984556,23.5149512576394));
#66758=CARTESIAN_POINT('Ctrl Pts',(31.1359831388577,0.997812339501797,23.4938953285128));
#66759=CARTESIAN_POINT('Ctrl Pts',(31.2530579642409,0.846112941875841,23.4845062745487));
#66760=CARTESIAN_POINT('Ctrl Pts',(31.4284239202414,0.499151075957345,23.465230615331));
#66761=CARTESIAN_POINT('Ctrl Pts',(31.4819315716114,0.305618089705,23.4544787827614));
#66762=CARTESIAN_POINT('Ctrl Pts',(31.5100720569101,-0.086682490418841,
23.4326843060879));
#66763=CARTESIAN_POINT('Ctrl Pts',(31.4861228872238,-0.281567854400411,
23.4218573414222));
#66764=CARTESIAN_POINT('Ctrl Pts',(31.3661326726942,-0.648296896097567,
23.4014835057724));
#66765=CARTESIAN_POINT('Ctrl Pts',(31.2724103712455,-0.817054396960877,
23.3926895837254));
#66766=CARTESIAN_POINT('Ctrl Pts',(31.0210775409326,-1.11685004948265,23.3722696702745));
#66767=CARTESIAN_POINT('Ctrl Pts',(30.8633432283804,-1.24281066274781,23.3611817686994));
#66768=CARTESIAN_POINT('Ctrl Pts',(30.5145869816219,-1.42202815813894,23.3394239621929));
#66769=CARTESIAN_POINT('Ctrl Pts',(30.3282514191413,-1.47622279958149,23.3289534815563));
#66770=CARTESIAN_POINT('Ctrl Pts',(30.0912045055574,-1.4979228580024,23.3169457772084));
#66771=CARTESIAN_POINT('Ctrl Pts',(30.0455768509778,-1.50000000000001,23.3146928172651));
#66772=CARTESIAN_POINT('Ctrl Pts',(30.0000000000002,-1.50000000000001,23.3125));
#66773=CARTESIAN_POINT('Origin',(30.,-1.32966554433622E-14,16.));
#66774=CARTESIAN_POINT('',(30.0000000000001,-1.50000000000001,22.75));
#66775=CARTESIAN_POINT('',(30.,-1.50000000000001,22.8125));
#66776=CARTESIAN_POINT('',(30.,-1.50000000000001,16.));
#66777=CARTESIAN_POINT('Ctrl Pts',(30.0000000000001,-1.50000000000001,22.75));
#66778=CARTESIAN_POINT('Ctrl Pts',(30.0238190927805,-1.50000000000001,22.7511459966357));
#66779=CARTESIAN_POINT('Ctrl Pts',(30.0476581179369,-1.49943265781826,22.7523087117734));
#66780=CARTESIAN_POINT('Ctrl Pts',(30.2627622738244,-1.48916810759789,22.7629430416939));
#66781=CARTESIAN_POINT('Ctrl Pts',(30.4504917710081,-1.44350305068679,22.7732436551414));
#66782=CARTESIAN_POINT('Ctrl Pts',(30.8053949324493,-1.28097942369943,22.7948334866517));
#66783=CARTESIAN_POINT('Ctrl Pts',(30.9679955997388,-1.16299746502374,22.8059338915341));
#66784=CARTESIAN_POINT('Ctrl Pts',(31.2335580340327,-0.874942371993705,
22.8267123004732));
#66785=CARTESIAN_POINT('Ctrl Pts',(31.3356903480274,-0.709308500806453,
22.8355939721774));
#66786=CARTESIAN_POINT('Ctrl Pts',(31.4719653898389,-0.347606806174152,
22.8556885107681));
#66787=CARTESIAN_POINT('Ctrl Pts',(31.5044992018676,-0.154858219876142,
22.8663967655625));
#66788=CARTESIAN_POINT('Ctrl Pts',(31.4943665307067,0.237510688978279,22.8881950382766));
#66789=CARTESIAN_POINT('Ctrl Pts',(31.4497537465181,0.433331528903234,22.899073973828));
#66790=CARTESIAN_POINT('Ctrl Pts',(31.2903519524536,0.78810181728577,22.9187834342937));
#66791=CARTESIAN_POINT('Ctrl Pts',(31.1802475750943,0.945060620681391,22.9278003293086));
#66792=CARTESIAN_POINT('Ctrl Pts',(30.9030507590494,1.21362000516214,22.948596950241));
#66793=CARTESIAN_POINT('Ctrl Pts',(30.7370141991215,1.32105257322674,22.9595696259569));
#66794=CARTESIAN_POINT('Ctrl Pts',(30.3702805499944,1.46712017353723,22.9812715402192));
#66795=CARTESIAN_POINT('Ctrl Pts',(30.1727871861063,1.50321114583692,22.991597574137));
#66796=CARTESIAN_POINT('Ctrl Pts',(29.7831928098337,1.49647610979574,23.0105290266394));
#66797=CARTESIAN_POINT('Ctrl Pts',(29.5947193673977,1.45676699750561,23.0206999902635));
#66798=CARTESIAN_POINT('Ctrl Pts',(29.2359911149794,1.30598838211349,23.0421476062271));
#66799=CARTESIAN_POINT('Ctrl Pts',(29.0702277888966,1.19366882317697,23.05324288572));
#66800=CARTESIAN_POINT('Ctrl Pts',(28.7948557226535,0.913971635465609,23.0742610967597));
#66801=CARTESIAN_POINT('Ctrl Pts',(28.686793719435,0.750466721324838,23.0833074043708));
#66802=CARTESIAN_POINT('Ctrl Pts',(28.5393908078851,0.39231449396832,23.1032047503351));
#66803=CARTESIAN_POINT('Ctrl Pts',(28.50107471408,0.201238476218244,23.1138200846545));
#66804=CARTESIAN_POINT('Ctrl Pts',(28.4989279287216,-0.192576857122968,
23.1356987142846));
#66805=CARTESIAN_POINT('Ctrl Pts',(28.5381471159066,-0.391544240809387,
23.1467524578227));
#66806=CARTESIAN_POINT('Ctrl Pts',(28.6885908974138,-0.752626531003943,
23.1668125850557));
#66807=CARTESIAN_POINT('Ctrl Pts',(28.7945746463293,-0.912795946069086,
23.1756927219105));
#66808=CARTESIAN_POINT('Ctrl Pts',(29.0643193882896,-1.1885583990927,23.1963308899987));
#66809=CARTESIAN_POINT('Ctrl Pts',(29.2269067570048,-1.30018824275338,23.2072542074138));
#66810=CARTESIAN_POINT('Ctrl Pts',(29.5888237919401,-1.45617120236401,23.228999808865));
#66811=CARTESIAN_POINT('Ctrl Pts',(29.7851989650319,-1.49779418034797,23.2396041076185));
#66812=CARTESIAN_POINT('Ctrl Pts',(29.9893352495882,-1.49997157194577,23.2494861022884));
#66813=CARTESIAN_POINT('Ctrl Pts',(29.9946682024469,-1.50000000000001,23.2497434737706));
#66814=CARTESIAN_POINT('Ctrl Pts',(30.,-1.50000000000001,23.25));
#66815=CARTESIAN_POINT('Ctrl Pts',(30.0000000000003,-1.50000000000001,23.3125));
#66816=CARTESIAN_POINT('Ctrl Pts',(29.8497176527518,-1.50000000000002,23.3052695371968));
#66817=CARTESIAN_POINT('Ctrl Pts',(29.7000480379928,-1.47742120454004,23.2974413657365));
#66818=CARTESIAN_POINT('Ctrl Pts',(29.3674490033452,-1.37435151569836,23.2785761403087));
#66819=CARTESIAN_POINT('Ctrl Pts',(29.1922818901849,-1.27927791742795,23.2675074753621));
#66820=CARTESIAN_POINT('Ctrl Pts',(28.8943459539799,-1.03136235914611,23.2462864826624));
#66821=CARTESIAN_POINT('Ctrl Pts',(28.7726494682524,-0.883034040962408,
23.2365574467202));
#66822=CARTESIAN_POINT('Ctrl Pts',(28.5870020748245,-0.541267982453404,
23.2175704434697));
#66823=CARTESIAN_POINT('Ctrl Pts',(28.5277906685824,-0.349440299767995,
23.2069133499871));
#66824=CARTESIAN_POINT('Ctrl Pts',(28.487963650694,0.0423711662580389,23.185146046319));
#66825=CARTESIAN_POINT('Ctrl Pts',(28.5062787794266,0.238440842104816,23.1742532865498));
#66826=CARTESIAN_POINT('Ctrl Pts',(28.6157002622386,0.608326552071247,23.1537040804405));
#66827=CARTESIAN_POINT('Ctrl Pts',(28.704120723826,0.779127514930934,23.1448722564411));
#66828=CARTESIAN_POINT('Ctrl Pts',(28.9463114752997,1.08624863564316,23.1246887062359));
#66829=CARTESIAN_POINT('Ctrl Pts',(29.100754465216,1.21718400346422,23.1136209708684));
#66830=CARTESIAN_POINT('Ctrl Pts',(29.4452036060534,1.40690072974557,23.0917787447896));
#66831=CARTESIAN_POINT('Ctrl Pts',(29.630453412942,1.46649956876065,23.0812103859941));
#66832=CARTESIAN_POINT('Ctrl Pts',(30.0154678344856,1.51253258675255,23.0614076760565));
#66833=CARTESIAN_POINT('Ctrl Pts',(30.2116518417758,1.49773354664468,23.052253938977));
#66834=CARTESIAN_POINT('Ctrl Pts',(30.5903886500576,1.39306917025536,23.031124612004));
#66835=CARTESIAN_POINT('Ctrl Pts',(30.7689034771477,1.3030667277533,23.0200357455338));
#66836=CARTESIAN_POINT('Ctrl Pts',(31.0748241700176,1.06351798971685,22.9986629977234));
#66837=CARTESIAN_POINT('Ctrl Pts',(31.2011381587389,0.918481956232081,22.9885569343996));
#66838=CARTESIAN_POINT('Ctrl Pts',(31.3967520547264,0.581861797904625,22.9697948964873));
#66839=CARTESIAN_POINT('Ctrl Pts',(31.4615014415134,0.391859484339943,22.9592699713522));
#66840=CARTESIAN_POINT('Ctrl Pts',(31.5127002734739,0.000740375396987882,
22.9375411319665));
#66841=CARTESIAN_POINT('Ctrl Pts',(31.4999079686113,-0.196327016676456,
22.9265929435179));
#66842=CARTESIAN_POINT('Ctrl Pts',(31.4007804390091,-0.569202940848263,
22.9058776143973));
#66843=CARTESIAN_POINT('Ctrl Pts',(31.3174135571943,-0.742018160934012,
22.8969391404085));
#66844=CARTESIAN_POINT('Ctrl Pts',(31.0853396535684,-1.05432624095891,22.8770982550692));
#66845=CARTESIAN_POINT('Ctrl Pts',(30.9361334950341,-1.18878161757634,22.8661846988469));
#66846=CARTESIAN_POINT('Ctrl Pts',(30.5987439832112,-1.38884930936682,22.8443946025078));
#66847=CARTESIAN_POINT('Ctrl Pts',(30.4148754905707,-1.45440359104526,22.8337272732621));
#66848=CARTESIAN_POINT('Ctrl Pts',(30.1494349053273,-1.49442202191131,22.8198446340705));
#66849=CARTESIAN_POINT('Ctrl Pts',(30.0746909808563,-1.50000000000001,22.816093571492));
#66850=CARTESIAN_POINT('Ctrl Pts',(30.0000000000001,-1.50000000000001,22.8125));
#66851=CARTESIAN_POINT('Origin',(30.,-1.32966554433622E-14,16.));
#66852=CARTESIAN_POINT('',(30.0000000000001,-1.50000000000001,22.25));
#66853=CARTESIAN_POINT('',(30.,-1.50000000000001,22.3125));
#66854=CARTESIAN_POINT('',(30.,-1.50000000000001,16.));
#66855=CARTESIAN_POINT('Ctrl Pts',(30.0000000000002,-1.50000000000001,22.25));
#66856=CARTESIAN_POINT('Ctrl Pts',(30.0511677444063,-1.50000000000001,22.2524618092506));
#66857=CARTESIAN_POINT('Ctrl Pts',(30.1023921263505,-1.49738203467576,22.254999064735));
#66858=CARTESIAN_POINT('Ctrl Pts',(30.3449868915282,-1.47242953219059,22.2673640358856));
#66859=CARTESIAN_POINT('Ctrl Pts',(30.5309019965201,-1.41604718249647,22.2778750569255));
#66860=CARTESIAN_POINT('Ctrl Pts',(30.8779534991821,-1.23257211766357,22.2996691097112));
#66861=CARTESIAN_POINT('Ctrl Pts',(31.0343750352224,-1.10459007945506,22.3107500009898));
#66862=CARTESIAN_POINT('Ctrl Pts',(31.2820199524192,-0.801819415517196,
22.3310751188442));
#66863=CARTESIAN_POINT('Ctrl Pts',(31.3735944009353,-0.632242273686504,
22.3398754292397));
#66864=CARTESIAN_POINT('Ctrl Pts',(31.4893318529591,-0.264232559817084,
22.3603204133435));
#66865=CARTESIAN_POINT('Ctrl Pts',(31.511019003439,-0.0688512669519718,
22.3711749296138));
#66866=CARTESIAN_POINT('Ctrl Pts',(31.4781740542578,0.32329452926424,22.3929608071814));
#66867=CARTESIAN_POINT('Ctrl Pts',(31.422363807823,0.516161881943181,22.403675660108));
#66868=CARTESIAN_POINT('Ctrl Pts',(31.2428531453717,0.861044634974944,22.4228358130542));
#66869=CARTESIAN_POINT('Ctrl Pts',(31.1239285676202,1.01138399102137,22.4323522946618));
#66870=CARTESIAN_POINT('Ctrl Pts',(30.8309115401787,1.26428053578999,22.4534749869891));
#66871=CARTESIAN_POINT('Ctrl Pts',(30.6578432463629,1.3623737449238,22.4645265505225));
#66872=CARTESIAN_POINT('Ctrl Pts',(30.2831279004866,1.48623532989505,22.4859956505893));
#66873=CARTESIAN_POINT('Ctrl Pts',(30.0851137662052,1.5105602610331,22.49561162143));
#66874=CARTESIAN_POINT('Ctrl Pts',(29.6966286981958,1.48149502237994,22.5151099857196));
#66875=CARTESIAN_POINT('Ctrl Pts',(29.5097167303907,1.43054672747056,22.5255180223776));
#66876=CARTESIAN_POINT('Ctrl Pts',(29.1585275612845,1.25766527467259,22.547216881732));
#66877=CARTESIAN_POINT('Ctrl Pts',(28.9988940242273,1.13472310971196,22.5583123140024));
#66878=CARTESIAN_POINT('Ctrl Pts',(28.7421191463059,0.839368453848379,22.5788706970727));
#66879=CARTESIAN_POINT('Ctrl Pts',(28.6452032661271,0.671810533827306,22.5876771925652));
#66880=CARTESIAN_POINT('Ctrl Pts',(28.5189623058816,0.306989072921277,22.6079450515044));
#66881=CARTESIAN_POINT('Ctrl Pts',(28.4917024287485,0.112879611784448,22.6187289104564));
#66882=CARTESIAN_POINT('Ctrl Pts',(28.5129271256702,-0.27954553838217,22.6405303076879));
#66883=CARTESIAN_POINT('Ctrl Pts',(28.5630339289139,-0.474005993650327,
22.6513336663139));
#66884=CARTESIAN_POINT('Ctrl Pts',(28.7322894218787,-0.823994430176359,
22.6707774683431));
#66885=CARTESIAN_POINT('Ctrl Pts',(28.8466683628132,-0.977702516203741,
22.680002042295));
#66886=CARTESIAN_POINT('Ctrl Pts',(29.1315598866997,-1.23870928805523,22.7009590802358));
#66887=CARTESIAN_POINT('Ctrl Pts',(29.301068288962,-1.34167114530826,22.7119746086325));
#66888=CARTESIAN_POINT('Ctrl Pts',(29.6506233621551,-1.46928601783117,22.732337442503));
#66889=CARTESIAN_POINT('Ctrl Pts',(29.8247316115896,-1.50000000000001,22.7415673957309));
#66890=CARTESIAN_POINT('Ctrl Pts',(30.0000000000001,-1.50000000000001,22.75));
#66891=CARTESIAN_POINT('Ctrl Pts',(30.0000000000001,-1.50000000000001,22.8125));
#66892=CARTESIAN_POINT('Ctrl Pts',(29.8821180181442,-1.50000000000001,22.8068284005036));
#66893=CARTESIAN_POINT('Ctrl Pts',(29.7644054408515,-1.48610745961779,22.8007790475884));
#66894=CARTESIAN_POINT('Ctrl Pts',(29.4561358619788,-1.41197523055228,22.7838881919746));
#66895=CARTESIAN_POINT('Ctrl Pts',(29.2741386603191,-1.32762177587115,22.7727886960081));
#66896=CARTESIAN_POINT('Ctrl Pts',(28.9596308471203,-1.09734948081223,22.7512604791499));
#66897=CARTESIAN_POINT('Ctrl Pts',(28.8283658665089,-0.955949757636784,
22.7410172197375));
#66898=CARTESIAN_POINT('Ctrl Pts',(28.6210784753189,-0.623528783846783,
22.7218101845402));
#66899=CARTESIAN_POINT('Ctrl Pts',(28.550139211662,-0.43377020073728,22.7115983444854));
#66900=CARTESIAN_POINT('Ctrl Pts',(28.4878128315539,-0.0419315259951405,
22.6898295292219));
#66901=CARTESIAN_POINT('Ctrl Pts',(28.4952899772074,0.155946448584049,22.678836308412));
#66902=CARTESIAN_POINT('Ctrl Pts',(28.5845546436209,0.531607574681399,22.657966245851));
#66903=CARTESIAN_POINT('Ctrl Pts',(28.6631729955745,0.706378968214403,22.6488631478995));
#66904=CARTESIAN_POINT('Ctrl Pts',(28.886581089556,1.02462509962909,22.6292742506491));
#66905=CARTESIAN_POINT('Ctrl Pts',(29.0320840520478,1.16304620087307,22.6184287055121));
#66906=CARTESIAN_POINT('Ctrl Pts',(29.3643456686259,1.37241961531272,22.5966268328521));
#66907=CARTESIAN_POINT('Ctrl Pts',(29.5468906971467,1.44301653433814,22.585883105544));
#66908=CARTESIAN_POINT('Ctrl Pts',(29.9272228832809,1.51053148619831,22.5657089493774));
#66909=CARTESIAN_POINT('Ctrl Pts',(30.1212939503538,1.50741198602448,22.5568701305933));
#66910=CARTESIAN_POINT('Ctrl Pts',(30.5044378408363,1.42661367919911,22.5361917141558));
#66911=CARTESIAN_POINT('Ctrl Pts',(30.6892182911204,1.34709011542225,22.5250924727137));
#66912=CARTESIAN_POINT('Ctrl Pts',(31.0107046879826,1.12481571216727,22.5034506622537));
#66913=CARTESIAN_POINT('Ctrl Pts',(31.1460355364563,0.986589014961116,22.4930999232927));
#66914=CARTESIAN_POINT('Ctrl Pts',(31.3611183370781,0.66090197936205,22.473704885123));
#66915=CARTESIAN_POINT('Ctrl Pts',(31.4365760335144,0.475089538086611,22.463893863227));
#66916=CARTESIAN_POINT('Ctrl Pts',(31.5103576978905,0.0866802952431828,
22.4423155719579));
#66917=CARTESIAN_POINT('Ctrl Pts',(31.5086976507443,-0.111919508747406,
22.431282249514));
#66918=CARTESIAN_POINT('Ctrl Pts',(31.4301969979147,-0.490528747223499,
22.410248402932));
#66919=CARTESIAN_POINT('Ctrl Pts',(31.3566667795852,-0.667467593155736,
22.4008985610562));
#66920=CARTESIAN_POINT('Ctrl Pts',(31.1425983489439,-0.991976419659515,
22.3815850548154));
#66921=CARTESIAN_POINT('Ctrl Pts',(31.0011829334274,-1.13452992378446,22.370821382905));
#66922=CARTESIAN_POINT('Ctrl Pts',(30.6747026750166,-1.35372782384191,22.3490247635913));
#66923=CARTESIAN_POINT('Ctrl Pts',(30.4937271061129,-1.42970164427305,22.3382071885718));
#66924=CARTESIAN_POINT('Ctrl Pts',(30.2032733713701,-1.48966742655325,22.322567010569));
#66925=CARTESIAN_POINT('Ctrl Pts',(30.1016602333963,-1.50000000000001,22.3173911302598));
#66926=CARTESIAN_POINT('Ctrl Pts',(30.,-1.50000000000001,22.3125));
#66927=CARTESIAN_POINT('Origin',(30.,-1.32966554433622E-14,16.));
#66928=CARTESIAN_POINT('',(30.,-1.50000000000001,21.75));
#66929=CARTESIAN_POINT('',(29.9999999999999,-1.50000000000001,21.8125));
#66930=CARTESIAN_POINT('',(30.,-1.50000000000001,16.));
#66931=CARTESIAN_POINT('Ctrl Pts',(30.,-1.50000000000001,21.75));
#66932=CARTESIAN_POINT('Ctrl Pts',(30.0799345840677,-1.50000000000001,21.7538458544691));
#66933=CARTESIAN_POINT('Ctrl Pts',(30.1599122998412,-1.4936114408734,21.7578712440892));
#66934=CARTESIAN_POINT('Ctrl Pts',(30.4303228176761,-1.44993500309235,21.7720946105773));
#66935=CARTESIAN_POINT('Ctrl Pts',(30.6136742893428,-1.38234553687229,21.7827935975436));
#66936=CARTESIAN_POINT('Ctrl Pts',(30.9490281775211,-1.17851150378185,21.8045903754862));
#66937=CARTESIAN_POINT('Ctrl Pts',(31.096754819913,-1.04244516916321,21.8154774972882));
#66938=CARTESIAN_POINT('Ctrl Pts',(31.3253413942278,-0.727732251316939,
21.8352173994684));
#66939=CARTESIAN_POINT('Ctrl Pts',(31.4067935410376,-0.554135842314364,
21.8442146754271));
#66940=CARTESIAN_POINT('Ctrl Pts',(31.5019658936778,-0.180133518226551,
21.8649925823208));
#66941=CARTESIAN_POINT('Ctrl Pts',(31.5126290136531,0.0172760533687308,
21.8759597807428));
#66942=CARTESIAN_POINT('Ctrl Pts',(31.457072059222,0.408029499969523,21.8976683055539));
#66943=CARTESIAN_POINT('Ctrl Pts',(31.3902144216195,0.597326073407902,21.9080390017153));
#66944=CARTESIAN_POINT('Ctrl Pts',(31.1907422817111,0.931962878929858,21.9269315763413));
#66945=CARTESIAN_POINT('Ctrl Pts',(31.0626495240423,1.07572029471252,21.9370877035676));
#66946=CARTESIAN_POINT('Ctrl Pts',(30.7536327605205,1.31199280194067,21.9585184047354));
#66947=CARTESIAN_POINT('Ctrl Pts',(30.5738554020277,1.39999410781883,21.9696124276475));
#66948=CARTESIAN_POINT('Ctrl Pts',(30.1942124641512,1.50002082255712,21.9906565268663));
#66949=CARTESIAN_POINT('Ctrl Pts',(29.9984550225415,1.51253833676667,21.9997260456303));
#66950=CARTESIAN_POINT('Ctrl Pts',(29.6143176021754,1.46236614670513,22.0196015378309));
#66951=CARTESIAN_POINT('Ctrl Pts',(29.4295365026789,1.40065016331119,22.0302061554976));
#66952=CARTESIAN_POINT('Ctrl Pts',(29.0868629977602,1.20683686352092,22.052076744962));
#66953=CARTESIAN_POINT('Ctrl Pts',(28.9337539891966,1.07396976987892,22.0631339581722));
#66954=CARTESIAN_POINT('Ctrl Pts',(28.6951751765203,0.763999003449345,22.0832228857165));
#66955=CARTESIAN_POINT('Ctrl Pts',(28.60882966791,0.592379173375639,22.0920900459236));
#66956=CARTESIAN_POINT('Ctrl Pts',(28.5036090779159,0.221263029136351,22.1127076094925));
#66957=CARTESIAN_POINT('Ctrl Pts',(28.4875441317865,0.0247675363524192,
22.1236240257582));
#66958=CARTESIAN_POINT('Ctrl Pts',(28.5320098906898,-0.36675262012417,22.1453751455625));
#66959=CARTESIAN_POINT('Ctrl Pts',(28.593470220051,-0.557855368091198,22.155991964894));
#66960=CARTESIAN_POINT('Ctrl Pts',(28.7831869687067,-0.897529793649072,
22.1748627663138));
#66961=CARTESIAN_POINT('Ctrl Pts',(28.9067443386156,-1.04452569047662,22.1847486483138));
#66962=CARTESIAN_POINT('Ctrl Pts',(29.2079650540828,-1.28908351396432,22.2060344096185));
#66963=CARTESIAN_POINT('Ctrl Pts',(29.3845091949262,-1.38211075548827,22.2171124835975));
#66964=CARTESIAN_POINT('Ctrl Pts',(29.7125665428598,-1.47927872450056,22.2355952603595));
#66965=CARTESIAN_POINT('Ctrl Pts',(29.8560312883098,-1.50000000000001,22.2430733021292));
#66966=CARTESIAN_POINT('Ctrl Pts',(30.0000000000002,-1.50000000000001,22.25));
#66967=CARTESIAN_POINT('Ctrl Pts',(30.,-1.50000000000001,22.3125));
#66968=CARTESIAN_POINT('Ctrl Pts',(29.9110895843884,-1.50000000000001,22.3082222956344));
#66969=CARTESIAN_POINT('Ctrl Pts',(29.8221645100457,-1.49209634975764,22.3037243401601));
#66970=CARTESIAN_POINT('Ctrl Pts',(29.5376207680931,-1.44087704391974,22.288611464497));
#66971=CARTESIAN_POINT('Ctrl Pts',(29.3500356587678,-1.36654835932947,22.2775215860335));
#66972=CARTESIAN_POINT('Ctrl Pts',(29.0213968226607,-1.15294073825471,22.2557763976293));
#66973=CARTESIAN_POINT('Ctrl Pts',(28.8818555948118,-1.01818896609304,22.2453196123919));
#66974=CARTESIAN_POINT('Ctrl Pts',(28.6586442869874,-0.699623440719697,
22.2257313109655));
#66975=CARTESIAN_POINT('Ctrl Pts',(28.5785399664869,-0.517856468116547,
22.2162698037842));
#66976=CARTESIAN_POINT('Ctrl Pts',(28.4929509348882,-0.133169441708886,
22.1948983023171));
#66977=CARTESIAN_POINT('Ctrl Pts',(28.4885197532221,0.0660037349236151,
22.1838331258375));
#66978=CARTESIAN_POINT('Ctrl Pts',(28.555761801385,0.44759093437612,22.1626338369791));
#66979=CARTESIAN_POINT('Ctrl Pts',(28.6240637192867,0.626835313372202,22.1529543398));
#66980=CARTESIAN_POINT('Ctrl Pts',(28.8284985352011,0.957663958533704,22.1339287805455));
#66981=CARTESIAN_POINT('Ctrl Pts',(28.9656007252824,1.10432288929781,22.1232585891618));
#66982=CARTESIAN_POINT('Ctrl Pts',(29.2858531479679,1.33342212875051,22.1014865695287));
#66983=CARTESIAN_POINT('Ctrl Pts',(29.4650586076933,1.41487321083335,22.0906020127698));
#66984=CARTESIAN_POINT('Ctrl Pts',(29.8404420905807,1.50363480947233,22.0700757665663));
#66985=CARTESIAN_POINT('Ctrl Pts',(30.0326825220108,1.51172235919918,22.0612531825154));
#66986=CARTESIAN_POINT('Ctrl Pts',(30.4195266402016,1.45401546056375,22.0410381667945));
#66987=CARTESIAN_POINT('Ctrl Pts',(30.6097995465824,1.38502427774371,22.029967235573));
#66988=CARTESIAN_POINT('Ctrl Pts',(30.9454244752463,1.18038733089544,22.0081351140291));
#66989=CARTESIAN_POINT('Ctrl Pts',(31.0891246269642,1.04926948856203,21.997579174969));
#66990=CARTESIAN_POINT('Ctrl Pts',(31.3204408508467,0.737906981306312,21.9778010094235));
#66991=CARTESIAN_POINT('Ctrl Pts',(31.4051230902783,0.560097094369773,21.9686165052427));
#66992=CARTESIAN_POINT('Ctrl Pts',(31.5023434434385,0.179258057369552,21.9474587809649));
#66993=CARTESIAN_POINT('Ctrl Pts',(31.5128623034415,-0.0203042234475934,
21.9363719875862));
#66994=CARTESIAN_POINT('Ctrl Pts',(31.4568810475112,-0.404757677376984,
21.9150134623679));
#66995=CARTESIAN_POINT('Ctrl Pts',(31.3937249627295,-0.586348141727015,
21.9049348418193));
#66996=CARTESIAN_POINT('Ctrl Pts',(31.1987850558466,-0.923274808506461,
21.8861967170992));
#66997=CARTESIAN_POINT('Ctrl Pts',(31.0660220732146,-1.07382111006007,21.8756273134093));
#66998=CARTESIAN_POINT('Ctrl Pts',(30.7521571303647,-1.31243843036869,21.8538982204082));
#66999=CARTESIAN_POINT('Ctrl Pts',(30.5748417786265,-1.39921326582906,21.8429567194739));
#67000=CARTESIAN_POINT('Ctrl Pts',(30.2597272838717,-1.48309858829145,21.8254656184301));
#67001=CARTESIAN_POINT('Ctrl Pts',(30.1300238421579,-1.50000000000003,21.8187557750226));
#67002=CARTESIAN_POINT('Ctrl Pts',(29.9999999999998,-1.50000000000001,21.8125));
#67003=CARTESIAN_POINT('Origin',(30.,-1.32966554433622E-14,16.));
#67004=CARTESIAN_POINT('',(30.,-1.50000000000001,21.25));
#67005=CARTESIAN_POINT('',(29.9999999999999,-1.50000000000001,21.3125));
#67006=CARTESIAN_POINT('',(30.,-1.50000000000001,16.));
#67007=CARTESIAN_POINT('Ctrl Pts',(30.,-1.50000000000001,21.25));
#67008=CARTESIAN_POINT('Ctrl Pts',(30.1075848726609,-1.50000000000001,21.2551761795993));
#67009=CARTESIAN_POINT('Ctrl Pts',(30.2150815962025,-1.48842822791985,21.2606695562356));
#67010=CARTESIAN_POINT('Ctrl Pts',(30.5108359622909,-1.42370950162225,21.2766967872056));
#67011=CARTESIAN_POINT('Ctrl Pts',(30.6910987866292,-1.34546461195666,21.2875431555427));
#67012=CARTESIAN_POINT('Ctrl Pts',(31.0150386063333,-1.12214805976604,21.3093319549459));
#67013=CARTESIAN_POINT('Ctrl Pts',(31.1546840327806,-0.977879417444189,
21.3200581109451));
#67014=CARTESIAN_POINT('Ctrl Pts',(31.3647735631693,-0.650743634461253,
21.3392531532717));
#67015=CARTESIAN_POINT('Ctrl Pts',(31.4361426481554,-0.472861434650035,
21.3487299202974));
#67016=CARTESIAN_POINT('Ctrl Pts',(31.5100129878737,-0.0930141634261118,
21.3698325464765));
#67017=CARTESIAN_POINT('Ctrl Pts',(31.5091680819865,0.105843895299734,21.3808802164057));
#67018=CARTESIAN_POINT('Ctrl Pts',(31.4305088048906,0.492738271362424,21.4023743484091));
#67019=CARTESIAN_POINT('Ctrl Pts',(31.3531309016418,0.676876453829759,21.4120329161916));
#67020=CARTESIAN_POINT('Ctrl Pts',(31.1347020158755,0.999644296815675,21.4315078542742));
#67021=CARTESIAN_POINT('Ctrl Pts',(30.9976338252526,1.13646112591015,21.4419030181452));
#67022=CARTESIAN_POINT('Ctrl Pts',(30.6731866853066,1.35520814296552,21.4635892944733));
#67023=CARTESIAN_POINT('Ctrl Pts',(30.4872391020676,1.43261266999426,21.474685827494));
#67024=CARTESIAN_POINT('Ctrl Pts',(30.1032980730075,1.50870030742653,21.4952717443516));
#67025=CARTESIAN_POINT('Ctrl Pts',(29.9096173130592,1.50952898426713,21.5040838450456));
#67026=CARTESIAN_POINT('Ctrl Pts',(29.5302606487566,1.43771855687004,21.5243303851611));
#67027=CARTESIAN_POINT('Ctrl Pts',(29.3483375586665,1.36492268311026,21.5351052715185));
#67028=CARTESIAN_POINT('Ctrl Pts',(29.0184009025148,1.15151905747937,21.5569072347786));
#67029=CARTESIAN_POINT('Ctrl Pts',(28.8745521744234,1.01139585435745,21.5677204711336));
#67030=CARTESIAN_POINT('Ctrl Pts',(28.6549505368779,0.690580628714703,21.5871975938919));
#67031=CARTESIAN_POINT('Ctrl Pts',(28.5784089748082,0.514933598952509,21.596392577836));
#67032=CARTESIAN_POINT('Ctrl Pts',(28.4935139297613,0.138064010695691,21.6173297771836));
#67033=CARTESIAN_POINT('Ctrl Pts',(28.4883967455728,-0.0601274794615553,
21.6283404155257));
#67034=CARTESIAN_POINT('Ctrl Pts',(28.5553929405263,-0.450590041266374,
21.6500327800704));
#67035=CARTESIAN_POINT('Ctrl Pts',(28.6281760530356,-0.63873783180513,21.6600741404618));
#67036=CARTESIAN_POINT('Ctrl Pts',(28.8386308155265,-0.968434016466414,
21.6793578772949));
#67037=CARTESIAN_POINT('Ctrl Pts',(28.9715505605447,-1.10856330761102,21.6896454618184));
#67038=CARTESIAN_POINT('Ctrl Pts',(29.2889068065357,-1.33562316156644,21.7112214894881));
#67039=CARTESIAN_POINT('Ctrl Pts',(29.4720453487169,-1.41803231498314,21.7223218898575));
#67040=CARTESIAN_POINT('Ctrl Pts',(29.7757758521236,-1.48742065117207,21.7388625842992));
#67041=CARTESIAN_POINT('Ctrl Pts',(29.8878284604463,-1.50000000000001,21.7446031442869));
#67042=CARTESIAN_POINT('Ctrl Pts',(30.,-1.50000000000001,21.75));
#67043=CARTESIAN_POINT('Ctrl Pts',(29.9999999999998,-1.50000000000001,21.8125));
#67044=CARTESIAN_POINT('Ctrl Pts',(29.9405204451645,-1.50000000000001,21.8096382885837));
#67045=CARTESIAN_POINT('Ctrl Pts',(29.8809833669271,-1.49646250510709,21.8066755458243));
#67046=CARTESIAN_POINT('Ctrl Pts',(29.6241950912386,-1.46572084178495,21.7934668790576));
#67047=CARTESIAN_POINT('Ctrl Pts',(29.4333772164259,-1.40302797833686,21.782544681346));
#67048=CARTESIAN_POINT('Ctrl Pts',(29.0921865820648,-1.20964665656295,21.760757435914));
#67049=CARTESIAN_POINT('Ctrl Pts',(28.9439925649252,-1.08269733302756,21.7501010778418));
#67050=CARTESIAN_POINT('Ctrl Pts',(28.7038088414644,-0.77933430694382,21.7301184823344));
#67051=CARTESIAN_POINT('Ctrl Pts',(28.6141674942217,-0.605760578772268,
21.7211533654873));
#67052=CARTESIAN_POINT('Ctrl Pts',(28.5043846389733,-0.22927416638246,21.7002374536878));
#67053=CARTESIAN_POINT('Ctrl Pts',(28.4872031236976,-0.0294943674923172,
21.6891385759717));
#67054=CARTESIAN_POINT('Ctrl Pts',(28.5307959749546,0.357711165892058,21.6676271574504));
#67055=CARTESIAN_POINT('Ctrl Pts',(28.588271358922,0.541814389624386,21.6573992005764));
#67056=CARTESIAN_POINT('Ctrl Pts',(28.7738533380075,0.887068805374046,21.6382183997014));
#67057=CARTESIAN_POINT('Ctrl Pts',(28.903512180976,1.043112470525,21.6279461150529));
#67058=CARTESIAN_POINT('Ctrl Pts',(29.2128905056455,1.29185751769652,21.6061515588234));
#67059=CARTESIAN_POINT('Ctrl Pts',(29.3882998946744,1.38356922217579,21.5951646233122));
#67060=CARTESIAN_POINT('Ctrl Pts',(29.7586487303438,1.49259838475184,21.5743176187989));
#67061=CARTESIAN_POINT('Ctrl Pts',(29.9494126813103,1.51113463524617,21.5652431789286));
#67062=CARTESIAN_POINT('Ctrl Pts',(30.3366113826679,1.4752126287187,21.5456162392091));
#67063=CARTESIAN_POINT('Ctrl Pts',(30.5290112502297,1.41763409463152,21.5347599925404));
#67064=CARTESIAN_POINT('Ctrl Pts',(30.8756573292315,1.23320190987312,21.512958859045));
#67065=CARTESIAN_POINT('Ctrl Pts',(31.0275193143428,1.10985575574539,21.5022261138206));
#67066=CARTESIAN_POINT('Ctrl Pts',(31.2750461098143,0.813213213668382,21.4820769047076));
#67067=CARTESIAN_POINT('Ctrl Pts',(31.3687657636095,0.643070885011216,21.4732261602783));
#67068=CARTESIAN_POINT('Ctrl Pts',(31.4888227697242,0.270291882918073,21.4525162157176));
#67069=CARTESIAN_POINT('Ctrl Pts',(31.5115128952941,0.0704953149593227,
21.4414164063865));
#67070=CARTESIAN_POINT('Ctrl Pts',(31.4782054807328,-0.318770290439176,
21.4197905394199));
#67071=CARTESIAN_POINT('Ctrl Pts',(31.4254475382382,-0.504803416717179,
21.4094553657378));
#67072=CARTESIAN_POINT('Ctrl Pts',(31.2494901966584,-0.853416070021567,
21.3900879961098));
#67073=CARTESIAN_POINT('Ctrl Pts',(31.1254658116588,-1.01138492328729,21.3802216401301));
#67074=CARTESIAN_POINT('Ctrl Pts',(30.8246930412984,-1.26828298434064,21.3586146462176));
#67075=CARTESIAN_POINT('Ctrl Pts',(30.6515224369356,-1.36534975789868,21.347586672365));
#67076=CARTESIAN_POINT('Ctrl Pts',(30.3143398429227,-1.47517879246933,21.3283131607309));
#67077=CARTESIAN_POINT('Ctrl Pts',(30.1575657374829,-1.50000000000003,21.3200808850792));
#67078=CARTESIAN_POINT('Ctrl Pts',(29.9999999999998,-1.50000000000001,21.3125));
#67079=CARTESIAN_POINT('Origin',(30.,-1.32966554433622E-14,16.));
#67080=CARTESIAN_POINT('',(29.9999999999999,-1.50000000000001,20.75));
#67081=CARTESIAN_POINT('',(30.0000000238974,-1.50000000000001,20.8125000022995));
#67082=CARTESIAN_POINT('',(30.,-1.50000000000001,16.));
#67083=CARTESIAN_POINT('Ctrl Pts',(29.9999999999998,-1.50000000000001,20.75));
#67084=CARTESIAN_POINT('Ctrl Pts',(30.1355873378723,-1.50000000000003,20.7565234488349));
#67085=CARTESIAN_POINT('Ctrl Pts',(30.2707763371628,-1.48162130053548,20.7635382520255));
#67086=CARTESIAN_POINT('Ctrl Pts',(30.5905052894202,-1.39270558594719,20.7813910993741));
#67087=CARTESIAN_POINT('Ctrl Pts',(30.767029784006,-1.30383501600373,20.7923527650226));
#67088=CARTESIAN_POINT('Ctrl Pts',(31.0784013127494,-1.06141205266722,20.8140676058879));
#67089=CARTESIAN_POINT('Ctrl Pts',(31.2094059572181,-0.909300433903993,
20.8244833092276));
#67090=CARTESIAN_POINT('Ctrl Pts',(31.4005633760122,-0.569930140644686,
20.8433372144086));
#67091=CARTESIAN_POINT('Ctrl Pts',(31.4616108021312,-0.387386085525011,
20.8534785508042));
#67092=CARTESIAN_POINT('Ctrl Pts',(31.5130288281118,-0.00193915990322278,
20.8748922688942));
#67093=CARTESIAN_POINT('Ctrl Pts',(31.5000564049022,0.197728440072968,20.8859849133374));
#67094=CARTESIAN_POINT('Ctrl Pts',(31.3981909189968,0.576981524645895,20.907054529147));
#67095=CARTESIAN_POINT('Ctrl Pts',(31.3116775745975,0.753220156722293,20.9161479987326));
#67096=CARTESIAN_POINT('Ctrl Pts',(31.0770964939546,1.06165196611475,20.9360018364982));
#67097=CARTESIAN_POINT('Ctrl Pts',(30.9317342971964,1.19125838532521,20.946595756762));
#67098=CARTESIAN_POINT('Ctrl Pts',(30.5933406580028,1.39218994814601,20.9684581606193));
#67099=CARTESIAN_POINT('Ctrl Pts',(30.4020178812766,1.458987498605,20.9795186695191));
#67100=CARTESIAN_POINT('Ctrl Pts',(30.0144815741343,1.51197726610397,20.999635956776));
#67101=CARTESIAN_POINT('Ctrl Pts',(29.8225847199203,1.50160380579917,21.0084913464817));
#67102=CARTESIAN_POINT('Ctrl Pts',(29.4482673839794,1.40844186112423,21.0290885295006));
#67103=CARTESIAN_POINT('Ctrl Pts',(29.2698358143887,1.32475295725216,21.0399980141694));
#67104=CARTESIAN_POINT('Ctrl Pts',(28.9522277915389,1.09163995424434,21.0617542984881));
#67105=CARTESIAN_POINT('Ctrl Pts',(28.8169317835683,0.943334467611102,21.0723833275575));
#67106=CARTESIAN_POINT('Ctrl Pts',(28.6164713965323,0.609937924996611,21.0912889974983));
#67107=CARTESIAN_POINT('Ctrl Pts',(28.5503235834348,0.429720618453307,21.1011266323083));
#67108=CARTESIAN_POINT('Ctrl Pts',(28.4877747716401,0.0469249157698905,
21.1223930602351));
#67109=CARTESIAN_POINT('Ctrl Pts',(28.4947443957624,-0.152432728065059,
21.1334684848926));
#67110=CARTESIAN_POINT('Ctrl Pts',(28.585202717896,-0.535530466260377,21.1547516925701));
#67111=CARTESIAN_POINT('Ctrl Pts',(28.6672227696192,-0.715637129073743,
21.1640888680802));
#67112=CARTESIAN_POINT('Ctrl Pts',(28.8938150388557,-1.03121039122832,21.1837567176656));
#67113=CARTESIAN_POINT('Ctrl Pts',(29.0350964807726,-1.16446677665445,21.1942556904709));
#67114=CARTESIAN_POINT('Ctrl Pts',(29.3666683501557,-1.37437197910307,21.2160391495426));
#67115=CARTESIAN_POINT('Ctrl Pts',(29.5553884234738,-1.44649304249621,21.2271223111757));
#67116=CARTESIAN_POINT('Ctrl Pts',(29.8346137979128,-1.49316573714005,21.2418530120072));
#67117=CARTESIAN_POINT('Ctrl Pts',(29.917323692752,-1.50000000000001,21.2460222343129));
#67118=CARTESIAN_POINT('Ctrl Pts',(30.,-1.50000000000001,21.25));
#67119=CARTESIAN_POINT('Ctrl Pts',(29.9999999999998,-1.50000000000001,21.3125));
#67120=CARTESIAN_POINT('Ctrl Pts',(29.9681380540405,-1.50000000000001,21.3109670414103));
#67121=CARTESIAN_POINT('Ctrl Pts',(29.9362464291016,-1.4989848402199,21.3094044560071));
#67122=CARTESIAN_POINT('Ctrl Pts',(29.7059061051266,-1.48427038685078,21.2979134671869));
#67123=CARTESIAN_POINT('Ctrl Pts',(29.5119585810338,-1.43225099507769,21.2871371794785));
#67124=CARTESIAN_POINT('Ctrl Pts',(29.1596955105172,-1.25764065487782,21.2653386273684));
#67125=CARTESIAN_POINT('Ctrl Pts',(29.0039750821709,-1.13829559847059,21.2545313843106));
#67126=CARTESIAN_POINT('Ctrl Pts',(28.7485987477413,-0.848934521932683,
21.2342067770101));
#67127=CARTESIAN_POINT('Ctrl Pts',(28.6505388148689,-0.682384621723858,
21.2254102567623));
#67128=CARTESIAN_POINT('Ctrl Pts',(28.5196273945211,-0.313661198442873,
21.2049256221356));
#67129=CARTESIAN_POINT('Ctrl Pts',(28.4910680085409,-0.114008266472331,
21.1938337925817));
#67130=CARTESIAN_POINT('Ctrl Pts',(28.5133617159534,0.277152561451723,21.1721026354748));
#67131=CARTESIAN_POINT('Ctrl Pts',(28.5610406223868,0.465104578293146,21.1616608567614));
#67132=CARTESIAN_POINT('Ctrl Pts',(28.7268127368948,0.817191792877632,21.1421004559512));
#67133=CARTESIAN_POINT('Ctrl Pts',(28.8450160186508,0.977157792197407,21.1325925873729));
#67134=CARTESIAN_POINT('Ctrl Pts',(29.1366994431696,1.24242044599111,21.1111905550177));
#67135=CARTESIAN_POINT('Ctrl Pts',(29.3073536529405,1.34504122266248,21.1001293733922));
#67136=CARTESIAN_POINT('Ctrl Pts',(29.6718885684984,1.47596994041667,21.0789537702634));
#67137=CARTESIAN_POINT('Ctrl Pts',(29.8613546451375,1.5056180641301,21.0693266350828));
#67138=CARTESIAN_POINT('Ctrl Pts',(30.2499905035945,1.49232790599687,21.0502592125655));
#67139=CARTESIAN_POINT('Ctrl Pts',(30.4453612619354,1.44608660162569,21.0395749518952));
#67140=CARTESIAN_POINT('Ctrl Pts',(30.8031247707546,1.28178759217525,21.017798185678));
#67141=CARTESIAN_POINT('Ctrl Pts',(30.9627170127615,1.16669332668992,21.0069227374242));
#67142=CARTESIAN_POINT('Ctrl Pts',(31.2261252563514,0.884888124749317,20.9864215801195));
#67143=CARTESIAN_POINT('Ctrl Pts',(31.3286136134484,0.721936793997485,20.9776075996665));
#67144=CARTESIAN_POINT('Ctrl Pts',(31.4704956794702,0.357450862099888,20.9573583812278));
#67145=CARTESIAN_POINT('Ctrl Pts',(31.5050292215643,0.158114714869949,20.9462841508261));
#67146=CARTESIAN_POINT('Ctrl Pts',(31.4940038450927,-0.234658795010768,
20.9244634002772));
#67147=CARTESIAN_POINT('Ctrl Pts',(31.4515503117875,-0.4244189406881,20.9139211699618));
#67148=CARTESIAN_POINT('Ctrl Pts',(31.2960889353342,-0.779942120592769,
20.8941698821893));
#67149=CARTESIAN_POINT('Ctrl Pts',(31.1836334516182,-0.941901166431575,
20.8849503363697));
#67150=CARTESIAN_POINT('Ctrl Pts',(30.9011214218994,-1.21536636315781,20.8637617145378));
#67151=CARTESIAN_POINT('Ctrl Pts',(30.7331593249481,-1.323483412269,20.8526773830162));
#67152=CARTESIAN_POINT('Ctrl Pts',(30.374104697925,-1.46471715060753,20.8314791998208));
#67153=CARTESIAN_POINT('Ctrl Pts',(30.1878361111775,-1.49999999700053,20.821537269196));
#67154=CARTESIAN_POINT('Ctrl Pts',(30.0000000239529,-1.50000000000001,20.8125000011524));
#67155=CARTESIAN_POINT('Origin',(30.,-1.32966554433622E-14,16.));
#67156=CARTESIAN_POINT('',(29.9999999999999,-1.50000000000001,20.25));
#67157=CARTESIAN_POINT('',(30.0000000000001,-1.50000000000001,20.3125));
#67158=CARTESIAN_POINT('',(30.,-1.50000000000001,16.));
#67159=CARTESIAN_POINT('Ctrl Pts',(29.9999999999999,-1.50000000000001,20.25));
#67160=CARTESIAN_POINT('Ctrl Pts',(30.1641246040904,-1.50000000000003,20.257896448696));
#67161=CARTESIAN_POINT('Ctrl Pts',(30.3273129308388,-1.47306839847894,20.2664959507697));
#67162=CARTESIAN_POINT('Ctrl Pts',(30.6694540696788,-1.35668483193177,20.2861901008358));
#67163=CARTESIAN_POINT('Ctrl Pts',(30.8415535621189,-1.25719932144175,20.2972337279289));
#67164=CARTESIAN_POINT('Ctrl Pts',(31.1383891848058,-0.996648092240175,
20.3187527726287));
#67165=CARTESIAN_POINT('Ctrl Pts',(31.2598762410215,-0.837810488997904,
20.3284549728335));
#67166=CARTESIAN_POINT('Ctrl Pts',(31.4314249865634,-0.487683998530185,
20.3479064445261));
#67167=CARTESIAN_POINT('Ctrl Pts',(31.4819950779928,-0.300804420279551,
20.3582886433178));
#67168=CARTESIAN_POINT('Ctrl Pts',(31.5105507066295,0.0893179172321859,
20.3799621065129));
#67169=CARTESIAN_POINT('Ctrl Pts',(31.4853246402279,0.289072829407564,20.3910596016338));
#67170=CARTESIAN_POINT('Ctrl Pts',(31.3605672791737,0.660112394093701,20.411672910783));
#67171=CARTESIAN_POINT('Ctrl Pts',(31.2649722312571,0.828695575895264,20.4204916500332));
#67172=CARTESIAN_POINT('Ctrl Pts',(31.0140581775355,1.12220790918685,20.4407168784407));
#67173=CARTESIAN_POINT('Ctrl Pts',(30.8605226301063,1.24384616367647,20.4514827013131));
#67174=CARTESIAN_POINT('Ctrl Pts',(30.5114243415045,1.42407146100134,20.4732849588136));
#67175=CARTESIAN_POINT('Ctrl Pts',(30.3183380047095,1.47926213924964,20.4841079039198));
#67176=CARTESIAN_POINT('Ctrl Pts',(29.9307960888716,1.51038882263748,20.5036181531332));
#67177=CARTESIAN_POINT('Ctrl Pts',(29.7403288665302,1.48951380456358,20.5127847164407));
#67178=CARTESIAN_POINT('Ctrl Pts',(29.3711639835748,1.37589985350485,20.5337021132381));
#67179=CARTESIAN_POINT('Ctrl Pts',(29.1966946677341,1.28188655628153,20.5447077525887));
#67180=CARTESIAN_POINT('Ctrl Pts',(28.8909965958092,1.02962579258236,20.5664229013678));
#67181=CARTESIAN_POINT('Ctrl Pts',(28.7637626025144,0.872753791453066,20.5765136782526));
#67182=CARTESIAN_POINT('Ctrl Pts',(28.582295287402,0.526054660802727,20.5957747410665));
#67183=CARTESIAN_POINT('Ctrl Pts',(28.5268265400693,0.341112810094873,20.6060492883281));
#67184=CARTESIAN_POINT('Ctrl Pts',(28.4876154625531,-0.0470049788678421,
20.6276113877149));
#67185=CARTESIAN_POINT('Ctrl Pts',(28.5071470207889,-0.246809925970759,
20.6387116625539));
#67186=CARTESIAN_POINT('Ctrl Pts',(28.6213243381125,-0.621726643029005,
20.6595403690571));
#67187=CARTESIAN_POINT('Ctrl Pts',(28.7127069454602,-0.793828860292424,
20.6684492190444));
#67188=CARTESIAN_POINT('Ctrl Pts',(28.9560213000323,-1.09433750409046,20.6885031487146));
#67189=CARTESIAN_POINT('Ctrl Pts',(29.1057854975977,-1.21976733917156,20.6991928441151));
#67190=CARTESIAN_POINT('Ctrl Pts',(29.4493247586543,-1.40936219023255,20.7209879081598));
#67191=CARTESIAN_POINT('Ctrl Pts',(29.6408325610402,-1.46988527163767,20.7318830283038));
#67192=CARTESIAN_POINT('Ctrl Pts',(29.8922912775479,-1.4971028845898,20.7447373862468));
#67193=CARTESIAN_POINT('Ctrl Pts',(29.9461731363168,-1.50000000000001,20.7474102538136));
#67194=CARTESIAN_POINT('Ctrl Pts',(29.9999999999998,-1.50000000000001,20.75));
#67195=CARTESIAN_POINT('Ctrl Pts',(30.0000000239529,-1.50000000000001,20.8125000011524));
#67196=CARTESIAN_POINT('Ctrl Pts',(29.9974904007656,-1.50000000004009,20.8123792568517));
#67197=CARTESIAN_POINT('Ctrl Pts',(29.994980514477,-1.49999370187214,20.8122583249421));
#67198=CARTESIAN_POINT('Ctrl Pts',(29.7936662704942,-1.49898314378545,20.8025445178046));
#67199=CARTESIAN_POINT('Ctrl Pts',(29.5970666373285,-1.45847246315053,20.7919603168594));
#67200=CARTESIAN_POINT('Ctrl Pts',(29.2341811004286,-1.30450218441903,20.7702240261379));
#67201=CARTESIAN_POINT('Ctrl Pts',(29.0708854167951,-1.19371554978206,20.7592900523783));
#67202=CARTESIAN_POINT('Ctrl Pts',(28.7996246113049,-0.919409908918738,
20.738619409654));
#67203=CARTESIAN_POINT('Ctrl Pts',(28.6928036628702,-0.759898893507146,
20.7297166051949));
#67204=CARTESIAN_POINT('Ctrl Pts',(28.540323338491,-0.399638425423168,20.7097021347457));
#67205=CARTESIAN_POINT('Ctrl Pts',(28.4999872115666,-0.200774562873281,
20.6986541423819));
#67206=CARTESIAN_POINT('Ctrl Pts',(28.5000123038317,0.193260173251348,20.6767633237083));
#67207=CARTESIAN_POINT('Ctrl Pts',(28.5373370740434,0.384636586987589,20.6661313007229));
#67208=CARTESIAN_POINT('Ctrl Pts',(28.6828216865171,0.743407395273799,20.6461995891515));
#67209=CARTESIAN_POINT('Ctrl Pts',(28.7898502936129,0.90727948583588,20.637187813622));
#67210=CARTESIAN_POINT('Ctrl Pts',(29.0635269308615,1.18843769395866,20.6162105900475));
#67211=CARTESIAN_POINT('Ctrl Pts',(29.228755223573,1.30174519776628,20.6051136094466));
#67212=CARTESIAN_POINT('Ctrl Pts',(29.5868470804747,1.45456710532649,20.5836398539607));
#67213=CARTESIAN_POINT('Ctrl Pts',(29.7752048690842,1.49530975495507,20.5734457453635));
#67214=CARTESIAN_POINT('Ctrl Pts',(30.1648759814307,1.50410182396658,20.5544534610902));
#67215=CARTESIAN_POINT('Ctrl Pts',(30.3625681263815,1.46904639647318,20.544196110566));
#67216=CARTESIAN_POINT('Ctrl Pts',(30.7301648562918,1.32486538129436,20.5225050764527));
#67217=CARTESIAN_POINT('Ctrl Pts',(30.8968384149473,1.21823387618242,20.5115240048699));
#67218=CARTESIAN_POINT('Ctrl Pts',(31.1754315899033,0.951036194862134,20.4906980266758));
#67219=CARTESIAN_POINT('Ctrl Pts',(31.2863099173977,0.794671992670377,20.4816484440372));
#67220=CARTESIAN_POINT('Ctrl Pts',(31.4475104523221,0.440765387920731,20.4619869659956));
#67221=CARTESIAN_POINT('Ctrl Pts',(31.4931266838049,0.245180433281527,20.4511211351823));
#67222=CARTESIAN_POINT('Ctrl Pts',(31.505277935416,-0.147222207316758,20.4293209884824));
#67223=CARTESIAN_POINT('Ctrl Pts',(31.4737006088925,-0.340229130529765,
20.4185983816372));
#67224=CARTESIAN_POINT('Ctrl Pts',(31.339252899941,-0.702504700740186,20.39847196107));
#67225=CARTESIAN_POINT('Ctrl Pts',(31.2380795698328,-0.868488363198902,
20.3896091209879));
#67226=CARTESIAN_POINT('Ctrl Pts',(30.9741217873874,-1.15788922779948,20.3688705333532));
#67227=CARTESIAN_POINT('Ctrl Pts',(30.8120536546578,-1.27678494801521,20.3577703677868));
#67228=CARTESIAN_POINT('Ctrl Pts',(30.4578087067642,-1.44121172280179,20.3361593393739));
#67229=CARTESIAN_POINT('Ctrl Pts',(30.2702179556352,-1.48784534045563,20.3258384968839));
#67230=CARTESIAN_POINT('Ctrl Pts',(30.052598998323,-1.49930896382792,20.3150498659359));
#67231=CARTESIAN_POINT('Ctrl Pts',(30.0262877690999,-1.50000000000001,20.3137647708805));
#67232=CARTESIAN_POINT('Ctrl Pts',(30.0000000000001,-1.50000000000001,20.3125));
#67233=CARTESIAN_POINT('Origin',(30.,-1.32966554433622E-14,16.));
#67234=CARTESIAN_POINT('',(29.9999999508795,-1.50000000000001,19.7499999952734));
#67235=CARTESIAN_POINT('',(30.0000000000001,-1.50000000000001,19.8125));
#67236=CARTESIAN_POINT('',(30.,-1.50000000000001,16.));
#67237=CARTESIAN_POINT('Ctrl Pts',(29.9999999507652,-1.50000000000001,19.7499999976312));
#67238=CARTESIAN_POINT('Ctrl Pts',(30.0036354883629,-1.50000000011934,19.7501749125187));
#67239=CARTESIAN_POINT('Ctrl Pts',(30.007271600744,-1.4999867831078,19.7503502221899));
#67240=CARTESIAN_POINT('Ctrl Pts',(30.201622915749,-1.49857339489822,19.7597402149765));
#67241=CARTESIAN_POINT('Ctrl Pts',(30.3903004853368,-1.46082693625102,19.769866481516));
#67242=CARTESIAN_POINT('Ctrl Pts',(30.7502056783764,-1.31393443624912,19.7912627754119));
#67243=CARTESIAN_POINT('Ctrl Pts',(30.9169691324023,-1.2034971179945,19.8023538891195));
#67244=CARTESIAN_POINT('Ctrl Pts',(31.1955532827852,-0.926587489668503,
19.8234492094243));
#67245=CARTESIAN_POINT('Ctrl Pts',(31.305583357368,-0.763777918932018,19.8325678933928));
#67246=CARTESIAN_POINT('Ctrl Pts',(31.4566154175894,-0.406803589900389,
19.8523998005612));
#67247=CARTESIAN_POINT('Ctrl Pts',(31.4968003232487,-0.216309448389897,
19.8629828084229));
#67248=CARTESIAN_POINT('Ctrl Pts',(31.5029527191874,0.177060648076386,19.884836702671));
#67249=CARTESIAN_POINT('Ctrl Pts',(31.4658451495388,0.376207311237188,19.8959004061799));
#67250=CARTESIAN_POINT('Ctrl Pts',(31.3192558360179,0.738832237635632,19.9160462354243));
#67251=CARTESIAN_POINT('Ctrl Pts',(31.2148503942445,0.900251242918639,19.9248907954582));
#67252=CARTESIAN_POINT('Ctrl Pts',(30.9479657510409,1.17875033469753,19.9454673747239));
#67253=CARTESIAN_POINT('Ctrl Pts',(30.7867234803792,1.29195591113542,19.9563697464337));
#67254=CARTESIAN_POINT('Ctrl Pts',(30.4266603329508,1.45171184585212,19.9781309575447));
#67255=CARTESIAN_POINT('Ctrl Pts',(30.2307253625385,1.49542562590392,19.9887721548721));
#67256=CARTESIAN_POINT('Ctrl Pts',(29.8418323593176,1.50370934578551,20.0077128815434));
#67257=CARTESIAN_POINT('Ctrl Pts',(29.6526184508184,1.47157346290215,20.0175030286082));
#67258=CARTESIAN_POINT('Ctrl Pts',(29.2894512067405,1.33570909972092,20.038749930874));
#67259=CARTESIAN_POINT('Ctrl Pts',(29.1199599079427,1.2306626568369,20.0498225415362));
#67260=CARTESIAN_POINT('Ctrl Pts',(28.8323016398048,0.961771765690436,20.0711316978356));
#67261=CARTESIAN_POINT('Ctrl Pts',(28.7166359490173,0.80092922531751,20.0805039319268));
#67262=CARTESIAN_POINT('Ctrl Pts',(28.5553841103709,0.447325657819572,20.1001485745656));
#67263=CARTESIAN_POINT('Ctrl Pts',(28.5099861175222,0.258564005548656,20.1106353330251));
#67264=CARTESIAN_POINT('Ctrl Pts',(28.4926188058233,-0.133342134639988,
20.1324078963689));
#67265=CARTESIAN_POINT('Ctrl Pts',(28.5237938243712,-0.332877530953282,
20.1434931961641));
#67266=CARTESIAN_POINT('Ctrl Pts',(28.6595170927538,-0.699759711689848,
20.1638755395383));
#67267=CARTESIAN_POINT('Ctrl Pts',(28.759513047986,-0.864726488741114,20.1726705572702));
#67268=CARTESIAN_POINT('Ctrl Pts',(29.0184002150316,-1.15079879551533,20.1930727248681));
#67269=CARTESIAN_POINT('Ctrl Pts',(29.1758229214277,-1.26830528519454,20.2039107975187));
#67270=CARTESIAN_POINT('Ctrl Pts',(29.5305217931358,-1.4384406773805,20.2257022380569));
#67271=CARTESIAN_POINT('Ctrl Pts',(29.7251117157194,-1.4879453135066,20.2364395788536));
#67272=CARTESIAN_POINT('Ctrl Pts',(29.9491466954872,-1.49935402178859,20.2475353754067));
#67273=CARTESIAN_POINT('Ctrl Pts',(29.9745837219083,-1.50000000000001,20.2487771587502));
#67274=CARTESIAN_POINT('Ctrl Pts',(29.9999999999999,-1.50000000000001,20.25));
#67275=CARTESIAN_POINT('Ctrl Pts',(30.0000000000001,-1.50000000000001,20.3125));
#67276=CARTESIAN_POINT('Ctrl Pts',(29.8275998140085,-1.50000000000001,20.3042053921841));
#67277=CARTESIAN_POINT('Ctrl Pts',(29.6562870357889,-1.47028352574469,20.2951376446808));
#67278=CARTESIAN_POINT('Ctrl Pts',(29.3085931862514,-1.34558031058123,20.2749452383464));
#67279=CARTESIAN_POINT('Ctrl Pts',(29.1384186293223,-1.24350663328035,20.2639223312337));
#67280=CARTESIAN_POINT('Ctrl Pts',(28.8520258822514,-0.983987574399218,
20.242934391019));
#67281=CARTESIAN_POINT('Ctrl Pts',(28.7368098691781,-0.830906588856551,
20.2336614771587));
#67282=CARTESIAN_POINT('Ctrl Pts',(28.5656483010559,-0.481857271883387,
20.214269848438));
#67283=CARTESIAN_POINT('Ctrl Pts',(28.5144799811963,-0.287679235979695,
20.2034821797766));
#67284=CARTESIAN_POINT('Ctrl Pts',(28.4911007681834,0.104720249591022,20.181682208356));
#67285=CARTESIAN_POINT('Ctrl Pts',(28.5173310962609,0.299077411990059,20.1708845882228));
#67286=CARTESIAN_POINT('Ctrl Pts',(28.6416246239434,0.664496311411631,20.1505835382549));
#67287=CARTESIAN_POINT('Ctrl Pts',(28.7375408574377,0.832427515421977,20.1417837739438));
#67288=CARTESIAN_POINT('Ctrl Pts',(28.9926175512114,1.12917452204563,20.1212684183864));
#67289=CARTESIAN_POINT('Ctrl Pts',(29.1516633795811,1.2530630770023,20.1101749736523));
#67290=CARTESIAN_POINT('Ctrl Pts',(29.5021040725661,1.42792836972927,20.0884570187074));
#67291=CARTESIAN_POINT('Ctrl Pts',(29.6888418601191,1.47989191267207,20.0780291609664));
#67292=CARTESIAN_POINT('Ctrl Pts',(30.0769287467939,1.5109546306831,20.0584944686474));
#67293=CARTESIAN_POINT('Ctrl Pts',(30.2747213678695,1.48776626200004,20.0489426359701));
#67294=CARTESIAN_POINT('Ctrl Pts',(30.6499367323256,1.36617967610523,20.027512673167));
#67295=CARTESIAN_POINT('Ctrl Pts',(30.8236685705517,1.26902858360925,20.0164553547449));
#67296=CARTESIAN_POINT('Ctrl Pts',(31.1182297704941,1.01768973269335,19.9953016376572));
#67297=CARTESIAN_POINT('Ctrl Pts',(31.2380227260335,0.867983838688731,19.9857213243715));
#67298=CARTESIAN_POINT('Ctrl Pts',(31.4194655172301,0.52407745893419,19.9666154143852));
#67299=CARTESIAN_POINT('Ctrl Pts',(31.4763477416476,0.331530482038543,19.9559183601132));
#67300=CARTESIAN_POINT('Ctrl Pts',(31.5113890098208,-0.0605236259430762,
19.9341375763365));
#67301=CARTESIAN_POINT('Ctrl Pts',(31.4907606610887,-0.256127601642152,
19.9232706887976));
#67302=CARTESIAN_POINT('Ctrl Pts',(31.3770092904839,-0.62473058770716,19.9027927451274));
#67303=CARTESIAN_POINT('Ctrl Pts',(31.2864311739689,-0.794691675228615,
19.8939853466257));
#67304=CARTESIAN_POINT('Ctrl Pts',(31.0405043429371,-1.09883901947073,19.8737046491109));
#67305=CARTESIAN_POINT('Ctrl Pts',(30.8847013390568,-1.22775605549742,19.8626275448131));
#67306=CARTESIAN_POINT('Ctrl Pts',(30.5384592288504,-1.41320441242881,19.8408176202706));
#67307=CARTESIAN_POINT('Ctrl Pts',(30.3527481344157,-1.47060245170435,19.8302882010938));
#67308=CARTESIAN_POINT('Ctrl Pts',(30.1075898199807,-1.49710947656403,19.8177567099449));
#67309=CARTESIAN_POINT('Ctrl Pts',(30.0537655536404,-1.50000000000001,19.8150867964056));
#67310=CARTESIAN_POINT('Ctrl Pts',(30.0000000000003,-1.50000000000001,19.8125));
#67311=CARTESIAN_POINT('Origin',(30.,-1.32966554433622E-14,16.));
#67312=CARTESIAN_POINT('',(30.0000000000001,-1.50000000000001,19.25));
#67313=CARTESIAN_POINT('',(30.,-1.50000000000001,19.3125));
#67314=CARTESIAN_POINT('',(30.,-1.50000000000001,16.));
#67315=CARTESIAN_POINT('Ctrl Pts',(30.0000000000001,-1.50000000000001,19.25));
#67316=CARTESIAN_POINT('Ctrl Pts',(30.0322695745912,-1.50000000000001,19.2515525706314));
#67317=CARTESIAN_POINT('Ctrl Pts',(30.0645714825038,-1.49895869986435,19.2531356219044));
#67318=CARTESIAN_POINT('Ctrl Pts',(30.2882590679586,-1.48448482383795,19.2642998479893));
#67319=CARTESIAN_POINT('Ctrl Pts',(30.4754930135539,-1.43550485550641,19.2746687000727));
#67320=CARTESIAN_POINT('Ctrl Pts',(30.8281012978914,-1.26647563555772,19.2963288301724));
#67321=CARTESIAN_POINT('Ctrl Pts',(30.9888581275123,-1.14537453755813,19.3074271661326));
#67322=CARTESIAN_POINT('Ctrl Pts',(31.2489169787693,-0.852727854965852,
19.328068327964));
#67323=CARTESIAN_POINT('Ctrl Pts',(31.3477723438117,-0.685891580063111,
19.3368949122188));
#67324=CARTESIAN_POINT('Ctrl Pts',(31.4777710225729,-0.322229436301838,
19.35709836465));
#67325=CARTESIAN_POINT('Ctrl Pts',(31.5070120496637,-0.128613045958812,
19.3678548307802));
#67326=CARTESIAN_POINT('Ctrl Pts',(31.4899431617665,0.263827999699887,19.3896571110945));
#67327=CARTESIAN_POINT('Ctrl Pts',(31.4418890858574,0.458816520684437,19.4004898067048));
#67328=CARTESIAN_POINT('Ctrl Pts',(31.2763170645903,0.810606892156535,19.420033716231));
#67329=CARTESIAN_POINT('Ctrl Pts',(31.1635461572557,0.965528328551652,19.4291724240899));
#67330=CARTESIAN_POINT('Ctrl Pts',(30.8815440072885,1.22938524433353,19.4500696176279));
#67331=CARTESIAN_POINT('Ctrl Pts',(30.713328176096,1.33404197013925,19.4610700368521));
#67332=CARTESIAN_POINT('Ctrl Pts',(30.3423586225268,1.47407873960012,19.4828082280827));
#67333=CARTESIAN_POINT('Ctrl Pts',(30.1427440803289,1.50655371354715,19.4929501746347));
#67334=CARTESIAN_POINT('Ctrl Pts',(29.7515262729803,1.4915957790601,19.5121881483469));
#67335=CARTESIAN_POINT('Ctrl Pts',(29.563545020268,1.44778515274356,19.522449362427));
#67336=CARTESIAN_POINT('Ctrl Pts',(29.2074099124303,1.28891068317319,19.5439971005021));
#67337=CARTESIAN_POINT('Ctrl Pts',(29.0438038910602,1.17268375630169,19.5550971246218));
#67338=CARTESIAN_POINT('Ctrl Pts',(28.7751767012687,0.88721540741588,19.5759511326745));
#67339=CARTESIAN_POINT('Ctrl Pts',(28.6712044325382,0.722248138115754,19.5848751034381));
#67340=CARTESIAN_POINT('Ctrl Pts',(28.5314450700553,0.361647735614998,19.6049084591326));
#67341=CARTESIAN_POINT('Ctrl Pts',(28.4970926988021,0.169404578017586,19.6155886345547));
#67342=CARTESIAN_POINT('Ctrl Pts',(28.5033789257342,-0.222871075081128,
19.6373817263935));
#67343=CARTESIAN_POINT('Ctrl Pts',(28.5460751647458,-0.419126971559099,
19.6482848317533));
#67344=CARTESIAN_POINT('Ctrl Pts',(28.7020419000445,-0.77553505760853,19.6680852809783));
#67345=CARTESIAN_POINT('Ctrl Pts',(28.8106757232385,-0.933630997355151,
19.6770461367592));
#67346=CARTESIAN_POINT('Ctrl Pts',(29.0852161697017,-1.20477024704427,19.697786615973));
#67347=CARTESIAN_POINT('Ctrl Pts',(29.2500326897204,-1.31371406923191,19.7087425717726));
#67348=CARTESIAN_POINT('Ctrl Pts',(29.611734771314,-1.46197087611401,19.7302632159228));
#67349=CARTESIAN_POINT('Ctrl Pts',(29.8049901134984,-1.49999999359916,19.7406175822833));
#67350=CARTESIAN_POINT('Ctrl Pts',(29.9999999507652,-1.50000000000001,19.7499999976312));
#67351=CARTESIAN_POINT('Ctrl Pts',(30.0000000000003,-1.50000000000001,19.8125));
#67352=CARTESIAN_POINT('Ctrl Pts',(29.8589500630315,-1.50000000000001,19.8057137317435));
#67353=CARTESIAN_POINT('Ctrl Pts',(29.7183576297039,-1.48011045726929,19.7983969878431));
#67354=CARTESIAN_POINT('Ctrl Pts',(29.392433533781,-1.38562863633522,19.7800914624408));
#67355=CARTESIAN_POINT('Ctrl Pts',(29.2152602016442,-1.29355450601908,19.7690095917929));
#67356=CARTESIAN_POINT('Ctrl Pts',(28.9125224323809,-1.05055621120639,19.7476941614444));
#67357=CARTESIAN_POINT('Ctrl Pts',(28.7881027470448,-0.904173072558181,
19.7377318373643));
#67358=CARTESIAN_POINT('Ctrl Pts',(28.5965141205021,-0.565467385757126,
19.7189148547643));
#67359=CARTESIAN_POINT('Ctrl Pts',(28.5340212729776,-0.374707579896709,
19.708317087772));
#67360=CARTESIAN_POINT('Ctrl Pts',(28.4874198303467,0.0166598622973653,
19.6865744520946));
#67361=CARTESIAN_POINT('Ctrl Pts',(28.5024461232084,0.213342923270549,19.6756476153738));
#67362=CARTESIAN_POINT('Ctrl Pts',(28.605730933148,0.585021358101511,19.6549988134388));
#67363=CARTESIAN_POINT('Ctrl Pts',(28.6911262279336,0.757019946925095,19.6461115535275));
#67364=CARTESIAN_POINT('Ctrl Pts',(28.9280450078188,1.06829223859541,19.6260663408692));
#67365=CARTESIAN_POINT('Ctrl Pts',(29.0805347242822,1.20204064727676,19.6150144423906));
#67366=CARTESIAN_POINT('Ctrl Pts',(29.4223784266326,1.3977266885599,19.5931317562239));
#67367=CARTESIAN_POINT('Ctrl Pts',(29.6069366918152,1.46041214264913,19.5825109299366));
#67368=CARTESIAN_POINT('Ctrl Pts',(29.9906687655378,1.51247863508202,19.562602320475));
#67369=CARTESIAN_POINT('Ctrl Pts',(30.1862339040192,1.50100007477566,19.55356759697));
#67370=CARTESIAN_POINT('Ctrl Pts',(30.5662821795392,1.40308967236277,19.5325627823883));
#67371=CARTESIAN_POINT('Ctrl Pts',(30.7466285872712,1.31600734425417,19.5214669082421));
#67372=CARTESIAN_POINT('Ctrl Pts',(31.0570470506688,1.08124306107491,19.5000106628701));
#67373=CARTESIAN_POINT('Ctrl Pts',(31.185947420448,0.938076365153711,19.4898320882731));
#67374=CARTESIAN_POINT('Ctrl Pts',(31.387173884418,0.604359282145194,19.4708806565388));
#67375=CARTESIAN_POINT('Ctrl Pts',(31.4549913450499,0.415392173173207,19.460577342954));
#67376=CARTESIAN_POINT('Ctrl Pts',(31.5125364736871,0.0248207245632997,
19.4388789291423));
#67377=CARTESIAN_POINT('Ctrl Pts',(31.5028468405333,-0.172737498474235,
19.4279034723069));
#67378=CARTESIAN_POINT('Ctrl Pts',(31.4094808313587,-0.547250043493136,
19.4070972198059));
#67379=CARTESIAN_POINT('Ctrl Pts',(31.3288984144444,-0.721204660777261,
19.3980698586427));
#67380=CARTESIAN_POINT('Ctrl Pts',(31.1018991125715,-1.03700530321776,19.3783761095713));
#67381=CARTESIAN_POINT('Ctrl Pts',(30.9548507096631,-1.17379817492847,19.3675014379958));
#67382=CARTESIAN_POINT('Ctrl Pts',(30.6204358823266,-1.37933694163779,19.3457024869274));
#67383=CARTESIAN_POINT('Ctrl Pts',(30.4373267027344,-1.44785012953098,19.3349894983086));
#67384=CARTESIAN_POINT('Ctrl Pts',(30.1646733538461,-1.49322482781476,19.3206110496582));
#67385=CARTESIAN_POINT('Ctrl Pts',(30.0823180279059,-1.50000000000001,19.3164605279642));
#67386=CARTESIAN_POINT('Ctrl Pts',(30.,-1.50000000000001,19.3125));
#67387=CARTESIAN_POINT('Origin',(30.,-1.32966554433622E-14,16.));
#67388=CARTESIAN_POINT('',(30.0000000000001,-1.50000000000001,18.75));
#67389=CARTESIAN_POINT('',(30.,-1.50000000000001,18.8125));
#67390=CARTESIAN_POINT('',(30.,-1.50000000000001,16.));
#67391=CARTESIAN_POINT('Ctrl Pts',(30.0000000000002,-1.50000000000001,18.75));
#67392=CARTESIAN_POINT('Ctrl Pts',(30.0598815861698,-1.50000000000001,18.7528810541579));
#67393=CARTESIAN_POINT('Ctrl Pts',(30.1198247627216,-1.4964145214846,18.7558646682098));
#67394=CARTESIAN_POINT('Ctrl Pts',(30.3709807388755,-1.46613984657296,18.7687893789386));
#67395=CARTESIAN_POINT('Ctrl Pts',(30.5561899070999,-1.40635296128044,18.7793610060131));
#67396=CARTESIAN_POINT('Ctrl Pts',(30.9004833554958,-1.21627199481911,18.8012058591186));
#67397=CARTESIAN_POINT('Ctrl Pts',(31.054808880873,-1.08516465668695,18.8122727199239));
#67398=CARTESIAN_POINT('Ctrl Pts',(31.2966795386424,-0.777790002612556,
18.832447912207));
#67399=CARTESIAN_POINT('Ctrl Pts',(31.3849156897549,-0.606916752329299,
18.8412824026485));
#67400=CARTESIAN_POINT('Ctrl Pts',(31.4939654845851,-0.236921615045211,
18.8618376880532));
#67401=CARTESIAN_POINT('Ctrl Pts',(31.5120817444602,-0.0408132290769898,
18.8727325983848));
#67402=CARTESIAN_POINT('Ctrl Pts',(31.4718441015158,0.350974679810523,18.8944985933229));
#67403=CARTESIAN_POINT('Ctrl Pts',(31.4124332725198,0.54273929222595,18.9051521829016));
#67404=CARTESIAN_POINT('Ctrl Pts',(31.2264254338517,0.884320880490274,18.9241289378051));
#67405=CARTESIAN_POINT('Ctrl Pts',(31.1045648671413,1.03253115218655,18.9338713522791));
#67406=CARTESIAN_POINT('Ctrl Pts',(30.8063387149155,1.2801510812434,18.9550980960807));
#67407=CARTESIAN_POINT('Ctrl Pts',(30.6310491381331,1.37504484021148,18.9661676575249));
#67408=CARTESIAN_POINT('Ctrl Pts',(30.2546711108962,1.4912245976519,18.9875033692879));
#67409=CARTESIAN_POINT('Ctrl Pts',(30.05740041095,1.51172051693628,18.9969127515258));
#67410=CARTESIAN_POINT('Ctrl Pts',(29.6702738320324,1.47589654334487,19.0165334981157));
#67411=CARTESIAN_POINT('Ctrl Pts',(29.4839742576828,1.42150925053353,19.0270075986994));
#67412=CARTESIAN_POINT('Ctrl Pts',(29.1353660189379,1.24191643228194,19.048768709802));
#67413=CARTESIAN_POINT('Ctrl Pts',(28.9777462443354,1.1157773991078,19.059856056776));
#67414=CARTESIAN_POINT('Ctrl Pts',(28.7267374929236,0.815719209989595,19.0802676706567));
#67415=CARTESIAN_POINT('Ctrl Pts',(28.6332044534767,0.64688991790973,19.0890616712273));
#67416=CARTESIAN_POINT('Ctrl Pts',(28.5135873974093,0.280047942578678,19.109441780968));
#67417=CARTESIAN_POINT('Ctrl Pts',(28.4898364137009,0.0851180238092936,
19.1202712208996));
#67418=CARTESIAN_POINT('Ctrl Pts',(28.5183897482981,-0.307171243363851,
19.1420650690759));
#67419=CARTESIAN_POINT('Ctrl Pts',(28.5720998196786,-0.500646940480604,
19.1528137189157));
#67420=CARTESIAN_POINT('Ctrl Pts',(28.747829861517,-0.847427013151625,19.1720792785085));
#67421=CARTESIAN_POINT('Ctrl Pts',(28.8650664758991,-0.999006868470888,
19.1814790094866));
#67422=CARTESIAN_POINT('Ctrl Pts',(29.1550741400796,-1.25492382568339,19.2025408141021));
#67423=CARTESIAN_POINT('Ctrl Pts',(29.3268372187205,-1.35483766663846,19.2135801535473));
#67424=CARTESIAN_POINT('Ctrl Pts',(29.6699517271029,-1.47262040644266,19.2333600008011));
#67425=CARTESIAN_POINT('Ctrl Pts',(29.8345144389513,-1.50000000000001,19.2420380722318));
#67426=CARTESIAN_POINT('Ctrl Pts',(30.0000000000001,-1.50000000000001,19.25));
#67427=CARTESIAN_POINT('Ctrl Pts',(30.,-1.50000000000001,19.3125));
#67428=CARTESIAN_POINT('Ctrl Pts',(29.8904115959066,-1.50000000000001,19.3072274254497));
#67429=CARTESIAN_POINT('Ctrl Pts',(29.7809217474217,-1.48799325955223,19.3016260720903));
#67430=CARTESIAN_POINT('Ctrl Pts',(29.479267613868,-1.42071467340943,19.2852438812078));
#67431=CARTESIAN_POINT('Ctrl Pts',(29.2956191224553,-1.33919024824593,19.2741435216794));
#67432=CARTESIAN_POINT('Ctrl Pts',(28.9769843310201,-1.11359538988626,19.2525466742853));
#67433=CARTESIAN_POINT('Ctrl Pts',(28.8433197059369,-0.97404728751911,19.2422393958357));
#67434=CARTESIAN_POINT('Ctrl Pts',(28.6314369352188,-0.64558462894177,19.2229212185382));
#67435=CARTESIAN_POINT('Ctrl Pts',(28.5578261508896,-0.458159789494097,
19.2129533216385));
#67436=CARTESIAN_POINT('Ctrl Pts',(28.4887314396478,-0.0683254796838233,
19.1912958599824));
#67437=CARTESIAN_POINT('Ctrl Pts',(28.4927829468086,0.129998312926432,19.180277871504));
#67438=CARTESIAN_POINT('Ctrl Pts',(28.5757061903925,0.507408017565263,19.1593106656908));
#67439=CARTESIAN_POINT('Ctrl Pts',(28.6513157241137,0.683452060166118,19.1500704896955));
#67440=CARTESIAN_POINT('Ctrl Pts',(28.8692063981292,1.00541452618758,19.1306438179201));
#67441=CARTESIAN_POINT('Ctrl Pts',(29.0123062748592,1.14629480240063,19.119845580885));
#67442=CARTESIAN_POINT('Ctrl Pts',(29.3411837772215,1.36149831072911,19.0980445794436));
#67443=CARTESIAN_POINT('Ctrl Pts',(29.5228193452006,1.43527924918368,19.0872561635921));
#67444=CARTESIAN_POINT('Ctrl Pts',(29.9017346505858,1.50901487689319,19.0669773805809));
#67445=CARTESIAN_POINT('Ctrl Pts',(30.095243866884,1.50920856983617,19.0581733709244));
#67446=CARTESIAN_POINT('Ctrl Pts',(30.4795337547919,1.43522535350299,19.0376291257293));
#67447=CARTESIAN_POINT('Ctrl Pts',(30.6659951148259,1.35877256279477,19.0265343107311));
#67448=CARTESIAN_POINT('Ctrl Pts',(30.9917525251624,1.14161337833726,19.0048291004505));
#67449=CARTESIAN_POINT('Ctrl Pts',(31.12959203788,1.00543319777699,18.9944145110095));
#67450=CARTESIAN_POINT('Ctrl Pts',(31.3495099297643,0.683969951441068,18.9749041718824));
#67451=CARTESIAN_POINT('Ctrl Pts',(31.4277388995994,0.500572833869038,18.9653096018815));
#67452=CARTESIAN_POINT('Ctrl Pts',(31.5085610210805,0.114360476914036,18.9438533598284));
#67453=CARTESIAN_POINT('Ctrl Pts',(31.510521839189,-0.0846024989690804,
18.9327998611683));
#67454=CARTESIAN_POINT('Ctrl Pts',(31.4387139095947,-0.464995267712227,
18.9116669295714));
#67455=CARTESIAN_POINT('Ctrl Pts',(31.3683024334794,-0.643299822803022,
18.9021297086694));
#67456=CARTESIAN_POINT('Ctrl Pts',(31.1599775839064,-0.97159308723095,18.8829874173259));
#67457=CARTESIAN_POINT('Ctrl Pts',(31.021122395481,-1.11661364586043,18.8722783951071));
#67458=CARTESIAN_POINT('Ctrl Pts',(30.6983237124874,-1.34174379218127,18.8504941210548));
#67459=CARTESIAN_POINT('Ctrl Pts',(30.5183853004494,-1.42099198981035,18.8396354913461));
#67460=CARTESIAN_POINT('Ctrl Pts',(30.220307982392,-1.48785706899676,18.8234368763837));
#67461=CARTESIAN_POINT('Ctrl Pts',(30.1102084329115,-1.50000000000001,18.8178024057007));
#67462=CARTESIAN_POINT('Ctrl Pts',(30.,-1.50000000000001,18.8125));
#67463=CARTESIAN_POINT('Origin',(30.,-1.32966554433622E-14,16.));
#67464=CARTESIAN_POINT('',(30.,-1.50000000000001,18.25));
#67465=CARTESIAN_POINT('',(29.9999999999999,-1.50000000000001,18.3125));
#67466=CARTESIAN_POINT('',(30.,-1.50000000000001,16.));
#67467=CARTESIAN_POINT('Ctrl Pts',(30.,-1.50000000000001,18.25));
#67468=CARTESIAN_POINT('Ctrl Pts',(30.0882156275205,-1.50000000000001,18.254244276358));
#67469=CARTESIAN_POINT('Ctrl Pts',(30.1764501130872,-1.49221937550789,18.2587055884823));
#67470=CARTESIAN_POINT('Ctrl Pts',(30.4546079281867,-1.44254775409159,18.2734682298626));
#67471=CARTESIAN_POINT('Ctrl Pts',(30.6370980720641,-1.37175281599007,18.2842148170619));
#67472=CARTESIAN_POINT('Ctrl Pts',(30.9691525442989,-1.16201577961996,18.3060168240942));
#67473=CARTESIAN_POINT('Ctrl Pts',(31.1145075241426,-1.02344071977941,18.3168595260404));
#67474=CARTESIAN_POINT('Ctrl Pts',(31.3375735551139,-0.704962761586156,
18.3364384054093));
#67475=CARTESIAN_POINT('Ctrl Pts',(31.4160050795816,-0.530113102524481,
18.345549272082));
#67476=CARTESIAN_POINT('Ctrl Pts',(31.5048780292219,-0.154342998497877,
18.3664253889724));
#67477=CARTESIAN_POINT('Ctrl Pts',(31.5121437205665,0.0435642244476196,
18.3774202346916));
#67478=CARTESIAN_POINT('Ctrl Pts',(31.4493976248982,0.435280459623824,18.3991822477569));
#67479=CARTESIAN_POINT('Ctrl Pts',(31.3782925123276,0.624894161678516,18.4093783750732));
#67480=CARTESIAN_POINT('Ctrl Pts',(31.1707210215853,0.957071364942045,18.428592307613));
#67481=CARTESIAN_POINT('Ctrl Pts',(31.0393074800838,1.09835818528463,18.4388395784748));
#67482=CARTESIAN_POINT('Ctrl Pts',(30.7245434883219,1.32834442072559,18.4603721746294));
#67483=CARTESIAN_POINT('Ctrl Pts',(30.5424433469957,1.41252449906513,18.4714718072734));
#67484=CARTESIAN_POINT('Ctrl Pts',(30.1611576166725,1.50380428740964,18.492351975203));
#67485=CARTESIAN_POINT('Ctrl Pts',(29.9661847612145,1.51203572283979,18.5012926108002));
#67486=CARTESIAN_POINT('Ctrl Pts',(29.583743920727,1.45401144673963,18.5213045897645));
#67487=CARTESIAN_POINT('Ctrl Pts',(29.3999206687447,1.38827539073469,18.5319747916547));
#67488=CARTESIAN_POINT('Ctrl Pts',(29.0627111089636,1.18787072518152,18.5537655904295));
#67489=CARTESIAN_POINT('Ctrl Pts',(28.9136362676481,1.05327089433686,18.5646768412665));
#67490=CARTESIAN_POINT('Ctrl Pts',(28.6818733006966,0.740747545450625,18.5845087463487));
#67491=CARTESIAN_POINT('Ctrl Pts',(28.5986773683508,0.567862991064222,18.593452056052));
#67492=CARTESIAN_POINT('Ctrl Pts',(28.4999017481138,0.194886335563048,18.6141729813576));
#67493=CARTESIAN_POINT('Ctrl Pts',(28.4872987443723,-0.0022124298529334,
18.6251229127696));
#67494=CARTESIAN_POINT('Ctrl Pts',(28.538885584329,-0.393300822235859,18.6468500456797));
#67495=CARTESIAN_POINT('Ctrl Pts',(28.6038229043615,-0.583241208522858,
18.6573608761808));
#67496=CARTESIAN_POINT('Ctrl Pts',(28.7997809979745,-0.919686600601166,
18.6761346196911));
#67497=CARTESIAN_POINT('Ctrl Pts',(28.9262538190534,-1.06460970419426,18.6862451878989));
#67498=CARTESIAN_POINT('Ctrl Pts',(29.2324514589516,-1.30386842227857,18.7076232042196));
#67499=CARTESIAN_POINT('Ctrl Pts',(29.4110795308611,-1.39369344460164,18.7187125908454));
#67500=CARTESIAN_POINT('Ctrl Pts',(29.7319270119205,-1.48199126728517,18.7366020897721));
#67501=CARTESIAN_POINT('Ctrl Pts',(29.8657845574029,-1.50000000000001,18.7435425565073));
#67502=CARTESIAN_POINT('Ctrl Pts',(30.0000000000002,-1.50000000000001,18.75));
#67503=CARTESIAN_POINT('Ctrl Pts',(30.,-1.50000000000001,18.8125));
#67504=CARTESIAN_POINT('Ctrl Pts',(29.9200694828282,-1.50000000000001,18.8086543411995));
#67505=CARTESIAN_POINT('Ctrl Pts',(29.8400989517173,-1.4936120985387,18.8046293155201));
#67506=CARTESIAN_POINT('Ctrl Pts',(29.5632380932733,-1.44889785862683,18.7900667790378));
#67507=CARTESIAN_POINT('Ctrl Pts',(29.3740258977232,-1.377754564609,18.7789871004233));
#67508=CARTESIAN_POINT('Ctrl Pts',(29.041174726881,-1.16949277461302,18.7571877412774));
#67509=CARTESIAN_POINT('Ctrl Pts',(28.8991316339595,-1.03690216726548,18.7466706173565));
#67510=CARTESIAN_POINT('Ctrl Pts',(28.6710550609186,-0.722648191218263,
18.7269680010074));
#67511=CARTESIAN_POINT('Ctrl Pts',(28.5881967902834,-0.543266122771758,
18.717681451265));
#67512=CARTESIAN_POINT('Ctrl Pts',(28.4956085723343,-0.160873384602161,
18.6964374102556));
#67513=CARTESIAN_POINT('Ctrl Pts',(28.4875239735192,0.0385552236194734,
18.6853580431322));
#67514=CARTESIAN_POINT('Ctrl Pts',(28.5480104653806,0.421875716785893,18.6640624601785));
#67515=CARTESIAN_POINT('Ctrl Pts',(28.6132160700899,0.602522755625134,18.6541515963916));
#67516=CARTESIAN_POINT('Ctrl Pts',(28.8119377533085,0.937035677616922,18.635298569339));
#67517=CARTESIAN_POINT('Ctrl Pts',(28.9464389491764,1.08605274148643,18.6246880146503));
#67518=CARTESIAN_POINT('Ctrl Pts',(29.2628767471001,1.32090830831045,18.6029396282541));
#67519=CARTESIAN_POINT('Ctrl Pts',(29.4409618987283,1.40557199772365,18.5920197332512));
#67520=CARTESIAN_POINT('Ctrl Pts',(29.814809484317,1.50065373381321,18.5713918235674));
#67521=CARTESIAN_POINT('Ctrl Pts',(30.0065604479866,1.51202122412194,18.5625182831912));
#67522=CARTESIAN_POINT('Ctrl Pts',(30.3943911928229,1.4610824148403,18.5424438008558));
#67523=CARTESIAN_POINT('Ctrl Pts',(30.58616263238,1.39524271133166,18.5313883125152));
#67524=CARTESIAN_POINT('Ctrl Pts',(30.9257469654151,1.19593240245758,18.5095136562056));
#67525=CARTESIAN_POINT('Ctrl Pts',(31.0718264769195,1.06698913560375,18.4989036450188));
#67526=CARTESIAN_POINT('Ctrl Pts',(31.3078217753803,0.759832047419874,18.4790171745892));
#67527=CARTESIAN_POINT('Ctrl Pts',(31.3951262846915,0.584269865007977,18.4699594369449));
#67528=CARTESIAN_POINT('Ctrl Pts',(31.4989966927882,0.205709858638526,18.4489283254799));
#67529=CARTESIAN_POINT('Ctrl Pts',(31.5130318328004,0.00600577899638372,
18.4378336543887));
#67530=CARTESIAN_POINT('Ctrl Pts',(31.4635867359632,-0.379900299649008,
18.4163944277973));
#67531=CARTESIAN_POINT('Ctrl Pts',(31.4034385131977,-0.562844950250642,
18.4062308360972));
#67532=CARTESIAN_POINT('Ctrl Pts',(31.213924427377,-0.903263174389702,18.387318712534));
#67533=CARTESIAN_POINT('Ctrl Pts',(31.0836707542498,-1.05603307941032,18.3769705479341));
#67534=CARTESIAN_POINT('Ctrl Pts',(30.7734274797909,-1.30006438227702,18.3552653141303));
#67535=CARTESIAN_POINT('Ctrl Pts',(30.5972523067208,-1.389838711312,18.3442953508018));
#67536=CARTESIAN_POINT('Ctrl Pts',(30.27555179434,-1.4809632576453,18.3262862902852));
#67537=CARTESIAN_POINT('Ctrl Pts',(30.1379932399681,-1.50000000000003,18.3191392028535));
#67538=CARTESIAN_POINT('Ctrl Pts',(29.9999999999998,-1.50000000000001,18.3125));
#67539=CARTESIAN_POINT('Origin',(30.,-1.32966554433622E-14,16.));
#67540=CARTESIAN_POINT('',(30.,-1.50000000000001,17.75));
#67541=CARTESIAN_POINT('',(30.,-1.50000000000001,17.8125));
#67542=CARTESIAN_POINT('',(30.,-1.50000000000001,16.));
#67543=CARTESIAN_POINT('Ctrl Pts',(30.,-1.50000000000001,17.75));
#67544=CARTESIAN_POINT('Ctrl Pts',(30.1165214576707,-1.50000000000002,17.755606141246));
#67545=CARTESIAN_POINT('Ctrl Pts',(30.2328774102524,-1.48642630258387,17.7615813667753));
#67546=CARTESIAN_POINT('Ctrl Pts',(30.5364815251301,-1.41429282343802,17.778192234317));
#67547=CARTESIAN_POINT('Ctrl Pts',(30.7156172892318,-1.33263663661631,17.7890791351975));
#67548=CARTESIAN_POINT('Ctrl Pts',(31.0356297737271,-1.1031687507031,17.8108498509785));
#67549=CARTESIAN_POINT('Ctrl Pts',(31.1725674881258,-0.956358157459637,
17.8215163418689));
#67550=CARTESIAN_POINT('Ctrl Pts',(31.376639002963,-0.625293846242278,17.8405309680715));
#67551=CARTESIAN_POINT('Ctrl Pts',(31.4447439774106,-0.445961069817197,
17.8502243850103));
#67552=CARTESIAN_POINT('Ctrl Pts',(31.5115582160321,-0.0642628969545898,
17.8714298390582));
#67553=CARTESIAN_POINT('Ctrl Pts',(31.5068955968845,0.134928419608339,17.8824960233117));
#67554=CARTESIAN_POINT('Ctrl Pts',(31.4208614242251,0.519471460613856,17.9038595255897));
#67555=CARTESIAN_POINT('Ctrl Pts',(31.3405819882652,0.701086441059189,17.9133091757132));
#67556=CARTESIAN_POINT('Ctrl Pts',(31.1170623100669,1.01937978501502,17.9329047530211));
#67557=CARTESIAN_POINT('Ctrl Pts',(30.9773620677606,1.15399638378434,17.9433654340287));
#67558=CARTESIAN_POINT('Ctrl Pts',(30.6484546459992,1.36726868066811,17.9651142302054));
#67559=CARTESIAN_POINT('Ctrl Pts',(30.4607652253454,1.44139714446346,17.9762035656613));
#67560=CARTESIAN_POINT('Ctrl Pts',(30.0756449322311,1.51026934438856,17.9966457910675));
#67561=CARTESIAN_POINT('Ctrl Pts',(29.8825476840369,1.50759466650969,18.005439964228));
#67562=CARTESIAN_POINT('Ctrl Pts',(29.5047175214704,1.42916638864856,18.025796889674));
#67563=CARTESIAN_POINT('Ctrl Pts',(29.323805468645,1.35298625851431,18.0366171395998));
#67564=CARTESIAN_POINT('Ctrl Pts',(28.9975535579724,1.13341344377778,18.0584131868245));
#67565=CARTESIAN_POINT('Ctrl Pts',(28.8562978602342,0.990703384015885,18.0691735230773));
#67566=CARTESIAN_POINT('Ctrl Pts',(28.6425900107442,0.665955504210131,18.088476321219));
#67567=CARTESIAN_POINT('Ctrl Pts',(28.5692557712623,0.488931672930093,18.0978371292817));
#67568=CARTESIAN_POINT('Ctrl Pts',(28.4911736103312,0.110209786397706,18.118877234089));
#67569=CARTESIAN_POINT('Ctrl Pts',(28.4897399259643,-0.0884146511275797,
18.1299119250627));
#67570=CARTESIAN_POINT('Ctrl Pts',(28.563963673652,-0.476687925939349,18.1514826625522));
#67571=CARTESIAN_POINT('Ctrl Pts',(28.6395954743022,-0.662348456736596,
18.1612794083161));
#67572=CARTESIAN_POINT('Ctrl Pts',(28.8549808751967,-0.987772207975308,
18.1806816918938));
#67573=CARTESIAN_POINT('Ctrl Pts',(28.9904690556508,-1.12587258901724,18.1910364917109));
#67574=CARTESIAN_POINT('Ctrl Pts',(29.3122241078786,-1.34783032180127,18.2126824314563));
#67575=CARTESIAN_POINT('Ctrl Pts',(29.4971108100191,-1.42716337813628,18.2237814930698));
#67576=CARTESIAN_POINT('Ctrl Pts',(29.7935943795659,-1.48934588454492,18.2397733573052));
#67577=CARTESIAN_POINT('Ctrl Pts',(29.8967698772032,-1.50000000000001,18.2450333384012));
#67578=CARTESIAN_POINT('Ctrl Pts',(30.,-1.50000000000001,18.25));
#67579=CARTESIAN_POINT('Ctrl Pts',(29.9999999999998,-1.50000000000001,18.3125));
#67580=CARTESIAN_POINT('Ctrl Pts',(29.9486057940186,-1.50000000000001,18.3100272951118));
#67581=CARTESIAN_POINT('Ctrl Pts',(29.8971583803719,-1.4973588143077,18.3074786639994));
#67582=CARTESIAN_POINT('Ctrl Pts',(29.6480074739756,-1.47161947014145,18.294776403644));
#67583=CARTESIAN_POINT('Ctrl Pts',(29.4562105276991,-1.41203266981329,18.2838933798658));
#67584=CARTESIAN_POINT('Ctrl Pts',(29.1116733937691,-1.22407639141983,18.2620958215476));
#67585=CARTESIAN_POINT('Ctrl Pts',(28.9612380534891,-1.09930641465076,18.2513921651757));
#67586=CARTESIAN_POINT('Ctrl Pts',(28.7165798694464,-0.800027931931824,
18.231307751621));
#67587=CARTESIAN_POINT('Ctrl Pts',(28.6244510402799,-0.628553460673264,
18.2224196367041));
#67588=CARTESIAN_POINT('Ctrl Pts',(28.5083938755392,-0.254315567480426,
18.2016286426378));
#67589=CARTESIAN_POINT('Ctrl Pts',(28.4878541874048,-0.054508044740069,
18.1905282247078));
#67590=CARTESIAN_POINT('Ctrl Pts',(28.5251827599344,0.333985841156563,18.1689452310469));
#67591=CARTESIAN_POINT('Ctrl Pts',(28.5797880070138,0.519280463308488,18.1586510853718));
#67592=CARTESIAN_POINT('Ctrl Pts',(28.7594942565881,0.866593796413574,18.1393559001993));
#67593=CARTESIAN_POINT('Ctrl Pts',(28.8856977548396,1.02381782162173,18.1293391744996));
#67594=CARTESIAN_POINT('Ctrl Pts',(29.1898211855382,1.2775694571787,18.1076583725746));
#67595=CARTESIAN_POINT('Ctrl Pts',(29.3638803222543,1.37256230066096,18.096645258358));
#67596=CARTESIAN_POINT('Ctrl Pts',(29.732534735318,1.48813273455022,18.0756980748094));
#67597=CARTESIAN_POINT('Ctrl Pts',(29.9228794435952,1.51000349618475,18.066488339394));
#67598=CARTESIAN_POINT('Ctrl Pts',(30.3105607244676,1.48091384388274,18.0470279691741));
#67599=CARTESIAN_POINT('Ctrl Pts',(30.5039294602603,1.4267400893485,18.0362196850207));
#67600=CARTESIAN_POINT('Ctrl Pts',(30.8540539626656,1.24831186951753,18.0144179726049));
#67601=CARTESIAN_POINT('Ctrl Pts',(31.0082947964679,1.12740587313612,18.0036385571291));
#67602=CARTESIAN_POINT('Ctrl Pts',(31.2606439376435,0.835225571389926,17.9833812839205));
#67603=CARTESIAN_POINT('Ctrl Pts',(31.3570327509323,0.667298431844612,17.9745721351024));
#67604=CARTESIAN_POINT('Ctrl Pts',(31.4837741625619,0.297001147228916,17.9540000637349));
#67605=CARTESIAN_POINT('Ctrl Pts',(31.5100733842477,0.0972732161684081,
17.9429040675649));
#67606=CARTESIAN_POINT('Ctrl Pts',(31.4835317838137,-0.293194316444828,
17.9212114268642));
#67607=CARTESIAN_POINT('Ctrl Pts',(31.4338905957024,-0.480424140062753,
17.9108097699965));
#67608=CARTESIAN_POINT('Ctrl Pts',(31.2642037542022,-0.83118542637216,17.8913230318682));
#67609=CARTESIAN_POINT('Ctrl Pts',(31.14378015867,-0.99038786521744,17.8816860411746));
#67610=CARTESIAN_POINT('Ctrl Pts',(30.8486060826855,-1.25246692848107,17.8602044978428));
#67611=CARTESIAN_POINT('Ctrl Pts',(30.6769673305094,-1.35296725332812,17.8491548488382));
#67612=CARTESIAN_POINT('Ctrl Pts',(30.3327732686651,-1.47215364288648,17.8292840712733));
#67613=CARTESIAN_POINT('Ctrl Pts',(30.1668871533766,-1.50000000000002,17.8205293619105));
#67614=CARTESIAN_POINT('Ctrl Pts',(29.9999999999999,-1.50000000000001,17.8125));
#67615=CARTESIAN_POINT('Origin',(30.,-1.32966554433622E-14,16.));
#67616=CARTESIAN_POINT('',(29.9999999999999,-1.50000000000001,17.25));
#67617=CARTESIAN_POINT('',(30.,-1.50000000000001,17.3125));
#67618=CARTESIAN_POINT('',(30.,-1.50000000000001,16.));
#67619=CARTESIAN_POINT('Ctrl Pts',(29.9999999999998,-1.50000000000001,17.25));
#67620=CARTESIAN_POINT('Ctrl Pts',(30.1437406795734,-1.50000000000003,17.2569157266704));
#67621=CARTESIAN_POINT('Ctrl Pts',(30.2869532673798,-1.47934432155244,17.2643798143597));
#67622=CARTESIAN_POINT('Ctrl Pts',(30.6133040117111,-1.38286217393555,17.2827614315232));
#67623=CARTESIAN_POINT('Ctrl Pts',(30.7886268831202,-1.29093521604786,17.2937501837148));
#67624=CARTESIAN_POINT('Ctrl Pts',(31.0976621700988,-1.04186059007729,17.3155373905022));
#67625=CARTESIAN_POINT('Ctrl Pts',(31.2270940102629,-0.885739363684009,
17.3257922575731));
#67626=CARTESIAN_POINT('Ctrl Pts',(31.4122925189225,-0.540349731904653,
17.3449805704497));
#67627=CARTESIAN_POINT('Ctrl Pts',(31.4695815451721,-0.356167506723217,
17.3552129162933));
#67628=CARTESIAN_POINT('Ctrl Pts',(31.5127670349393,0.0311250181831806,
17.376729167677));
#67629=CARTESIAN_POINT('Ctrl Pts',(31.4953668358477,0.230908289106308,17.3878282382838));
#67630=CARTESIAN_POINT('Ctrl Pts',(31.3851742993692,0.607249385403804,17.408736076967));
#67631=CARTESIAN_POINT('Ctrl Pts',(31.2953707932844,0.78068569360338,17.4176954906944));
#67632=CARTESIAN_POINT('Ctrl Pts',(31.054895847731,1.08378386704463,17.4376847406135));
#67633=CARTESIAN_POINT('Ctrl Pts',(30.9065553840191,1.21059289157644,17.4483442474051));
#67634=CARTESIAN_POINT('Ctrl Pts',(30.5651448786952,1.40362381134034,17.4701323379946));
#67635=CARTESIAN_POINT('Ctrl Pts',(30.3742618691092,1.46611551598061,17.4810520817598));
#67636=CARTESIAN_POINT('Ctrl Pts',(29.9878426931301,1.51196372025337,17.5009172442622));
#67637=CARTESIAN_POINT('Ctrl Pts',(29.7964276873605,1.49824842026232,17.5098430324513));
#67638=CARTESIAN_POINT('Ctrl Pts',(29.423704438961,1.39861791618851,17.5305432021031));
#67639=CARTESIAN_POINT('Ctrl Pts',(29.2464613140656,1.31164870813791,17.5414866272603));
#67640=CARTESIAN_POINT('Ctrl Pts',(28.9327465597656,1.07261781027188,17.5632199825769));
#67641=CARTESIAN_POINT('Ctrl Pts',(28.8001758891987,0.921899105215767,17.5737833830436));
#67642=CARTESIAN_POINT('Ctrl Pts',(28.6055876448106,0.584753731199478,17.5925136816001));
#67643=CARTESIAN_POINT('Ctrl Pts',(28.5426610065469,0.403064732761888,17.6026075148466));
#67644=CARTESIAN_POINT('Ctrl Pts',(28.487113056257,0.0186136653436067,17.623965907481));
#67645=CARTESIAN_POINT('Ctrl Pts',(28.4978576022209,-0.180959534499292,
17.6350533074722));
#67646=CARTESIAN_POINT('Ctrl Pts',(28.5955062015491,-0.561653522812593,
17.6562029734896));
#67647=CARTESIAN_POINT('Ctrl Pts',(28.6803571582567,-0.739318323214391,
17.6653786075964));
#67648=CARTESIAN_POINT('Ctrl Pts',(28.9119736981394,-1.05041195534416,17.6851637533487));
#67649=CARTESIAN_POINT('Ctrl Pts',(29.0558270731865,-1.1813919096406,17.6957232341464));
#67650=CARTESIAN_POINT('Ctrl Pts',(29.3917078154049,-1.38569020760041,17.7175582566121));
#67651=CARTESIAN_POINT('Ctrl Pts',(29.5820781032457,-1.45448064464283,17.7286282968298));
#67652=CARTESIAN_POINT('Ctrl Pts',(29.8532284268276,-1.49461899708891,17.7427889770903));
#67653=CARTESIAN_POINT('Ctrl Pts',(29.9266397495672,-1.50000000000001,17.7464704533054));
#67654=CARTESIAN_POINT('Ctrl Pts',(30.,-1.50000000000001,17.75));
#67655=CARTESIAN_POINT('Ctrl Pts',(29.9999999999999,-1.50000000000001,17.8125));
#67656=CARTESIAN_POINT('Ctrl Pts',(29.9772840745252,-1.50000000000001,17.811407079526));
#67657=CARTESIAN_POINT('Ctrl Pts',(29.9545509622526,-1.49948399224778,17.8102989986031));
#67658=CARTESIAN_POINT('Ctrl Pts',(29.7331702393738,-1.48941079200354,17.7993680024896));
#67659=CARTESIAN_POINT('Ctrl Pts',(29.5383211874472,-1.44096198242896,17.7886475228419));
#67660=CARTESIAN_POINT('Ctrl Pts',(29.1826189299973,-1.27271128807371,17.7668601596023));
#67661=CARTESIAN_POINT('Ctrl Pts',(29.0244894301944,-1.15598200374574,17.7560096703756));
#67662=CARTESIAN_POINT('Ctrl Pts',(28.764135320164,-0.871290254073719,17.7355752732588));
#67663=CARTESIAN_POINT('Ctrl Pts',(28.6633306533142,-0.706980266162622,
17.7267766814534));
#67664=CARTESIAN_POINT('Ctrl Pts',(28.5256044330412,-0.340872542641299,
17.70643736348));
#67665=CARTESIAN_POINT('Ctrl Pts',(28.4933384090279,-0.141395913779689,
17.6953553285433));
#67666=CARTESIAN_POINT('Ctrl Pts',(28.5086475773052,0.250803035896437,17.6735664980057));
#67667=CARTESIAN_POINT('Ctrl Pts',(28.5530910089168,0.439894111123241,17.6630614382709));
#67668=CARTESIAN_POINT('Ctrl Pts',(28.7124602775381,0.794124581104987,17.6433819677164));
#67669=CARTESIAN_POINT('Ctrl Pts',(28.8270773285161,0.955330804312479,17.6340619682235));
#67670=CARTESIAN_POINT('Ctrl Pts',(29.1130611662184,1.22571784831621,17.6127918131944));
#67671=CARTESIAN_POINT('Ctrl Pts',(29.2820600929988,1.33176716482588,17.6017150341911));
#67672=CARTESIAN_POINT('Ctrl Pts',(29.6446531268203,1.46968030941703,17.5804388480344));
#67673=CARTESIAN_POINT('Ctrl Pts',(29.8337664889299,1.50284763615596,17.5705770145346));
#67674=CARTESIAN_POINT('Ctrl Pts',(30.2227595353817,1.49663210693258,17.5516889242716));
#67675=CARTESIAN_POINT('Ctrl Pts',(30.4189176611452,1.45396403183943,17.5410660377374));
#67676=CARTESIAN_POINT('Ctrl Pts',(30.7799134803451,1.29609345193241,17.5193123244018));
#67677=CARTESIAN_POINT('Ctrl Pts',(30.9418307309724,1.18367445855365,17.5083993272327));
#67678=CARTESIAN_POINT('Ctrl Pts',(31.2101475557693,0.906543829758461,17.4877918549585));
#67679=CARTESIAN_POINT('Ctrl Pts',(31.3153431699375,0.745751786456619,17.478930654803));
#67680=CARTESIAN_POINT('Ctrl Pts',(31.463864637894,0.383898047749162,17.4588276693193));
#67681=CARTESIAN_POINT('Ctrl Pts',(31.5020303054666,0.184838532612863,17.4477688073673));
#67682=CARTESIAN_POINT('Ctrl Pts',(31.4978841524782,-0.208759642694536,
17.4259022420724));
#67683=CARTESIAN_POINT('Ctrl Pts',(31.4586348080642,-0.399547636290809,
17.4153029090948));
#67684=CARTESIAN_POINT('Ctrl Pts',(31.3094217036004,-0.757113584921528,
17.3954381341709));
#67685=CARTESIAN_POINT('Ctrl Pts',(31.200380183046,-0.920271802442848,17.3863568795276));
#67686=CARTESIAN_POINT('Ctrl Pts',(30.923406682912,-1.19858244148629,17.3653001347046));
#67687=CARTESIAN_POINT('Ctrl Pts',(30.7571425046312,-1.30996529750999,17.3542067774745));
#67688=CARTESIAN_POINT('Ctrl Pts',(30.3978227489156,-1.45880886920802,17.3327844540089));
#67689=CARTESIAN_POINT('Ctrl Pts',(30.2092450764931,-1.49754020852369,17.3226356359777));
#67690=CARTESIAN_POINT('Ctrl Pts',(30.0122952852091,-1.49996221637769,17.3130926067305));
#67691=CARTESIAN_POINT('Ctrl Pts',(30.0061468402235,-1.50000000000001,17.3127957399881));
#67692=CARTESIAN_POINT('Ctrl Pts',(30.,-1.50000000000001,17.3125));
#67693=CARTESIAN_POINT('Origin',(30.,-1.32966554433622E-14,16.));
#67694=CARTESIAN_POINT('',(30.,-1.50000000000001,16.75));
#67695=CARTESIAN_POINT('',(30.0000000000001,-1.50000000000001,16.8125));
#67696=CARTESIAN_POINT('',(30.,-1.50000000000001,16.));
#67697=CARTESIAN_POINT('Ctrl Pts',(30.,-1.50000000000001,16.75));
#67698=CARTESIAN_POINT('Ctrl Pts',(30.1733135774153,-1.50000000000002,16.7583385533812));
#67699=CARTESIAN_POINT('Ctrl Pts',(30.3454665850143,-1.46996630625128,16.767455538092));
#67700=CARTESIAN_POINT('Ctrl Pts',(30.6943533649566,-1.34416445320596,16.7877358570363));
#67701=CARTESIAN_POINT('Ctrl Pts',(30.8648984846931,-1.24131259552183,16.7987982089822));
#67702=CARTESIAN_POINT('Ctrl Pts',(31.1561999433551,-0.975703692756434,
16.8201914820235));
#67703=CARTESIAN_POINT('Ctrl Pts',(31.2741613882488,-0.815654351280513,
16.8296858693734));
#67704=CARTESIAN_POINT('Ctrl Pts',(31.4395048489934,-0.463422668720622,
16.8492542961822));
#67705=CARTESIAN_POINT('Ctrl Pts',(31.4869681438372,-0.275392752547583,
16.8597004026363));
#67706=CARTESIAN_POINT('Ctrl Pts',(31.5087956503657,0.115841301406496,16.881435627856));
#67707=CARTESIAN_POINT('Ctrl Pts',(31.4799884843839,0.315484512989904,16.8925269173884));
#67708=CARTESIAN_POINT('Ctrl Pts',(31.3486206066034,0.684034451059388,16.9130019139478));
#67709=CARTESIAN_POINT('Ctrl Pts',(31.2503774147184,0.850433854559545,16.9217976845453));
#67710=CARTESIAN_POINT('Ctrl Pts',(30.994668844219,1.13948462780369,16.9421296570253));
#67711=CARTESIAN_POINT('Ctrl Pts',(30.8387866934565,1.25865700214481,16.9529398842324));
#67712=CARTESIAN_POINT('Ctrl Pts',(30.4862910667067,1.43284604521895,16.9747379225116));
#67713=CARTESIAN_POINT('Ctrl Pts',(30.2922814189341,1.48462820882751,16.9855106094757));
#67714=CARTESIAN_POINT('Ctrl Pts',(29.904287970164,1.50893843055208,17.0048532369201));
#67715=CARTESIAN_POINT('Ctrl Pts',(29.714222422622,1.48472560659638,17.014173768808));
#67716=CARTESIAN_POINT('Ctrl Pts',(29.3467837907597,1.36454370703768,17.0351905543248));
#67717=CARTESIAN_POINT('Ctrl Pts',(29.1737126610206,1.26724866527873,17.0462200829857));
#67718=CARTESIAN_POINT('Ctrl Pts',(28.8733100927186,1.01000510192613,17.0678188628294));
#67719=CARTESIAN_POINT('Ctrl Pts',(28.7495253450837,0.851954282658887,17.0776692065189));
#67720=CARTESIAN_POINT('Ctrl Pts',(28.5739823591041,0.503198698880474,17.0970445167289));
#67721=CARTESIAN_POINT('Ctrl Pts',(28.5214293436323,0.317084997718663,17.1073841667934));
#67722=CARTESIAN_POINT('Ctrl Pts',(28.4885674976081,-0.0722634762162506,
17.1290146375676));
#67723=CARTESIAN_POINT('Ctrl Pts',(28.5114956545415,-0.272057456078969,
17.1401143031155));
#67724=CARTESIAN_POINT('Ctrl Pts',(28.6319945909535,-0.644674063533988,
17.1608152257519));
#67725=CARTESIAN_POINT('Ctrl Pts',(28.7258902835189,-0.814669507709904,
17.1696624095652));
#67726=CARTESIAN_POINT('Ctrl Pts',(28.9737348011573,-1.1110192567928,17.1898187719544));
#67727=CARTESIAN_POINT('Ctrl Pts',(29.1257542814876,-1.2342064357884,17.2005546786951));
#67728=CARTESIAN_POINT('Ctrl Pts',(29.4726321438156,-1.41824610841819,17.2223560607564));
#67729=CARTESIAN_POINT('Ctrl Pts',(29.6650975807577,-1.47560141498182,17.2332092613688));
#67730=CARTESIAN_POINT('Ctrl Pts',(29.9087297050291,-1.49791971441829,17.2455509701752));
#67731=CARTESIAN_POINT('Ctrl Pts',(29.9543886563371,-1.50000000000001,17.2478055232048));
#67732=CARTESIAN_POINT('Ctrl Pts',(29.9999999999998,-1.50000000000001,17.25));
#67733=CARTESIAN_POINT('Ctrl Pts',(30.,-1.50000000000001,17.3125));
#67734=CARTESIAN_POINT('Ctrl Pts',(29.8075276745562,-1.50000000000001,17.3032396709245));
#67735=CARTESIAN_POINT('Ctrl Pts',(29.6167265402445,-1.46295509134636,17.2930307218294));
#67736=CARTESIAN_POINT('Ctrl Pts',(29.2565239800332,-1.31741270776536,17.2716576240826));
#67737=CARTESIAN_POINT('Ctrl Pts',(29.0910935230227,-1.20922562866616,17.2606931508671));
#67738=CARTESIAN_POINT('Ctrl Pts',(28.8152192771185,-0.939380042859163,
17.2399244343056));
#67739=CARTESIAN_POINT('Ctrl Pts',(28.7058473428781,-0.781856067083356,
17.2309364481713));
#67740=CARTESIAN_POINT('Ctrl Pts',(28.5481536416827,-0.426269472803969,
17.211181637378));
#67741=CARTESIAN_POINT('Ctrl Pts',(28.5044938401357,-0.230229772369996,
17.2002905429095));
#67742=CARTESIAN_POINT('Ctrl Pts',(28.4962752409133,0.162097483734217,17.178494584237));
#67743=CARTESIAN_POINT('Ctrl Pts',(28.5297146688179,0.3545967167103,17.167800182405));
#67744=CARTESIAN_POINT('Ctrl Pts',(28.6677231734513,0.715751667501951,17.1477360184722));
#67745=CARTESIAN_POINT('Ctrl Pts',(28.7707689938353,0.881053857184024,17.1388343527704));
#67746=CARTESIAN_POINT('Ctrl Pts',(29.0378553430027,1.16782543883526,17.1180182775366));
#67747=CARTESIAN_POINT('Ctrl Pts',(29.2009578477084,1.28493633443696,17.1069179241867));
#67748=CARTESIAN_POINT('Ctrl Pts',(29.5564777297123,1.44564779283652,17.0853487587108));
#67749=CARTESIAN_POINT('Ctrl Pts',(29.7443345881639,1.49039149544099,17.0750676107666));
#67750=CARTESIAN_POINT('Ctrl Pts',(30.1352017346056,1.50720082969336,17.0557950804638));
#67751=CARTESIAN_POINT('Ctrl Pts',(30.3346031531762,1.47580805773789,17.0457293998907));
#67752=CARTESIAN_POINT('Ctrl Pts',(30.7060862860091,1.33790450333634,17.02402575504));
#67753=CARTESIAN_POINT('Ctrl Pts',(30.8749553104054,1.23409963004519,17.0130175716131));
#67754=CARTESIAN_POINT('Ctrl Pts',(31.1584137835032,0.971677105747927,16.9920901549037));
#67755=CARTESIAN_POINT('Ctrl Pts',(31.271994699923,0.817368296550736,16.9829093498084));
#67756=CARTESIAN_POINT('Ctrl Pts',(31.4394257557863,0.466485221859018,16.9634158456588));
#67757=CARTESIAN_POINT('Ctrl Pts',(31.488516036617,0.271760297088586,16.9525977942827));
#67758=CARTESIAN_POINT('Ctrl Pts',(31.5076810248584,-0.120678265071266,
16.9307956519405));
#67759=CARTESIAN_POINT('Ctrl Pts',(31.4794384691607,-0.314545865899112,
16.9200252296723));
#67760=CARTESIAN_POINT('Ctrl Pts',(31.3513352758344,-0.678794152386266,
16.8997892137563));
#67761=CARTESIAN_POINT('Ctrl Pts',(31.2534603041453,-0.845994238167287,
16.890973963719));
#67762=CARTESIAN_POINT('Ctrl Pts',(30.9950590391717,-1.14001068930543,16.8703745034186));
#67763=CARTESIAN_POINT('Ctrl Pts',(30.8348670617779,-1.26204295887652,16.8592774780469));
#67764=CARTESIAN_POINT('Ctrl Pts',(30.4829704713108,-1.43301939771413,16.8375974999208));
#67765=CARTESIAN_POINT('Ctrl Pts',(30.2958966065637,-1.48299380376918,16.8272087264607));
#67766=CARTESIAN_POINT('Ctrl Pts',(30.0696474084832,-1.49878860163674,16.8158845624575));
#67767=CARTESIAN_POINT('Ctrl Pts',(30.0348056486057,-1.50000000000001,16.8141745875493));
#67768=CARTESIAN_POINT('Ctrl Pts',(30.0000000000002,-1.50000000000001,16.8125));
#67769=CARTESIAN_POINT('Origin',(30.,-1.32966554433622E-14,16.));
#67770=CARTESIAN_POINT('',(30.0000000000023,1.33373412263454,16.1584936490537));
#67771=CARTESIAN_POINT('',(30.,1.1752404735808,16.));
#67772=CARTESIAN_POINT('',(30.,1.17524047358083,16.));
#67773=CARTESIAN_POINT('',(30.,-1.17524047358085,16.));
#67774=CARTESIAN_POINT('Ctrl Pts',(30.,-1.17524047358083,16.));
#67775=CARTESIAN_POINT('Ctrl Pts',(30.0938726776238,-1.17889502189498,16.0036545483141));
#67776=CARTESIAN_POINT('Ctrl Pts',(30.2222715669962,-1.17292308708929,16.0088746896198));
#67777=CARTESIAN_POINT('Ctrl Pts',(30.4821758748939,-1.10061359842964,16.0205734257761));
#67778=CARTESIAN_POINT('Ctrl Pts',(30.5904809486724,-1.05245648363552,16.0257840816621));
#67779=CARTESIAN_POINT('Ctrl Pts',(30.8133642274912,-0.91102859460423,16.0372929849601));
#67780=CARTESIAN_POINT('Ctrl Pts',(30.9213977318432,-0.810903247446717,
16.0434573291476));
#67781=CARTESIAN_POINT('Ctrl Pts',(31.1067869536601,-0.562636269482013,
16.0555173993883));
#67782=CARTESIAN_POINT('Ctrl Pts',(31.1779495349821,-0.411557996758087,
16.0617064115579));
#67783=CARTESIAN_POINT('Ctrl Pts',(31.2569648094213,-0.0966670523057213,
16.075198195417));
#67784=CARTESIAN_POINT('Ctrl Pts',(31.2657685184509,0.0650399419384585,
16.0820144838088));
#67785=CARTESIAN_POINT('Ctrl Pts',(31.2286447980599,0.334175553677255,16.0931820826379));
#67786=CARTESIAN_POINT('Ctrl Pts',(31.1927617340632,0.495209878479218,16.0995752755442));
#67787=CARTESIAN_POINT('Ctrl Pts',(31.0046982036223,0.825162649859306,16.1133508913014));
#67788=CARTESIAN_POINT('Ctrl Pts',(30.8901527526008,0.956864086379422,16.1201881413696));
#67789=CARTESIAN_POINT('Ctrl Pts',(30.6234294043457,1.16264469041258,16.1337830625282));
#67790=CARTESIAN_POINT('Ctrl Pts',(30.4758334589096,1.2374906559331,16.1404068749596));
#67791=CARTESIAN_POINT('Ctrl Pts',(30.2026344427889,1.31649705751482,16.1513204506313));
#67792=CARTESIAN_POINT('Ctrl Pts',(30.094862299376,1.33047991225226,16.1552394386714));
#67793=CARTESIAN_POINT('Ctrl Pts',(30.0000000000046,1.33373412263454,16.1584936490537));
#67794=CARTESIAN_POINT('Origin',(30.,-1.32966554433622E-14,16.));
#67795=CARTESIAN_POINT('Origin',(30.,-1.21864324187371E-14,15.78125));
#67796=CARTESIAN_POINT('',(30.0000000000002,-1.17524047358085,16.0625));
#67797=CARTESIAN_POINT('',(30.,-1.17524047358085,15.78125));
#67798=CARTESIAN_POINT('',(29.1765921258349,-0.838564036615843,16.));
#67799=CARTESIAN_POINT('Ctrl Pts',(30.0000000000004,-1.17524047358085,16.0625));
#67800=CARTESIAN_POINT('Ctrl Pts',(29.8936372832897,-1.17524047358089,16.0559685129868));
#67801=CARTESIAN_POINT('Ctrl Pts',(29.7875857388152,-1.16080842474563,16.0489444642731));
#67802=CARTESIAN_POINT('Ctrl Pts',(29.5893382840682,-1.10559796441283,16.034813132098));
#67803=CARTESIAN_POINT('Ctrl Pts',(29.4977179176601,-1.06709869274158,16.0278219954706));
#67804=CARTESIAN_POINT('Ctrl Pts',(29.3263212626278,-0.968061456605931,
16.0137856854629));
#67805=CARTESIAN_POINT('Ctrl Pts',(29.2472234502441,-0.90791877416947,16.0067961899552));
#67806=CARTESIAN_POINT('Ctrl Pts',(29.176592125834,-0.838564036614912,15.9999999999999));
#67807=CARTESIAN_POINT('Origin',(30.,-1.32966554433622E-14,16.));
#67808=CARTESIAN_POINT('Origin',(30.,-1.21864324187371E-14,15.78125));
#67809=CARTESIAN_POINT('',(30.0000000000002,-1.17524047358085,16.5625));
#67810=CARTESIAN_POINT('',(30.,-1.17524047358085,16.5));
#67811=CARTESIAN_POINT('',(30.,-1.17524047358085,15.78125));
#67812=CARTESIAN_POINT('Ctrl Pts',(30.0000000000004,-1.17524047358085,16.5625));
#67813=CARTESIAN_POINT('Ctrl Pts',(29.8712710011335,-1.17524047358089,16.5545950516279));
#67814=CARTESIAN_POINT('Ctrl Pts',(29.7432544697015,-1.15409887958747,16.5459843057103));
#67815=CARTESIAN_POINT('Ctrl Pts',(29.4749058017838,-1.06268366571272,16.5262646272929));
#67816=CARTESIAN_POINT('Ctrl Pts',(29.3400104190766,-0.984598569044377,
16.515212607152));
#67817=CARTESIAN_POINT('Ctrl Pts',(29.1121607207208,-0.784303734398693,
16.4941196868072));
#67818=CARTESIAN_POINT('Ctrl Pts',(29.0200231478196,-0.665589512335134,
16.4846952710458));
#67819=CARTESIAN_POINT('Ctrl Pts',(28.8817974975863,-0.393869611486594,
16.465428299239));
#67820=CARTESIAN_POINT('Ctrl Pts',(28.83947486215,-0.242215228858268,16.4546748700446));
#67821=CARTESIAN_POINT('Ctrl Pts',(28.8167032491755,0.0653802904577292,
16.4328640487538));
#67822=CARTESIAN_POINT('Ctrl Pts',(28.8351718353917,0.218291541824621,16.422021498172));
#67823=CARTESIAN_POINT('Ctrl Pts',(28.9287391651494,0.506051914833821,16.4016171370023));
#67824=CARTESIAN_POINT('Ctrl Pts',(29.0019741006921,0.638460005621421,16.3928173224174));
#67825=CARTESIAN_POINT('Ctrl Pts',(29.1986594960153,0.873851822283252,16.3723938102577));
#67826=CARTESIAN_POINT('Ctrl Pts',(29.3222166226463,0.972810188230982,16.3612980106481));
#67827=CARTESIAN_POINT('Ctrl Pts',(29.5955374213776,1.11370354874836,16.3395188200451));
#67828=CARTESIAN_POINT('Ctrl Pts',(29.7416409158841,1.1563714827732,16.3290342066007));
#67829=CARTESIAN_POINT('Ctrl Pts',(30.0452139523297,1.18442751027465,16.309397801581));
#67830=CARTESIAN_POINT('Ctrl Pts',(30.1998697024494,1.16832333055968,16.2999812279383));
#67831=CARTESIAN_POINT('Ctrl Pts',(30.4949641982123,1.07710916023858,16.2786262781941));
#67832=CARTESIAN_POINT('Ctrl Pts',(30.6323783558426,1.00262103976947,16.2675471121926));
#67833=CARTESIAN_POINT('Ctrl Pts',(30.8661146099677,0.80826573510396,16.246303290685));
#67834=CARTESIAN_POINT('Ctrl Pts',(30.9615634972897,0.691955855651338,16.2365648418493));
#67835=CARTESIAN_POINT('Ctrl Pts',(31.1071384709944,0.423965303495795,16.217562308738));
#67836=CARTESIAN_POINT('Ctrl Pts',(31.153539286677,0.273539680121433,16.2068960077584));
#67837=CARTESIAN_POINT('Ctrl Pts',(31.1846742020807,-0.0336925499575308,
16.1851109463897));
#67838=CARTESIAN_POINT('Ctrl Pts',(31.1702391074247,-0.187447361382806,
16.174208581095));
#67839=CARTESIAN_POINT('Ctrl Pts',(31.0842361864784,-0.477469105777865,
16.1536438717926));
#67840=CARTESIAN_POINT('Ctrl Pts',(31.0147909316618,-0.611342914691707,
16.1448082262658));
#67841=CARTESIAN_POINT('Ctrl Pts',(30.8246452237759,-0.851973319529638,
16.1246005735716));
#67842=CARTESIAN_POINT('Ctrl Pts',(30.7034471847234,-0.954486386541281,
16.1135236126058));
#67843=CARTESIAN_POINT('Ctrl Pts',(30.4332129266933,-1.10289061678379,16.0916676708875));
#67844=CARTESIAN_POINT('Ctrl Pts',(30.2878849143487,-1.14942616400118,16.0810935566577));
#67845=CARTESIAN_POINT('Ctrl Pts',(30.0919105154022,-1.17254804866719,16.0682394674743));
#67846=CARTESIAN_POINT('Ctrl Pts',(30.0459321343385,-1.17524047358084,16.0653205855228));
#67847=CARTESIAN_POINT('Ctrl Pts',(30.0000000000004,-1.17524047358085,16.0625));
#67848=CARTESIAN_POINT('Ctrl Pts',(29.9999999999986,-1.17524047358085,15.9999999999999));
#67849=CARTESIAN_POINT('Ctrl Pts',(30.1214028111116,-1.17524047358099,16.0074550642242));
#67850=CARTESIAN_POINT('Ctrl Pts',(30.2421537204218,-1.15643017464734,16.0155369920666));
#67851=CARTESIAN_POINT('Ctrl Pts',(30.4776301337898,-1.08113291233427,16.0326666201836));
#67852=CARTESIAN_POINT('Ctrl Pts',(30.5903997908,-1.02391620718435,16.0416200885134));
#67853=CARTESIAN_POINT('Ctrl Pts',(30.8179173133188,-0.858187726048923,
16.0614671043063));
#67854=CARTESIAN_POINT('Ctrl Pts',(30.9244135286053,-0.742266950950034,
16.0721166138301));
#67855=CARTESIAN_POINT('Ctrl Pts',(31.0824458543846,-0.481384401141323,
16.0910702726526));
#67856=CARTESIAN_POINT('Ctrl Pts',(31.1347636661213,-0.340257482296023,
16.1008732014181));
#67857=CARTESIAN_POINT('Ctrl Pts',(31.1847167047507,-0.0402726429290417,
16.1221443686182));
#67858=CARTESIAN_POINT('Ctrl Pts',(31.1797095913038,0.116033015525934,16.1332276080324));
#67859=CARTESIAN_POINT('Ctrl Pts',(31.1096057651028,0.416692954381308,16.1545466448319));
#67860=CARTESIAN_POINT('Ctrl Pts',(31.0456145958404,0.558153128413804,16.1639131875247));
#67861=CARTESIAN_POINT('Ctrl Pts',(30.868452148125,0.806074678480504,16.1835820667589));
#67862=CARTESIAN_POINT('Ctrl Pts',(30.7578944192075,0.910792535772415,16.1940837990854));
#67863=CARTESIAN_POINT('Ctrl Pts',(30.4982839285527,1.07586594639843,16.2158783446996));
#67864=CARTESIAN_POINT('Ctrl Pts',(30.350445183185,1.13268560339106,16.2269712473271));
#67865=CARTESIAN_POINT('Ctrl Pts',(30.0480054721768,1.18378716120051,16.2473551076386));
#67866=CARTESIAN_POINT('Ctrl Pts',(29.8968386090012,1.18026105605562,16.2561569026374));
#67867=CARTESIAN_POINT('Ctrl Pts',(29.6011798659176,1.11599305250821,16.276591159187));
#67868=CARTESIAN_POINT('Ctrl Pts',(29.4597499374869,1.05480717934155,16.2874453099545));
#67869=CARTESIAN_POINT('Ctrl Pts',(29.2055652972218,0.87997645163687,16.3092526000714));
#67870=CARTESIAN_POINT('Ctrl Pts',(29.0959568884663,0.766951615708884,16.3199905502909));
#67871=CARTESIAN_POINT('Ctrl Pts',(28.9310246543964,0.510549118020342,16.3392090818415));
#67872=CARTESIAN_POINT('Ctrl Pts',(28.8749728808886,0.371095429589151,16.348686560472));
#67873=CARTESIAN_POINT('Ctrl Pts',(28.8169184420094,0.0732292943615943,
16.3698074957134));
#67874=CARTESIAN_POINT('Ctrl Pts',(28.817543647408,-0.0827153411142831,
16.3808651359001));
#67875=CARTESIAN_POINT('Ctrl Pts',(28.8792006517981,-0.386085589929172,
16.4023763539327));
#67876=CARTESIAN_POINT('Ctrl Pts',(28.9398691853048,-0.530428612710414,
16.4120388426041));
#67877=CARTESIAN_POINT('Ctrl Pts',(29.1111806434797,-0.783487027051828,
16.4315305472161));
#67878=CARTESIAN_POINT('Ctrl Pts',(29.2187204550675,-0.890749010718532,
16.441937155047));
#67879=CARTESIAN_POINT('Ctrl Pts',(29.4732317621912,-1.06214794881238,16.4636428352494));
#67880=CARTESIAN_POINT('Ctrl Pts',(29.6190899112583,-1.1227476098516,16.4747481293347));
#67881=CARTESIAN_POINT('Ctrl Pts',(29.8476395120001,-1.16783357420714,16.490381294589));
#67882=CARTESIAN_POINT('Ctrl Pts',(29.9238084968367,-1.17524047358085,16.4953212570267));
#67883=CARTESIAN_POINT('Ctrl Pts',(30.,-1.17524047358085,16.5));
#67884=CARTESIAN_POINT('Origin',(30.,-1.21864324187371E-14,15.78125));
#67885=CARTESIAN_POINT('',(30.,-1.17524047358085,17.0625));
#67886=CARTESIAN_POINT('',(30.0000000000001,-1.17524047358085,17.));
#67887=CARTESIAN_POINT('',(30.,-1.17524047358085,15.78125));
#67888=CARTESIAN_POINT('Ctrl Pts',(30.,-1.17524047358085,17.0625));
#67889=CARTESIAN_POINT('Ctrl Pts',(29.8500434788821,-1.17524047358086,17.0532915188657));
#67890=CARTESIAN_POINT('Ctrl Pts',(29.7013448813168,-1.14654165820119,17.0431428036379));
#67891=CARTESIAN_POINT('Ctrl Pts',(29.4194581258723,-1.03331719487298,17.0218185633632));
#67892=CARTESIAN_POINT('Ctrl Pts',(29.2895397758247,-0.948696042884902,
17.0108404436342));
#67893=CARTESIAN_POINT('Ctrl Pts',(29.0728347660888,-0.737413048700427,
16.9900423213744));
#67894=CARTESIAN_POINT('Ctrl Pts',(28.9869014388118,-0.614031092098323,
16.9810393937031));
#67895=CARTESIAN_POINT('Ctrl Pts',(28.8628735458866,-0.335358890642938,
16.9612794518217));
#67896=CARTESIAN_POINT('Ctrl Pts',(28.82846267168,-0.181667965469806,16.9503816165397));
#67897=CARTESIAN_POINT('Ctrl Pts',(28.8217124648996,0.125982959524893,16.9285668665722));
#67898=CARTESIAN_POINT('Ctrl Pts',(28.8478169965895,0.276986540894418,16.9178595840512));
#67899=CARTESIAN_POINT('Ctrl Pts',(28.9558731518301,0.560261316962501,16.89777328523));
#67900=CARTESIAN_POINT('Ctrl Pts',(29.0365906245512,0.68988311408331,16.8888684608487));
#67901=CARTESIAN_POINT('Ctrl Pts',(29.2459337687842,0.914815990147539,16.868038474302));
#67902=CARTESIAN_POINT('Ctrl Pts',(29.3738173058995,1.00667300394252,16.8569287693601));
#67903=CARTESIAN_POINT('Ctrl Pts',(29.6525904034611,1.13269913332434,16.8353418646716));
#67904=CARTESIAN_POINT('Ctrl Pts',(29.7999172965718,1.16777128086699,16.825051424181));
#67905=CARTESIAN_POINT('Ctrl Pts',(30.1064062467105,1.18085135988937,16.8057669130232));
#67906=CARTESIAN_POINT('Ctrl Pts',(30.2627337376109,1.15617395633467,16.7956901530542));
#67907=CARTESIAN_POINT('Ctrl Pts',(30.5539694020395,1.04785975388265,16.7739659051239));
#67908=CARTESIAN_POINT('Ctrl Pts',(30.6863296582614,0.96635719030164,16.7629483992302));
#67909=CARTESIAN_POINT('Ctrl Pts',(30.9084297587183,0.760352988428474,16.7420061299136));
#67910=CARTESIAN_POINT('Ctrl Pts',(30.9973576321623,0.639251123876904,16.7328276824508));
#67911=CARTESIAN_POINT('Ctrl Pts',(31.1283061935881,0.363925745860841,16.7133050553655));
#67912=CARTESIAN_POINT('Ctrl Pts',(31.1665770325591,0.21117202309341,16.7024736747387));
#67913=CARTESIAN_POINT('Ctrl Pts',(31.1811107740607,-0.0965571386816749,
16.6806533771987));
#67914=CARTESIAN_POINT('Ctrl Pts',(31.1587010998539,-0.248535347285279,
16.6698769863224));
#67915=CARTESIAN_POINT('Ctrl Pts',(31.0576874952353,-0.534014859537023,
16.6496343552276));
#67916=CARTESIAN_POINT('Ctrl Pts',(30.9806443499075,-0.664990212129755,
16.6408093669374));
#67917=CARTESIAN_POINT('Ctrl Pts',(30.7774744062741,-0.895077677115282,
16.6201757128395));
#67918=CARTESIAN_POINT('Ctrl Pts',(30.6516599935628,-0.990433515302137,
16.6090690216144));
#67919=CARTESIAN_POINT('Ctrl Pts',(30.3754577665479,-1.12376244747141,16.5873810764564));
#67920=CARTESIAN_POINT('Ctrl Pts',(30.2286809422177,-1.16255586785604,16.5769924813814));
#67921=CARTESIAN_POINT('Ctrl Pts',(30.0523684587312,-1.17436628643519,16.5657468184328));
#67922=CARTESIAN_POINT('Ctrl Pts',(30.0261713894288,-1.17524047358084,16.5641071241452));
#67923=CARTESIAN_POINT('Ctrl Pts',(30.0000000000004,-1.17524047358085,16.5625));
#67924=CARTESIAN_POINT('Ctrl Pts',(30.,-1.17524047358085,16.5));
#67925=CARTESIAN_POINT('Ctrl Pts',(30.073608323754,-1.17524047358085,16.5045201159347));
#67926=CARTESIAN_POINT('Ctrl Pts',(30.1472072638744,-1.16832718018639,16.5092847577281));
#67927=CARTESIAN_POINT('Ctrl Pts',(30.369441082132,-1.12600740446215,16.5244320137475));
#67928=CARTESIAN_POINT('Ctrl Pts',(30.5120596783037,-1.06872004059094,16.5352209411127));
#67929=CARTESIAN_POINT('Ctrl Pts',(30.770540092832,-0.900978381413799,16.5570406907631));
#67930=CARTESIAN_POINT('Ctrl Pts',(30.8831588051698,-0.790914789141215,
16.5678585095693));
#67931=CARTESIAN_POINT('Ctrl Pts',(31.0548992370084,-0.539025681589464,
16.5873351001607));
#67932=CARTESIAN_POINT('Ctrl Pts',(31.1146464335618,-0.40117702528207,16.5965535505072));
#67933=CARTESIAN_POINT('Ctrl Pts',(31.1805926646682,-0.105443065986663,
16.6175232985392));
#67934=CARTESIAN_POINT('Ctrl Pts',(31.1842348048322,0.0500317177053629,
16.6285476227227));
#67935=CARTESIAN_POINT('Ctrl Pts',(31.1309192517252,0.355959076743607,16.650240158982));
#67936=CARTESIAN_POINT('Ctrl Pts',(31.0735350939833,0.503164977113694,16.6602491192277));
#67937=CARTESIAN_POINT('Ctrl Pts',(30.9079406905516,0.761174069707616,16.6795652728517));
#67938=CARTESIAN_POINT('Ctrl Pts',(30.8033709986449,0.870813111599809,16.6898737681392));
#67939=CARTESIAN_POINT('Ctrl Pts',(30.5539282192807,1.04817985026245,16.7114797826742));
#67940=CARTESIAN_POINT('Ctrl Pts',(30.4100715847777,1.1123704677318,16.7225894812308));
#67941=CARTESIAN_POINT('Ctrl Pts',(30.1103488398163,1.179778360742,16.7433846194973));
#67942=CARTESIAN_POINT('Ctrl Pts',(29.957856215253,1.1841771173115,16.7522711143702));
#67943=CARTESIAN_POINT('Ctrl Pts',(29.6587896018035,1.13483145500942,16.7723855875496));
#67944=CARTESIAN_POINT('Ctrl Pts',(29.5151366653971,1.08127741557342,16.7831056710399));
#67945=CARTESIAN_POINT('Ctrl Pts',(29.252747940286,0.920389087589127,16.80492244475));
#67946=CARTESIAN_POINT('Ctrl Pts',(29.137337166046,0.813224513877345,16.8158089365411));
#67947=CARTESIAN_POINT('Ctrl Pts',(28.9591466935998,0.565701034789473,16.8355268312788));
#67948=CARTESIAN_POINT('Ctrl Pts',(28.8958814901205,0.429333298679841,16.8445570602832));
#67949=CARTESIAN_POINT('Ctrl Pts',(28.8225467136217,0.135655218439199,16.8653810311245));
#67950=CARTESIAN_POINT('Ctrl Pts',(28.8149165149687,-0.0192736957647923,
16.8763666490815));
#67951=CARTESIAN_POINT('Ctrl Pts',(28.8600359901893,-0.325574492875678,
16.8980856648912));
#67952=CARTESIAN_POINT('Ctrl Pts',(28.9132427466147,-0.473736863683124,
16.908393840582));
#67953=CARTESIAN_POINT('Ctrl Pts',(29.0711075417097,-0.735375844223955,
16.9273640300312));
#67954=CARTESIAN_POINT('Ctrl Pts',(29.1722563389189,-0.847605887640186,
16.9375543168196));
#67955=CARTESIAN_POINT('Ctrl Pts',(29.4158032201734,-1.03154789820323,16.9590313959273));
#67956=CARTESIAN_POINT('Ctrl Pts',(29.5572939812199,-1.09972494823153,16.97013714563));
#67957=CARTESIAN_POINT('Ctrl Pts',(29.8035947514828,-1.1629117021743,16.9875021095456));
#67958=CARTESIAN_POINT('Ctrl Pts',(29.9016938547886,-1.17524047358087,16.9939632483014));
#67959=CARTESIAN_POINT('Ctrl Pts',(30.0000000000002,-1.17524047358085,17.));
#67960=CARTESIAN_POINT('Origin',(30.,-1.21864324187371E-14,15.78125));
#67961=CARTESIAN_POINT('',(30.,-1.17524047358085,17.5625));
#67962=CARTESIAN_POINT('',(30.0000000000003,-1.17524047358085,17.5));
#67963=CARTESIAN_POINT('',(30.,-1.17524047358085,15.78125));
#67964=CARTESIAN_POINT('Ctrl Pts',(29.9999999999999,-1.17524047358085,17.5625));
#67965=CARTESIAN_POINT('Ctrl Pts',(29.9853039952848,-1.17524047358085,17.5615975525362));
#67966=CARTESIAN_POINT('Ctrl Pts',(29.9705988101993,-1.17496482223763,17.560684768457));
#67967=CARTESIAN_POINT('Ctrl Pts',(29.8000675583885,-1.16856010727206,17.5499857698916));
#67968=CARTESIAN_POINT('Ctrl Pts',(29.6469974366404,-1.13175546252589,17.53928122759));
#67969=CARTESIAN_POINT('Ctrl Pts',(29.3669883306193,-1.00191414640604,17.51748315987));
#67970=CARTESIAN_POINT('Ctrl Pts',(29.2422159979844,-0.911212372037981,
17.5066054643129));
#67971=CARTESIAN_POINT('Ctrl Pts',(29.0365009193432,-0.689398438610156,
17.4861088470066));
#67972=CARTESIAN_POINT('Ctrl Pts',(28.9566358845376,-0.561238966410083,
17.477296037423));
#67973=CARTESIAN_POINT('Ctrl Pts',(28.8466374529962,-0.274946499836391,
17.4569957617908));
#67974=CARTESIAN_POINT('Ctrl Pts',(28.8202715815142,-0.118602529031394,
17.4459098057446));
#67975=CARTESIAN_POINT('Ctrl Pts',(28.8303001790337,0.189193535952347,17.4240847642671));
#67976=CARTESIAN_POINT('Ctrl Pts',(28.8642598713376,0.337792935402822,17.413547956213));
#67977=CARTESIAN_POINT('Ctrl Pts',(28.9875332190235,0.616132121834573,17.3938116275857));
#67978=CARTESIAN_POINT('Ctrl Pts',(29.0764632180064,0.742831294355827,17.3845427667776));
#67979=CARTESIAN_POINT('Ctrl Pts',(29.2992557500629,0.956131495581886,17.3632993064049));
#67980=CARTESIAN_POINT('Ctrl Pts',(29.431365525465,1.04013508414132,17.3522085112739));
#67981=CARTESIAN_POINT('Ctrl Pts',(29.7152659077079,1.14996876403328,17.3308808348058));
#67982=CARTESIAN_POINT('Ctrl Pts',(29.8634965281812,1.17678287245723,17.3209370444755));
#67983=CARTESIAN_POINT('Ctrl Pts',(30.1685869462377,1.17348866615416,17.3020853596773));
#67984=CARTESIAN_POINT('Ctrl Pts',(30.3225567032231,1.14080144678595,17.291471550985));
#67985=CARTESIAN_POINT('Ctrl Pts',(30.6062809135034,1.01837161133764,17.269708112041));
#67986=CARTESIAN_POINT('Ctrl Pts',(30.7337302229979,0.930754504232001,17.2587753925441));
#67987=CARTESIAN_POINT('Ctrl Pts',(30.9451039338725,0.714326579760782,17.2381222459404));
#67988=CARTESIAN_POINT('Ctrl Pts',(31.0280898505948,0.588650269560749,17.2292397036887));
#67989=CARTESIAN_POINT('Ctrl Pts',(31.1457356989614,0.305390771140385,17.209154488167));
#67990=CARTESIAN_POINT('Ctrl Pts',(31.1762844162632,0.149369866697047,17.1980914399405));
#67991=CARTESIAN_POINT('Ctrl Pts',(31.1741828829317,-0.159374372954329,
17.1761991657924));
#67992=CARTESIAN_POINT('Ctrl Pts',(31.1439148549186,-0.309160960295119,
17.1655781772438));
#67993=CARTESIAN_POINT('Ctrl Pts',(31.0278391895685,-0.589863984020037,
17.1456742348851));
#67994=CARTESIAN_POINT('Ctrl Pts',(30.9428415818715,-0.717947604052165,
17.1366104494432));
#67995=CARTESIAN_POINT('Ctrl Pts',(30.7264277284841,-0.936836489561928,
17.1155605491468));
#67996=CARTESIAN_POINT('Ctrl Pts',(30.5962729133073,-1.02460346942682,17.10445637729));
#67997=CARTESIAN_POINT('Ctrl Pts',(30.3147671476396,-1.1421454095557,17.0830024620243));
#67998=CARTESIAN_POINT('Ctrl Pts',(30.1669216238945,-1.17291749944691,17.0728326267459));
#67999=CARTESIAN_POINT('Ctrl Pts',(30.0114948569556,-1.17519832475422,17.06320736676));
#68000=CARTESIAN_POINT('Ctrl Pts',(30.0057465951805,-1.17524047358085,17.0628528850424));
#68001=CARTESIAN_POINT('Ctrl Pts',(30.,-1.17524047358085,17.0625));
#68002=CARTESIAN_POINT('Ctrl Pts',(30.0000000000002,-1.17524047358085,17.));
#68003=CARTESIAN_POINT('Ctrl Pts',(30.0532026451947,-1.17524047358084,17.0032670506819));
#68004=CARTESIAN_POINT('Ctrl Pts',(30.1064500803375,-1.17162840402792,17.0066649131742));
#68005=CARTESIAN_POINT('Ctrl Pts',(30.3094843531048,-1.14383638948677,17.0201181063427));
#68006=CARTESIAN_POINT('Ctrl Pts',(30.4541770343026,-1.0944632219883,17.0307538106078));
#68007=CARTESIAN_POINT('Ctrl Pts',(30.7220117324143,-0.94057404805184,17.0526568626846));
#68008=CARTESIAN_POINT('Ctrl Pts',(30.8414109395085,-0.835479490322757,
17.0637148850572));
#68009=CARTESIAN_POINT('Ctrl Pts',(31.0267110546809,-0.591037021798696,
17.0837601330781));
#68010=CARTESIAN_POINT('Ctrl Pts',(31.0933788874677,-0.456058910657645,
17.0926620146465));
#68011=CARTESIAN_POINT('Ctrl Pts',(31.1737387540124,-0.16438811954927,17.1133436536858));
#68012=CARTESIAN_POINT('Ctrl Pts',(31.1851490819135,-0.0100732318962758,
17.1242857325711));
#68013=CARTESIAN_POINT('Ctrl Pts',(31.1477867853133,0.296739304676255,17.1460410345334));
#68014=CARTESIAN_POINT('Ctrl Pts',(31.0983725298423,0.446176311422578,17.156637235205));
#68015=CARTESIAN_POINT('Ctrl Pts',(30.9473434585081,0.711342976495719,17.1754395336164));
#68016=CARTESIAN_POINT('Ctrl Pts',(30.8493881217234,0.825870653120103,17.1854545855523));
#68017=CARTESIAN_POINT('Ctrl Pts',(30.6112318646727,1.01569990967513,17.2068093638384));
#68018=CARTESIAN_POINT('Ctrl Pts',(30.4719800604887,1.0874234537732,17.2179033608764));
#68019=CARTESIAN_POINT('Ctrl Pts',(30.1755334231398,1.17210985582506,17.2391099087106));
#68020=CARTESIAN_POINT('Ctrl Pts',(30.0214941231326,1.18498177307235,17.2483347304275));
#68021=CARTESIAN_POINT('Ctrl Pts',(29.7191034448427,1.1511421779865,17.2681035786673));
#68022=CARTESIAN_POINT('Ctrl Pts',(29.5735822533488,1.10552321949792,17.2786570590835));
#68023=CARTESIAN_POINT('Ctrl Pts',(29.3025973986068,0.958895356196027,17.3004961143537));
#68024=CARTESIAN_POINT('Ctrl Pts',(29.1808306521913,0.85722095928387,17.3115782643265));
#68025=CARTESIAN_POINT('Ctrl Pts',(28.9891285746956,0.617827320312939,17.3318376420863));
#68026=CARTESIAN_POINT('Ctrl Pts',(28.918785924397,0.484304768960115,17.3406591721831));
#68027=CARTESIAN_POINT('Ctrl Pts',(28.8309775509286,0.194817478373176,17.361185984716));
#68028=CARTESIAN_POINT('Ctrl Pts',(28.8155773691905,0.0412543792472424,
17.3720747561758));
#68029=CARTESIAN_POINT('Ctrl Pts',(28.8447173912596,-0.266085346871024,
17.3938674398171));
#68030=CARTESIAN_POINT('Ctrl Pts',(28.8901486797617,-0.416814366578493,
17.4045552538642));
#68031=CARTESIAN_POINT('Ctrl Pts',(29.0339735284972,-0.685700945089528,
17.423621321941));
#68032=CARTESIAN_POINT('Ctrl Pts',(29.1286271803726,-0.802582950507819,
17.4332789203108));
#68033=CARTESIAN_POINT('Ctrl Pts',(29.3609543925255,-0.998368963070605,
17.45448693977));
#68034=CARTESIAN_POINT('Ctrl Pts',(29.4977729352126,-1.07372697749091,17.4655603714348));
#68035=CARTESIAN_POINT('Ctrl Pts',(29.7602131749374,-1.15682002764215,17.484622175217));
#68036=CARTESIAN_POINT('Ctrl Pts',(29.879837116137,-1.1752404735809,17.4926210768238));
#68037=CARTESIAN_POINT('Ctrl Pts',(30.0000000000005,-1.17524047358085,17.5));
#68038=CARTESIAN_POINT('Origin',(30.,-1.21864324187371E-14,15.78125));
#68039=CARTESIAN_POINT('',(29.9999999999998,-1.17524047358085,18.0625));
#68040=CARTESIAN_POINT('',(30.,-1.17524047358085,18.));
#68041=CARTESIAN_POINT('',(30.,-1.17524047358085,15.78125));
#68042=CARTESIAN_POINT('Ctrl Pts',(29.9999999999995,-1.17524047358085,18.0625));
#68043=CARTESIAN_POINT('Ctrl Pts',(29.9645254254169,-1.17524047358085,18.0603215888955));
#68044=CARTESIAN_POINT('Ctrl Pts',(29.929015100466,-1.17363438891304,18.0580840407407));
#68045=CARTESIAN_POINT('Ctrl Pts',(29.7382382629168,-1.15628718990462,18.0457538558988));
#68046=CARTESIAN_POINT('Ctrl Pts',(29.5872914572777,-1.11138228831714,18.0348925171245));
#68047=CARTESIAN_POINT('Ctrl Pts',(29.315235711072,-0.96715790012321,18.0130729130751));
#68048=CARTESIAN_POINT('Ctrl Pts',(29.1959940490486,-0.870565282945587,
18.0023259907432));
#68049=CARTESIAN_POINT('Ctrl Pts',(29.0016396885941,-0.638155310236294,
17.9821513395236));
#68050=CARTESIAN_POINT('Ctrl Pts',(28.9280461950896,-0.504858426874225,
17.9732982357813));
#68051=CARTESIAN_POINT('Ctrl Pts',(28.8336569152641,-0.212647772939916,
17.9525783164326));
#68052=CARTESIAN_POINT('Ctrl Pts',(28.8157570812338,-0.0559802507924535,
17.9414694181781));
#68053=CARTESIAN_POINT('Ctrl Pts',(28.841716723376,0.249283949869151,17.9198239048041));
#68054=CARTESIAN_POINT('Ctrl Pts',(28.8830393993721,0.395199804389445,17.9094773801424));
#68055=CARTESIAN_POINT('Ctrl Pts',(29.0209639808548,0.668562290928518,17.8900939367334));
#68056=CARTESIAN_POINT('Ctrl Pts',(29.1181759703235,0.792402282110926,17.8802238069267));
#68057=CARTESIAN_POINT('Ctrl Pts',(29.3540263292146,0.993822233016871,17.8585996950535));
#68058=CARTESIAN_POINT('Ctrl Pts',(29.4898462594122,1.06991069869815,17.8475616886318));
#68059=CARTESIAN_POINT('Ctrl Pts',(29.7781387158762,1.16368326761588,17.8265337315072));
#68060=CARTESIAN_POINT('Ctrl Pts',(29.9272121099849,1.18239624377936,17.817223433802));
#68061=CARTESIAN_POINT('Ctrl Pts',(30.231427568808,1.16273575019751,17.7978452321702));
#68062=CARTESIAN_POINT('Ctrl Pts',(30.3834744853667,1.1218012564522,17.7870571039388));
#68063=CARTESIAN_POINT('Ctrl Pts',(30.6595367886018,0.984593855649311,17.7652402449678));
#68064=CARTESIAN_POINT('Ctrl Pts',(30.78153371397,0.890859052478792,17.7544254485094));
#68065=CARTESIAN_POINT('Ctrl Pts',(30.9814968973686,0.663646825098318,17.7340906520159));
#68066=CARTESIAN_POINT('Ctrl Pts',(31.0581916579204,0.532910080900297,17.7252873077101));
#68067=CARTESIAN_POINT('Ctrl Pts',(31.1603311881744,0.243593094566313,17.7047725710215));
#68068=CARTESIAN_POINT('Ctrl Pts',(31.1824208985569,0.0870303935487086,
17.6936711053685));
#68069=CARTESIAN_POINT('Ctrl Pts',(31.1643265939555,-0.219589452433675,
17.6719294666093));
#68070=CARTESIAN_POINT('Ctrl Pts',(31.126629625228,-0.366880394031282,17.6614854379963));
#68071=CARTESIAN_POINT('Ctrl Pts',(30.9959732548856,-0.642739672382233,
17.6419249533869));
#68072=CARTESIAN_POINT('Ctrl Pts',(30.9029171297163,-0.76800751067264,17.6323839709445));
#68073=CARTESIAN_POINT('Ctrl Pts',(30.6735549835348,-0.97540763183831,17.6109462657373));
#68074=CARTESIAN_POINT('Ctrl Pts',(30.5395284406378,-1.05546393695081,17.5998777123224));
#68075=CARTESIAN_POINT('Ctrl Pts',(30.2672665806154,-1.15230702152505,17.5797252955804));
#68076=CARTESIAN_POINT('Ctrl Pts',(30.1340643685791,-1.17524047358085,17.5707325810151));
#68077=CARTESIAN_POINT('Ctrl Pts',(29.9999999999999,-1.17524047358085,17.5625));
#68078=CARTESIAN_POINT('Ctrl Pts',(30.0000000000005,-1.17524047358085,17.5));
#68079=CARTESIAN_POINT('Ctrl Pts',(30.033668671514,-1.17524047358084,17.5020675147979));
#68080=CARTESIAN_POINT('Ctrl Pts',(30.0673733741507,-1.17379373295066,17.504188534545));
#68081=CARTESIAN_POINT('Ctrl Pts',(30.2512194694897,-1.15793171152857,17.5160404635345));
#68082=CARTESIAN_POINT('Ctrl Pts',(30.3974945854731,-1.11619705184184,17.5265025277916));
#68083=CARTESIAN_POINT('Ctrl Pts',(30.6715286389123,-0.977122112696594,
17.5482610478741));
#68084=CARTESIAN_POINT('Ctrl Pts',(30.7956391457863,-0.8790277241657,17.559360198049));
#68085=CARTESIAN_POINT('Ctrl Pts',(30.9938921656194,-0.644908297614295,
17.579834863399));
#68086=CARTESIAN_POINT('Ctrl Pts',(31.0680432549382,-0.51284781086492,17.5886352571811));
#68087=CARTESIAN_POINT('Ctrl Pts',(31.1634155774875,-0.225635628704456,
17.6090007475224));
#68088=CARTESIAN_POINT('Ctrl Pts',(31.1828424433655,-0.0729412614644995,
17.6198279193986));
#68089=CARTESIAN_POINT('Ctrl Pts',(31.1620678214981,0.234707081573543,17.6416424862861));
#68090=CARTESIAN_POINT('Ctrl Pts',(31.120724241081,0.386638085314584,17.6524155299848));
#68091=CARTESIAN_POINT('Ctrl Pts',(30.9842587758127,0.659238100700609,17.6717449084903));
#68092=CARTESIAN_POINT('Ctrl Pts',(30.8929036275603,0.778529076192667,17.6811039637465));
#68093=CARTESIAN_POINT('Ctrl Pts',(30.6664518626416,0.98022024209091,17.7021605454119));
#68094=CARTESIAN_POINT('Ctrl Pts',(30.5321662358965,1.05914504613978,17.7132048926221));
#68095=CARTESIAN_POINT('Ctrl Pts',(30.2394356343315,1.16107865610412,17.7347947253164));
#68096=CARTESIAN_POINT('Ctrl Pts',(30.0837395746803,1.18253750639866,17.7445990404306));
#68097=CARTESIAN_POINT('Ctrl Pts',(29.7783085058998,1.16389753061854,17.7640157086725));
#68098=CARTESIAN_POINT('Ctrl Pts',(29.6313883618284,1.12601470121935,17.7743808208261));
#68099=CARTESIAN_POINT('Ctrl Pts',(29.3545393068819,0.994469365010162,17.7960452510406));
#68100=CARTESIAN_POINT('Ctrl Pts',(29.2282096618696,0.899966183720928,17.8071533516094));
#68101=CARTESIAN_POINT('Ctrl Pts',(29.0235241701317,0.671134004766118,17.8278355674102));
#68102=CARTESIAN_POINT('Ctrl Pts',(28.9455840780504,0.540492245953914,17.8366750601186));
#68103=CARTESIAN_POINT('Ctrl Pts',(28.8428376707835,0.255550540540784,17.8568795566889));
#68104=CARTESIAN_POINT('Ctrl Pts',(28.819515816648,0.103803872119581,17.8676395296357));
#68105=CARTESIAN_POINT('Ctrl Pts',(28.8321334408652,-0.203924479248023,
17.8894597697118));
#68106=CARTESIAN_POINT('Ctrl Pts',(28.8694569005926,-0.356918085677502,
17.9003081598831));
#68107=CARTESIAN_POINT('Ctrl Pts',(28.9987062002081,-0.633072693900888,
17.9198895855878));
#68108=CARTESIAN_POINT('Ctrl Pts',(29.0868937988439,-0.754733453808526,
17.9290197269592));
#68109=CARTESIAN_POINT('Ctrl Pts',(29.3076626510103,-0.962047131353844,
17.9499266732212));
#68110=CARTESIAN_POINT('Ctrl Pts',(29.439425880769,-1.04432722335896,17.9609350833968));
#68111=CARTESIAN_POINT('Ctrl Pts',(29.7165797609128,-1.14942800619046,17.981680673977));
#68112=CARTESIAN_POINT('Ctrl Pts',(29.857771536572,-1.17524047358086,17.9912660809114));
#68113=CARTESIAN_POINT('Ctrl Pts',(30.0000000000001,-1.17524047358085,18.));
#68114=CARTESIAN_POINT('Origin',(30.,-1.21864324187371E-14,15.78125));
#68115=CARTESIAN_POINT('',(29.9999999999999,-1.17524047358085,18.5625));
#68116=CARTESIAN_POINT('',(30.,-1.17524047358085,18.5));
#68117=CARTESIAN_POINT('',(30.,-1.17524047358085,15.78125));
#68118=CARTESIAN_POINT('Ctrl Pts',(29.9999999999998,-1.17524047358085,18.5625));
#68119=CARTESIAN_POINT('Ctrl Pts',(29.9448799883238,-1.17524047358085,18.5591152083026));
#68120=CARTESIAN_POINT('Ctrl Pts',(29.8897199177939,-1.17136342891428,18.5555905009623));
#68121=CARTESIAN_POINT('Ctrl Pts',(29.6792216999803,-1.14149919812993,18.5416054964814));
#68122=CARTESIAN_POINT('Ctrl Pts',(29.5295600411529,-1.08838822549331,18.5305321396985));
#68123=CARTESIAN_POINT('Ctrl Pts',(29.2651715824486,-0.929562358041593,
18.5086656889335));
#68124=CARTESIAN_POINT('Ctrl Pts',(29.1517563578462,-0.827380506823195,
18.4980783953365));
#68125=CARTESIAN_POINT('Ctrl Pts',(28.9690035888602,-0.584433789122884,
18.4782426038757));
#68126=CARTESIAN_POINT('Ctrl Pts',(28.9018681826973,-0.445680079983302,
18.4691020486872));
#68127=CARTESIAN_POINT('Ctrl Pts',(28.8237798560613,-0.147691887525462,
18.4479724586759));
#68128=CARTESIAN_POINT('Ctrl Pts',(28.8145788645707,0.00884554058040183,
18.4368727850612));
#68129=CARTESIAN_POINT('Ctrl Pts',(28.8567482751501,0.310649796974269,18.4154726075955));
#68130=CARTESIAN_POINT('Ctrl Pts',(28.9054833559201,0.453415390787842,18.4053494599629));
#68131=CARTESIAN_POINT('Ctrl Pts',(29.0569965845258,0.718468314308288,18.3865552266777));
#68132=CARTESIAN_POINT('Ctrl Pts',(29.1604683184012,0.83707730034545,18.3760428358642));
#68133=CARTESIAN_POINT('Ctrl Pts',(29.4058248734932,1.0255154952049,18.3542952223602));
#68134=CARTESIAN_POINT('Ctrl Pts',(29.544631443668,1.0942445155017,18.3433347331662));
#68135=CARTESIAN_POINT('Ctrl Pts',(29.8366929775619,1.17335763361873,18.3225950580774));
#68136=CARTESIAN_POINT('Ctrl Pts',(29.986714530993,1.18458952273488,18.3136472884771));
#68137=CARTESIAN_POINT('Ctrl Pts',(30.2898186404183,1.14957783224746,18.2937930749288));
#68138=CARTESIAN_POINT('Ctrl Pts',(30.4396462258347,1.10100720458506,18.2828705011767));
#68139=CARTESIAN_POINT('Ctrl Pts',(30.7078144176317,0.95036138884417,18.2610619591969));
#68140=CARTESIAN_POINT('Ctrl Pts',(30.8244348872713,0.851181456147988,18.250384268188));
#68141=CARTESIAN_POINT('Ctrl Pts',(31.0135314789776,0.613960284599869,18.2303619093383));
#68142=CARTESIAN_POINT('Ctrl Pts',(31.0842069749077,0.478217809229905,18.2214092168781));
#68143=CARTESIAN_POINT('Ctrl Pts',(31.1712537448649,0.183351777827692,18.2005010114207));
#68144=CARTESIAN_POINT('Ctrl Pts',(31.1852144107931,0.026684835425868,18.1893921542744));
#68145=CARTESIAN_POINT('Ctrl Pts',(31.151894218573,-0.277120859310672,18.1678500598715));
#68146=CARTESIAN_POINT('Ctrl Pts',(31.1071955868466,-0.421659698179358,
18.1576011759113));
#68147=CARTESIAN_POINT('Ctrl Pts',(30.9623980704004,-0.692609521716023,
18.1383888083414));
#68148=CARTESIAN_POINT('Ctrl Pts',(30.8611688824271,-0.815074867780112,
18.1281515944925));
#68149=CARTESIAN_POINT('Ctrl Pts',(30.6191698348665,-1.010677278137,18.1063561595037));
#68150=CARTESIAN_POINT('Ctrl Pts',(30.481744547401,-1.08294295672688,18.0953551039148));
#68151=CARTESIAN_POINT('Ctrl Pts',(30.2255864017037,-1.15894806928573,18.0769303627887));
#68152=CARTESIAN_POINT('Ctrl Pts',(30.1130100641695,-1.17524047358085,18.0694396851576));
#68153=CARTESIAN_POINT('Ctrl Pts',(29.9999999999995,-1.17524047358085,18.0625));
#68154=CARTESIAN_POINT('Ctrl Pts',(30.0000000000001,-1.17524047358085,18.));
#68155=CARTESIAN_POINT('Ctrl Pts',(30.0145244311397,-1.17524047358085,18.0008919115297));
#68156=CARTESIAN_POINT('Ctrl Pts',(30.0290585224951,-1.1749712210064,18.0017939622806));
#68157=CARTESIAN_POINT('Ctrl Pts',(30.1935181174434,-1.16886648233729,18.0121094792412));
#68158=CARTESIAN_POINT('Ctrl Pts',(30.3409577753235,-1.13464684718278,18.022376619604));
#68159=CARTESIAN_POINT('Ctrl Pts',(30.6202928748417,-1.01029888563142,18.0439385382044));
#68160=CARTESIAN_POINT('Ctrl Pts',(30.7486368752819,-0.919248747112441,
18.055047912384));
#68161=CARTESIAN_POINT('Ctrl Pts',(30.9593869332128,-0.695506306327382,
18.0759220888488));
#68162=CARTESIAN_POINT('Ctrl Pts',(31.0409497614259,-0.566191331080132,
18.084852802908));
#68163=CARTESIAN_POINT('Ctrl Pts',(31.1506054030915,-0.283424289026694,
18.1049030995926));
#68164=CARTESIAN_POINT('Ctrl Pts',(31.1775442736485,-0.132654402671248,
18.1155938113905));
#68165=CARTESIAN_POINT('Ctrl Pts',(31.1725598607287,0.174951078257229,18.1374053390341));
#68166=CARTESIAN_POINT('Ctrl Pts',(31.1390289434739,0.328840847644919,18.148317273857));
#68167=CARTESIAN_POINT('Ctrl Pts',(31.0165781905916,0.608264397522364,18.1681304919571));
#68168=CARTESIAN_POINT('Ctrl Pts',(30.9313199722933,0.732167484063905,18.1771012136858));
#68169=CARTESIAN_POINT('Ctrl Pts',(30.7158345492886,0.944633593585631,18.1978663898215));
#68170=CARTESIAN_POINT('Ctrl Pts',(30.5864762504196,1.02994768568734,18.208834685427));
#68171=CARTESIAN_POINT('Ctrl Pts',(30.3000115977578,1.14695518635867,18.2305741665317));
#68172=CARTESIAN_POINT('Ctrl Pts',(30.1454149851266,1.17656763909288,18.2410233510493));
#68173=CARTESIAN_POINT('Ctrl Pts',(29.8400425266379,1.17387642244061,18.2598709770579));
#68174=CARTESIAN_POINT('Ctrl Pts',(29.6921041520777,1.14400535739554,18.2700145693908));
#68175=CARTESIAN_POINT('Ctrl Pts',(29.4100579886469,1.02824734385133,18.2914384223622));
#68176=CARTESIAN_POINT('Ctrl Pts',(29.2794434337127,0.941343746808855,18.3025402156205));
#68177=CARTESIAN_POINT('Ctrl Pts',(29.061555804029,0.723734320476339,18.3236352554819));
#68178=CARTESIAN_POINT('Ctrl Pts',(28.9756558249342,0.595970538008072,18.3327412345668));
#68179=CARTESIAN_POINT('Ctrl Pts',(28.8579142725366,0.315809924655313,18.3526067159761));
#68180=CARTESIAN_POINT('Ctrl Pts',(28.8267878271973,0.166290213657428,18.3632087809973));
#68181=CARTESIAN_POINT('Ctrl Pts',(28.8228465258246,-0.142252171918218,
18.3850867421828));
#68182=CARTESIAN_POINT('Ctrl Pts',(28.8524261916584,-0.298357527348321,
18.3961557786154));
#68183=CARTESIAN_POINT('Ctrl Pts',(28.9683032793772,-0.582326286319503,
18.4162912860112));
#68184=CARTESIAN_POINT('Ctrl Pts',(29.0505638845767,-0.708574806470949,
18.4251522948912));
#68185=CARTESIAN_POINT('Ctrl Pts',(29.2606233813178,-0.926260402003281,
18.4457693278011));
#68186=CARTESIAN_POINT('Ctrl Pts',(29.3874559625716,-1.01460273580079,18.4566898874478));
#68187=CARTESIAN_POINT('Ctrl Pts',(29.670332667393,-1.13876808411125,18.4784628134696));
#68188=CARTESIAN_POINT('Ctrl Pts',(29.8241031351402,-1.17241612945781,18.4890984491449));
#68189=CARTESIAN_POINT('Ctrl Pts',(29.9866645216768,-1.17518374723239,18.4991790881359));
#68190=CARTESIAN_POINT('Ctrl Pts',(29.9933333092278,-1.17524047358085,18.4995906140276));
#68191=CARTESIAN_POINT('Ctrl Pts',(30.,-1.17524047358085,18.5));
#68192=CARTESIAN_POINT('Origin',(30.,-1.21864324187371E-14,15.78125));
#68193=CARTESIAN_POINT('',(30.,-1.17524047358085,19.0625));
#68194=CARTESIAN_POINT('',(29.9999999999998,-1.17524047358085,18.9999999999999));
#68195=CARTESIAN_POINT('',(30.,-1.17524047358085,15.78125));
#68196=CARTESIAN_POINT('Ctrl Pts',(30.,-1.17524047358085,19.0625));
#68197=CARTESIAN_POINT('Ctrl Pts',(29.9235115354988,-1.17524047358085,19.0578030213218));
#68198=CARTESIAN_POINT('Ctrl Pts',(29.84704716558,-1.16777574293408,19.0528428696387));
#68199=CARTESIAN_POINT('Ctrl Pts',(29.6182505756017,-1.12246086107485,19.0371864213689));
#68200=CARTESIAN_POINT('Ctrl Pts',(29.4724485773796,-1.06175746863862,19.0260808977107));
#68201=CARTESIAN_POINT('Ctrl Pts',(29.2180805672544,-0.890185564352666,
19.0043778847458));
#68202=CARTESIAN_POINT('Ctrl Pts',(29.1106251205818,-0.782854361416016,
18.9939740034863));
#68203=CARTESIAN_POINT('Ctrl Pts',(28.9394765622835,-0.529653947083613,
18.9744872677464));
#68204=CARTESIAN_POINT('Ctrl Pts',(28.8789010658566,-0.385229961133875,
18.9648156834562));
#68205=CARTESIAN_POINT('Ctrl Pts',(28.8174805423046,-0.0817855742350542,
18.9432992084794));
#68206=CARTESIAN_POINT('Ctrl Pts',(28.8169771571136,0.0741472763924911,
18.9322424039265));
#68207=CARTESIAN_POINT('Ctrl Pts',(28.8752567923883,0.371953492557534,18.9111257173945));
#68208=CARTESIAN_POINT('Ctrl Pts',(28.9314131886074,0.511361040736907,18.9016564371649));
#68209=CARTESIAN_POINT('Ctrl Pts',(29.0965385184593,0.767636822695621,18.8824305405978));
#68210=CARTESIAN_POINT('Ctrl Pts',(29.2062331582591,0.880579083863968,18.8716902227143));
#68211=CARTESIAN_POINT('Ctrl Pts',(29.4605419802015,1.05521085002794,18.8498823608196));
#68212=CARTESIAN_POINT('Ctrl Pts',(29.6020069692685,1.11628678080371,18.8390299549287));
#68213=CARTESIAN_POINT('Ctrl Pts',(29.8977163387384,1.18033932535056,18.8186002283572));
#68214=CARTESIAN_POINT('Ctrl Pts',(30.0489012110254,1.18375239923791,18.8097988699583));
#68215=CARTESIAN_POINT('Ctrl Pts',(30.351304458352,1.13241772416719,18.7894089839185));
#68216=CARTESIAN_POINT('Ctrl Pts',(30.4990888608278,1.07549105419273,18.7783156243515));
#68217=CARTESIAN_POINT('Ctrl Pts',(30.7585582244441,0.910237971254531,18.7565233749656));
#68218=CARTESIAN_POINT('Ctrl Pts',(30.869032001546,0.80544751578808,18.7460242240482));
#68219=CARTESIAN_POINT('Ctrl Pts',(31.0460310070461,0.557381504027199,18.7263602597134));
#68220=CARTESIAN_POINT('Ctrl Pts',(31.1099298338315,0.41584148204013,18.7169862690792));
#68221=CARTESIAN_POINT('Ctrl Pts',(31.1797989523814,0.115104609901925,18.6956617771348));
#68222=CARTESIAN_POINT('Ctrl Pts',(31.1846835245906,-0.0411926090939851,
18.6845791361414));
#68223=CARTESIAN_POINT('Ctrl Pts',(31.134503841219,-0.341119161052378,18.6633121019541));
#68224=CARTESIAN_POINT('Ctrl Pts',(31.082082323541,-0.482198917475646,18.6535190714213));
#68225=CARTESIAN_POINT('Ctrl Pts',(30.9238582069445,-0.74295817680152,18.6345580062792));
#68226=CARTESIAN_POINT('Ctrl Pts',(30.8172746962663,-0.85879990158245,18.6239059387776));
#68227=CARTESIAN_POINT('Ctrl Pts',(30.5674863902569,-1.04046451233651,18.6021263306283));
#68228=CARTESIAN_POINT('Ctrl Pts',(30.4273223446806,-1.10544579712631,18.5912153532567));
#68229=CARTESIAN_POINT('Ctrl Pts',(30.1872213612661,-1.164041447155,18.5743938756203));
#68230=CARTESIAN_POINT('Ctrl Pts',(30.0936931422672,-1.17524047358085,18.5682534779185));
#68231=CARTESIAN_POINT('Ctrl Pts',(29.9999999999998,-1.17524047358085,18.5625));
#68232=CARTESIAN_POINT('Ctrl Pts',(30.,-1.17524047358085,18.5));
#68233=CARTESIAN_POINT('Ctrl Pts',(30.1423690472132,-1.17524047358085,18.5087425520117));
#68234=CARTESIAN_POINT('Ctrl Pts',(30.2836710124158,-1.14937338085773,18.5183366621019));
#68235=CARTESIAN_POINT('Ctrl Pts',(30.561858730089,-1.04379601878612,18.5391626347549));
#68236=CARTESIAN_POINT('Ctrl Pts',(30.6944274791866,-0.96071277520592,18.550248984724));
#68237=CARTESIAN_POINT('Ctrl Pts',(30.9187624839086,-0.748784365111015,
18.5715385296331));
#68238=CARTESIAN_POINT('Ctrl Pts',(31.0086541273172,-0.622420436396325,
18.5808657390843));
#68239=CARTESIAN_POINT('Ctrl Pts',(31.1336634286392,-0.344659292163419,
18.6005610801994));
#68240=CARTESIAN_POINT('Ctrl Pts',(31.1685065373813,-0.196359387070609,
18.6110766518651));
#68241=CARTESIAN_POINT('Ctrl Pts',(31.1804379609257,0.111178530247992,18.6328833887437));
#68242=CARTESIAN_POINT('Ctrl Pts',(31.1550790566304,0.267584160665563,18.6439737169172));
#68243=CARTESIAN_POINT('Ctrl Pts',(31.0469271232095,0.554595748580105,18.6643249836272));
#68244=CARTESIAN_POINT('Ctrl Pts',(30.9678100781097,0.68335841703765,18.6731299773448));
#68245=CARTESIAN_POINT('Ctrl Pts',(30.763452167876,0.90645295543942,18.6935886563282));
#68246=CARTESIAN_POINT('Ctrl Pts',(30.6393299618342,0.997879761179756,18.7044521341951));
#68247=CARTESIAN_POINT('Ctrl Pts',(30.3602369836734,1.12947461105548,18.7262561139589));
#68248=CARTESIAN_POINT('Ctrl Pts',(30.207398548302,1.16725893034935,18.7369811620628));
#68249=CARTESIAN_POINT('Ctrl Pts',(29.9028111520737,1.18064726329168,18.7561598319717));
#68250=CARTESIAN_POINT('Ctrl Pts',(29.7540809815473,1.15884794274813,18.7656824913455));
#68251=CARTESIAN_POINT('Ctrl Pts',(29.4674235177593,1.05897426017317,18.7868263546523));
#68252=CARTESIAN_POINT('Ctrl Pts',(29.332959967187,0.979858413005439,18.7978884009434));
#68253=CARTESIAN_POINT('Ctrl Pts',(29.1020498086111,0.773870883761844,18.8193710843283));
#68254=CARTESIAN_POINT('Ctrl Pts',(29.0080096312967,0.648942084974305,18.8289851559772));
#68255=CARTESIAN_POINT('Ctrl Pts',(28.8756172989166,0.373674108747255,18.8485037128466));
#68256=CARTESIAN_POINT('Ctrl Pts',(28.8370493704244,0.226703861544607,18.85892500183));
#68257=CARTESIAN_POINT('Ctrl Pts',(28.8170693542027,-0.0796098764074361,
18.8806449352421));
#68258=CARTESIAN_POINT('Ctrl Pts',(28.838156352639,-0.236207536581086,18.8917488797605));
#68259=CARTESIAN_POINT('Ctrl Pts',(28.9384458248014,-0.526222673597261,
18.9123131205504));
#68260=CARTESIAN_POINT('Ctrl Pts',(29.0143989785152,-0.657569956199922,
18.921123179589));
#68261=CARTESIAN_POINT('Ctrl Pts',(29.2130173163762,-0.886033452067211,
18.9414197543903));
#68262=CARTESIAN_POINT('Ctrl Pts',(29.3343580168877,-0.980462303689547,
18.9522188602181));
#68263=CARTESIAN_POINT('Ctrl Pts',(29.609473809437,-1.11936682716347,18.9740377655105));
#68264=CARTESIAN_POINT('Ctrl Pts',(29.7612660994758,-1.16125829944545,18.9848441861849));
#68265=CARTESIAN_POINT('Ctrl Pts',(29.9445511530895,-1.1742603871282,18.9965602675684));
#68266=CARTESIAN_POINT('Ctrl Pts',(29.9722886221142,-1.17524047358085,18.998298308746));
#68267=CARTESIAN_POINT('Ctrl Pts',(29.9999999999996,-1.17524047358085,18.9999999999999));
#68268=CARTESIAN_POINT('Origin',(30.,-1.21864324187371E-14,15.78125));
#68269=CARTESIAN_POINT('',(30.0000000000001,-1.17524047358085,19.5625));
#68270=CARTESIAN_POINT('',(29.9999999999998,-1.17524047358085,19.4999999999999));
#68271=CARTESIAN_POINT('',(30.,-1.17524047358085,15.78125));
#68272=CARTESIAN_POINT('Ctrl Pts',(30.0000000000003,-1.17524047358085,19.5625));
#68273=CARTESIAN_POINT('Ctrl Pts',(29.9013941092948,-1.17524047358088,19.5564448416279));
#68274=CARTESIAN_POINT('Ctrl Pts',(29.8029987638489,-1.16283641906691,19.549962842264));
#68275=CARTESIAN_POINT('Ctrl Pts',(29.5564668004839,-1.09938994466242,19.5325744732568));
#68276=CARTESIAN_POINT('Ctrl Pts',(29.415037771559,-1.03111229808663,19.5214689478566));
#68277=CARTESIAN_POINT('Ctrl Pts',(29.1716434679328,-0.847005065425004,
19.4999953804452));
#68278=CARTESIAN_POINT('Ctrl Pts',(29.0705827398005,-0.734710314058229,
19.4898082076353));
#68279=CARTESIAN_POINT('Ctrl Pts',(28.9129094963582,-0.472970867922037,
19.4708462190468));
#68280=CARTESIAN_POINT('Ctrl Pts',(28.8598073237114,-0.32477237703938,19.4605287888834));
#68281=CARTESIAN_POINT('Ctrl Pts',(28.8149047814539,-0.0184511328725056,
19.4388083232246));
#68282=CARTESIAN_POINT('Ctrl Pts',(28.8226412643137,0.136461808695805,19.4278238378469));
#68283=CARTESIAN_POINT('Ctrl Pts',(28.8961732267534,0.430084241574931,19.4070038128194));
#68284=CARTESIAN_POINT('Ctrl Pts',(28.9595331463533,0.5664127336681,19.3979778677293));
#68285=CARTESIAN_POINT('Ctrl Pts',(29.137896746023,0.813817787616469,19.3782535402653));
#68286=CARTESIAN_POINT('Ctrl Pts',(29.2533816215898,0.92090330809607,19.3673653008166));
#68287=CARTESIAN_POINT('Ctrl Pts',(29.5158730245192,1.08160589182486,19.3455488072285));
#68288=CARTESIAN_POINT('Ctrl Pts',(29.6595524720356,1.13505921849913,19.3348306663965));
#68289=CARTESIAN_POINT('Ctrl Pts',(29.9586626554596,1.18420822106571,19.3147204900089));
#68290=CARTESIAN_POINT('Ctrl Pts',(30.1111738123977,1.17970362181747,19.305831310076));
#68291=CARTESIAN_POINT('Ctrl Pts',(30.4108580361143,1.11207867833533,19.2850308420592));
#68292=CARTESIAN_POINT('Ctrl Pts',(30.5546592354692,1.0477915906526,19.2739211274165));
#68293=CARTESIAN_POINT('Ctrl Pts',(30.8039627363725,0.870265103601911,19.2523180019705));
#68294=CARTESIAN_POINT('Ctrl Pts',(30.9084512058835,0.760562755820576,19.242012249931));
#68295=CARTESIAN_POINT('Ctrl Pts',(31.0738897348627,0.502419631313023,19.2227009162624));
#68296=CARTESIAN_POINT('Ctrl Pts',(31.1311837638208,0.355135076925594,19.2126817312365));
#68297=CARTESIAN_POINT('Ctrl Pts',(31.1842706831827,0.04913932312708,19.1909843452775));
#68298=CARTESIAN_POINT('Ctrl Pts',(31.1805124566442,-0.106321035688241,
19.1799610439256));
#68299=CARTESIAN_POINT('Ctrl Pts',(31.1143513914742,-0.401996025434437,
19.1589954772754));
#68300=CARTESIAN_POINT('Ctrl Pts',(31.0545027280943,-0.539801328735837,
19.1497832518808));
#68301=CARTESIAN_POINT('Ctrl Pts',(30.8825757787308,-0.791565442014421,
19.1302996391962));
#68302=CARTESIAN_POINT('Ctrl Pts',(30.7698754890686,-0.90154647307845,19.1194797380197));
#68303=CARTESIAN_POINT('Ctrl Pts',(30.5112798180774,-1.06909180183037,19.0976598713853));
#68304=CARTESIAN_POINT('Ctrl Pts',(30.3686300461772,-1.12627173763864,19.0868728383175));
#68305=CARTESIAN_POINT('Ctrl Pts',(30.146651557919,-1.16837939048486,19.071748782068));
#68306=CARTESIAN_POINT('Ctrl Pts',(30.0733297917687,-1.17524047358085,19.0670030119334));
#68307=CARTESIAN_POINT('Ctrl Pts',(30.,-1.17524047358085,19.0625));
#68308=CARTESIAN_POINT('Ctrl Pts',(29.9999999999996,-1.17524047358085,18.9999999999999));
#68309=CARTESIAN_POINT('Ctrl Pts',(30.1208018343283,-1.17524047358085,19.0074181596379));
#68310=CARTESIAN_POINT('Ctrl Pts',(30.2410273417982,-1.15662316578329,19.0154609815185));
#68311=CARTESIAN_POINT('Ctrl Pts',(30.5033214237856,-1.07312795539109,19.0345280681775));
#68312=CARTESIAN_POINT('Ctrl Pts',(30.6395388198866,-0.997960158889978,
19.0455578408927));
#68313=CARTESIAN_POINT('Ctrl Pts',(30.876878941369,-0.797935916319293,19.067223952545));
#68314=CARTESIAN_POINT('Ctrl Pts',(30.9750570407496,-0.674426741281125,
19.0771781033725));
#68315=CARTESIAN_POINT('Ctrl Pts',(31.1146479426385,-0.401644540658674,
19.0965204001729));
#68316=CARTESIAN_POINT('Ctrl Pts',(31.1567939343853,-0.256055794064216,
19.1068437304378));
#68317=CARTESIAN_POINT('Ctrl Pts',(31.1845453028865,0.0488704061743495,
19.1284652770555));
#68318=CARTESIAN_POINT('Ctrl Pts',(31.1676027188842,0.205546638234067,19.1395747929079));
#68319=CARTESIAN_POINT('Ctrl Pts',(31.0749923240704,0.498408501569657,19.1603408878703));
#68320=CARTESIAN_POINT('Ctrl Pts',(31.0021074917097,0.632295920687204,19.1692134966416));
#68321=CARTESIAN_POINT('Ctrl Pts',(30.8090318381138,0.865881565613648,19.1893513074212));
#68322=CARTESIAN_POINT('Ctrl Pts',(30.6904244547157,0.963111668252584,19.2000818814201));
#68323=CARTESIAN_POINT('Ctrl Pts',(30.419302827982,1.10891198567697,19.2218999959461));
#68324=CARTESIAN_POINT('Ctrl Pts',(30.2686205389783,1.15471361101177,19.232776883577));
#68325=CARTESIAN_POINT('Ctrl Pts',(29.9650775926592,1.18413115670169,19.2524597117397));
#68326=CARTESIAN_POINT('Ctrl Pts',(29.8154193388389,1.17018311968912,19.2615139711268));
#68327=CARTESIAN_POINT('Ctrl Pts',(29.5246945745281,1.08577187830739,19.2823593965739));
#68328=CARTESIAN_POINT('Ctrl Pts',(29.3869225275025,1.01437069769904,19.2933510961767));
#68329=CARTESIAN_POINT('Ctrl Pts',(29.1449076103833,0.821179121928182,19.3150620325829));
#68330=CARTESIAN_POINT('Ctrl Pts',(29.0436548787038,0.700625409307818,19.3253204220004));
#68331=CARTESIAN_POINT('Ctrl Pts',(28.8969987915807,0.43246305184088,19.3443351373923));
#68332=CARTESIAN_POINT('Ctrl Pts',(28.8509250755758,0.288512534702925,19.3545423049446));
#68333=CARTESIAN_POINT('Ctrl Pts',(28.8145962917767,-0.0146433580687103,
19.3760383235316));
#68334=CARTESIAN_POINT('Ctrl Pts',(28.8269416915671,-0.171282191603316,
19.3871451875491));
#68335=CARTESIAN_POINT('Ctrl Pts',(28.9109596159865,-0.467218400914038,
19.4081292766188));
#68336=CARTESIAN_POINT('Ctrl Pts',(28.9804361831083,-0.603975745967944,
19.4171374882925));
#68337=CARTESIAN_POINT('Ctrl Pts',(29.167379298401,-0.843150163563664,19.4370968570367));
#68338=CARTESIAN_POINT('Ctrl Pts',(29.2829166096857,-0.943363871775425,
19.447744685016));
#68339=CARTESIAN_POINT('Ctrl Pts',(29.5508199561077,-1.09737775425148,19.4696563740096));
#68340=CARTESIAN_POINT('Ctrl Pts',(29.7018004358378,-1.14764798506443,19.4807100016028));
#68341=CARTESIAN_POINT('Ctrl Pts',(29.9053565213586,-1.17238533019257,19.4940869386326));
#68342=CARTESIAN_POINT('Ctrl Pts',(29.9526999581129,-1.17524047358085,19.4970954144566));
#68343=CARTESIAN_POINT('Ctrl Pts',(29.9999999999997,-1.17524047358085,19.4999999999999));
#68344=CARTESIAN_POINT('Origin',(30.,-1.21864324187371E-14,15.78125));
#68345=CARTESIAN_POINT('',(30.0000000000003,-1.17524047358085,20.0625));
#68346=CARTESIAN_POINT('',(30.,-1.17524047358085,20.));
#68347=CARTESIAN_POINT('',(30.,-1.17524047358085,15.78125));
#68348=CARTESIAN_POINT('Ctrl Pts',(30.0000000000005,-1.17524047358085,20.0625));
#68349=CARTESIAN_POINT('Ctrl Pts',(29.8795085612599,-1.17524047358091,20.0551009010331));
#68350=CARTESIAN_POINT('Ctrl Pts',(29.7595622632698,-1.15671912815303,20.0470786269818));
#68351=CARTESIAN_POINT('Ctrl Pts',(29.4968909328774,-1.07331217196907,20.0279915033172));
#68352=CARTESIAN_POINT('Ctrl Pts',(29.3601452160293,-0.997848639613717,
20.0169188027128));
#68353=CARTESIAN_POINT('Ctrl Pts',(29.1279895360134,-0.801888849412877,
19.9957151555763));
#68354=CARTESIAN_POINT('Ctrl Pts',(29.0334325756294,-0.684937055319331,
19.9860671564471));
#68355=CARTESIAN_POINT('Ctrl Pts',(28.8898211655935,-0.415941538872162,
19.9669933638564));
#68356=CARTESIAN_POINT('Ctrl Pts',(28.8445081931777,-0.265175978908636,
19.956302958832));
#68357=CARTESIAN_POINT('Ctrl Pts',(28.8156113317766,0.0421759568632406,
19.934509409435));
#68358=CARTESIAN_POINT('Ctrl Pts',(28.8311290214712,0.195715280521655,19.9236223238335));
#68359=CARTESIAN_POINT('Ctrl Pts',(28.9191574051752,0.485137216573778,19.9031001454256));
#68360=CARTESIAN_POINT('Ctrl Pts',(28.9896097101006,0.618617028321211,19.8942800985803));
#68361=CARTESIAN_POINT('Ctrl Pts',(29.1815016413357,0.8578593810217,19.8740144260076));
#68362=CARTESIAN_POINT('Ctrl Pts',(29.3033374545183,0.95943115864218,19.8629316730427));
#68363=CARTESIAN_POINT('Ctrl Pts',(29.5744131919249,1.10584185120943,19.8410947363937));
#68364=CARTESIAN_POINT('Ctrl Pts',(29.7199575824398,1.1513488317962,19.8305438014147));
#68365=CARTESIAN_POINT('Ctrl Pts',(30.0223936436952,1.18496921575338,19.8107799381662));
#68366=CARTESIAN_POINT('Ctrl Pts',(30.17645595477,1.17197553997772,19.8015484961906));
#68367=CARTESIAN_POINT('Ctrl Pts',(30.4728526803367,1.08704252391974,19.7803362699347));
#68368=CARTESIAN_POINT('Ctrl Pts',(30.6120360120599,1.01521369720442,19.7692427449689));
#68369=CARTESIAN_POINT('Ctrl Pts',(30.8500255075595,0.825212607475584,19.7478921149936));
#68370=CARTESIAN_POINT('Ctrl Pts',(30.9478859340228,0.710618012755788,19.7378881282691));
#68371=CARTESIAN_POINT('Ctrl Pts',(31.0987101974267,0.445344450081356,19.7190782500187));
#68372=CARTESIAN_POINT('Ctrl Pts',(31.148011535677,0.295869142851177,19.7084793335565));
#68373=CARTESIAN_POINT('Ctrl Pts',(31.1851397417262,-0.0109614779842622,
19.6867227492848));
#68374=CARTESIAN_POINT('Ctrl Pts',(31.1736153786499,-0.165256365490512,
19.6757820885594));
#68375=CARTESIAN_POINT('Ctrl Pts',(31.093043155488,-0.456865689692268,19.6551048079831));
#68376=CARTESIAN_POINT('Ctrl Pts',(31.0262715370984,-0.591802059151614,
19.6462060198927));
#68377=CARTESIAN_POINT('Ctrl Pts',(30.8407896047275,-0.836102523209368,
19.6261546414896));
#68378=CARTESIAN_POINT('Ctrl Pts',(30.7213221432726,-0.941101033293042,
19.6150958330235));
#68379=CARTESIAN_POINT('Ctrl Pts',(30.4533957183897,-1.09478566221008,19.5931944001043));
#68380=CARTESIAN_POINT('Ctrl Pts',(30.3086782810935,-1.14405280540599,19.5825609345826));
#68381=CARTESIAN_POINT('Ctrl Pts',(30.1059062370161,-1.17166523878134,19.5691302110914));
#68382=CARTESIAN_POINT('Ctrl Pts',(30.0529306288365,-1.17524047358084,19.5657503467901));
#68383=CARTESIAN_POINT('Ctrl Pts',(30.0000000000003,-1.17524047358085,19.5625));
#68384=CARTESIAN_POINT('Ctrl Pts',(29.9999999999997,-1.17524047358085,19.4999999999999));
#68385=CARTESIAN_POINT('Ctrl Pts',(30.1013134091967,-1.17524047358085,19.5062214207844));
#68386=CARTESIAN_POINT('Ctrl Pts',(30.2023703512557,-1.16214610944681,19.5128913366607));
#68387=CARTESIAN_POINT('Ctrl Pts',(30.4489451189351,-1.0968832859302,19.530346730545));
#68388=CARTESIAN_POINT('Ctrl Pts',(30.5880725807912,-1.02901377075515,19.5412964522821));
#68389=CARTESIAN_POINT('Ctrl Pts',(30.8343712795547,-0.842194481571482,
19.5630445243813));
#68390=CARTESIAN_POINT('Ctrl Pts',(30.9385897374703,-0.724253666071193,
19.5736257801046));
#68391=CARTESIAN_POINT('Ctrl Pts',(31.0916505061583,-0.460199205120922,
19.5923866032744));
#68392=CARTESIAN_POINT('Ctrl Pts',(31.1412805360793,-0.317836464065441,
19.6024630191855));
#68393=CARTESIAN_POINT('Ctrl Pts',(31.1853286010408,-0.0163533735884271,
19.6238404235873));
#68394=CARTESIAN_POINT('Ctrl Pts',(31.1771308821554,0.140138676220234,19.6349368795415));
#68395=CARTESIAN_POINT('Ctrl Pts',(31.1009443941398,0.438772825443172,19.6561122727154));
#68396=CARTESIAN_POINT('Ctrl Pts',(31.0345585763112,0.578169376036336,19.6653017627446));
#68397=CARTESIAN_POINT('Ctrl Pts',(30.8531427469532,0.82231181712456,19.6850978487155));
#68398=CARTESIAN_POINT('Ctrl Pts',(30.7404083067898,0.925109501957493,19.6956651705268));
#68399=CARTESIAN_POINT('Ctrl Pts',(30.4771535858122,1.08544747135218,19.7175156107599));
#68400=CARTESIAN_POINT('Ctrl Pts',(30.3279214291812,1.13945389596675,19.7285943399309));
#68401=CARTESIAN_POINT('Ctrl Pts',(30.0245530133835,1.1844610145353,19.7488191591971));
#68402=CARTESIAN_POINT('Ctrl Pts',(29.8738446796079,1.17798106878653,19.7576497404222));
#68403=CARTESIAN_POINT('Ctrl Pts',(29.5795308296296,1.10805786067705,19.7782019083499));
#68404=CARTESIAN_POINT('Ctrl Pts',(29.4390520876789,1.04399036655414,19.7890998131999));
#68405=CARTESIAN_POINT('Ctrl Pts',(29.1881857877585,0.86396490371117,19.8108875045287));
#68406=CARTESIAN_POINT('Ctrl Pts',(29.0808654270878,0.748795351686304,19.8215609892382));
#68407=CARTESIAN_POINT('Ctrl Pts',(28.9210185508111,0.489082061917269,19.8405846207479));
#68408=CARTESIAN_POINT('Ctrl Pts',(28.8677194354805,0.348399842158546,19.8502958472478));
#68409=CARTESIAN_POINT('Ctrl Pts',(28.8156254684423,0.0489678765559477,
19.8715278115659));
#68410=CARTESIAN_POINT('Ctrl Pts',(28.8194748723048,-0.107254256712007,
19.88260512842));
#68411=CARTESIAN_POINT('Ctrl Pts',(28.8873579337553,-0.408638429267571,
19.9039755188019));
#68412=CARTESIAN_POINT('Ctrl Pts',(28.9504754704978,-0.550854728104584,
19.9134143320288));
#68413=CARTESIAN_POINT('Ctrl Pts',(29.1260934520651,-0.800139160205639,
19.9330366884507));
#68414=CARTESIAN_POINT('Ctrl Pts',(29.2358570179041,-0.905539531949709,
19.9435138507578));
#68415=CARTESIAN_POINT('Ctrl Pts',(29.4941308064619,-1.07230397107708,19.9652862658853));
#68416=CARTESIAN_POINT('Ctrl Pts',(29.6414537313008,-1.13013161490591,19.9763832300743));
#68417=CARTESIAN_POINT('Ctrl Pts',(29.8633704190017,-1.16928660340085,19.9913988083098));
#68418=CARTESIAN_POINT('Ctrl Pts',(29.9316910379181,-1.17524047358085,19.9958053055382));
#68419=CARTESIAN_POINT('Ctrl Pts',(30.,-1.17524047358085,20.));
#68420=CARTESIAN_POINT('Origin',(30.,-1.21864324187371E-14,15.78125));
#68421=CARTESIAN_POINT('',(30.,-1.17524047358085,20.5625));
#68422=CARTESIAN_POINT('',(30.,-1.17524047358085,20.5));
#68423=CARTESIAN_POINT('',(30.,-1.17524047358085,15.78125));
#68424=CARTESIAN_POINT('Ctrl Pts',(30.0000000000001,-1.17524047358085,20.5625));
#68425=CARTESIAN_POINT('Ctrl Pts',(29.857466677664,-1.17524047358086,20.5537473602351));
#68426=CARTESIAN_POINT('Ctrl Pts',(29.7159780885029,-1.14931710991913,20.5441397949867));
#68427=CARTESIAN_POINT('Ctrl Pts',(29.4386327044728,-1.04389937724848,20.5233712075421));
#68428=CARTESIAN_POINT('Ctrl Pts',(29.3069416102485,-0.961526015490682,
20.5123639202805));
#68429=CARTESIAN_POINT('Ctrl Pts',(29.086333053172,-0.75405497378,20.4914612382194));
#68430=CARTESIAN_POINT('Ctrl Pts',(28.998234525789,-0.632326756560098,20.4823366930552));
#68431=CARTESIAN_POINT('Ctrl Pts',(28.8691902031313,-0.356072447869899,
20.4627481978422));
#68432=CARTESIAN_POINT('Ctrl Pts',(28.8319810448841,-0.203050335093991,
20.4518977863579));
#68433=CARTESIAN_POINT('Ctrl Pts',(28.8195943462911,0.104677105391675,20.4300776108702));
#68434=CARTESIAN_POINT('Ctrl Pts',(28.8430260194231,0.256395499280261,20.419319642799));
#68435=CARTESIAN_POINT('Ctrl Pts',(28.9459812899286,0.541272174450661,20.399119757359));
#68436=CARTESIAN_POINT('Ctrl Pts',(29.0240298052411,0.671873753047622,20.3902782906932));
#68437=CARTESIAN_POINT('Ctrl Pts',(29.2288981247322,0.900554058537053,20.3695902323474));
#68438=CARTESIAN_POINT('Ctrl Pts',(29.3552896087803,0.99495410007641,20.3584819910769));
#68439=CARTESIAN_POINT('Ctrl Pts',(29.6322160097862,1.12628386030684,20.3368204541948));
#68440=CARTESIAN_POINT('Ctrl Pts',(29.7791530812878,1.16405670631925,20.3264582018892));
#68441=CARTESIAN_POINT('Ctrl Pts',(30.0846260087116,1.18247957174534,20.3070466605788));
#68442=CARTESIAN_POINT('Ctrl Pts',(30.2403465146444,1.16089584876694,20.297232309072));
#68443=CARTESIAN_POINT('Ctrl Pts',(30.5330201521523,1.05871377596515,20.2756371654718));
#68444=CARTESIAN_POINT('Ctrl Pts',(30.6672316693715,0.979687699230499,20.2645937786601));
#68445=CARTESIAN_POINT('Ctrl Pts',(30.8935142020877,0.777827856358351,20.2435416089216));
#68446=CARTESIAN_POINT('Ctrl Pts',(30.9847747247484,0.658466900361099,20.2341902246224));
#68447=CARTESIAN_POINT('Ctrl Pts',(31.1210267097183,0.385760488516485,20.2148533018128));
#68448=CARTESIAN_POINT('Ctrl Pts',(31.1622514979646,0.233796400148884,20.2040779121667));
#68449=CARTESIAN_POINT('Ctrl Pts',(31.1827840987885,-0.0738574566284658,
20.1822629543138));
#68450=CARTESIAN_POINT('Ctrl Pts',(31.1632412224874,-0.226525134572718,
20.1714376749082));
#68451=CARTESIAN_POINT('Ctrl Pts',(31.0676501608268,-0.513670659031922,
20.1510769110961));
#68452=CARTESIAN_POINT('Ctrl Pts',(30.9933877261944,-0.645689071009633,
20.1422762056128));
#68453=CARTESIAN_POINT('Ctrl Pts',(30.7949445520148,-0.879653706050947,
20.1217953512642));
#68454=CARTESIAN_POINT('Ctrl Pts',(30.670767244765,-0.977642983856647,20.1106958256016));
#68455=CARTESIAN_POINT('Ctrl Pts',(30.3966473841018,-1.11649688166864,20.0889398730384));
#68456=CARTESIAN_POINT('Ctrl Pts',(30.2503518300705,-1.15811817698529,20.0784805729189));
#68457=CARTESIAN_POINT('Ctrl Pts',(30.0667947188483,-1.17381847353791,20.0666521235228));
#68458=CARTESIAN_POINT('Ctrl Pts',(30.0333795266192,-1.17524047358084,20.0645497590825));
#68459=CARTESIAN_POINT('Ctrl Pts',(30.0000000000005,-1.17524047358085,20.0625));
#68460=CARTESIAN_POINT('Ctrl Pts',(30.,-1.17524047358085,20.));
#68461=CARTESIAN_POINT('Ctrl Pts',(30.0810461612404,-1.17524047358085,20.0049768562329));
#68462=CARTESIAN_POINT('Ctrl Pts',(30.1620390634994,-1.16685998246121,20.0102475616837));
#68463=CARTESIAN_POINT('Ctrl Pts',(30.3910188268312,-1.11873616439623,20.0260148454886));
#68464=CARTESIAN_POINT('Ctrl Pts',(30.5327757448135,-1.05858684074315,20.0368523263699));
#68465=CARTESIAN_POINT('Ctrl Pts',(30.7881241531233,-0.885634167315425,
20.0586644967329));
#68466=CARTESIAN_POINT('Ctrl Pts',(30.8985424642913,-0.773390023616368,
20.0694245027186));
#68467=CARTESIAN_POINT('Ctrl Pts',(31.0652926267422,-0.518183463935382,
20.0887122685505));
#68468=CARTESIAN_POINT('Ctrl Pts',(31.1223297618129,-0.379162720763723,
20.0981145292327));
#68469=CARTESIAN_POINT('Ctrl Pts',(31.182501138976,-0.0818619977066759,
20.1191953725253));
#68470=CARTESIAN_POINT('Ctrl Pts',(31.1830210318339,0.0739680814447177,
20.1302448898124));
#68471=CARTESIAN_POINT('Ctrl Pts',(31.1235906320717,0.378032609170699,20.1518053374088));
#68472=CARTESIAN_POINT('Ctrl Pts',(31.0637982215859,0.523138441463073,20.1615551718639));
#68473=CARTESIAN_POINT('Ctrl Pts',(30.8940186419568,0.777530022608243,20.1810000731231));
#68474=CARTESIAN_POINT('Ctrl Pts',(30.7872728375238,0.885439479392022,20.1913808781633));
#68475=CARTESIAN_POINT('Ctrl Pts',(30.5341117586616,1.05845819784869,20.2130610712561));
#68476=CARTESIAN_POINT('Ctrl Pts',(30.3887837233288,1.12003007025227,20.2241682808161));
#68477=CARTESIAN_POINT('Ctrl Pts',(30.0880464072922,1.18158358213937,20.2448181618436));
#68478=CARTESIAN_POINT('Ctrl Pts',(29.9360438868879,1.18313176496437,20.2536476203627));
#68479=CARTESIAN_POINT('Ctrl Pts',(29.6381705506099,1.1284628410545,20.2738775466838));
#68480=CARTESIAN_POINT('Ctrl Pts',(29.4952627894061,1.07218329111658,20.2846485002308));
#68481=CARTESIAN_POINT('Ctrl Pts',(29.2357076507194,0.906285518142771,20.3064688735353));
#68482=CARTESIAN_POINT('Ctrl Pts',(29.1223265216238,0.796998466553187,20.3173059793119));
#68483=CARTESIAN_POINT('Ctrl Pts',(28.94883850375,0.546283376626024,20.3368482617845));
#68484=CARTESIAN_POINT('Ctrl Pts',(28.8881400415123,0.408839661433748,20.3460102123335));
#68485=CARTESIAN_POINT('Ctrl Pts',(28.8201837019616,0.113659356458156,20.3669407021362));
#68486=CARTESIAN_POINT('Ctrl Pts',(28.8154556440784,-0.0416770716817043,
20.377955215877));
#68487=CARTESIAN_POINT('Ctrl Pts',(28.8666287496698,-0.348241759389233,
20.3996929435023));
#68488=CARTESIAN_POINT('Ctrl Pts',(28.923168044506,-0.496185032937023,20.4097992015263));
#68489=CARTESIAN_POINT('Ctrl Pts',(29.0873034963183,-0.755446668555585,
20.4290701716561));
#68490=CARTESIAN_POINT('Ctrl Pts',(29.1911125253156,-0.865675121623956,
20.4393528532326));
#68491=CARTESIAN_POINT('Ctrl Pts',(29.4392495659902,-1.04453090441881,20.4609314775711));
#68492=CARTESIAN_POINT('Ctrl Pts',(29.5825856119781,-1.10962145963742,20.4720411141544));
#68493=CARTESIAN_POINT('Ctrl Pts',(29.8217321396476,-1.16509155071327,20.4886931681386));
#68494=CARTESIAN_POINT('Ctrl Pts',(29.9108091908387,-1.17524047358086,20.4945229998842));
#68495=CARTESIAN_POINT('Ctrl Pts',(30.0000000000001,-1.17524047358085,20.5));
#68496=CARTESIAN_POINT('Origin',(30.,-1.21864324187371E-14,15.78125));
#68497=CARTESIAN_POINT('',(30.,-1.17524047358085,21.0625));
#68498=CARTESIAN_POINT('',(30.0000000000003,-1.17524047358085,21.));
#68499=CARTESIAN_POINT('',(30.,-1.17524047358085,15.78125));
#68500=CARTESIAN_POINT('Ctrl Pts',(30.,-1.17524047358085,21.0625));
#68501=CARTESIAN_POINT('Ctrl Pts',(29.9930425354756,-1.17524047358085,21.062072758288));
#68502=CARTESIAN_POINT('Ctrl Pts',(29.9860827950433,-1.17517869098314,21.0616431863938));
#68503=CARTESIAN_POINT('Ctrl Pts',(29.8232316065342,-1.17228514735699,21.0515402867957));
#68504=CARTESIAN_POINT('Ctrl Pts',(29.6694853244495,-1.13852257202281,21.0409020757897));
#68505=CARTESIAN_POINT('Ctrl Pts',(29.3867104280309,-1.01415059452875,21.0191280758083));
#68506=CARTESIAN_POINT('Ctrl Pts',(29.2599516823908,-0.925722033008617,
21.0082089931399));
#68507=CARTESIAN_POINT('Ctrl Pts',(29.0500490851207,-0.707886564567504,
20.9875962815068));
#68508=CARTESIAN_POINT('Ctrl Pts',(28.9678750474644,-0.58156955059427,20.9787376277926));
#68509=CARTESIAN_POINT('Ctrl Pts',(28.852209421352,-0.297516308143681,20.9585961298867));
#68510=CARTESIAN_POINT('Ctrl Pts',(28.8227455494544,-0.141401249035421,
20.9475264053908));
#68511=CARTESIAN_POINT('Ctrl Pts',(28.8269065561122,0.16711629798966,20.9256502054441));
#68512=CARTESIAN_POINT('Ctrl Pts',(28.8581354481118,0.316603790040456,20.915050424987));
#68513=CARTESIAN_POINT('Ctrl Pts',(28.9760761175465,0.596699382404322,20.8951895540518));
#68514=CARTESIAN_POINT('Ctrl Pts',(29.0620842641545,0.724424918144287,20.8860783197069));
#68515=CARTESIAN_POINT('Ctrl Pts',(29.2801481558297,0.941880855388224,20.8649778977684));
#68516=CARTESIAN_POINT('Ctrl Pts',(29.4108173740059,1.02868094436595,20.8538764175153));
#68517=CARTESIAN_POINT('Ctrl Pts',(29.6929274853784,1.14422525088517,20.8324562143623));
#68518=CARTESIAN_POINT('Ctrl Pts',(29.8408766090356,1.17398844910975,20.8223157862342));
#68519=CARTESIAN_POINT('Ctrl Pts',(30.146238089068,1.17646530253954,20.8034764343644));
#68520=CARTESIAN_POINT('Ctrl Pts',(30.3008127704194,1.14674523024735,20.7930175246536));
#68521=CARTESIAN_POINT('Ctrl Pts',(30.5871854304481,1.02954198948055,20.7712767528846));
#68522=CARTESIAN_POINT('Ctrl Pts',(30.7164764357369,0.944145175747713,20.7603096568304));
#68523=CARTESIAN_POINT('Ctrl Pts',(30.9318157386174,0.731537563311469,20.7395484367846));
#68524=CARTESIAN_POINT('Ctrl Pts',(31.0169931096024,0.607571893797524,20.7305813882675));
#68525=CARTESIAN_POINT('Ctrl Pts',(31.1392545858023,0.328058458126713,20.7107617965928));
#68526=CARTESIAN_POINT('Ctrl Pts',(31.1726798971535,0.174145191638854,20.6998481956499));
#68527=CARTESIAN_POINT('Ctrl Pts',(31.177452605602,-0.133454152417299,20.6780371031564));
#68528=CARTESIAN_POINT('Ctrl Pts',(31.1504138008343,-0.284195707834949,
20.6673484002337));
#68529=CARTESIAN_POINT('Ctrl Pts',(31.0405663350578,-0.566901684154618,
20.647302433566));
#68530=CARTESIAN_POINT('Ctrl Pts',(30.9589018497076,-0.696179869646961,
20.6383684206626));
#68531=CARTESIAN_POINT('Ctrl Pts',(30.7479829469593,-0.919779045347213,
20.6174889551129));
#68532=CARTESIAN_POINT('Ctrl Pts',(30.6195839675717,-1.0107321163549,20.6063796462101));
#68533=CARTESIAN_POINT('Ctrl Pts',(30.3401820261614,-1.13487834149049,20.5848207753144));
#68534=CARTESIAN_POINT('Ctrl Pts',(30.1927291526794,-1.16899555973842,20.5745564544744));
#68535=CARTESIAN_POINT('Ctrl Pts',(30.02853673898,-1.17498080122699,20.5642615811144));
#68536=CARTESIAN_POINT('Ctrl Pts',(30.0142636931895,-1.17524047358085,20.5633759002187));
#68537=CARTESIAN_POINT('Ctrl Pts',(30.0000000000001,-1.17524047358085,20.5625));
#68538=CARTESIAN_POINT('Ctrl Pts',(30.0000000000001,-1.17524047358085,20.5));
#68539=CARTESIAN_POINT('Ctrl Pts',(30.0615320920417,-1.17524047358085,20.5037785426368));
#68540=CARTESIAN_POINT('Ctrl Pts',(30.1230970944725,-1.17040913175211,20.5077303953467));
#68541=CARTESIAN_POINT('Ctrl Pts',(30.3340845761439,-1.13693724894346,20.5218733491291));
#68542=CARTESIAN_POINT('Ctrl Pts',(30.4779822284686,-1.08432359797014,20.5325751197693));
#68543=CARTESIAN_POINT('Ctrl Pts',(30.7413240882277,-0.925171378815601,
20.5543888717152));
#68544=CARTESIAN_POINT('Ctrl Pts',(30.8574242886598,-0.818746672756081,
20.5652914684918));
#68545=CARTESIAN_POINT('Ctrl Pts',(31.0372296037246,-0.572330389441825,
20.5850692727305));
#68546=CARTESIAN_POINT('Ctrl Pts',(31.1013789298939,-0.436327710632643,
20.5940611041994));
#68547=CARTESIAN_POINT('Ctrl Pts',(31.1765507195451,-0.143169609179877,
20.6148482046583));
#68548=CARTESIAN_POINT('Ctrl Pts',(31.1851707108535,0.0116076749541518,
20.6258230709101));
#68549=CARTESIAN_POINT('Ctrl Pts',(31.1420730921553,0.318093458162843,20.6475552036167));
#68550=CARTESIAN_POINT('Ctrl Pts',(31.0898417933348,0.466589648702242,20.6579510306787));
#68551=CARTESIAN_POINT('Ctrl Pts',(30.9337645237733,0.729159361106415,20.6768444502657));
#68552=CARTESIAN_POINT('Ctrl Pts',(30.8334379992983,0.84198975683026,20.6870055279311));
#68553=CARTESIAN_POINT('Ctrl Pts',(30.591317195237,1.02746666327729,20.7084494527507));
#68554=CARTESIAN_POINT('Ctrl Pts',(30.4504043784541,1.09657907803444,20.7195528744157));
#68555=CARTESIAN_POINT('Ctrl Pts',(30.1527579068286,1.17519666342875,20.7406179390521));
#68556=CARTESIAN_POINT('Ctrl Pts',(29.9992772327099,1.18508027808452,20.7496955256169));
#68557=CARTESIAN_POINT('Ctrl Pts',(29.6980213394833,1.14582802600215,20.7695865882633));
#68558=CARTESIAN_POINT('Ctrl Pts',(29.5531012936116,1.09744171629364,20.7802012666676));
#68559=CARTESIAN_POINT('Ctrl Pts',(29.2844190436536,0.945457598499347,20.8020888235724));
#68560=CARTESIAN_POINT('Ctrl Pts',(29.1643876737344,0.84125826030012,20.8131539267157));
#68561=CARTESIAN_POINT('Ctrl Pts',(28.9773975743441,0.59813879267389,20.8332560474103));
#68562=CARTESIAN_POINT('Ctrl Pts',(28.9097638018428,0.463547729800393,20.8421310013978));
#68563=CARTESIAN_POINT('Ctrl Pts',(28.8274319674294,0.172449502758382,20.8627720413655));
#68564=CARTESIAN_POINT('Ctrl Pts',(28.8149632933605,0.0183235810432114,
20.8737007211534));
#68565=CARTESIAN_POINT('Ctrl Pts',(28.850150967155,-0.288650006351519,20.8954674428227));
#68566=CARTESIAN_POINT('Ctrl Pts',(28.898515176706,-0.438439388541448,20.906088629547));
#68567=CARTESIAN_POINT('Ctrl Pts',(29.047641063206,-0.704596833168998,20.9249611816339));
#68568=CARTESIAN_POINT('Ctrl Pts',(29.1447168471359,-0.819746341645053,
20.9348754556746));
#68569=CARTESIAN_POINT('Ctrl Pts',(29.381325819526,-1.01116668011756,20.9561916286088));
#68570=CARTESIAN_POINT('Ctrl Pts',(29.5199396968772,-1.08386414625954,20.96728098122));
#68571=CARTESIAN_POINT('Ctrl Pts',(29.7764916553148,-1.15925176815251,20.9857080131187));
#68572=CARTESIAN_POINT('Ctrl Pts',(29.8880479255875,-1.1752404735809,20.9931252835322));
#68573=CARTESIAN_POINT('Ctrl Pts',(30.0000000000005,-1.17524047358085,21.));
#68574=CARTESIAN_POINT('Origin',(30.,-1.21864324187371E-14,15.78125));
#68575=CARTESIAN_POINT('',(29.9999999999998,-1.17524047358085,21.5625));
#68576=CARTESIAN_POINT('',(30.0000000000001,-1.17524047358085,21.5));
#68577=CARTESIAN_POINT('',(30.,-1.17524047358085,15.78125));
#68578=CARTESIAN_POINT('Ctrl Pts',(29.9999999999996,-1.17524047358085,21.5625));
#68579=CARTESIAN_POINT('Ctrl Pts',(29.9719988088573,-1.17524047358085,21.5607805119881));
#68580=CARTESIAN_POINT('Ctrl Pts',(29.9439711363572,-1.17423978092491,21.5590239195234));
#68581=CARTESIAN_POINT('Ctrl Pts',(29.7604047377572,-1.16108096387714,21.547285004757));
#68582=CARTESIAN_POINT('Ctrl Pts',(29.6086428973266,-1.11907669828182,21.5364764549777));
#68583=CARTESIAN_POINT('Ctrl Pts',(29.3336394628651,-0.979972388454951,
21.5146573661612));
#68584=CARTESIAN_POINT('Ctrl Pts',(29.2123764352237,-0.885461951955829,
21.503860137555));
#68585=CARTESIAN_POINT('Ctrl Pts',(29.0139169118187,-0.656850944948416,
21.4835680853588));
#68586=CARTESIAN_POINT('Ctrl Pts',(28.9380513713638,-0.525431379870783,
21.4747570119112));
#68587=CARTESIAN_POINT('Ctrl Pts',(28.8379806985326,-0.235334014126339,
21.4541869404899));
#68588=CARTESIAN_POINT('Ctrl Pts',(28.81701218115,-0.0787326333033737,21.4430827321496));
#68589=CARTESIAN_POINT('Ctrl Pts',(28.8372148732154,0.227544173701852,21.4213654174177));
#68590=CARTESIAN_POINT('Ctrl Pts',(28.8758855793473,0.374476178993786,21.4109468400715));
#68591=CARTESIAN_POINT('Ctrl Pts',(29.008483168462,0.64967403277934,21.3914332554072));
#68592=CARTESIAN_POINT('Ctrl Pts',(29.1026400510551,0.774562668949264,21.3818103125428));
#68593=CARTESIAN_POINT('Ctrl Pts',(29.3337333173752,0.980382528955385,21.3603223294383));
#68594=CARTESIAN_POINT('Ctrl Pts',(29.4682481852686,1.05938687455618,21.3492610850172));
#68595=CARTESIAN_POINT('Ctrl Pts',(29.7549668128984,1.15903498567807,21.3281214631321));
#68596=CARTESIAN_POINT('Ctrl Pts',(29.9037091563498,1.1807204220266,21.3186072813687));
#68597=CARTESIAN_POINT('Ctrl Pts',(30.2082836909242,1.16710140483065,21.2994212226452));
#68598=CARTESIAN_POINT('Ctrl Pts',(30.3610942123922,1.12920096767185,21.2886937718569));
#68599=CARTESIAN_POINT('Ctrl Pts',(30.6400777787282,0.99739853025376,21.2668891510646));
#68600=CARTESIAN_POINT('Ctrl Pts',(30.7641225887122,0.905886016702667,21.2560273872475));
#68601=CARTESIAN_POINT('Ctrl Pts',(30.9683193471767,0.682639701404097,21.2355732231612));
#68602=CARTESIAN_POINT('Ctrl Pts',(31.0473475790777,0.553805208866279,21.2267689284532));
#68603=CARTESIAN_POINT('Ctrl Pts',(31.1552799375254,0.266708452111841,21.2064116226359));
#68604=CARTESIAN_POINT('Ctrl Pts',(31.1805191858716,0.110295910456217,21.195320804404));
#68605=CARTESIAN_POINT('Ctrl Pts',(31.1683617956532,-0.197210560675315,
21.173516297295));
#68606=CARTESIAN_POINT('Ctrl Pts',(31.1334138492448,-0.345474524238407,
21.1630032741523));
#68607=CARTESIAN_POINT('Ctrl Pts',(31.0081981695942,-0.623166742222595,
21.1433128204234));
#68608=CARTESIAN_POINT('Ctrl Pts',(30.9181918552343,-0.749490769431124,
21.1339784439808));
#68609=CARTESIAN_POINT('Ctrl Pts',(30.6936733778382,-0.961255467276285,
21.1126834366527));
#68610=CARTESIAN_POINT('Ctrl Pts',(30.5610503971428,-1.04422897430134,21.1015976470182));
#68611=CARTESIAN_POINT('Ctrl Pts',(30.283074075588,-1.14948332004627,21.080796107845));
#68612=CARTESIAN_POINT('Ctrl Pts',(30.1420666819575,-1.17524047358085,21.0712239844648));
#68613=CARTESIAN_POINT('Ctrl Pts',(30.,-1.17524047358085,21.0625));
#68614=CARTESIAN_POINT('Ctrl Pts',(30.0000000000005,-1.17524047358085,21.));
#68615=CARTESIAN_POINT('Ctrl Pts',(30.0409368563611,-1.17524047358083,21.0025138371222));
#68616=CARTESIAN_POINT('Ctrl Pts',(30.0819173014533,-1.17310176285816,21.0051061762144));
#68617=CARTESIAN_POINT('Ctrl Pts',(30.2729829235624,-1.15303120950392,21.0175506477331));
#68618=CARTESIAN_POINT('Ctrl Pts',(30.4187156327833,-1.10844931428969,21.0280803491923));
#68619=CARTESIAN_POINT('Ctrl Pts',(30.6905353954506,-0.963834030798816,
21.0498993207407));
#68620=CARTESIAN_POINT('Ctrl Pts',(30.8129383742835,-0.863111359129209,
21.0609867980498));
#68621=CARTESIAN_POINT('Ctrl Pts',(31.0063964161767,-0.625120486728277,
21.0813042721815));
#68622=CARTESIAN_POINT('Ctrl Pts',(31.0777548462909,-0.49199236060375,21.0901140644785));
#68623=CARTESIAN_POINT('Ctrl Pts',(31.1675962416571,-0.203110857145286,
21.1105979221763));
#68624=CARTESIAN_POINT('Ctrl Pts',(31.1840814343856,-0.0497708726068158,
21.1214708731443));
#68625=CARTESIAN_POINT('Ctrl Pts',(31.1571888276141,0.257674311285982,21.14327103453));
#68626=CARTESIAN_POINT('Ctrl Pts',(31.1128522255693,0.408737402730974,21.1539825367601));
#68627=CARTESIAN_POINT('Ctrl Pts',(30.9710010878299,0.678628541040232,21.1731198356347));
#68628=CARTESIAN_POINT('Ctrl Pts',(30.8772391714915,0.796156039182743,21.1826908232652));
#68629=CARTESIAN_POINT('Ctrl Pts',(30.6464955823919,0.993543206250726,21.2038583630273));
#68630=CARTESIAN_POINT('Ctrl Pts',(30.5103519798164,1.06987223749504,21.214924774365));
#68631=CARTESIAN_POINT('Ctrl Pts',(30.2162079552513,1.16549604568273,21.2363776960251));
#68632=CARTESIAN_POINT('Ctrl Pts',(30.061127965963,1.18379547472913,21.2459429670447));
#68633=CARTESIAN_POINT('Ctrl Pts',(29.7567781749822,1.15962478754955,21.2654893209196));
#68634=CARTESIAN_POINT('Ctrl Pts',(29.6103180879013,1.11893466526318,21.2759257110673));
#68635=CARTESIAN_POINT('Ctrl Pts',(29.3355002124366,0.981897695520532,21.2976601102058));
#68636=CARTESIAN_POINT('Ctrl Pts',(29.2107776319456,0.884773136393355,21.3087624623211));
#68637=CARTESIAN_POINT('Ctrl Pts',(29.0107746609087,0.652081932742376,21.3292939522647));
#68638=CARTESIAN_POINT('Ctrl Pts',(28.9355970901093,0.52040794626517,21.3380991870768));
#68639=CARTESIAN_POINT('Ctrl Pts',(28.8382134265824,0.233810524699486,21.3584210862971));
#68640=CARTESIAN_POINT('Ctrl Pts',(28.8177208295725,0.0813648692728661,
21.3692306226469));
#68641=CARTESIAN_POINT('Ctrl Pts',(28.8362699803681,-0.22632694032349,21.3910482716382));
#68642=CARTESIAN_POINT('Ctrl Pts',(28.8765201026755,-0.378558584509325,
21.4018426329915));
#68643=CARTESIAN_POINT('Ctrl Pts',(29.0110211856253,-0.652134791815677,
21.4212412308003));
#68644=CARTESIAN_POINT('Ctrl Pts',(29.1015077791443,-0.772069972681635,
21.4305317818752));
#68645=CARTESIAN_POINT('Ctrl Pts',(29.3264048767426,-0.975307798634206,
21.4515477299157));
#68646=CARTESIAN_POINT('Ctrl Pts',(29.4600073333855,-1.05515984377402,21.4625829994009));
#68647=CARTESIAN_POINT('Ctrl Pts',(29.7321091399909,-1.15220558787994,21.4827327726726));
#68648=CARTESIAN_POINT('Ctrl Pts',(29.8656344449969,-1.17524047358088,21.4917489238272));
#68649=CARTESIAN_POINT('Ctrl Pts',(30.0000000000003,-1.17524047358085,21.5));
#68650=CARTESIAN_POINT('Origin',(30.,-1.21864324187371E-14,15.78125));
#68651=CARTESIAN_POINT('',(29.9999999999998,-1.17524047358085,22.0625));
#68652=CARTESIAN_POINT('',(30.000000003784,-1.17524047358085,22.0000000004647));
#68653=CARTESIAN_POINT('',(30.,-1.17524047358085,15.78125));
#68654=CARTESIAN_POINT('Ctrl Pts',(29.9999999999997,-1.17524047358085,22.0625));
#68655=CARTESIAN_POINT('Ctrl Pts',(29.9524010211782,-1.17524047358085,22.0595770574349));
#68656=CARTESIAN_POINT('Ctrl Pts',(29.9047586284152,-1.17234913259513,22.0565489400777));
#68657=CARTESIAN_POINT('Ctrl Pts',(29.7009349924679,-1.1474210952591,22.0431488126472));
#68658=CARTESIAN_POINT('Ctrl Pts',(29.5500039838267,-1.09704169086814,22.0320943523472));
#68659=CARTESIAN_POINT('Ctrl Pts',(29.2822334508411,-0.942842462410207,
22.01018424791));
#68660=CARTESIAN_POINT('Ctrl Pts',(29.1667766500969,-0.842552714869588,
21.9995386680174));
#68661=CARTESIAN_POINT('Ctrl Pts',(28.9799931885339,-0.603233884932394,
21.9795839832802));
#68662=CARTESIAN_POINT('Ctrl Pts',(28.910605612196,-0.466400997640195,21.9705713166174));
#68663=CARTESIAN_POINT('Ctrl Pts',(28.8268127379948,-0.170385863417145,
21.9495816311816));
#68664=CARTESIAN_POINT('Ctrl Pts',(28.8145871174915,-0.0137497615287427,
21.9384749608582));
#68665=CARTESIAN_POINT('Ctrl Pts',(28.85113877829,0.289356743861303,21.9169824442057));
#68666=CARTESIAN_POINT('Ctrl Pts',(28.8973142483913,0.433263084581444,21.9067784090915));
#68667=CARTESIAN_POINT('Ctrl Pts',(29.0441562961032,0.701308793511537,21.8877719649526));
#68668=CARTESIAN_POINT('Ctrl Pts',(29.145494108998,0.821789237943167,21.8775043861745));
#68669=CARTESIAN_POINT('Ctrl Pts',(29.3876377187977,1.01480099788269,21.8557919221934));
#68670=CARTESIAN_POINT('Ctrl Pts',(29.5254500415353,1.08610079854932,21.8448013436507));
#68671=CARTESIAN_POINT('Ctrl Pts',(29.8162261597603,1.17031056565349,21.8239599076952));
#68672=CARTESIAN_POINT('Ctrl Pts',(29.965897796871,1.18415559330363,21.814910211276));
#68673=CARTESIAN_POINT('Ctrl Pts',(30.2694248477664,1.15452627142302,21.7952208509568));
#68674=CARTESIAN_POINT('Ctrl Pts',(30.4200757340443,1.10861951539323,21.7843421644183));
#68675=CARTESIAN_POINT('Ctrl Pts',(30.6910871340011,0.962634653497324,21.762524275871));
#68676=CARTESIAN_POINT('Ctrl Pts',(30.8096198631452,0.865330005993902,21.7517956433222));
#68677=CARTESIAN_POINT('Ctrl Pts',(31.0025452942337,0.631606479581076,21.7316621689435));
#68678=CARTESIAN_POINT('Ctrl Pts',(31.075346835895,0.497649504779323,21.7227870693252));
#68679=CARTESIAN_POINT('Ctrl Pts',(31.1677479593254,0.204711362167963,21.7020155655921));
#68680=CARTESIAN_POINT('Ctrl Pts',(31.1845780485819,0.0480344792828584,
21.6909060035913));
#68681=CARTESIAN_POINT('Ctrl Pts',(31.1566162472742,-0.256851307753155,
21.6692873225717));
#68682=CARTESIAN_POINT('Ctrl Pts',(31.1143736239456,-0.402401296420415,
21.6589667405334));
#68683=CARTESIAN_POINT('Ctrl Pts',(30.9745867433069,-0.675115053903835,
21.6396292968631));
#68684=CARTESIAN_POINT('Ctrl Pts',(30.8762946890393,-0.798585224220405,
21.6296650545771));
#68685=CARTESIAN_POINT('Ctrl Pts',(30.6387793080734,-0.998444700485959,
21.6079940222289));
#68686=CARTESIAN_POINT('Ctrl Pts',(30.5025155082578,-1.07350395293815,21.5969652482617));
#68687=CARTESIAN_POINT('Ctrl Pts',(30.2404480736925,-1.15671325182863,21.5779222161248));
#68688=CARTESIAN_POINT('Ctrl Pts',(30.1205093503255,-1.17524047358085,21.5699001988757));
#68689=CARTESIAN_POINT('Ctrl Pts',(29.9999999999996,-1.17524047358085,21.5625));
#68690=CARTESIAN_POINT('Ctrl Pts',(30.0000000000003,-1.17524047358085,21.5));
#68691=CARTESIAN_POINT('Ctrl Pts',(30.0212839202784,-1.17524047358085,21.5013069960338));
#68692=CARTESIAN_POINT('Ctrl Pts',(30.0425864419315,-1.17466229796956,21.5026356328208));
#68693=CARTESIAN_POINT('Ctrl Pts',(30.2139454930837,-1.16533366693515,21.5134891283695));
#68694=CARTESIAN_POINT('Ctrl Pts',(30.3610177391346,-1.12845915530085,21.523827832119));
#68695=CARTESIAN_POINT('Ctrl Pts',(30.6385696146112,-0.998891400827412,
21.5454653082446));
#68696=CARTESIAN_POINT('Ctrl Pts',(30.7654630357173,-0.905335035089088,
21.5565744608423));
#68697=CARTESIAN_POINT('Ctrl Pts',(30.9718229035628,-0.677897335355307,
21.5773100566854));
#68698=CARTESIAN_POINT('Ctrl Pts',(31.0507577571561,-0.547623084998762,
21.5861694304673));
#68699=CARTESIAN_POINT('Ctrl Pts',(31.1570604439752,-0.258809326298121,
21.6066484845527));
#68700=CARTESIAN_POINT('Ctrl Pts',(31.1812214838473,-0.102338491331391,
21.6177434360859));
#68701=CARTESIAN_POINT('Ctrl Pts',(31.1670292938221,0.204877234262332,21.6395273271632));
#68702=CARTESIAN_POINT('Ctrl Pts',(31.1311379778152,0.352813947812694,21.6500171458341));
#68703=CARTESIAN_POINT('Ctrl Pts',(31.0040616369159,0.629882761963365,21.6696633955718));
#68704=CARTESIAN_POINT('Ctrl Pts',(30.9130181373807,0.755846555951633,21.6790645983814));
#68705=CARTESIAN_POINT('Ctrl Pts',(30.6868446220844,0.966129203413541,21.7004086935125));
#68706=CARTESIAN_POINT('Ctrl Pts',(30.553735937256,1.0481102897547,21.711489124086));
#68707=CARTESIAN_POINT('Ctrl Pts',(30.2686762405413,1.15380487275931,21.7327412449065));
#68708=CARTESIAN_POINT('Ctrl Pts',(30.1202468756007,1.17853792824007,21.7424990119962));
#68709=CARTESIAN_POINT('Ctrl Pts',(29.8153503696085,1.17107054155024,21.7614867439455));
#68710=CARTESIAN_POINT('Ctrl Pts',(29.661826921183,1.13627251461424,21.7721479818837));
#68711=CARTESIAN_POINT('Ctrl Pts',(29.3799800833098,1.01003478165367,21.7939311399523));
#68712=CARTESIAN_POINT('Ctrl Pts',(29.253891997555,0.920828765085568,21.8048366026441));
#68713=CARTESIAN_POINT('Ctrl Pts',(29.0454103417907,0.701638656512355,21.8254100846196));
#68714=CARTESIAN_POINT('Ctrl Pts',(28.9640200854668,0.5746995746724,21.8342495048467));
#68715=CARTESIAN_POINT('Ctrl Pts',(28.8502724171258,0.289883112959693,21.8544451207025));
#68716=CARTESIAN_POINT('Ctrl Pts',(28.8218581810328,0.133683866085342,21.8655208147403));
#68717=CARTESIAN_POINT('Ctrl Pts',(28.8280094580603,-0.174601530686287,
21.8873805534988));
#68718=CARTESIAN_POINT('Ctrl Pts',(28.8601657562679,-0.323793761637004,
21.8979593977371));
#68719=CARTESIAN_POINT('Ctrl Pts',(28.9799119697649,-0.603297917389521,
21.9177783313962));
#68720=CARTESIAN_POINT('Ctrl Pts',(29.0669039974813,-0.730676428244075,
21.9269392883002));
#68721=CARTESIAN_POINT('Ctrl Pts',(29.2865672059309,-0.946735069741176,
21.9480883812055));
#68722=CARTESIAN_POINT('Ctrl Pts',(29.4177292577255,-1.03259356038437,21.9591867420451));
#68723=CARTESIAN_POINT('Ctrl Pts',(29.7004129009365,-1.14619538664958,21.98057329627));
#68724=CARTESIAN_POINT('Ctrl Pts',(29.8484560704769,-1.17497884076058,21.9906847639469));
#68725=CARTESIAN_POINT('Ctrl Pts',(29.9986381885534,-1.17523988185415,21.9999163533479));
#68726=CARTESIAN_POINT('Ctrl Pts',(29.9993191103818,-1.17524047358524,21.9999581881525));
#68727=CARTESIAN_POINT('Ctrl Pts',(30.0000000075681,-1.17524047358085,22.0000000004647));
#68728=CARTESIAN_POINT('Origin',(30.,-1.21864324187371E-14,15.78125));
#68729=CARTESIAN_POINT('',(30.,-1.17524047358085,22.5625));
#68730=CARTESIAN_POINT('',(29.9999999999999,-1.17524047358085,22.4999999999999));
#68731=CARTESIAN_POINT('',(30.,-1.17524047358085,15.78125));
#68732=CARTESIAN_POINT('Ctrl Pts',(30.,-1.17524047358085,22.5625));
#68733=CARTESIAN_POINT('Ctrl Pts',(29.9313687068489,-1.17524047358085,22.5582855119371));
#68734=CARTESIAN_POINT('Ctrl Pts',(29.8627268799626,-1.16923029327301,22.55385729367));
#68735=CARTESIAN_POINT('Ctrl Pts',(29.6405360439417,-1.12983827415446,22.5388164770024));
#68736=CARTESIAN_POINT('Ctrl Pts',(29.4932720438495,-1.07189657475161,22.5277190875488));
#68737=CARTESIAN_POINT('Ctrl Pts',(29.2351505504649,-0.904940984815958,
22.505949247503));
#68738=CARTESIAN_POINT('Ctrl Pts',(29.125477326134,-0.799463570556349,22.4954749014128));
#68739=CARTESIAN_POINT('Ctrl Pts',(28.9500348086396,-0.550024618450246,
22.4758578415198));
#68740=CARTESIAN_POINT('Ctrl Pts',(28.8870166724079,-0.407722193677489,
22.4664105508506));
#68741=CARTESIAN_POINT('Ctrl Pts',(28.8193863135494,-0.106256134735224,
22.4450343541119));
#68742=CARTESIAN_POINT('Ctrl Pts',(28.8156683957017,0.0499559751614321,
22.4339577479897));
#68743=CARTESIAN_POINT('Ctrl Pts',(28.8680054797788,0.349324836623415,22.4127302582268));
#68744=CARTESIAN_POINT('Ctrl Pts',(28.9214162690158,0.489956671932254,22.4030291896045));
#68745=CARTESIAN_POINT('Ctrl Pts',(29.0814696037689,0.749536525817022,22.3839976107609));
#68746=CARTESIAN_POINT('Ctrl Pts',(29.1888834831425,0.864620134172483,22.3733214303097));
#68747=CARTESIAN_POINT('Ctrl Pts',(29.4398862783311,1.04443640573476,22.3515327737366));
#68748=CARTESIAN_POINT('Ctrl Pts',(29.5804046735503,1.10838743829029,22.3406365628695));
#68749=CARTESIAN_POINT('Ctrl Pts',(29.874773559948,1.17808176091705,22.320089130129));
#68750=CARTESIAN_POINT('Ctrl Pts',(30.0254999210416,1.18444262102585,22.3112603596819));
#68751=CARTESIAN_POINT('Ctrl Pts',(30.3288317944626,1.13918974891494,22.2910290715165));
#68752=CARTESIAN_POINT('Ctrl Pts',(30.4780087858284,1.08506931516396,22.2799496878662));
#68753=CARTESIAN_POINT('Ctrl Pts',(30.7411182596149,0.924538989516088,22.2581013471772));
#68754=CARTESIAN_POINT('Ctrl Pts',(30.8537656083098,0.82166305580017,22.2475365992352));
#68755=CARTESIAN_POINT('Ctrl Pts',(31.0350106463268,0.577368135111118,22.2277455951917));
#68756=CARTESIAN_POINT('Ctrl Pts',(31.1013006049905,0.437889260334813,22.2185496213456));
#68757=CARTESIAN_POINT('Ctrl Pts',(31.1772437890897,0.139172903087767,22.1973683990083));
#68758=CARTESIAN_POINT('Ctrl Pts',(31.185313349087,-0.0173128950364053,
22.1862723863453));
#68759=CARTESIAN_POINT('Ctrl Pts',(31.1410279217834,-0.318736522964712,
22.1648991982826));
#68760=CARTESIAN_POINT('Ctrl Pts',(31.0912903592309,-0.461049327500964,
22.1548343474741));
#68761=CARTESIAN_POINT('Ctrl Pts',(30.9380306919572,-0.724977765907907,
22.136065778375));
#68762=CARTESIAN_POINT('Ctrl Pts',(30.8337205687989,-0.842838844072579,
22.1254817206889));
#68763=CARTESIAN_POINT('Ctrl Pts',(30.5872857957992,-1.02946130111843,22.1037322710222));
#68764=CARTESIAN_POINT('Ctrl Pts',(30.4481174203718,-1.09722011431045,22.0927839616769));
#68765=CARTESIAN_POINT('Ctrl Pts',(30.2017882631029,-1.16222172164091,22.0753529112466));
#68766=CARTESIAN_POINT('Ctrl Pts',(30.1010204315162,-1.17524047358085,22.0687034297066));
#68767=CARTESIAN_POINT('Ctrl Pts',(29.9999999999997,-1.17524047358085,22.0625));
#68768=CARTESIAN_POINT('Ctrl Pts',(30.0000000075681,-1.17524047358085,22.0000000004647));
#68769=CARTESIAN_POINT('Ctrl Pts',(30.1550617076756,-1.17524047258231,22.0095219788006));
#68770=CARTESIAN_POINT('Ctrl Pts',(30.3087125624576,-1.14455036320512,22.020045399438));
#68771=CARTESIAN_POINT('Ctrl Pts',(30.5936146237504,-1.02583437646268,22.0417494976575));
#68772=CARTESIAN_POINT('Ctrl Pts',(30.7222919834293,-0.9396884903777,22.0527054685765));
#68773=CARTESIAN_POINT('Ctrl Pts',(30.9363028934711,-0.725796874489648,
22.0734306378289));
#68774=CARTESIAN_POINT('Ctrl Pts',(31.0207456221836,-0.60126080890756,22.0823661148205));
#68775=CARTESIAN_POINT('Ctrl Pts',(31.1412832329984,-0.320931550152795,
22.1022435544492));
#68776=CARTESIAN_POINT('Ctrl Pts',(31.1737467539974,-0.166807893544759,
22.1131720736242));
#68777=CARTESIAN_POINT('Ctrl Pts',(31.1765934878998,0.140728845238564,22.1349787269359));
#68778=CARTESIAN_POINT('Ctrl Pts',(31.148646481366,0.291209583454888,22.1456489359696));
#68779=CARTESIAN_POINT('Ctrl Pts',(31.0370532707971,0.573358102978206,22.165655374784));
#68780=CARTESIAN_POINT('Ctrl Pts',(30.9544609034821,0.702301510156061,22.1746213225474));
#68781=CARTESIAN_POINT('Ctrl Pts',(30.7420042686145,0.924591934894812,22.1955488165371));
#68782=CARTESIAN_POINT('Ctrl Pts',(30.6131073712558,1.01465868002552,22.2066572778597));
#68783=CARTESIAN_POINT('Ctrl Pts',(30.3331026676289,1.1369643062698,22.228187906872));
#68784=CARTESIAN_POINT('Ctrl Pts',(30.1855325771707,1.17014774287538,22.2384263196851));
#68785=CARTESIAN_POINT('Ctrl Pts',(29.8783465649041,1.17947691083341,22.2576206519922));
#68786=CARTESIAN_POINT('Ctrl Pts',(29.7215875906434,1.15260328305267,22.2678992314176));
#68787=CARTESIAN_POINT('Ctrl Pts',(29.4314038660401,1.03996407151785,22.2897122199048));
#68788=CARTESIAN_POINT('Ctrl Pts',(29.3003745517226,0.9567417174806,22.3007089687507));
#68789=CARTESIAN_POINT('Ctrl Pts',(29.0812311411824,0.747835374300097,22.3215725663721));
#68790=CARTESIAN_POINT('Ctrl Pts',(28.9939461402353,0.625488946274541,22.3306481587999));
#68791=CARTESIAN_POINT('Ctrl Pts',(28.866779072646,0.34832483100282,22.3503011660994));
#68792=CARTESIAN_POINT('Ctrl Pts',(28.8306169080572,0.195045951299282,22.3611697842779));
#68793=CARTESIAN_POINT('Ctrl Pts',(28.8203429359976,-0.112665031360941,
22.3829887927828));
#68794=CARTESIAN_POINT('Ctrl Pts',(28.844778193878,-0.264121048518041,22.3937281563827));
#68795=CARTESIAN_POINT('Ctrl Pts',(28.9496447173484,-0.548400594969454,
22.4138857009336));
#68796=CARTESIAN_POINT('Ctrl Pts',(29.0286885091485,-0.678634752036216,
22.4227474921567));
#68797=CARTESIAN_POINT('Ctrl Pts',(29.2352313232766,-0.905919594975383,
22.4434889029608));
#68798=CARTESIAN_POINT('Ctrl Pts',(29.3621859947411,-0.999372204838993,
22.454598138267));
#68799=CARTESIAN_POINT('Ctrl Pts',(29.6398139077013,-1.12872343697434,22.4762326071516));
#68800=CARTESIAN_POINT('Ctrl Pts',(29.7869023742936,-1.1654876328242,22.4865683958599));
#68801=CARTESIAN_POINT('Ctrl Pts',(29.9579757834663,-1.17467745886044,22.4973994296432));
#68802=CARTESIAN_POINT('Ctrl Pts',(29.9789969929607,-1.17524047358085,22.4987102541947));
#68803=CARTESIAN_POINT('Ctrl Pts',(29.9999999999997,-1.17524047358085,22.4999999999999));
#68804=CARTESIAN_POINT('Origin',(30.,-1.21864324187371E-14,15.78125));
#68805=CARTESIAN_POINT('',(30.,-1.17524047358085,23.0625));
#68806=CARTESIAN_POINT('',(29.9999999999997,-1.17524047358085,22.9999999999999));
#68807=CARTESIAN_POINT('',(30.,-1.17524047358085,15.78125));
#68808=CARTESIAN_POINT('Ctrl Pts',(30.0000000000001,-1.17524047358085,23.0625));
#68809=CARTESIAN_POINT('Ctrl Pts',(29.9105144759955,-1.17524047358086,23.0570049021313));
#68810=CARTESIAN_POINT('Ctrl Pts',(29.8211453329131,-1.16502438899623,23.0511547525684));
#68811=CARTESIAN_POINT('Ctrl Pts',(29.5817638222111,-1.10931034878277,23.0344796199141));
#68812=CARTESIAN_POINT('Ctrl Pts',(29.4384864599594,-1.04411918186912,23.0233700199021));
#68813=CARTESIAN_POINT('Ctrl Pts',(29.1904963016638,-0.865097093142698,
23.001794519102));
#68814=CARTESIAN_POINT('Ctrl Pts',(29.0867727283959,-0.754802905276228,
22.9915147546188));
#68815=CARTESIAN_POINT('Ctrl Pts',(28.9228010666229,-0.495400927229172,
22.9722488667908));
#68816=CARTESIAN_POINT('Ctrl Pts',(28.8663568012591,-0.347374707529959,
22.9621314630453));
#68817=CARTESIAN_POINT('Ctrl Pts',(28.8154245654916,-0.0407388679671123,
22.9403886902216));
#68818=CARTESIAN_POINT('Ctrl Pts',(28.820274444704,0.114581560721945,22.9293753109615));
#68819=CARTESIAN_POINT('Ctrl Pts',(28.8884563534747,0.409699470717337,22.9084492454292));
#68820=CARTESIAN_POINT('Ctrl Pts',(28.9492618301764,0.547097841052301,22.8992933904858));
#68821=CARTESIAN_POINT('Ctrl Pts',(29.1229462954904,0.797680554149997,22.8797437378863));
#68822=CARTESIAN_POINT('Ctrl Pts',(29.2364128570735,0.906879897838648,22.8689044954722));
#68823=CARTESIAN_POINT('Ctrl Pts',(29.4960880788397,1.07256979024568,22.8470841182882));
#68824=CARTESIAN_POINT('Ctrl Pts',(29.6390279331417,1.12873587584898,22.8363152167134));
#68825=CARTESIAN_POINT('Ctrl Pts',(29.9369514995214,1.18318311725145,22.8160900653519));
#68826=CARTESIAN_POINT('Ctrl Pts',(30.0889739777062,1.18151676550276,22.8072588330028));
#68827=CARTESIAN_POINT('Ctrl Pts',(30.3896701123462,1.11972025811827,22.7866028657307));
#68828=CARTESIAN_POINT('Ctrl Pts',(30.5349379950004,1.05803905954289,22.7754954739854));
#68829=CARTESIAN_POINT('Ctrl Pts',(30.7879462278465,0.88483838172195,22.7538182156715));
#68830=CARTESIAN_POINT('Ctrl Pts',(30.894602280459,0.776856295524231,22.7434403470977));
#68831=CARTESIAN_POINT('Ctrl Pts',(31.0642088755634,0.522314474535101,22.7240007418519));
#68832=CARTESIAN_POINT('Ctrl Pts',(31.1239021773863,0.377122301428262,22.7142407897863));
#68833=CARTESIAN_POINT('Ctrl Pts',(31.1830807507881,0.07297978420699,22.6926748121518));
#68834=CARTESIAN_POINT('Ctrl Pts',(31.1824316194307,-0.0828368341019099,
22.681626249339));
#68835=CARTESIAN_POINT('Ctrl Pts',(31.1220212984731,-0.380073436416841,
22.6605499526862));
#68836=CARTESIAN_POINT('Ctrl Pts',(31.0648726782981,-0.5190454232441,22.6511559208149));
#68837=CARTESIAN_POINT('Ctrl Pts',(30.897916936256,-0.774116322820778,22.6318603404761));
#68838=CARTESIAN_POINT('Ctrl Pts',(30.7874073117601,-0.886271721025917,
22.6210978735108));
#68839=CARTESIAN_POINT('Ctrl Pts',(30.5319280571356,-1.05901132752472,22.5992852221989));
#68840=CARTESIAN_POINT('Ctrl Pts',(30.390134598554,-1.11904322637321,22.5884496605924));
#68841=CARTESIAN_POINT('Ctrl Pts',(30.1614293865023,-1.16692310230727,22.5727078850032));
#68842=CARTESIAN_POINT('Ctrl Pts',(30.0807402688424,-1.17524047358085,22.5674580720923));
#68843=CARTESIAN_POINT('Ctrl Pts',(30.,-1.17524047358085,22.5625));
#68844=CARTESIAN_POINT('Ctrl Pts',(29.9999999999997,-1.17524047358085,22.4999999999999));
#68845=CARTESIAN_POINT('Ctrl Pts',(30.1346907701741,-1.17524047358085,22.5082710468799));
#68846=CARTESIAN_POINT('Ctrl Pts',(30.2685335864829,-1.15209385827977,22.5173106568969));
#68847=CARTESIAN_POINT('Ctrl Pts',(30.5408486178537,-1.05471955701661,22.5374851723845));
#68848=CARTESIAN_POINT('Ctrl Pts',(30.6743758210798,-0.974766233245233,
22.5485194114384));
#68849=CARTESIAN_POINT('Ctrl Pts',(30.8991023951896,-0.771359157149707,
22.5695308885782));
#68850=CARTESIAN_POINT('Ctrl Pts',(30.9894938192057,-0.651353133995038,
22.5788141945814));
#68851=CARTESIAN_POINT('Ctrl Pts',(31.1237789969096,-0.377670022359416,
22.598220372706));
#68852=CARTESIAN_POINT('Ctrl Pts',(31.1639088895479,-0.225405854113982,
22.6090170402582));
#68853=CARTESIAN_POINT('Ctrl Pts',(31.1822136536976,0.0822897394418652,
22.6308349575606));
#68854=CARTESIAN_POINT('Ctrl Pts',(31.1616041653703,0.234707632570292,22.6416425253559));
#68855=CARTESIAN_POINT('Ctrl Pts',(31.0639996311159,0.521237294982461,22.6619596199458));
#68856=CARTESIAN_POINT('Ctrl Pts',(30.9887089758802,0.652868889710107,22.6707656569643));
#68857=CARTESIAN_POINT('Ctrl Pts',(30.7885136410845,0.885402585167096,22.6913033752648));
#68858=CARTESIAN_POINT('Ctrl Pts',(30.6637241461389,0.982420191755087,22.7024060445739));
#68859=CARTESIAN_POINT('Ctrl Pts',(30.38882091141,1.11923262290395,22.724137724694));
#68860=CARTESIAN_POINT('Ctrl Pts',(30.2423409189137,1.15980775171446,22.7345712602384));
#68861=CARTESIAN_POINT('Ctrl Pts',(29.9379463484727,1.1837522744206,22.75411234554));
#68862=CARTESIAN_POINT('Ctrl Pts',(29.7828414350779,1.1653244529442,22.7636867623073));
#68863=CARTESIAN_POINT('Ctrl Pts',(29.4887538037787,1.06944336967731,22.7851453423512));
#68864=CARTESIAN_POINT('Ctrl Pts',(29.3526850446683,0.993007607592932,22.7962109417328));
#68865=CARTESIAN_POINT('Ctrl Pts',(29.1221162292212,0.795444169323972,22.8173739985243));
#68866=CARTESIAN_POINT('Ctrl Pts',(29.0284526004007,0.677845266859518,22.8269357043589));
#68867=CARTESIAN_POINT('Ctrl Pts',(28.8868197290406,0.407843425299078,22.8460808529214));
#68868=CARTESIAN_POINT('Ctrl Pts',(28.8426042638403,0.256743916657897,22.8567949374029));
#68869=CARTESIAN_POINT('Ctrl Pts',(28.8159600292804,-0.0507119050410385,
22.8785958530886));
#68870=CARTESIAN_POINT('Ctrl Pts',(28.8325649861531,-0.204026768591548,
22.8894670227908));
#68871=CARTESIAN_POINT('Ctrl Pts',(28.9226310063267,-0.492841082076786,
22.9099461162173));
#68872=CARTESIAN_POINT('Ctrl Pts',(28.994102015515,-0.625925698199416,22.918754883105));
#68873=CARTESIAN_POINT('Ctrl Pts',(29.1877542901984,-0.863760919482141,
22.9390787662067));
#68874=CARTESIAN_POINT('Ctrl Pts',(29.3102272892874,-0.964377961033194,
22.9501667983144));
#68875=CARTESIAN_POINT('Ctrl Pts',(29.5821386201159,-1.10877008329771,22.9719834809511));
#68876=CARTESIAN_POINT('Ctrl Pts',(29.7278943046296,-1.1532370774207,22.9825105195965));
#68877=CARTESIAN_POINT('Ctrl Pts',(29.9186700556686,-1.17313232338821,22.9949309755051));
#68878=CARTESIAN_POINT('Ctrl Pts',(29.9593567068785,-1.17524047358085,22.9975041899134));
#68879=CARTESIAN_POINT('Ctrl Pts',(29.9999999999995,-1.17524047358085,22.9999999999999));
#68880=CARTESIAN_POINT('Origin',(30.,-1.21864324187371E-14,15.78125));
#68881=CARTESIAN_POINT('',(30.0000000000003,-1.17524047358085,23.5625));
#68882=CARTESIAN_POINT('',(30.,-1.17524047358085,23.5));
#68883=CARTESIAN_POINT('',(30.,-1.17524047358085,15.78125));
#68884=CARTESIAN_POINT('Ctrl Pts',(30.0000000000005,-1.17524047358085,23.5625));
#68885=CARTESIAN_POINT('Ctrl Pts',(29.8877180837681,-1.1752404735809,23.5556050287134));
#68886=CARTESIAN_POINT('Ctrl Pts',(29.7758372881673,-1.15915740880452,23.548164484563));
#68887=CARTESIAN_POINT('Ctrl Pts',(29.5190446425994,-1.08346545175016,23.5297118828087));
#68888=CARTESIAN_POINT('Ctrl Pts',(29.3805019669677,-1.01066023747548,23.5186230824555));
#68889=CARTESIAN_POINT('Ctrl Pts',(29.1440648218203,-0.81906365611398,23.4973112125635));
#68890=CARTESIAN_POINT('Ctrl Pts',(29.0470865676084,-0.703844960553528,
23.4874078682461));
#68891=CARTESIAN_POINT('Ctrl Pts',(28.8981724330839,-0.43757763652763,23.4685275248886));
#68892=CARTESIAN_POINT('Ctrl Pts',(28.8499251562346,-0.287749538271772,
23.4579035929059));
#68893=CARTESIAN_POINT('Ctrl Pts',(28.8149793372208,0.0192409990811535,
23.4361356693579));
#68894=CARTESIAN_POINT('Ctrl Pts',(28.8275655785823,0.173345465604893,23.4252085109033));
#68895=CARTESIAN_POINT('Ctrl Pts',(28.9101166290744,0.46437979734691,23.4045720015899));
#68896=CARTESIAN_POINT('Ctrl Pts',(28.9778580847147,0.598927911512345,23.3956997913279));
#68897=CARTESIAN_POINT('Ctrl Pts',(29.1650362747697,0.841899704480849,23.3755913560416));
#68898=CARTESIAN_POINT('Ctrl Pts',(29.2851376881026,0.945999066866448,23.3645254962114));
#68899=CARTESIAN_POINT('Ctrl Pts',(29.5539135664443,1.09777062977422,23.3426397256705));
#68900=CARTESIAN_POINT('Ctrl Pts',(29.6988585362439,1.14604691671332,23.3320274174642));
#68901=CARTESIAN_POINT('Ctrl Pts',(30.0001600354305,1.18508412542801,23.3121411783529));
#68902=CARTESIAN_POINT('Ctrl Pts',(30.1536625413848,1.17508243739145,23.3030583378086));
#68903=CARTESIAN_POINT('Ctrl Pts',(30.4512625228178,1.09622449574564,23.2819876064994));
#68904=CARTESIAN_POINT('Ctrl Pts',(30.592110439614,1.02700793469459,23.2708844778163));
#68905=CARTESIAN_POINT('Ctrl Pts',(30.8340714315268,0.841360319080231,23.2494443144111));
#68906=CARTESIAN_POINT('Ctrl Pts',(30.9343059293982,0.728463261371192,23.2392865244689));
#68907=CARTESIAN_POINT('Ctrl Pts',(31.0901832738534,0.465790392750319,23.2204017245443));
#68908=CARTESIAN_POINT('Ctrl Pts',(31.1423055420081,0.317257314781848,23.2099959148018));
#68909=CARTESIAN_POINT('Ctrl Pts',(31.1851773743111,0.010751647338072,23.1882623721543));
#68910=CARTESIAN_POINT('Ctrl Pts',(31.1764469607209,-0.144008319910697,
23.1772887337992));
#68911=CARTESIAN_POINT('Ctrl Pts',(31.1010701340243,-0.437108167734962,
23.1565057639579));
#68912=CARTESIAN_POINT('Ctrl Pts',(31.0368218842674,-0.573070176242618,
23.1475180074206));
#68913=CARTESIAN_POINT('Ctrl Pts',(30.8568360573785,-0.819362332337596,
23.1277335191445));
#68914=CARTESIAN_POINT('Ctrl Pts',(30.7406590361852,-0.925703986430565,
23.1168291494862));
#68915=CARTESIAN_POINT('Ctrl Pts',(30.477211273408,-1.08466164141258,23.0950157923094));
#68916=CARTESIAN_POINT('Ctrl Pts',(30.3332866239118,-1.13717003604433,23.0843160955662));
#68917=CARTESIAN_POINT('Ctrl Pts',(30.1225555529996,-1.17045159552602,23.0701956350453));
#68918=CARTESIAN_POINT('Ctrl Pts',(30.0612610274847,-1.17524047358085,23.066261897193));
#68919=CARTESIAN_POINT('Ctrl Pts',(30.0000000000001,-1.17524047358085,23.0625));
#68920=CARTESIAN_POINT('Ctrl Pts',(29.9999999999995,-1.17524047358085,22.9999999999999));
#68921=CARTESIAN_POINT('Ctrl Pts',(30.1122819160637,-1.17524047358085,23.0068949712763));
#68922=CARTESIAN_POINT('Ctrl Pts',(30.2241627114991,-1.15915740885253,23.0143355154149));
#68923=CARTESIAN_POINT('Ctrl Pts',(30.4809553569443,-1.08346545195345,23.0327881171562));
#68924=CARTESIAN_POINT('Ctrl Pts',(30.6194980326123,-1.01066023773368,23.0438769175097));
#68925=CARTESIAN_POINT('Ctrl Pts',(30.8559351778473,-0.819063656461988,
23.0651887874038));
#68926=CARTESIAN_POINT('Ctrl Pts',(30.952913432109,-0.703844960936813,23.0750921317269));
#68927=CARTESIAN_POINT('Ctrl Pts',(31.1018275667414,-0.437577636966923,
23.0939724750804));
#68928=CARTESIAN_POINT('Ctrl Pts',(31.1500748436503,-0.287749538730812,
23.1045964070617));
#68929=CARTESIAN_POINT('Ctrl Pts',(31.1850206627874,0.0192409986134863,
23.126364330609));
#68930=CARTESIAN_POINT('Ctrl Pts',(31.1724344214858,0.173345465148191,23.1372914890643));
#68931=CARTESIAN_POINT('Ctrl Pts',(31.0898833711054,0.464379796922714,23.15792799838));
#68932=CARTESIAN_POINT('Ctrl Pts',(31.0221419155201,0.598927911110121,23.1668002086434));
#68933=CARTESIAN_POINT('Ctrl Pts',(30.8349637255609,0.841899704153978,23.1869086439265));
#68934=CARTESIAN_POINT('Ctrl Pts',(30.7148623122637,0.945999066590532,23.1979745037564));
#68935=CARTESIAN_POINT('Ctrl Pts',(30.4460864339697,1.09777062960664,23.2198602742982));
#68936=CARTESIAN_POINT('Ctrl Pts',(30.3011414641827,1.1460469166018,23.2304725825058));
#68937=CARTESIAN_POINT('Ctrl Pts',(29.9998399650194,1.18508412542607,23.2503588216195));
#68938=CARTESIAN_POINT('Ctrl Pts',(29.8463374590763,1.17508243744973,23.2594416621611));
#68939=CARTESIAN_POINT('Ctrl Pts',(29.5487374776195,1.09622449592641,23.2805123934674));
#68940=CARTESIAN_POINT('Ctrl Pts',(29.4078895607902,1.02700793492841,23.2916155221506));
#68941=CARTESIAN_POINT('Ctrl Pts',(29.1659285687959,0.841360319401014,23.3130556855578));
#68942=CARTESIAN_POINT('Ctrl Pts',(29.0656940708777,0.72846326172594,23.3232134755017));
#68943=CARTESIAN_POINT('Ctrl Pts',(28.9098167263205,0.465790393157422,23.3420982754308));
#68944=CARTESIAN_POINT('Ctrl Pts',(28.8576944581104,0.317257315207477,23.3525040851682));
#68945=CARTESIAN_POINT('Ctrl Pts',(28.8148226256923,0.0107516477743395,
23.3742376278149));
#68946=CARTESIAN_POINT('Ctrl Pts',(28.8235530392262,-0.144008319483296,
23.3852112661707));
#68947=CARTESIAN_POINT('Ctrl Pts',(28.8989298658185,-0.437108167337535,
23.4059942360141));
#68948=CARTESIAN_POINT('Ctrl Pts',(28.9631781155251,-0.573070175865714,
23.4149819925535));
#68949=CARTESIAN_POINT('Ctrl Pts',(29.1431639423218,-0.819362332023802,
23.4347664808262));
#68950=CARTESIAN_POINT('Ctrl Pts',(29.2593409634759,-0.925703986159073,
23.4456708504836));
#68951=CARTESIAN_POINT('Ctrl Pts',(29.5227887261992,-1.08466164124026,23.4674842076606));
#68952=CARTESIAN_POINT('Ctrl Pts',(29.6667133756817,-1.13717003592563,23.4781839044047));
#68953=CARTESIAN_POINT('Ctrl Pts',(29.8774444467245,-1.17045159550418,23.4923043649371));
#68954=CARTESIAN_POINT('Ctrl Pts',(29.9387389723772,-1.17524047358085,23.4962381027985));
#68955=CARTESIAN_POINT('Ctrl Pts',(29.9999999999999,-1.17524047358085,23.5));
#68956=CARTESIAN_POINT('Origin',(30.,-1.21864324187371E-14,15.78125));
#68957=CARTESIAN_POINT('',(30.0000000000001,-1.17524047358085,24.0625));
#68958=CARTESIAN_POINT('',(30.,-1.17524047358085,24.));
#68959=CARTESIAN_POINT('',(30.,-1.17524047358085,15.78125));
#68960=CARTESIAN_POINT('Ctrl Pts',(30.0000000000002,-1.17524047358085,24.0625));
#68961=CARTESIAN_POINT('Ctrl Pts',(29.8653092296601,-1.17524047358088,24.0542289531099));
#68962=CARTESIAN_POINT('Ctrl Pts',(29.7314664131893,-1.15209385822287,24.045189343081));
#68963=CARTESIAN_POINT('Ctrl Pts',(29.4591513817099,-1.05471955679206,24.0250148275808));
#68964=CARTESIAN_POINT('Ctrl Pts',(29.3256241785221,-0.974766232969058,
24.0139805885274));
#68965=CARTESIAN_POINT('Ctrl Pts',(29.1008976044993,-0.771359156787199,
23.99296911139));
#68966=CARTESIAN_POINT('Ctrl Pts',(29.0105061805318,-0.651353133596405,
23.9836858053905));
#68967=CARTESIAN_POINT('Ctrl Pts',(28.876221002938,-0.377670021906335,23.9642796272619));
#68968=CARTESIAN_POINT('Ctrl Pts',(28.8360911103609,-0.225405853644338,
23.9534829597086));
#68969=CARTESIAN_POINT('Ctrl Pts',(28.8177863463358,0.0822897399134218,
23.931665042406));
#68970=CARTESIAN_POINT('Ctrl Pts',(28.8383958347227,0.234707633027682,23.9208574746117));
#68971=CARTESIAN_POINT('Ctrl Pts',(28.9360003690899,0.521237295405437,23.9005403800242));
#68972=CARTESIAN_POINT('Ctrl Pts',(29.0112910243832,0.652868890111379,23.8917343430053));
#68973=CARTESIAN_POINT('Ctrl Pts',(29.211486359277,0.885402585487968,23.8711966247017));
#68974=CARTESIAN_POINT('Ctrl Pts',(29.3362758542566,0.98242019202142,23.8600939553924));
#68975=CARTESIAN_POINT('Ctrl Pts',(29.611179089029,1.11923262305578,23.8383622752737));
#68976=CARTESIAN_POINT('Ctrl Pts',(29.7576590815354,1.15980775180767,23.8279287397307));
#68977=CARTESIAN_POINT('Ctrl Pts',(30.0620536519992,1.1837522743985,23.8083876544318));
#68978=CARTESIAN_POINT('Ctrl Pts',(30.2171585654068,1.16532445285658,23.7988132376599));
#68979=CARTESIAN_POINT('Ctrl Pts',(30.5112461966771,1.06944336945855,23.7773546576131));
#68980=CARTESIAN_POINT('Ctrl Pts',(30.6473149557494,0.993007607319778,23.7662890582319));
#68981=CARTESIAN_POINT('Ctrl Pts',(30.8778837711073,0.795444168961031,23.7451260014428));
#68982=CARTESIAN_POINT('Ctrl Pts',(30.9715473998777,0.67784526646015,23.735564295613));
#68983=CARTESIAN_POINT('Ctrl Pts',(31.1131802711266,0.407843424843195,23.7164191470464));
#68984=CARTESIAN_POINT('Ctrl Pts',(31.1573957362652,0.25674391618342,23.7057050625635));
#68985=CARTESIAN_POINT('Ctrl Pts',(31.1840399706984,-0.0507119055208601,
23.6839041468775));
#68986=CARTESIAN_POINT('Ctrl Pts',(31.1674350137646,-0.204026769058537,
23.6730329771762));
#68987=CARTESIAN_POINT('Ctrl Pts',(31.0773689934766,-0.492841082509219,
23.6525538837521));
#68988=CARTESIAN_POINT('Ctrl Pts',(31.0058979842309,-0.625925698609867,
23.643745116865));
#68989=CARTESIAN_POINT('Ctrl Pts',(30.8122457094484,-0.863760919813326,
23.62342123376));
#68990=CARTESIAN_POINT('Ctrl Pts',(30.6897727103237,-0.964377961310509,
23.612333201652));
#68991=CARTESIAN_POINT('Ctrl Pts',(30.4178613794486,-1.10877008346121,23.5905165190165));
#68992=CARTESIAN_POINT('Ctrl Pts',(30.2721056949232,-1.15323707752562,23.5799894803724));
#68993=CARTESIAN_POINT('Ctrl Pts',(30.081329944032,-1.17313232340388,23.5675690244761));
#68994=CARTESIAN_POINT('Ctrl Pts',(30.0406432929718,-1.17524047358083,23.5649958100773));
#68995=CARTESIAN_POINT('Ctrl Pts',(30.0000000000005,-1.17524047358085,23.5625));
#68996=CARTESIAN_POINT('Ctrl Pts',(29.9999999999999,-1.17524047358085,23.5));
#68997=CARTESIAN_POINT('Ctrl Pts',(30.0894855238544,-1.17524047358085,23.5054950978594));
#68998=CARTESIAN_POINT('Ctrl Pts',(30.178854666788,-1.16502438903023,23.5113452474122));
#68999=CARTESIAN_POINT('Ctrl Pts',(30.4182361773703,-1.10931034894115,23.5280203800546));
#69000=CARTESIAN_POINT('Ctrl Pts',(30.5615135396518,-1.04411918207875,23.5391299800668));
#69001=CARTESIAN_POINT('Ctrl Pts',(30.8095036980223,-0.865097093436967,
23.5607054808684));
#69002=CARTESIAN_POINT('Ctrl Pts',(30.9132272713337,-0.75480290560396,23.5709852453531));
#69003=CARTESIAN_POINT('Ctrl Pts',(31.0771989331901,-0.495400927628404,
23.5902511331837));
#69004=CARTESIAN_POINT('Ctrl Pts',(31.1336431986023,-0.347374707971562,
23.6003685369235));
#69005=CARTESIAN_POINT('Ctrl Pts',(31.1845754344926,-0.0407388684447008,
23.6221113097446));
#69006=CARTESIAN_POINT('Ctrl Pts',(31.1797255553422,0.114581560252514,23.6331246890053));
#69007=CARTESIAN_POINT('Ctrl Pts',(31.1115436466863,0.409699470279596,23.6540507545398));
#69008=CARTESIAN_POINT('Ctrl Pts',(31.0507381700391,0.547097840637693,23.6632066094863));
#69009=CARTESIAN_POINT('Ctrl Pts',(30.877053704825,0.797680553802843,23.6827562620821));
#69010=CARTESIAN_POINT('Ctrl Pts',(30.7635871432854,0.906879897536129,23.6935955044951));
#69011=CARTESIAN_POINT('Ctrl Pts',(30.5039119215803,1.07256979004896,23.7154158816792));
#69012=CARTESIAN_POINT('Ctrl Pts',(30.3609720672946,1.12873587571,23.726184783255));
#69013=CARTESIAN_POINT('Ctrl Pts',(30.0630485009405,1.18318311722529,23.7464099346189));
#69014=CARTESIAN_POINT('Ctrl Pts',(29.9110260227659,1.18151676553675,23.755241166967));
#69015=CARTESIAN_POINT('Ctrl Pts',(29.6103298881048,1.1197202582759,23.7758971342361));
#69016=CARTESIAN_POINT('Ctrl Pts',(29.46506200542,1.05803905975613,23.7870045259814));
#69017=CARTESIAN_POINT('Ctrl Pts',(29.2120537724961,0.884838382027716,23.8086817842968));
#69018=CARTESIAN_POINT('Ctrl Pts',(29.1053977198379,0.776856295866943,23.8190596528721));
#69019=CARTESIAN_POINT('Ctrl Pts',(28.9357911246459,0.52231447495466,23.8384992581206));
#69020=CARTESIAN_POINT('Ctrl Pts',(28.8760978227722,0.377122301892393,23.8482592101808));
#69021=CARTESIAN_POINT('Ctrl Pts',(28.816919249242,0.0729797847098555,23.8698251878126));
#69022=CARTESIAN_POINT('Ctrl Pts',(28.8175683805337,-0.0828368336059415,
23.8808737506258));
#69023=CARTESIAN_POINT('Ctrl Pts',(28.8779787013698,-0.380073435953635,
23.9019500472809));
#69024=CARTESIAN_POINT('Ctrl Pts',(28.9351273214881,-0.519045422805617,
23.9113440791565));
#69025=CARTESIAN_POINT('Ctrl Pts',(29.1020830634255,-0.774116322451291,
23.9306396594913));
#69026=CARTESIAN_POINT('Ctrl Pts',(29.212592687875,-0.88627172070161,23.9414021264554));
#69027=CARTESIAN_POINT('Ctrl Pts',(29.4680719424329,-1.05901132730886,23.963214777767));
#69028=CARTESIAN_POINT('Ctrl Pts',(29.609865400996,-1.11904322621712,23.9740503393744));
#69029=CARTESIAN_POINT('Ctrl Pts',(29.8385706131875,-1.1669231022752,23.9897921149766));
#69030=CARTESIAN_POINT('Ctrl Pts',(29.9192597310019,-1.17524047358085,23.9950419278981));
#69031=CARTESIAN_POINT('Ctrl Pts',(30.,-1.17524047358085,24.));
#69032=CARTESIAN_POINT('Origin',(30.,-1.21864324187371E-14,15.78125));
#69033=CARTESIAN_POINT('',(29.9999999962159,-1.17524047358085,24.5624999995353));
#69034=CARTESIAN_POINT('',(30.0000000000002,-1.17524047358085,24.5));
#69035=CARTESIAN_POINT('',(30.,-1.17524047358085,15.78125));
#69036=CARTESIAN_POINT('Ctrl Pts',(29.9999999924319,-1.17524047358085,24.5624999995353));
#69037=CARTESIAN_POINT('Ctrl Pts',(29.8449382921852,-1.17524047258231,24.5529780211908));
#69038=CARTESIAN_POINT('Ctrl Pts',(29.6912874372683,-1.14455036315003,24.5424546005433));
#69039=CARTESIAN_POINT('Ctrl Pts',(29.4063853758944,-1.0258343762565,24.5207505023134));
#69040=CARTESIAN_POINT('Ctrl Pts',(29.2777080162496,-0.939688490130196,
24.5097945313951));
#69041=CARTESIAN_POINT('Ctrl Pts',(29.0636971062813,-0.72579687417109,24.4890693621447));
#69042=CARTESIAN_POINT('Ctrl Pts',(28.9792543776096,-0.601260808557374,
24.4801338851547));
#69043=CARTESIAN_POINT('Ctrl Pts',(28.8587167668904,-0.3209315497576,24.4602564455228));
#69044=CARTESIAN_POINT('Ctrl Pts',(28.8262532459446,-0.166807893138082,
24.449327926347));
#69045=CARTESIAN_POINT('Ctrl Pts',(28.823406512149,0.140728845641508,24.4275212730356));
#69046=CARTESIAN_POINT('Ctrl Pts',(28.851353518733,0.291209583843224,24.4168510640028));
#69047=CARTESIAN_POINT('Ctrl Pts',(28.9629467293987,0.573358103335639,24.3968446251906));
#69048=CARTESIAN_POINT('Ctrl Pts',(29.0455390967654,0.702301510494977,24.3878786774254));
#69049=CARTESIAN_POINT('Ctrl Pts',(29.2579957317181,0.924591935160839,24.3669511834331));
#69050=CARTESIAN_POINT('Ctrl Pts',(29.3868926291043,1.01465868024229,24.3558427221105));
#69051=CARTESIAN_POINT('Ctrl Pts',(29.6668973327643,1.13696430638437,24.3343120930999));
#69052=CARTESIAN_POINT('Ctrl Pts',(29.8144674232288,1.17014774293813,24.3240736802882));
#69053=CARTESIAN_POINT('Ctrl Pts',(30.1216534355145,1.17947691079308,24.3048793479835));
#69054=CARTESIAN_POINT('Ctrl Pts',(30.2784124097871,1.15260328295164,24.2946007685524));
#69055=CARTESIAN_POINT('Ctrl Pts',(30.5685961343608,1.03996407129779,24.2727877800628));
#69056=CARTESIAN_POINT('Ctrl Pts',(30.6996254486415,0.956741717213513,24.2617910312175));
#69057=CARTESIAN_POINT('Ctrl Pts',(30.9187688591,0.747835373953449,24.2409274335984));
#69058=CARTESIAN_POINT('Ctrl Pts',(31.006053860002,0.625488945893405,24.2318518411732));
#69059=CARTESIAN_POINT('Ctrl Pts',(31.1332209274868,0.348324830571042,24.2121988338701));
#69060=CARTESIAN_POINT('Ctrl Pts',(31.1693830920172,0.195045950853365,24.2013302156905));
#69061=CARTESIAN_POINT('Ctrl Pts',(31.1796570639592,-0.112665031805443,
24.1795112071857));
#69062=CARTESIAN_POINT('Ctrl Pts',(31.1552218060231,-0.264121048947789,
24.1687718435869));
#69063=CARTESIAN_POINT('Ctrl Pts',(31.0503552824464,-0.548400595365726,
24.1486142990383));
#69064=CARTESIAN_POINT('Ctrl Pts',(30.9713114905908,-0.678634752411996,
24.1397525078141));
#69065=CARTESIAN_POINT('Ctrl Pts',(30.7647686763693,-0.905919595273436,
24.119011097007));
#69066=CARTESIAN_POINT('Ctrl Pts',(30.6378140048735,-0.999372205084128,
24.1079018617007));
#69067=CARTESIAN_POINT('Ctrl Pts',(30.3601860918747,-1.12872343710904,24.0862673928177));
#69068=CARTESIAN_POINT('Ctrl Pts',(30.2130976252741,-1.16548763290266,24.0759316041108));
#69069=CARTESIAN_POINT('Ctrl Pts',(30.042024216247,-1.17467745886824,24.065100570339));
#69070=CARTESIAN_POINT('Ctrl Pts',(30.021003006896,-1.17524047358085,24.0637897457965));
#69071=CARTESIAN_POINT('Ctrl Pts',(30.0000000000002,-1.17524047358085,24.0625));
#69072=CARTESIAN_POINT('Ctrl Pts',(30.,-1.17524047358085,24.));
#69073=CARTESIAN_POINT('Ctrl Pts',(30.068631292987,-1.17524047358085,24.0042144880528));
#69074=CARTESIAN_POINT('Ctrl Pts',(30.1372731197099,-1.16923029330172,24.0086427063088));
#69075=CARTESIAN_POINT('Ctrl Pts',(30.3594639555913,-1.12983827430394,24.0236835229636));
#69076=CARTESIAN_POINT('Ctrl Pts',(30.5067279557135,-1.07189657495913,24.034780912417));
#69077=CARTESIAN_POINT('Ctrl Pts',(30.7648494491756,-0.904940985120749,
24.0565507524641));
#69078=CARTESIAN_POINT('Ctrl Pts',(30.8745226735525,-0.799463570900332,
24.0670250985558));
#69079=CARTESIAN_POINT('Ctrl Pts',(31.0499651911362,-0.550024618872908,
24.0866421584515));
#69080=CARTESIAN_POINT('Ctrl Pts',(31.1129833274185,-0.407722194144101,
24.0960894491163));
#69081=CARTESIAN_POINT('Ctrl Pts',(31.1806136864057,-0.106256135243321,
24.117465645852));
#69082=CARTESIAN_POINT('Ctrl Pts',(31.1843316043204,0.0499559746584703,
24.1285422519746));
#69083=CARTESIAN_POINT('Ctrl Pts',(31.131994520367,0.349324836152535,24.1497697417397));
#69084=CARTESIAN_POINT('Ctrl Pts',(31.0785837311869,0.489956671487056,24.1594708103671));
#69085=CARTESIAN_POINT('Ctrl Pts',(30.9185303965388,0.749536525439823,24.1785023892068));
#69086=CARTESIAN_POINT('Ctrl Pts',(30.8111165172128,0.864620133839068,24.1891785696567));
#69087=CARTESIAN_POINT('Ctrl Pts',(30.5601137220937,1.04443640550787,24.2109672262292));
#69088=CARTESIAN_POINT('Ctrl Pts',(30.4195953268947,1.10838743812269,24.2218634370972));
#69089=CARTESIAN_POINT('Ctrl Pts',(30.125226440525,1.17808176086598,24.2424108698401));
#69090=CARTESIAN_POINT('Ctrl Pts',(29.9745000794406,1.18444262103543,24.2512396402881));
#69091=CARTESIAN_POINT('Ctrl Pts',(29.671168206001,1.13918974904968,24.2714709284502));
#69092=CARTESIAN_POINT('Ctrl Pts',(29.5219912146071,1.08506931535676,24.2825503121002));
#69093=CARTESIAN_POINT('Ctrl Pts',(29.2588817407465,0.924538989806815,24.3043986527903));
#69094=CARTESIAN_POINT('Ctrl Pts',(29.1462343920073,0.821663056130735,24.3149634007337));
#69095=CARTESIAN_POINT('Ctrl Pts',(28.9649893539032,0.577368135519195,24.3347544047798));
#69096=CARTESIAN_POINT('Ctrl Pts',(28.8986993951907,0.437889260784583,24.3439503786226));
#69097=CARTESIAN_POINT('Ctrl Pts',(28.8227562109677,0.139172903579825,24.3651316009568));
#69098=CARTESIAN_POINT('Ctrl Pts',(28.814686650905,-0.0173128945475468,
24.3762276136201));
#69099=CARTESIAN_POINT('Ctrl Pts',(28.8589720780878,-0.318736522506238,
24.3976008016849));
#69100=CARTESIAN_POINT('Ctrl Pts',(28.9087096405855,-0.46104932706788,24.4076656524993));
#69101=CARTESIAN_POINT('Ctrl Pts',(29.0619693077579,-0.724977765539007,
24.4264342215945));
#69102=CARTESIAN_POINT('Ctrl Pts',(29.1662794308695,-0.84283884374432,24.4370182792792));
#69103=CARTESIAN_POINT('Ctrl Pts',(29.4127142037999,-1.0294613008905,24.4587677289451));
#69104=CARTESIAN_POINT('Ctrl Pts',(29.5518825792064,-1.09722011413893,24.4697160382912));
#69105=CARTESIAN_POINT('Ctrl Pts',(29.7982117366005,-1.1622217216024,24.4871470887339));
#69106=CARTESIAN_POINT('Ctrl Pts',(29.8989795683345,-1.17524047358088,24.4937965702842));
#69107=CARTESIAN_POINT('Ctrl Pts',(30.0000000000003,-1.17524047358085,24.5));
#69108=CARTESIAN_POINT('Origin',(30.,-1.21864324187371E-14,15.78125));
#69109=CARTESIAN_POINT('',(29.9999999999999,-1.17524047358085,25.0625));
#69110=CARTESIAN_POINT('',(30.0000000000002,-1.17524047358085,25.));
#69111=CARTESIAN_POINT('',(30.,-1.17524047358085,15.78125));
#69112=CARTESIAN_POINT('Ctrl Pts',(29.9999999999998,-1.17524047358085,25.0625));
#69113=CARTESIAN_POINT('Ctrl Pts',(29.9787160795735,-1.17524047358085,25.0611930039571));
#69114=CARTESIAN_POINT('Ctrl Pts',(29.9574135577721,-1.17466229796152,25.0598643671606));
#69115=CARTESIAN_POINT('Ctrl Pts',(29.7860545064693,-1.16533366685381,25.0490108716001));
#69116=CARTESIAN_POINT('Ctrl Pts',(29.638982260427,-1.12845915516134,25.0386721678491));
#69117=CARTESIAN_POINT('Ctrl Pts',(29.3614303849904,-0.998891400573746,
25.0170346917219));
#69118=CARTESIAN_POINT('Ctrl Pts',(29.2345369639167,-0.905335034780717,
25.0059255391243));
#69119=CARTESIAN_POINT('Ctrl Pts',(29.0281770961676,-0.677897334966365,
24.9851899432843));
#69120=CARTESIAN_POINT('Ctrl Pts',(28.9492422426318,-0.547623084588669,
24.9763305695037));
#69121=CARTESIAN_POINT('Ctrl Pts',(28.8429395559285,-0.25880932586385,24.9558515154165));
#69122=CARTESIAN_POINT('Ctrl Pts',(28.8187785161156,-0.102338490894112,
24.9447565638831));
#69123=CARTESIAN_POINT('Ctrl Pts',(28.8329707062525,0.20487723468326,24.9229726728069));
#69124=CARTESIAN_POINT('Ctrl Pts',(28.8688620223111,0.352813948215486,24.9124828541373));
#69125=CARTESIAN_POINT('Ctrl Pts',(28.9959383633127,0.629882762331914,24.8928366044019));
#69126=CARTESIAN_POINT('Ctrl Pts',(29.0869818629053,0.755846556300386,24.8834354015886));
#69127=CARTESIAN_POINT('Ctrl Pts',(29.3131553782924,0.966129203680405,24.8620913064548));
#69128=CARTESIAN_POINT('Ctrl Pts',(29.4462640631474,1.04811028996687,24.8510108758816));
#69129=CARTESIAN_POINT('Ctrl Pts',(29.731323759893,1.1538048728599,24.8297587550632));
#69130=CARTESIAN_POINT('Ctrl Pts',(29.8797531248391,1.17853792828451,24.8200009879783));
#69131=CARTESIAN_POINT('Ctrl Pts',(30.1846496308258,1.17107054148177,24.8010132560253));
#69132=CARTESIAN_POINT('Ctrl Pts',(30.3381730792388,1.13627251448872,24.7903520180859));
#69133=CARTESIAN_POINT('Ctrl Pts',(30.6200199170605,1.01003478142549,24.7685688600169));
#69134=CARTESIAN_POINT('Ctrl Pts',(30.7461080027782,0.920828764814659,24.7576633973259));
#69135=CARTESIAN_POINT('Ctrl Pts',(30.954589658464,0.701638656166971,24.7370899153526));
#69136=CARTESIAN_POINT('Ctrl Pts',(31.0359799147447,0.574699574292555,24.7282504951265));
#69137=CARTESIAN_POINT('Ctrl Pts',(31.1497275829798,0.289883112537678,24.7080548792676));
#69138=CARTESIAN_POINT('Ctrl Pts',(31.1781418190148,0.133683865658838,24.6969791852295));
#69139=CARTESIAN_POINT('Ctrl Pts',(31.1719905418774,-0.174601531099527,
24.6751194464719));
#69140=CARTESIAN_POINT('Ctrl Pts',(31.1398342436188,-0.323793762033814,
24.6645406022347));
#69141=CARTESIAN_POINT('Ctrl Pts',(31.020088030022,-0.603297917753395,24.644721668578));
#69142=CARTESIAN_POINT('Ctrl Pts',(30.9330960022514,-0.730676428588708,
24.6355607116713));
#69143=CARTESIAN_POINT('Ctrl Pts',(30.7134327937131,-0.946735070008641,
24.6144116187632));
#69144=CARTESIAN_POINT('Ctrl Pts',(30.5822707418913,-1.03259356059966,24.6033132579239));
#69145=CARTESIAN_POINT('Ctrl Pts',(30.299587098649,-1.14619538675731,24.5819267037008));
#69146=CARTESIAN_POINT('Ctrl Pts',(30.1515439291036,-1.17497884081411,24.5718152360255));
#69147=CARTESIAN_POINT('Ctrl Pts',(30.0013618111703,-1.17523988185447,24.5625836466351));
#69148=CARTESIAN_POINT('Ctrl Pts',(30.0006808894801,-1.17524047358524,24.5625418118389));
#69149=CARTESIAN_POINT('Ctrl Pts',(29.9999999924319,-1.17524047358085,24.5624999995353));
#69150=CARTESIAN_POINT('Ctrl Pts',(30.0000000000003,-1.17524047358085,24.5));
#69151=CARTESIAN_POINT('Ctrl Pts',(30.0475989786694,-1.17524047358084,24.5029229425557));
#69152=CARTESIAN_POINT('Ctrl Pts',(30.0952413712801,-1.17234913261358,24.5059510599029));
#69153=CARTESIAN_POINT('Ctrl Pts',(30.2990650070911,-1.14742109537484,24.5193511873216));
#69154=CARTESIAN_POINT('Ctrl Pts',(30.4499960157575,-1.0970416910395,24.5304056476212));
#69155=CARTESIAN_POINT('Ctrl Pts',(30.7177665488108,-0.942842462676014,
24.5523157520592));
#69156=CARTESIAN_POINT('Ctrl Pts',(30.833223349596,-0.842552715174129,24.5629613319529));
#69157=CARTESIAN_POINT('Ctrl Pts',(31.0200068112404,-0.603233885310555,
24.5829160166926));
#69158=CARTESIAN_POINT('Ctrl Pts',(31.0893943876237,-0.466400998056969,
24.591928683353));
#69159=CARTESIAN_POINT('Ctrl Pts',(31.1731872619397,-0.170385863873932,
24.612918368786));
#69160=CARTESIAN_POINT('Ctrl Pts',(31.185412882504,-0.0137497619841131,
24.6240250391094));
#69161=CARTESIAN_POINT('Ctrl Pts',(31.1488612218191,0.289356743431089,24.6455175557638));
#69162=CARTESIAN_POINT('Ctrl Pts',(31.1026857517696,0.433263084173784,24.6557215908795));
#69163=CARTESIAN_POINT('Ctrl Pts',(30.9558437041525,0.701308793163264,24.6747280350226));
#69164=CARTESIAN_POINT('Ctrl Pts',(30.8545058913013,0.821789237632239,24.6849956137961));
#69165=CARTESIAN_POINT('Ctrl Pts',(30.6123622815668,1.01480099766359,24.7067080777764));
#69166=CARTESIAN_POINT('Ctrl Pts',(30.4745499588497,1.08610079838188,24.7176986563197));
#69167=CARTESIAN_POINT('Ctrl Pts',(30.1837738406509,1.17031056558872,24.7385400922772));
#69168=CARTESIAN_POINT('Ctrl Pts',(30.0341022035471,1.18415559329136,24.7475897886987));
#69169=CARTESIAN_POINT('Ctrl Pts',(29.7305751526436,1.15452627151871,24.7672791490145));
#69170=CARTESIAN_POINT('Ctrl Pts',(29.5799242663497,1.10861951554252,24.7781578355522));
#69171=CARTESIAN_POINT('Ctrl Pts',(29.3089128663366,0.962634653740643,24.7999757240996));
#69172=CARTESIAN_POINT('Ctrl Pts',(29.1903801371545,0.865330006275208,24.8107043566494));
#69173=CARTESIAN_POINT('Ctrl Pts',(28.9974547059893,0.631606479932577,24.8308378310304));
#69174=CARTESIAN_POINT('Ctrl Pts',(28.9246531642855,0.497649505166107,24.8397129306474));
#69175=CARTESIAN_POINT('Ctrl Pts',(28.8322520407485,0.204711362593916,24.8604844343777));
#69176=CARTESIAN_POINT('Ctrl Pts',(28.8154219514347,0.0480344797090969,
24.8715939963785));
#69177=CARTESIAN_POINT('Ctrl Pts',(28.8433837526351,-0.256851307347509,
24.8932126773996));
#69178=CARTESIAN_POINT('Ctrl Pts',(28.8856263759144,-0.402401296034548,
24.9035332594392));
#69179=CARTESIAN_POINT('Ctrl Pts',(29.0254132564532,-0.675115053553108,
24.9228707031121));
#69180=CARTESIAN_POINT('Ctrl Pts',(29.1237053106631,-0.798585223889617,
24.932834945393));
#69181=CARTESIAN_POINT('Ctrl Pts',(29.3612206915393,-0.998444700238917,
24.9545059777387));
#69182=CARTESIAN_POINT('Ctrl Pts',(29.4974844913312,-1.07350395274647,24.9655347517064));
#69183=CARTESIAN_POINT('Ctrl Pts',(29.7595519260122,-1.15671325178265,24.9845777838555));
#69184=CARTESIAN_POINT('Ctrl Pts',(29.8794906495254,-1.17524047358089,24.9925998011151));
#69185=CARTESIAN_POINT('Ctrl Pts',(30.0000000000004,-1.17524047358085,25.));
#69186=CARTESIAN_POINT('Origin',(30.,-1.21864324187371E-14,15.78125));
#69187=CARTESIAN_POINT('',(29.9999999999997,-1.17524047358085,25.5625));
#69188=CARTESIAN_POINT('',(30.,-1.17524047358085,25.5));
#69189=CARTESIAN_POINT('',(30.,-1.17524047358085,15.78125));
#69190=CARTESIAN_POINT('Ctrl Pts',(29.9999999999995,-1.17524047358085,25.5625));
#69191=CARTESIAN_POINT('Ctrl Pts',(29.9590631434842,-1.17524047358085,25.5599861628683));
#69192=CARTESIAN_POINT('Ctrl Pts',(29.9180826982373,-1.17310176284205,25.557393823766));
#69193=CARTESIAN_POINT('Ctrl Pts',(29.7270170759755,-1.15303120939534,25.5449493522346));
#69194=CARTESIAN_POINT('Ctrl Pts',(29.5812843667667,-1.10844931412058,25.534419650774));
#69195=CARTESIAN_POINT('Ctrl Pts',(29.3094646041477,-0.963834030512161,
25.5126006792245));
#69196=CARTESIAN_POINT('Ctrl Pts',(29.1870616253517,-0.863111358786919,
25.5015132019157));
#69197=CARTESIAN_POINT('Ctrl Pts',(28.9936035835609,-0.625120486304078,
25.4811957277874));
#69198=CARTESIAN_POINT('Ctrl Pts',(28.922245153506,-0.491992360156719,25.4723859354899));
#69199=CARTESIAN_POINT('Ctrl Pts',(28.8324037582581,-0.203110856662721,
25.4519020777895));
#69200=CARTESIAN_POINT('Ctrl Pts',(28.8159185655927,-0.0497708721110285,
25.4410291268206));
#69201=CARTESIAN_POINT('Ctrl Pts',(28.8428111724951,0.257674311776114,25.4192289654353));
#69202=CARTESIAN_POINT('Ctrl Pts',(28.8871477746036,0.408737403201897,25.4085174632064));
#69203=CARTESIAN_POINT('Ctrl Pts',(29.028998912458,0.678628541452795,25.389380164336));
#69204=CARTESIAN_POINT('Ctrl Pts',(29.1227608288482,0.796156039557689,25.3798091767006));
#69205=CARTESIAN_POINT('Ctrl Pts',(29.3535044180399,0.99354320653279,25.3586416369362));
#69206=CARTESIAN_POINT('Ctrl Pts',(29.4896480206548,1.06987223772086,25.3475752255981));
#69207=CARTESIAN_POINT('Ctrl Pts',(29.7837920452496,1.16549604577304,25.326122303941));
#69208=CARTESIAN_POINT('Ctrl Pts',(29.9388720345248,1.18379547475176,25.3165570329261));
#69209=CARTESIAN_POINT('Ctrl Pts',(30.243221825482,1.15962478745302,25.2970106790485));
#69210=CARTESIAN_POINT('Ctrl Pts',(30.3896819125524,1.11893466510606,25.2865742888993));
#69211=CARTESIAN_POINT('Ctrl Pts',(30.664499787972,0.981897695245122,25.2648398897594));
#69212=CARTESIAN_POINT('Ctrl Pts',(30.7892223684277,0.884773136061606,25.2537375376443));
#69213=CARTESIAN_POINT('Ctrl Pts',(30.9892253393634,0.652081932327525,25.233206047704));
#69214=CARTESIAN_POINT('Ctrl Pts',(31.0644029101032,0.520407945827758,25.2244008128923));
#69215=CARTESIAN_POINT('Ctrl Pts',(31.1617865735135,0.233810524226684,25.2040789136694));
#69216=CARTESIAN_POINT('Ctrl Pts',(31.1822791704619,0.0813648687854731,
25.1932693773186));
#69217=CARTESIAN_POINT('Ctrl Pts',(31.1637300195375,-0.226326940808914,
25.1714517283273));
#69218=CARTESIAN_POINT('Ctrl Pts',(31.1234798971667,-0.378558584977568,
25.1606573669753));
#69219=CARTESIAN_POINT('Ctrl Pts',(30.9889788141031,-0.652134792227603,
25.1412587691706));
#69220=CARTESIAN_POINT('Ctrl Pts',(30.8984922205339,-0.772069973056249,
25.1319682180917));
#69221=CARTESIAN_POINT('Ctrl Pts',(30.6735951228457,-0.975307798919531,
25.1109522700489));
#69222=CARTESIAN_POINT('Ctrl Pts',(30.5399926661631,-1.05515984400593,25.0999170005632));
#69223=CARTESIAN_POINT('Ctrl Pts',(30.2678908596704,-1.15220558793873,25.0797672273045));
#69224=CARTESIAN_POINT('Ctrl Pts',(30.1343655548317,-1.17524047358085,25.0707510761622));
#69225=CARTESIAN_POINT('Ctrl Pts',(29.9999999999998,-1.17524047358085,25.0625));
#69226=CARTESIAN_POINT('Ctrl Pts',(30.0000000000004,-1.17524047358085,25.));
#69227=CARTESIAN_POINT('Ctrl Pts',(30.0280011909949,-1.17524047358084,25.0017194880028));
#69228=CARTESIAN_POINT('Ctrl Pts',(30.056028863347,-1.17423978093536,25.0034760804581));
#69229=CARTESIAN_POINT('Ctrl Pts',(30.2395952618035,-1.16108096396762,25.0152149952129));
#69230=CARTESIAN_POINT('Ctrl Pts',(30.3913571022497,-1.11907669842983,25.0260235449911));
#69231=CARTESIAN_POINT('Ctrl Pts',(30.6663605367685,-0.979972388704826,
25.0478426338075));
#69232=CARTESIAN_POINT('Ctrl Pts',(30.7876235644496,-0.885461952247295,
25.0586398624147));
#69233=CARTESIAN_POINT('Ctrl Pts',(30.9860830879355,-0.656850945315206,
25.0789319146131));
#69234=CARTESIAN_POINT('Ctrl Pts',(31.0619486284351,-0.525431380274417,
25.0877429880603));
#69235=CARTESIAN_POINT('Ctrl Pts',(31.162019301378,-0.235334014571736,25.1083130594786));
#69236=CARTESIAN_POINT('Ctrl Pts',(31.182987818821,-0.0787326337506094,
25.1194172678187));
#69237=CARTESIAN_POINT('Ctrl Pts',(31.162785126869,0.227544173273347,25.1411345825519));
#69238=CARTESIAN_POINT('Ctrl Pts',(31.1241144207896,0.374476178584838,25.1515531598995));
#69239=CARTESIAN_POINT('Ctrl Pts',(30.9915168317796,0.649674032406111,25.1710667445663));
#69240=CARTESIAN_POINT('Ctrl Pts',(30.8973599492461,0.774562668596496,25.1806896874262));
#69241=CARTESIAN_POINT('Ctrl Pts',(30.6662666830193,0.980382528688255,25.202177670528));
#69242=CARTESIAN_POINT('Ctrl Pts',(30.531751815152,1.05938687434591,25.2132389149495));
#69243=CARTESIAN_POINT('Ctrl Pts',(30.2450331875533,1.15903498558282,25.2343785368368));
#69244=CARTESIAN_POINT('Ctrl Pts',(30.0962908441082,1.18072042198942,25.2438927186044));
#69245=CARTESIAN_POINT('Ctrl Pts',(29.7917163095273,1.16710140491111,25.2630787773242));
#69246=CARTESIAN_POINT('Ctrl Pts',(29.638905788045,1.12920096781154,25.2738062281113));
#69247=CARTESIAN_POINT('Ctrl Pts',(29.3599222216531,0.997398530499289,25.2956108489033));
#69248=CARTESIAN_POINT('Ctrl Pts',(29.2358774116296,0.905886016991888,25.3064726127214));
#69249=CARTESIAN_POINT('Ctrl Pts',(29.0316806530828,0.682639701770527,25.32692677681));
#69250=CARTESIAN_POINT('Ctrl Pts',(28.9526524211366,0.553805209269406,25.3357310715183));
#69251=CARTESIAN_POINT('Ctrl Pts',(28.844720062577,0.266708452558536,25.3560883773325));
#69252=CARTESIAN_POINT('Ctrl Pts',(28.8194808141697,0.110295910906438,25.3671791955642));
#69253=CARTESIAN_POINT('Ctrl Pts',(28.8316382042729,-0.197210560241239,
25.3889837026743));
#69254=CARTESIAN_POINT('Ctrl Pts',(28.8665861506279,-0.345474523822663,
25.3994967258182));
#69255=CARTESIAN_POINT('Ctrl Pts',(28.9918018301732,-0.623166741842213,
25.4191871795497));
#69256=CARTESIAN_POINT('Ctrl Pts',(29.081808144475,-0.749490769071139,25.4285215559887));
#69257=CARTESIAN_POINT('Ctrl Pts',(29.3063266217772,-0.961255466999539,
25.449816563314));
#69258=CARTESIAN_POINT('Ctrl Pts',(29.438949602445,-1.04422897408056,25.4609023529488));
#69259=CARTESIAN_POINT('Ctrl Pts',(29.7169259241077,-1.14948331999011,25.4817038921344));
#69260=CARTESIAN_POINT('Ctrl Pts',(29.8579333178884,-1.17524047358086,25.4912760155257));
#69261=CARTESIAN_POINT('Ctrl Pts',(30.,-1.17524047358085,25.5));
#69262=CARTESIAN_POINT('Origin',(30.,-1.21864324187371E-14,15.78125));
#69263=CARTESIAN_POINT('',(30.,-1.17524047358085,26.0625));
#69264=CARTESIAN_POINT('',(30.,-1.17524047358085,26.));
#69265=CARTESIAN_POINT('',(30.,-1.17524047358085,15.78125));
#69266=CARTESIAN_POINT('Ctrl Pts',(29.9999999999999,-1.17524047358085,26.0625));
#69267=CARTESIAN_POINT('Ctrl Pts',(29.9384679078155,-1.17524047358085,26.0587214573544));
#69268=CARTESIAN_POINT('Ctrl Pts',(29.8769029052424,-1.17040913172972,26.054769604635));
#69269=CARTESIAN_POINT('Ctrl Pts',(29.6659154234359,-1.13693724882076,26.0406266508408));
#69270=CARTESIAN_POINT('Ctrl Pts',(29.5220177711255,-1.084323597792,26.0299248801994));
#69271=CARTESIAN_POINT('Ctrl Pts',(29.2586759114222,-0.925171378535031,
26.0081111282534));
#69272=CARTESIAN_POINT('Ctrl Pts',(29.1425757110306,-0.818746672431791,
25.9972085314777));
#69273=CARTESIAN_POINT('Ctrl Pts',(28.9627703960609,-0.572330389052239,
25.9774307272425));
#69274=CARTESIAN_POINT('Ctrl Pts',(28.8986210699436,-0.436327710221708,
25.9684388957715));
#69275=CARTESIAN_POINT('Ctrl Pts',(28.8234492804003,-0.143169608738148,
25.9476517953103));
#69276=CARTESIAN_POINT('Ctrl Pts',(28.8148292891501,0.0116076754049962,
25.936676929058));
#69277=CARTESIAN_POINT('Ctrl Pts',(28.8579269079672,0.318093458602922,25.9149447963521));
#69278=CARTESIAN_POINT('Ctrl Pts',(28.910158206845,0.466589649123026,25.9045489692953));
#69279=CARTESIAN_POINT('Ctrl Pts',(29.0662354765119,0.729159361472922,25.8856555497038));
#69280=CARTESIAN_POINT('Ctrl Pts',(29.1665620010353,0.841989757161643,25.8754944720367));
#69281=CARTESIAN_POINT('Ctrl Pts',(29.4086828051808,1.02746666351878,25.8540505472151));
#69282=CARTESIAN_POINT('Ctrl Pts',(29.5495956219979,1.09657907822105,25.84294712555));
#69283=CARTESIAN_POINT('Ctrl Pts',(29.8472420936479,1.17519666348882,25.8218820609165));
#69284=CARTESIAN_POINT('Ctrl Pts',(30.000722767755,1.18508027808238,25.8128044743545));
#69285=CARTESIAN_POINT('Ctrl Pts',(30.3019786609575,1.14582802588677,25.7929134117055));
#69286=CARTESIAN_POINT('Ctrl Pts',(30.4468987068161,1.09744171612032,25.7822987333));
#69287=CARTESIAN_POINT('Ctrl Pts',(30.7155809567247,0.94545759821414,25.7604111763944));
#69288=CARTESIAN_POINT('Ctrl Pts',(30.835612326607,0.841258259962285,25.7493460732515));
#69289=CARTESIAN_POINT('Ctrl Pts',(31.0226024258984,0.598138792258194,25.7292439525602));
#69290=CARTESIAN_POINT('Ctrl Pts',(31.0902361983429,0.463547729361891,25.7203689985712));
#69291=CARTESIAN_POINT('Ctrl Pts',(31.1725680326408,0.172449502286477,25.6997279586011));
#69292=CARTESIAN_POINT('Ctrl Pts',(31.1850367066478,0.0183235805600113,
25.6887992788123));
#69293=CARTESIAN_POINT('Ctrl Pts',(31.149849032726,-0.288650006825612,25.6670325571437));
#69294=CARTESIAN_POINT('Ctrl Pts',(31.1014848231134,-0.438439388995189,
25.6564113704209));
#69295=CARTESIAN_POINT('Ctrl Pts',(30.9523589365019,-0.704596833564904,
25.637538818338));
#69296=CARTESIAN_POINT('Ctrl Pts',(30.8552831525205,-0.819746342004528,
25.6276245442916));
#69297=CARTESIAN_POINT('Ctrl Pts',(30.6186741800399,-1.01116668038418,25.6063083713552));
#69298=CARTESIAN_POINT('Ctrl Pts',(30.4800603026513,-1.08386414646939,25.5952190187437));
#69299=CARTESIAN_POINT('Ctrl Pts',(30.2235083443405,-1.15925176820215,25.5767919868584));
#69300=CARTESIAN_POINT('Ctrl Pts',(30.1119520742388,-1.17524047358085,25.5693747164571));
#69301=CARTESIAN_POINT('Ctrl Pts',(29.9999999999995,-1.17524047358085,25.5625));
#69302=CARTESIAN_POINT('Ctrl Pts',(30.,-1.17524047358085,25.5));
#69303=CARTESIAN_POINT('Ctrl Pts',(30.0069574643761,-1.17524047358085,25.5004272417029));
#69304=CARTESIAN_POINT('Ctrl Pts',(30.01391720466,-1.17517869098561,25.5008568135879));
#69305=CARTESIAN_POINT('Ctrl Pts',(30.1767683930213,-1.17228514742378,25.5109597131747));
#69306=CARTESIAN_POINT('Ctrl Pts',(30.3305146751184,-1.13852257214804,25.5215979241794));
#69307=CARTESIAN_POINT('Ctrl Pts',(30.613289571589,-1.01415059475931,25.5433719241602));
#69308=CARTESIAN_POINT('Ctrl Pts',(30.7400483172667,-0.925722033283128,
25.5542910068295));
#69309=CARTESIAN_POINT('Ctrl Pts',(30.9499509146168,-0.707886564918499,
25.5749037184647));
#69310=CARTESIAN_POINT('Ctrl Pts',(31.0321249523172,-0.581569550980178,
25.5837623721801));
#69311=CARTESIAN_POINT('Ctrl Pts',(31.1477905785375,-0.297516308572578,
25.6039038700829));
#69312=CARTESIAN_POINT('Ctrl Pts',(31.1772544504942,-0.141401249469257,
25.6149735945785));
#69313=CARTESIAN_POINT('Ctrl Pts',(31.1730934439483,0.167116297568546,25.636849794526));
#69314=CARTESIAN_POINT('Ctrl Pts',(31.1418645520009,0.316603789635784,25.6474495749843));
#69315=CARTESIAN_POINT('Ctrl Pts',(31.0239238826678,0.596699382032703,25.6673104459219));
#69316=CARTESIAN_POINT('Ctrl Pts',(30.9379157361151,0.724424917792123,25.6764216802641));
#69317=CARTESIAN_POINT('Ctrl Pts',(30.7198518445296,0.941880855114492,25.6975221021999));
#69318=CARTESIAN_POINT('Ctrl Pts',(30.5891826263813,1.02868094414498,25.7086235824532));
#69319=CARTESIAN_POINT('Ctrl Pts',(30.3070725150413,1.14422525077315,25.730043785608));
#69320=CARTESIAN_POINT('Ctrl Pts',(30.1591233913896,1.1739884490527,25.7401842137377));
#69321=CARTESIAN_POINT('Ctrl Pts',(29.8537619113516,1.17646530259176,25.7590235656117));
#69322=CARTESIAN_POINT('Ctrl Pts',(29.6991872299891,1.1467452303545,25.7694824753175));
#69323=CARTESIAN_POINT('Ctrl Pts',(29.4128145699134,1.02954198968741,25.7912232470859));
#69324=CARTESIAN_POINT('Ctrl Pts',(29.2835235645903,0.944145175996724,25.8021903431407));
#69325=CARTESIAN_POINT('Ctrl Pts',(29.0681842616351,0.731537563632497,25.8229515631887));
#69326=CARTESIAN_POINT('Ctrl Pts',(28.9830068906091,0.607571894150497,25.8319186117076));
#69327=CARTESIAN_POINT('Ctrl Pts',(28.8607454143127,0.328058458525624,25.851738203379));
#69328=CARTESIAN_POINT('Ctrl Pts',(28.8273201029076,0.174145192049772,25.8626518043211));
#69329=CARTESIAN_POINT('Ctrl Pts',(28.8225473943512,-0.133454152009573,
25.8844628968148));
#69330=CARTESIAN_POINT('Ctrl Pts',(28.849586199068,-0.284195707441678,25.8951515997385));
#69331=CARTESIAN_POINT('Ctrl Pts',(28.9594336647467,-0.566901683792667,
25.9151975664084));
#69332=CARTESIAN_POINT('Ctrl Pts',(29.0410981500453,-0.696179869303813,
25.9241315793102));
#69333=CARTESIAN_POINT('Ctrl Pts',(29.2520170527073,-0.919779045076863,
25.9450110448572));
#69334=CARTESIAN_POINT('Ctrl Pts',(29.3804160320669,-1.01073211613404,25.95612035376));
#69335=CARTESIAN_POINT('Ctrl Pts',(29.6598179734432,-1.13487834137248,25.9776792246572));
#69336=CARTESIAN_POINT('Ctrl Pts',(29.8072708469184,-1.1689955596726,25.9879435454987));
#69337=CARTESIAN_POINT('Ctrl Pts',(29.9714632607541,-1.17498080122199,25.9982384188692));
#69338=CARTESIAN_POINT('Ctrl Pts',(29.9857363066776,-1.17524047358085,25.9991240997731));
#69339=CARTESIAN_POINT('Ctrl Pts',(29.9999999999999,-1.17524047358085,26.));
#69340=CARTESIAN_POINT('Origin',(30.,-1.21864324187371E-14,15.78125));
#69341=CARTESIAN_POINT('',(30.,-1.17524047358085,26.5625));
#69342=CARTESIAN_POINT('',(29.9999999999997,-1.17524047358085,26.4999999999999));
#69343=CARTESIAN_POINT('',(30.,-1.17524047358085,15.78125));
#69344=CARTESIAN_POINT('Ctrl Pts',(30.,-1.17524047358085,26.5625));
#69345=CARTESIAN_POINT('Ctrl Pts',(29.9189538385986,-1.17524047358085,26.5575231437572));
#69346=CARTESIAN_POINT('Ctrl Pts',(29.8379609361797,-1.16685998242801,26.5522524382954));
#69347=CARTESIAN_POINT('Ctrl Pts',(29.6089811727034,-1.1187361642345,26.5364851544771));
#69348=CARTESIAN_POINT('Ctrl Pts',(29.4672242547403,-1.05858684051961,26.5256476735947));
#69349=CARTESIAN_POINT('Ctrl Pts',(29.2118758464994,-0.885634166979752,
26.5038355032321));
#69350=CARTESIAN_POINT('Ctrl Pts',(29.1014575353795,-0.773390023233997,
26.4930754972477));
#69351=CARTESIAN_POINT('Ctrl Pts',(28.9347073730369,-0.518183463481665,
26.4737877314199));
#69352=CARTESIAN_POINT('Ctrl Pts',(28.8776702380248,-0.379162720284378,
26.4643854707334));
#69353=CARTESIAN_POINT('Ctrl Pts',(28.8174988609875,-0.0818619971934983,
26.4433046274383));
#69354=CARTESIAN_POINT('Ctrl Pts',(28.8169789681977,0.0739680819649894,
26.4322551101507));
#69355=CARTESIAN_POINT('Ctrl Pts',(28.8764093680924,0.378032609649621,26.4106946625572));
#69356=CARTESIAN_POINT('Ctrl Pts',(28.9362017786302,0.523138441896699,26.4009448281074));
#69357=CARTESIAN_POINT('Ctrl Pts',(29.1059813583505,0.777530022962841,26.3814999268455));
#69358=CARTESIAN_POINT('Ctrl Pts',(29.2127271628307,0.885439479708375,26.3711191218038));
#69359=CARTESIAN_POINT('Ctrl Pts',(29.4658882417733,1.05845819806925,26.3494389287095));
#69360=CARTESIAN_POINT('Ctrl Pts',(29.6112162771377,1.12003007041528,26.3383317191495));
#69361=CARTESIAN_POINT('Ctrl Pts',(29.9119535931961,1.18158358217449,26.3176818381253));
#69362=CARTESIAN_POINT('Ctrl Pts',(30.0639561135899,1.18313176493728,26.308852379607));
#69363=CARTESIAN_POINT('Ctrl Pts',(30.3618294498414,1.12846284091072,26.2886224532834));
#69364=CARTESIAN_POINT('Ctrl Pts',(30.5047372110283,1.07218329091309,26.2778514997354));
#69365=CARTESIAN_POINT('Ctrl Pts',(30.7642923496518,0.906285517829887,26.2560311264309));
#69366=CARTESIAN_POINT('Ctrl Pts',(30.8776734787023,0.796998466194141,26.2451940206555));
#69367=CARTESIAN_POINT('Ctrl Pts',(31.0511614964728,0.546283376197254,26.2256517381869));
#69368=CARTESIAN_POINT('Ctrl Pts',(31.1118599586541,0.408839660981002,26.2164897876345));
#69369=CARTESIAN_POINT('Ctrl Pts',(31.179816298086,0.113659355972694,26.1955592978295));
#69370=CARTESIAN_POINT('Ctrl Pts',(31.1845443559052,-0.0416770721755796,
26.1845447840881));
#69371=CARTESIAN_POINT('Ctrl Pts',(31.1333712501869,-0.348241759846019,
26.1628070564654));
#69372=CARTESIAN_POINT('Ctrl Pts',(31.0768319553006,-0.496185033349922,
26.1527007984472));
#69373=CARTESIAN_POINT('Ctrl Pts',(30.9126965034022,-0.755446668894444,
26.1334298283147));
#69374=CARTESIAN_POINT('Ctrl Pts',(30.8088874743598,-0.865675121928193,
26.1231471467367));
#69375=CARTESIAN_POINT('Ctrl Pts',(30.5607504336079,-1.04453090463544,26.1015685223966));
#69376=CARTESIAN_POINT('Ctrl Pts',(30.4174143875892,-1.10962145980108,26.0904588858133));
#69377=CARTESIAN_POINT('Ctrl Pts',(30.1782678600435,-1.16509155074858,26.0738068318412));
#69378=CARTESIAN_POINT('Ctrl Pts',(30.0891908090061,-1.17524047358085,26.0679770001062));
#69379=CARTESIAN_POINT('Ctrl Pts',(29.9999999999999,-1.17524047358085,26.0625));
#69380=CARTESIAN_POINT('Ctrl Pts',(29.9999999999999,-1.17524047358085,26.));
#69381=CARTESIAN_POINT('Ctrl Pts',(30.1425333221801,-1.17524047358085,26.0087526397553));
#69382=CARTESIAN_POINT('Ctrl Pts',(30.2840219111895,-1.14931710997616,26.0183602049923));
#69383=CARTESIAN_POINT('Ctrl Pts',(30.561367295123,-1.04389937746679,26.0391287924253));
#69384=CARTESIAN_POINT('Ctrl Pts',(30.6930583893841,-0.961526015756511,
26.0501360796874));
#69385=CARTESIAN_POINT('Ctrl Pts',(30.9136669465422,-0.754054974126117,
26.0710387617507));
#69386=CARTESIAN_POINT('Ctrl Pts',(31.0017654739708,-0.632326756940585,
26.0801633069178));
#69387=CARTESIAN_POINT('Ctrl Pts',(31.130809796733,-0.356072448301099,26.0997518021271));
#69388=CARTESIAN_POINT('Ctrl Pts',(31.1680189550385,-0.20305033553964,26.1106022136104));
#69389=CARTESIAN_POINT('Ctrl Pts',(31.1804056537492,0.10467710494643,26.1324223890981));
#69390=CARTESIAN_POINT('Ctrl Pts',(31.1569739806732,0.256395498849484,26.1431803571703));
#69391=CARTESIAN_POINT('Ctrl Pts',(31.0540187102742,0.541272174052999,26.1633802426127));
#69392=CARTESIAN_POINT('Ctrl Pts',(30.9759701950171,0.671873752670431,26.1722217092774));
#69393=CARTESIAN_POINT('Ctrl Pts',(30.7711018756191,0.900554058237447,26.1929097676203));
#69394=CARTESIAN_POINT('Ctrl Pts',(30.6447103916025,0.994954099829424,26.2040180088908));
#69395=CARTESIAN_POINT('Ctrl Pts',(30.3677839906361,1.12628386016982,26.2256795457743));
#69396=CARTESIAN_POINT('Ctrl Pts',(30.2208469191431,1.16405670623833,26.2360417980814));
#69397=CARTESIAN_POINT('Ctrl Pts',(29.9153739917407,1.18247957177519,26.2554533393943));
#69398=CARTESIAN_POINT('Ctrl Pts',(29.7596534858204,1.16089584886057,26.265267690896));
#69399=CARTESIAN_POINT('Ctrl Pts',(29.4669798482834,1.05871377618554,26.2868628344935));
#69400=CARTESIAN_POINT('Ctrl Pts',(29.3327683310263,0.97968769950255,26.2979062213058));
#69401=CARTESIAN_POINT('Ctrl Pts',(29.1064857982236,0.777827856716442,26.3189583910466));
#69402=CARTESIAN_POINT('Ctrl Pts',(29.0152252755147,0.658466900754918,26.3283097753497));
#69403=CARTESIAN_POINT('Ctrl Pts',(28.8789732904358,0.385760488964649,26.3476466981555));
#69404=CARTESIAN_POINT('Ctrl Pts',(28.8377485021289,0.233796400613908,26.3584220878003));
#69405=CARTESIAN_POINT('Ctrl Pts',(28.8172159011814,-0.0738574561607104,
26.3802370456529));
#69406=CARTESIAN_POINT('Ctrl Pts',(28.8367587774233,-0.226525134118623,
26.3910623250595));
#69407=CARTESIAN_POINT('Ctrl Pts',(28.9323498389723,-0.513670658612161,
26.411423088874));
#69408=CARTESIAN_POINT('Ctrl Pts',(29.0066122735479,-0.645689070611162,
26.4202237943573));
#69409=CARTESIAN_POINT('Ctrl Pts',(29.2050554476303,-0.879653705731429,
26.4407046487027));
#69410=CARTESIAN_POINT('Ctrl Pts',(29.329232754846,-0.977642983590833,26.4518041743651));
#69411=CARTESIAN_POINT('Ctrl Pts',(29.6033526154654,-1.11649688151574,26.4735601269295));
#69412=CARTESIAN_POINT('Ctrl Pts',(29.7496481694863,-1.15811817689029,26.4840194270505));
#69413=CARTESIAN_POINT('Ctrl Pts',(29.9332052808561,-1.1738184735254,26.4958478764586));
#69414=CARTESIAN_POINT('Ctrl Pts',(29.9666204732331,-1.17524047358085,26.4979502409084));
#69415=CARTESIAN_POINT('Ctrl Pts',(29.9999999999995,-1.17524047358085,26.4999999999999));
#69416=CARTESIAN_POINT('Origin',(30.,-1.21864324187371E-14,15.78125));
#69417=CARTESIAN_POINT('',(30.0000000000002,-1.17524047358085,27.0625));
#69418=CARTESIAN_POINT('',(29.9999999999999,-1.17524047358085,26.9999999999999));
#69419=CARTESIAN_POINT('',(30.,-1.17524047358085,15.78125));
#69420=CARTESIAN_POINT('Ctrl Pts',(30.0000000000003,-1.17524047358085,27.0625));
#69421=CARTESIAN_POINT('Ctrl Pts',(29.898686590649,-1.17524047358088,27.0562785792061));
#69422=CARTESIAN_POINT('Ctrl Pts',(29.7976296484377,-1.16214610940709,27.0496086633191));
#69423=CARTESIAN_POINT('Ctrl Pts',(29.5510548806291,-1.0968832857528,27.032153269422));
#69424=CARTESIAN_POINT('Ctrl Pts',(29.4119274187945,-1.02901377051944,27.0212035476842));
#69425=CARTESIAN_POINT('Ctrl Pts',(29.1656287201027,-0.842194481232163,
26.9994554755857));
#69426=CARTESIAN_POINT('Ctrl Pts',(29.0614102622354,-0.72425366568988,26.9888742198639));
#69427=CARTESIAN_POINT('Ctrl Pts',(28.9083494936521,-0.460199204673261,
26.9701133966982));
#69428=CARTESIAN_POINT('Ctrl Pts',(28.8587194637877,-0.317836463591476,
26.960036980781));
#69429=CARTESIAN_POINT('Ctrl Pts',(28.8146713989512,-0.0163533730831442,
26.9386595763769));
#69430=CARTESIAN_POINT('Ctrl Pts',(28.8228691179041,0.140138676728786,26.9275631204225));
#69431=CARTESIAN_POINT('Ctrl Pts',(28.8990556060477,0.438772825908234,26.9063877272517));
#69432=CARTESIAN_POINT('Ctrl Pts',(28.9654414239268,0.578169376458166,26.8971982372258));
#69433=CARTESIAN_POINT('Ctrl Pts',(29.1468572533747,0.822311817466142,26.8774021512523));
#69434=CARTESIAN_POINT('Ctrl Pts',(29.259591693584,0.925109502257862,26.8668348294397));
#69435=CARTESIAN_POINT('Ctrl Pts',(29.522846414638,1.08544747155122,26.8449843892055));
#69436=CARTESIAN_POINT('Ctrl Pts',(29.672078571298,1.13945389610578,26.8339056600349));
#69437=CARTESIAN_POINT('Ctrl Pts',(29.9754469871149,1.18446101454497,26.813680840772));
#69438=CARTESIAN_POINT('Ctrl Pts',(30.1261553208811,1.17798106873351,26.804850259546));
#69439=CARTESIAN_POINT('Ctrl Pts',(30.4204691708303,1.10805786050355,26.7842980916158));
#69440=CARTESIAN_POINT('Ctrl Pts',(30.5609479127602,1.04399036631935,26.7734001867649));
#69441=CARTESIAN_POINT('Ctrl Pts',(30.8118142126087,0.8639649033663,26.7516124954367));
#69442=CARTESIAN_POINT('Ctrl Pts',(30.9191345732301,0.748795351296203,26.7409390107287));
#69443=CARTESIAN_POINT('Ctrl Pts',(31.0789814493982,0.489082061456906,26.7219153792232));
#69444=CARTESIAN_POINT('Ctrl Pts',(31.13228056467,0.348399841671576,26.7122041527178));
#69445=CARTESIAN_POINT('Ctrl Pts',(31.1843745315803,0.0489678760358684,
26.6909721883974));
#69446=CARTESIAN_POINT('Ctrl Pts',(31.1805251276485,-0.10725425723734,26.6798948715428));
#69447=CARTESIAN_POINT('Ctrl Pts',(31.112642066065,-0.408638429750164,26.658524481164));
#69448=CARTESIAN_POINT('Ctrl Pts',(31.04952452927,-0.550854728541633,26.6490856679416));
#69449=CARTESIAN_POINT('Ctrl Pts',(30.8739065476105,-0.80013916056119,26.6294633115169));
#69450=CARTESIAN_POINT('Ctrl Pts',(30.7641429817239,-0.90553953226469,26.6189861492083));
#69451=CARTESIAN_POINT('Ctrl Pts',(30.5058691930861,-1.0723039712914,26.5972137340794));
#69452=CARTESIAN_POINT('Ctrl Pts',(30.3585462682162,-1.13013161506019,26.5861167698907));
#69453=CARTESIAN_POINT('Ctrl Pts',(30.1366295806596,-1.1692866034305,26.5711011916684));
#69454=CARTESIAN_POINT('Ctrl Pts',(30.0683089619122,-1.17524047358085,26.5666946944513));
#69455=CARTESIAN_POINT('Ctrl Pts',(30.,-1.17524047358085,26.5625));
#69456=CARTESIAN_POINT('Ctrl Pts',(29.9999999999995,-1.17524047358085,26.4999999999999));
#69457=CARTESIAN_POINT('Ctrl Pts',(30.1204914385722,-1.17524047358085,26.5073990989566));
#69458=CARTESIAN_POINT('Ctrl Pts',(30.2404377363977,-1.1567191282047,26.5154213729959));
#69459=CARTESIAN_POINT('Ctrl Pts',(30.503109066672,-1.07331217218126,26.5345084966475));
#69460=CARTESIAN_POINT('Ctrl Pts',(30.6398547835573,-0.997848639879795,
26.5455811972524));
#69461=CARTESIAN_POINT('Ctrl Pts',(30.8720104636609,-0.801888849767787,
26.566784844391));
#69462=CARTESIAN_POINT('Ctrl Pts',(30.9665674240944,-0.684937055709897,
26.5764328435252));
#69463=CARTESIAN_POINT('Ctrl Pts',(31.1101788342394,-0.415941539318355,
26.595506636112));
#69464=CARTESIAN_POINT('Ctrl Pts',(31.1554918067157,-0.265175979373474,
26.606197041135));
#69465=CARTESIAN_POINT('Ctrl Pts',(31.184388668241,0.0421759563922281,26.6279905905315));
#69466=CARTESIAN_POINT('Ctrl Pts',(31.1688709786064,0.195715280062819,26.6388776761339));
#69467=CARTESIAN_POINT('Ctrl Pts',(31.080842595015,0.4851372161482,26.6593998545441));
#69468=CARTESIAN_POINT('Ctrl Pts',(31.0103902901456,0.618617027917578,26.6682199013902));
#69469=CARTESIAN_POINT('Ctrl Pts',(30.8184983590075,0.857859380695496,26.6884855739597));
#69470=CARTESIAN_POINT('Ctrl Pts',(30.6966625458602,0.959431158368461,26.6995683269243));
#69471=CARTESIAN_POINT('Ctrl Pts',(30.4255868085001,1.10584185104675,26.7214052635744));
#69472=CARTESIAN_POINT('Ctrl Pts',(30.280042417997,1.15134883169079,26.7319561985547));
#69473=CARTESIAN_POINT('Ctrl Pts',(29.9776063567648,1.18496921576007,26.7517200618056));
#69474=CARTESIAN_POINT('Ctrl Pts',(29.8235440457018,1.17197554004672,26.7609515037779));
#69475=CARTESIAN_POINT('Ctrl Pts',(29.5271473201095,1.08704252411486,26.7821637300309));
#69476=CARTESIAN_POINT('Ctrl Pts',(29.3879639883513,1.01521369745337,26.7932572549969));
#69477=CARTESIAN_POINT('Ctrl Pts',(29.1499744927664,0.825212607812385,26.8146078849744));
#69478=CARTESIAN_POINT('Ctrl Pts',(29.0521140662545,0.710618013126823,26.8246118717047));
#69479=CARTESIAN_POINT('Ctrl Pts',(28.9012898027458,0.445344450507133,26.8434217499511));
#69480=CARTESIAN_POINT('Ctrl Pts',(28.8519884644377,0.295869143296566,26.8540206664119));
#69481=CARTESIAN_POINT('Ctrl Pts',(28.8148602582687,-0.0109614775297701,
26.8757772506829));
#69482=CARTESIAN_POINT('Ctrl Pts',(28.8263846212866,-0.165256365046284,
26.886717911409));
#69483=CARTESIAN_POINT('Ctrl Pts',(28.90695684434,-0.456865689279699,26.9073951919876));
#69484=CARTESIAN_POINT('Ctrl Pts',(28.9737284626765,-0.591802058760263,
26.9162939800796));
#69485=CARTESIAN_POINT('Ctrl Pts',(29.1592103949543,-0.836102522890621,
26.9363453584795));
#69486=CARTESIAN_POINT('Ctrl Pts',(29.2786778563743,-0.94110103302348,26.9474041669452));
#69487=CARTESIAN_POINT('Ctrl Pts',(29.5466042812102,-1.09478566204523,26.9693055998652));
#69488=CARTESIAN_POINT('Ctrl Pts',(29.6913217184938,-1.14405280529544,26.9799390653881));
#69489=CARTESIAN_POINT('Ctrl Pts',(29.8940937627055,-1.17166523876262,26.9933697888908));
#69490=CARTESIAN_POINT('Ctrl Pts',(29.9470693710243,-1.17524047358085,26.9967496532013));
#69491=CARTESIAN_POINT('Ctrl Pts',(29.9999999999997,-1.17524047358085,26.9999999999999));
#69492=CARTESIAN_POINT('Origin',(30.,-1.21864324187371E-14,15.78125));
#69493=CARTESIAN_POINT('',(30.0000000000002,-1.17524047358085,27.5625));
#69494=CARTESIAN_POINT('',(30.,-1.17524047358085,27.5));
#69495=CARTESIAN_POINT('',(30.,-1.17524047358085,15.78125));
#69496=CARTESIAN_POINT('Ctrl Pts',(30.0000000000004,-1.17524047358085,27.5625));
#69497=CARTESIAN_POINT('Ctrl Pts',(29.8791981655177,-1.17524047358089,27.5550818403526));
#69498=CARTESIAN_POINT('Ctrl Pts',(29.7589726578968,-1.15662316573575,27.547039018461));
#69499=CARTESIAN_POINT('Ctrl Pts',(29.4966785757901,-1.0731279551929,27.5279719317893));
#69500=CARTESIAN_POINT('Ctrl Pts',(29.3604611797136,-0.99796015863462,27.5169421590736));
#69501=CARTESIAN_POINT('Ctrl Pts',(29.1231210583237,-0.797935915977368,
27.495276047424));
#69502=CARTESIAN_POINT('Ctrl Pts',(29.0249429590029,-0.674426740918645,
27.4853218966019));
#69503=CARTESIAN_POINT('Ctrl Pts',(28.8853520572172,-0.401644540260052,
27.4659795997989));
#69504=CARTESIAN_POINT('Ctrl Pts',(28.8432060655213,-0.256055793645229,
27.4556562695324));
#69505=CARTESIAN_POINT('Ctrl Pts',(28.8154546971309,0.0488704066146756,
27.4340347229132));
#69506=CARTESIAN_POINT('Ctrl Pts',(28.8323972811925,0.205546638674019,27.4229252070608));
#69507=CARTESIAN_POINT('Ctrl Pts',(28.9250076761164,0.498408501969224,27.4021591121013));
#69508=CARTESIAN_POINT('Ctrl Pts',(28.997892508521,0.632295921050251,27.3932865033313));
#69509=CARTESIAN_POINT('Ctrl Pts',(29.1909681621961,0.865881565904131,27.3731486925495));
#69510=CARTESIAN_POINT('Ctrl Pts',(29.3095755456334,0.963111668503783,27.3624181185496));
#69511=CARTESIAN_POINT('Ctrl Pts',(29.5806971724252,1.10891198583092,27.3406000040234));
#69512=CARTESIAN_POINT('Ctrl Pts',(29.7313794614454,1.15471361111034,27.3297231163935));
#69513=CARTESIAN_POINT('Ctrl Pts',(30.0349224077729,1.1841311566887,27.3100402882342));
#69514=CARTESIAN_POINT('Ctrl Pts',(30.1845806615862,1.17018311962186,27.3009860288447));
#69515=CARTESIAN_POINT('Ctrl Pts',(30.4753054258698,1.08577187813399,27.2801406033955));
#69516=CARTESIAN_POINT('Ctrl Pts',(30.6130774728742,1.01437069747224,27.2691489037921));
#69517=CARTESIAN_POINT('Ctrl Pts',(30.8550923899249,0.82117912160722,27.2474379673869));
#69518=CARTESIAN_POINT('Ctrl Pts',(30.9563451215602,0.700625408948211,27.2371795779744));
#69519=CARTESIAN_POINT('Ctrl Pts',(31.1030012085855,0.43246305141941,27.218164862578));
#69520=CARTESIAN_POINT('Ctrl Pts',(31.1490749245368,0.288512534258167,27.207957695024));
#69521=CARTESIAN_POINT('Ctrl Pts',(31.1854037082186,-0.0146433585393976,
27.1864616764351));
#69522=CARTESIAN_POINT('Ctrl Pts',(31.173058308365,-0.171282192075426,27.1753548124176));
#69523=CARTESIAN_POINT('Ctrl Pts',(31.089040383827,-0.467218401344852,27.1543707233508));
#69524=CARTESIAN_POINT('Ctrl Pts',(31.0195638166583,-0.603975746358807,
27.1453625116794));
#69525=CARTESIAN_POINT('Ctrl Pts',(30.8326207012815,-0.843150163878356,
27.1254031429327));
#69526=CARTESIAN_POINT('Ctrl Pts',(30.7170833899544,-0.943363872050058,
27.1147553149523));
#69527=CARTESIAN_POINT('Ctrl Pts',(30.4491800434626,-1.09737775442843,27.0928436259578));
#69528=CARTESIAN_POINT('Ctrl Pts',(30.2981995637065,-1.14764798518389,27.0817899983651));
#69529=CARTESIAN_POINT('Ctrl Pts',(30.0946434783266,-1.17238533021172,27.0684130613475));
#69530=CARTESIAN_POINT('Ctrl Pts',(30.0473000417297,-1.17524047358084,27.0654045855337));
#69531=CARTESIAN_POINT('Ctrl Pts',(30.0000000000003,-1.17524047358085,27.0625));
#69532=CARTESIAN_POINT('Ctrl Pts',(29.9999999999997,-1.17524047358085,26.9999999999999));
#69533=CARTESIAN_POINT('Ctrl Pts',(30.0986058905517,-1.17524047358085,27.0060551583626));
#69534=CARTESIAN_POINT('Ctrl Pts',(30.197001235846,-1.16283641910558,27.0125371577158));
#69535=CARTESIAN_POINT('Ctrl Pts',(30.4435331990926,-1.0993899448342,27.029925526711));
#69536=CARTESIAN_POINT('Ctrl Pts',(30.5849622280491,-1.0311122983099,27.0410310521114));
#69537=CARTESIAN_POINT('Ctrl Pts',(30.8283565317534,-0.84700506573289,27.0625046195245));
#69538=CARTESIAN_POINT('Ctrl Pts',(30.9294172599309,-0.734710314399227,
27.0726917923361));
#69539=CARTESIAN_POINT('Ctrl Pts',(31.0870905034712,-0.472970868314495,
27.0916537809288));
#69540=CARTESIAN_POINT('Ctrl Pts',(31.1401926761717,-0.324772377450416,
27.1019712110874));
#69541=CARTESIAN_POINT('Ctrl Pts',(31.1850952185403,-0.0184511332937437,
27.1236916767454));
#69542=CARTESIAN_POINT('Ctrl Pts',(31.1773587357349,0.136461808282747,27.1346761621237));
#69543=CARTESIAN_POINT('Ctrl Pts',(31.1038267733963,0.430084241190232,27.1554961871532));
#69544=CARTESIAN_POINT('Ctrl Pts',(31.0404668538449,0.566412733303589,27.1645221322455));
#69545=CARTESIAN_POINT('Ctrl Pts',(30.8621032542639,0.813817787312719,27.1842464597062));
#69546=CARTESIAN_POINT('Ctrl Pts',(30.746618378735,0.920903307832853,27.195134699154));
#69547=CARTESIAN_POINT('Ctrl Pts',(30.4841269758582,1.08160589165682,27.2169511927423));
#69548=CARTESIAN_POINT('Ctrl Pts',(30.3404475283553,1.13505921838268,27.2276693335753));
#69549=CARTESIAN_POINT('Ctrl Pts',(30.0413373449537,1.18420822105003,27.2477795099651));
#69550=CARTESIAN_POINT('Ctrl Pts',(29.8888261880251,1.17970362185606,27.2566686898965));
#69551=CARTESIAN_POINT('Ctrl Pts',(29.5891419642887,1.11207867848515,27.2774691579106));
#69552=CARTESIAN_POINT('Ctrl Pts',(29.4453407649054,1.04779159085184,27.2885788725534));
#69553=CARTESIAN_POINT('Ctrl Pts',(29.1960372639306,0.870265103883027,27.3101819980009));
#69554=CARTESIAN_POINT('Ctrl Pts',(29.091548794378,0.760562756134129,27.3204877500418));
#69555=CARTESIAN_POINT('Ctrl Pts',(28.9261102653187,0.502419631695097,27.3397990837129));
#69556=CARTESIAN_POINT('Ctrl Pts',(28.8688162363146,0.355135077347701,27.3498182687336));
#69557=CARTESIAN_POINT('Ctrl Pts',(28.8157293168355,0.0491393235848099,
27.3715156546901));
#69558=CARTESIAN_POINT('Ctrl Pts',(28.8194875433144,-0.106321035237959,
27.3825389560425));
#69559=CARTESIAN_POINT('Ctrl Pts',(28.8856486083743,-0.401996025014571,
27.4035045226948));
#69560=CARTESIAN_POINT('Ctrl Pts',(28.9454972717022,-0.539801328338099,
27.4127167480926));
#69561=CARTESIAN_POINT('Ctrl Pts',(29.11742422097,-0.791565441680741,27.4322003607736));
#69562=CARTESIAN_POINT('Ctrl Pts',(29.2301245105903,-0.901546472787143,
27.4430202619491));
#69563=CARTESIAN_POINT('Ctrl Pts',(29.4887201815225,-1.06909180163981,27.4648401285834));
#69564=CARTESIAN_POINT('Ctrl Pts',(29.6313699534066,-1.1262717375032,27.4756271616522));
#69565=CARTESIAN_POINT('Ctrl Pts',(29.853348441796,-1.16837939045814,27.4907512179135));
#69566=CARTESIAN_POINT('Ctrl Pts',(29.9266702080884,-1.17524047358085,27.4954969880578));
#69567=CARTESIAN_POINT('Ctrl Pts',(30.,-1.17524047358085,27.5));
#69568=CARTESIAN_POINT('Origin',(30.,-1.21864324187371E-14,15.78125));
#69569=CARTESIAN_POINT('',(30.,-1.17524047358085,28.0625));
#69570=CARTESIAN_POINT('',(30.0000000000001,-1.17524047358085,28.));
#69571=CARTESIAN_POINT('',(30.,-1.17524047358085,15.78125));
#69572=CARTESIAN_POINT('Ctrl Pts',(30.,-1.17524047358085,28.0625));
#69573=CARTESIAN_POINT('Ctrl Pts',(29.8576309526277,-1.17524047358085,28.0537574479785));
#69574=CARTESIAN_POINT('Ctrl Pts',(29.7163289872701,-1.14937338079985,28.0441633378768));
#69575=CARTESIAN_POINT('Ctrl Pts',(29.4381412694858,-1.0437960185582,28.0233373652109));
#69576=CARTESIAN_POINT('Ctrl Pts',(29.3055725204167,-0.960712774920266,
28.0122510152415));
#69577=CARTESIAN_POINT('Ctrl Pts',(29.0812375157914,-0.748784364739409,
27.9909614703353));
#69578=CARTESIAN_POINT('Ctrl Pts',(28.991345872443,-0.622420436003701,27.9816342608879));
#69579=CARTESIAN_POINT('Ctrl Pts',(28.8663365712296,-0.344659291734443,
27.9619389197703));
#69580=CARTESIAN_POINT('Ctrl Pts',(28.8314934625426,-0.196359386622749,
27.9514233481032));
#69581=CARTESIAN_POINT('Ctrl Pts',(28.8195620391171,0.111178530712451,27.9296166112233));
#69582=CARTESIAN_POINT('Ctrl Pts',(28.8449209434754,0.267584161126331,27.9185262830501));
#69583=CARTESIAN_POINT('Ctrl Pts',(28.9530728770119,0.554595748995939,27.8981750163432));
#69584=CARTESIAN_POINT('Ctrl Pts',(29.0321899221582,0.683358417415679,27.8893700226253));
#69585=CARTESIAN_POINT('Ctrl Pts',(29.2365478324768,0.90645295573766,27.8689113436395));
#69586=CARTESIAN_POINT('Ctrl Pts',(29.3606700385593,0.997879761432882,27.8580478657718));
#69587=CARTESIAN_POINT('Ctrl Pts',(29.6397630167776,1.12947461119937,27.8362438860083));
#69588=CARTESIAN_POINT('Ctrl Pts',(29.7926014521638,1.16725893043214,27.8255188379057));
#69589=CARTESIAN_POINT('Ctrl Pts',(30.0971888483988,1.18064726325309,27.8063401680006));
#69590=CARTESIAN_POINT('Ctrl Pts',(30.2459190189188,1.15884794264961,27.7968175086224));
#69591=CARTESIAN_POINT('Ctrl Pts',(30.5325764826745,1.05897425995597,27.7756736453134));
#69592=CARTESIAN_POINT('Ctrl Pts',(30.6670400332198,0.979858412729581,27.7646115990219));
#69593=CARTESIAN_POINT('Ctrl Pts',(30.8979501916997,0.773870883397489,27.7431289156398));
#69594=CARTESIAN_POINT('Ctrl Pts',(30.9919903689524,0.648942084588862,27.7335148439956));
#69595=CARTESIAN_POINT('Ctrl Pts',(31.1243827012244,0.373674108325156,27.7139962871235));
#69596=CARTESIAN_POINT('Ctrl Pts',(31.1629506296625,0.226703861102418,27.7035749981386));
#69597=CARTESIAN_POINT('Ctrl Pts',(31.182930645767,-0.0796098768690557,
27.6818550647252));
#69598=CARTESIAN_POINT('Ctrl Pts',(31.1618436472684,-0.236207537040712,
27.6707511202069));
#69599=CARTESIAN_POINT('Ctrl Pts',(31.0615541749908,-0.526222674013738,
27.6501868794201));
#69600=CARTESIAN_POINT('Ctrl Pts',(30.9856010212307,-0.657569956578418,
27.641376820382));
#69601=CARTESIAN_POINT('Ctrl Pts',(30.7869826832863,-0.886033452367878,
27.6210802455783));
#69602=CARTESIAN_POINT('Ctrl Pts',(30.6656419827339,-0.980462303947253,
27.6102811397496));
#69603=CARTESIAN_POINT('Ctrl Pts',(30.3905261901255,-1.11936682731598,27.5884622344572));
#69604=CARTESIAN_POINT('Ctrl Pts',(30.2387339000707,-1.16125829953858,27.5776558137839));
#69605=CARTESIAN_POINT('Ctrl Pts',(30.0554488466051,-1.17426038713893,27.5659397324124));
#69606=CARTESIAN_POINT('Ctrl Pts',(30.0277113777332,-1.17524047358084,27.5642016912446));
#69607=CARTESIAN_POINT('Ctrl Pts',(30.0000000000004,-1.17524047358085,27.5625));
#69608=CARTESIAN_POINT('Ctrl Pts',(30.,-1.17524047358085,27.5));
#69609=CARTESIAN_POINT('Ctrl Pts',(30.0764884643488,-1.17524047358085,27.5046969786688));
#69610=CARTESIAN_POINT('Ctrl Pts',(30.1529528341161,-1.16777574296381,27.5096571303415));
#69611=CARTESIAN_POINT('Ctrl Pts',(30.3817494239676,-1.12246086122216,27.5253135785994));
#69612=CARTESIAN_POINT('Ctrl Pts',(30.5275514222186,-1.06175746883915,27.5364191022575));
#69613=CARTESIAN_POINT('Ctrl Pts',(30.7819194324173,-0.890185564641921,
27.5581221152238));
#69614=CARTESIAN_POINT('Ctrl Pts',(30.8893748791333,-0.782854361740771,
27.5685259964847));
#69615=CARTESIAN_POINT('Ctrl Pts',(31.0605234375151,-0.529653947481304,
27.5880127322271));
#69616=CARTESIAN_POINT('Ctrl Pts',(31.1210989339899,-0.385229961573254,
27.5976843165126));
#69617=CARTESIAN_POINT('Ctrl Pts',(31.1825194576632,-0.0817855747122669,
27.6192007914867));
#69618=CARTESIAN_POINT('Ctrl Pts',(31.1830228429167,0.0741472759213479,
27.63025759604));
#69619=CARTESIAN_POINT('Ctrl Pts',(31.1247432077576,0.371953492117145,27.6513742825742));
#69620=CARTESIAN_POINT('Ctrl Pts',(31.0685868115923,0.511361040320207,27.6608435628079));
#69621=CARTESIAN_POINT('Ctrl Pts',(30.9034614818395,0.767636822344003,27.6800694593713));
#69622=CARTESIAN_POINT('Ctrl Pts',(30.7937668420839,0.880579083554765,27.6908097772536));
#69623=CARTESIAN_POINT('Ctrl Pts',(30.5394580202052,1.05521084982092,27.712617639148));
#69624=CARTESIAN_POINT('Ctrl Pts',(30.3979930311562,1.11628678065312,27.7234700450399));
#69625=CARTESIAN_POINT('Ctrl Pts',(30.102283661711,1.18033932531086,27.7438997716137));
#69626=CARTESIAN_POINT('Ctrl Pts',(29.9510987894339,1.18375239925559,27.752701130013));
#69627=CARTESIAN_POINT('Ctrl Pts',(29.6486955420892,1.13241772430468,27.7730910160496));
#69628=CARTESIAN_POINT('Ctrl Pts',(29.5009111395855,1.07549105438516,27.7841843756164));
#69629=CARTESIAN_POINT('Ctrl Pts',(29.2414417758967,0.910237971539166,27.8059766250036));
#69630=CARTESIAN_POINT('Ctrl Pts',(29.1309679987517,0.805447516109976,27.8164757759223));
#69631=CARTESIAN_POINT('Ctrl Pts',(28.9539689931679,0.557381504423619,27.8361397402596));
#69632=CARTESIAN_POINT('Ctrl Pts',(28.8900701663349,0.415841482478183,27.8455137308899));
#69633=CARTESIAN_POINT('Ctrl Pts',(28.8202010476643,0.115104610378523,27.8668382228314));
#69634=CARTESIAN_POINT('Ctrl Pts',(28.8153164753922,-0.0411926086217122,
27.8779208638252));
#69635=CARTESIAN_POINT('Ctrl Pts',(28.8654961586475,-0.341119160610214,
27.8991878980145));
#69636=CARTESIAN_POINT('Ctrl Pts',(28.9179176762722,-0.482198917057609,
27.9089809285524));
#69637=CARTESIAN_POINT('Ctrl Pts',(29.0761417927703,-0.742958176446737,
27.9279419936907));
#69638=CARTESIAN_POINT('Ctrl Pts',(29.1827253034037,-0.858799901268264,
27.938594061191));
#69639=CARTESIAN_POINT('Ctrl Pts',(29.4325136093474,-1.04046451212148,27.9603736693398));
#69640=CARTESIAN_POINT('Ctrl Pts',(29.5726776549044,-1.10544579696665,27.9712846467122));
#69641=CARTESIAN_POINT('Ctrl Pts',(29.8127786384444,-1.16404144712018,27.9881061243607));
#69642=CARTESIAN_POINT('Ctrl Pts',(29.9063068575872,-1.17524047358087,27.9942465220726));
#69643=CARTESIAN_POINT('Ctrl Pts',(30.0000000000002,-1.17524047358085,28.));
#69644=CARTESIAN_POINT('Origin',(30.,-1.21864324187371E-14,15.78125));
#69645=CARTESIAN_POINT('',(30.,-1.17524047358085,28.5625));
#69646=CARTESIAN_POINT('',(30.0000000000002,-1.17524047358085,28.5));
#69647=CARTESIAN_POINT('',(30.,-1.17524047358085,15.78125));
#69648=CARTESIAN_POINT('Ctrl Pts',(29.9999999999999,-1.17524047358085,28.5625));
#69649=CARTESIAN_POINT('Ctrl Pts',(29.9854755687231,-1.17524047358085,28.5616080884619));
#69650=CARTESIAN_POINT('Ctrl Pts',(29.9709414772303,-1.17497122100143,28.5607060377023));
#69651=CARTESIAN_POINT('Ctrl Pts',(29.8064818821414,-1.16886648226933,28.5503905207309));
#69652=CARTESIAN_POINT('Ctrl Pts',(29.6590422242683,-1.13464684706092,28.5401233803667));
#69653=CARTESIAN_POINT('Ctrl Pts',(29.3797071247853,-1.01029888540339,28.5185614617647));
#69654=CARTESIAN_POINT('Ctrl Pts',(29.251363124374,-0.919248746833339,28.507452087585));
#69655=CARTESIAN_POINT('Ctrl Pts',(29.0406130665321,-0.695506305973089,
28.486577911123));
#69656=CARTESIAN_POINT('Ctrl Pts',(28.9590502383724,-0.56619133070644,28.4776471970656));
#69657=CARTESIAN_POINT('Ctrl Pts',(28.8493945968077,-0.283424288620792,
28.4575969003786));
#69658=CARTESIAN_POINT('Ctrl Pts',(28.8224557263032,-0.132654402250458,
28.4469061885797));
#69659=CARTESIAN_POINT('Ctrl Pts',(28.8274401393345,0.174951078681269,28.4250946609358));
#69660=CARTESIAN_POINT('Ctrl Pts',(28.8609710566448,0.328840848056597,28.4141827261138));
#69661=CARTESIAN_POINT('Ctrl Pts',(28.9834218096268,0.608264397886715,28.394369508017));
#69662=CARTESIAN_POINT('Ctrl Pts',(29.0686800279675,0.732167484395331,28.3853987862865));
#69663=CARTESIAN_POINT('Ctrl Pts',(29.2841654510491,0.944633593842617,28.3646336101487));
#69664=CARTESIAN_POINT('Ctrl Pts',(29.4135237499535,1.0299476859008,28.3536653145426));
#69665=CARTESIAN_POINT('Ctrl Pts',(29.6999884026637,1.14695518646917,28.3319258334386));
#69666=CARTESIAN_POINT('Ctrl Pts',(29.8545850153065,1.1765676391467,28.321476648926));
#69667=CARTESIAN_POINT('Ctrl Pts',(30.1599574738008,1.17387642238167,28.3026290229131));
#69668=CARTESIAN_POINT('Ctrl Pts',(30.3078958483554,1.14400535727984,28.2924854305785));
#69669=CARTESIAN_POINT('Ctrl Pts',(30.5899420117525,1.02824734362325,28.2710615776053));
#69670=CARTESIAN_POINT('Ctrl Pts',(30.7205565666579,0.941343746526345,28.2599597843468));
#69671=CARTESIAN_POINT('Ctrl Pts',(30.9384441962492,0.723734320112842,28.2388647444883));
#69672=CARTESIAN_POINT('Ctrl Pts',(31.0243441752868,0.5959705376245,28.2297587654061));
#69673=CARTESIAN_POINT('Ctrl Pts',(31.1420857275796,0.315809924237744,28.2098932839944));
#69674=CARTESIAN_POINT('Ctrl Pts',(31.1732121728651,0.166290213222924,28.1992912189719));
#69675=CARTESIAN_POINT('Ctrl Pts',(31.1771534741222,-0.14225217236566,28.1774132577855));
#69676=CARTESIAN_POINT('Ctrl Pts',(31.1475738082276,-0.298357527790664,
28.1663442213532));
#69677=CARTESIAN_POINT('Ctrl Pts',(31.0316967203975,-0.582326286717529,
28.1462087139606));
#69678=CARTESIAN_POINT('Ctrl Pts',(30.9494361151523,-0.708574806833004,
28.1373477050794));
#69679=CARTESIAN_POINT('Ctrl Pts',(30.7393766183288,-0.926260402286338,
28.1167306721673));
#69680=CARTESIAN_POINT('Ctrl Pts',(30.6125440370362,-1.01460273603848,28.1058101125197));
#69681=CARTESIAN_POINT('Ctrl Pts',(30.3296673321613,-1.13876808424026,28.0840371864985));
#69682=CARTESIAN_POINT('Ctrl Pts',(30.1758968644013,-1.17241612952657,28.0734015508245));
#69683=CARTESIAN_POINT('Ctrl Pts',(30.0133354780172,-1.17518374723503,28.0633209118452));
#69684=CARTESIAN_POINT('Ctrl Pts',(30.0066666906193,-1.17524047358085,28.0629093859629));
#69685=CARTESIAN_POINT('Ctrl Pts',(30.,-1.17524047358085,28.0625));
#69686=CARTESIAN_POINT('Ctrl Pts',(30.0000000000002,-1.17524047358085,28.));
#69687=CARTESIAN_POINT('Ctrl Pts',(30.055120011526,-1.17524047358084,28.0033847916881));
#69688=CARTESIAN_POINT('Ctrl Pts',(30.1102800819057,-1.17136342893539,28.0069094990185));
#69689=CARTESIAN_POINT('Ctrl Pts',(30.320778299587,-1.14149919825233,28.0208945034877));
#69690=CARTESIAN_POINT('Ctrl Pts',(30.4704399584402,-1.08838822567003,28.0319678602702));
#69691=CARTESIAN_POINT('Ctrl Pts',(30.7348284172129,-0.929562358310031,
28.0538343110362));
#69692=CARTESIAN_POINT('Ctrl Pts',(30.8482436418564,-0.827380507129033,
28.0644216046344));
#69693=CARTESIAN_POINT('Ctrl Pts',(31.0309964109232,-0.58443378950115,28.0842573960977));
#69694=CARTESIAN_POINT('Ctrl Pts',(31.0981318171314,-0.445680080400429,
28.0933979512832));
#69695=CARTESIAN_POINT('Ctrl Pts',(31.1762201438822,-0.147691887981632,
28.1145275412917));
#69696=CARTESIAN_POINT('Ctrl Pts',(31.1854211354334,0.00884554012676132,
28.1256272149066));
#69697=CARTESIAN_POINT('Ctrl Pts',(31.1432517249665,0.310649796547867,28.1470273923742));
#69698=CARTESIAN_POINT('Ctrl Pts',(31.0945166442476,0.453415390384783,28.1571505400084));
#69699=CARTESIAN_POINT('Ctrl Pts',(30.9430034157352,0.718468313966014,28.1759447732979));
#69700=CARTESIAN_POINT('Ctrl Pts',(30.8395316819024,0.837077300041102,28.1864571641064));
#69701=CARTESIAN_POINT('Ctrl Pts',(30.594175126874,1.02551549499305,28.2082047776097));
#69702=CARTESIAN_POINT('Ctrl Pts',(30.4553685567187,1.0942445153416,28.2191652668043));
#69703=CARTESIAN_POINT('Ctrl Pts',(30.1633070228503,1.17335763356101,28.2399049418951));
#69704=CARTESIAN_POINT('Ctrl Pts',(30.0132854694265,1.18458952272981,28.2488527114972));
#69705=CARTESIAN_POINT('Ctrl Pts',(29.7101813599922,1.14957783235101,28.2687069250423));
#69706=CARTESIAN_POINT('Ctrl Pts',(29.5603537745588,1.10100720474222,28.2796294987935));
#69707=CARTESIAN_POINT('Ctrl Pts',(29.2921855827035,0.950361389094781,28.3014380407736));
#69708=CARTESIAN_POINT('Ctrl Pts',(29.1755651130251,0.851181456436058,28.3121157317836));
#69709=CARTESIAN_POINT('Ctrl Pts',(28.9864685212412,0.613960284958293,28.3321380906356));
#69710=CARTESIAN_POINT('Ctrl Pts',(28.9157930252681,0.478217809624506,28.341090783094));
#69711=CARTESIAN_POINT('Ctrl Pts',(28.8287462552022,0.18335177826131,28.3619989885486));
#69712=CARTESIAN_POINT('Ctrl Pts',(28.8147855892159,0.0266848358587583,
28.3731078456949));
#69713=CARTESIAN_POINT('Ctrl Pts',(28.8481057813277,-0.277120858900621,
28.3946499400995));
#69714=CARTESIAN_POINT('Ctrl Pts',(28.8928044130046,-0.421659697790202,
28.4048988240612));
#69715=CARTESIAN_POINT('Ctrl Pts',(29.0376019293491,-0.692609521363159,
28.4241111916336));
#69716=CARTESIAN_POINT('Ctrl Pts',(29.1388311172626,-0.815074867447836,
28.4343484054768));
#69717=CARTESIAN_POINT('Ctrl Pts',(29.3808301647318,-1.01067727789171,28.456143840463));
#69718=CARTESIAN_POINT('Ctrl Pts',(29.5182554521743,-1.08294295653866,28.4671448960526));
#69719=CARTESIAN_POINT('Ctrl Pts',(29.7744135979937,-1.15894806924162,28.4855696371912));
#69720=CARTESIAN_POINT('Ctrl Pts',(29.8869899356779,-1.1752404735809,28.493060314833));
#69721=CARTESIAN_POINT('Ctrl Pts',(30.0000000000005,-1.17524047358085,28.5));
#69722=CARTESIAN_POINT('Origin',(30.,-1.21864324187371E-14,15.78125));
#69723=CARTESIAN_POINT('',(29.9999999999997,-1.17524047358085,29.0625));
#69724=CARTESIAN_POINT('',(30.,-1.17524047358085,29.));
#69725=CARTESIAN_POINT('',(30.,-1.17524047358085,15.78125));
#69726=CARTESIAN_POINT('Ctrl Pts',(29.9999999999995,-1.17524047358085,29.0625));
#69727=CARTESIAN_POINT('Ctrl Pts',(29.9663313283337,-1.17524047358085,29.0604324851927));
#69728=CARTESIAN_POINT('Ctrl Pts',(29.9326266255446,-1.17379373293774,29.0583114654359));
#69729=CARTESIAN_POINT('Ctrl Pts',(29.7487805300534,-1.15793171143038,29.046459536434));
#69730=CARTESIAN_POINT('Ctrl Pts',(29.6025054140808,-1.11619705168394,29.0359974721754));
#69731=CARTESIAN_POINT('Ctrl Pts',(29.3284713606868,-0.977122112422326,
29.0142389520917));
#69732=CARTESIAN_POINT('Ctrl Pts',(29.204360853848,-0.879027723836093,29.003139801917));
#69733=CARTESIAN_POINT('Ctrl Pts',(29.0061078341151,-0.644908297203287,
28.9826651365702));
#69734=CARTESIAN_POINT('Ctrl Pts',(28.9319567448549,-0.512847810431858,
28.9738647427883));
#69735=CARTESIAN_POINT('Ctrl Pts',(28.8365844224207,-0.225635628236165,
28.9534992524445));
#69736=CARTESIAN_POINT('Ctrl Pts',(28.8171575566038,-0.0729412609821712,
28.9426720805673));
#69737=CARTESIAN_POINT('Ctrl Pts',(28.8379321785986,0.234707082052963,28.92085751368));
#69738=CARTESIAN_POINT('Ctrl Pts',(28.8792757590782,0.386638085776581,28.9100844699825));
#69739=CARTESIAN_POINT('Ctrl Pts',(29.0157412244589,0.659238101106546,28.8907550914809));
#69740=CARTESIAN_POINT('Ctrl Pts',(29.107096372761,0.778529076561771,28.8813960362208));
#69741=CARTESIAN_POINT('Ctrl Pts',(29.3335481377689,0.980220242371224,28.8603394545531));
#69742=CARTESIAN_POINT('Ctrl Pts',(29.4678337645529,1.05914504636678,28.8492951073424));
#69743=CARTESIAN_POINT('Ctrl Pts',(29.760564366148,1.1610786562004,28.8277052746509));
#69744=CARTESIAN_POINT('Ctrl Pts',(29.9162604257863,1.18253750642917,28.8179009595418));
#69745=CARTESIAN_POINT('Ctrl Pts',(30.2216914945448,1.16389753053477,28.7984842912973));
#69746=CARTESIAN_POINT('Ctrl Pts',(30.3686116386073,1.12601470107769,28.7881191791422));
#69747=CARTESIAN_POINT('Ctrl Pts',(30.645460693513,0.994469364755083,28.7664547489262));
#69748=CARTESIAN_POINT('Ctrl Pts',(30.7717903384927,0.899966183411579,28.7553466483575));
#69749=CARTESIAN_POINT('Ctrl Pts',(30.9764758301347,0.671134004376585,28.7346644325598));
#69750=CARTESIAN_POINT('Ctrl Pts',(31.0544159221586,0.540492245543279,28.7258249398524));
#69751=CARTESIAN_POINT('Ctrl Pts',(31.1571623293156,0.255550540096121,28.7056204432797));
#69752=CARTESIAN_POINT('Ctrl Pts',(31.1804841833933,0.103803871660056,28.6948604703318));
#69753=CARTESIAN_POINT('Ctrl Pts',(31.1678665590545,-0.203924479708025,
28.6730402302557));
#69754=CARTESIAN_POINT('Ctrl Pts',(31.130543099267,-0.356918086122505,28.6621918400855));
#69755=CARTESIAN_POINT('Ctrl Pts',(31.0012937995436,-0.633072694293491,
28.6426104143845));
#69756=CARTESIAN_POINT('Ctrl Pts',(30.9131062008608,-0.754733454165662,
28.6334802730101));
#69757=CARTESIAN_POINT('Ctrl Pts',(30.6923373486102,-0.962047131628042,
28.6125733267459));
#69758=CARTESIAN_POINT('Ctrl Pts',(30.5605741188135,-1.04432722358406,28.6015649165697));
#69759=CARTESIAN_POINT('Ctrl Pts',(30.2834202387706,-1.14942800624881,28.5808193260016));
#69760=CARTESIAN_POINT('Ctrl Pts',(30.1422284632676,-1.17524047358085,28.5712339190787));
#69761=CARTESIAN_POINT('Ctrl Pts',(29.9999999999999,-1.17524047358085,28.5625));
#69762=CARTESIAN_POINT('Ctrl Pts',(30.0000000000005,-1.17524047358085,28.5));
#69763=CARTESIAN_POINT('Ctrl Pts',(30.0354745744302,-1.17524047358084,28.5021784110951));
#69764=CARTESIAN_POINT('Ctrl Pts',(30.070984899228,-1.17363438892678,28.50441595924));
#69765=CARTESIAN_POINT('Ctrl Pts',(30.2617617366305,-1.15628719000694,28.5167461440698));
#69766=CARTESIAN_POINT('Ctrl Pts',(30.4127085422869,-1.11138228847866,28.527607482843));
#69767=CARTESIAN_POINT('Ctrl Pts',(30.6847642885538,-0.967157900388871,
28.5494270868925));
#69768=CARTESIAN_POINT('Ctrl Pts',(30.804005950619,-0.870565283253422,28.5601740092255));
#69769=CARTESIAN_POINT('Ctrl Pts',(30.9983603111577,-0.638155310621775,
28.5803486604476));
#69770=CARTESIAN_POINT('Ctrl Pts',(31.0719538047089,-0.504858427298666,
28.5892017641887));
#69771=CARTESIAN_POINT('Ctrl Pts',(31.1663430846515,-0.212647773407092,
28.6099216835343));
#69772=CARTESIAN_POINT('Ctrl Pts',(31.1842429187448,-0.0559802512603478,
28.6210305817888));
#69773=CARTESIAN_POINT('Ctrl Pts',(31.1582832767207,0.249283949423046,28.6426760951642));
#69774=CARTESIAN_POINT('Ctrl Pts',(31.1169606007789,0.395199803964739,28.6530226198275));
#69775=CARTESIAN_POINT('Ctrl Pts',(30.9790360194058,0.668562290541804,28.6724060632391));
#69776=CARTESIAN_POINT('Ctrl Pts',(30.8818240300007,0.792402281745908,28.6822761930404));
#69777=CARTESIAN_POINT('Ctrl Pts',(30.6459736712074,0.993822232743541,28.7039003049109));
#69778=CARTESIAN_POINT('Ctrl Pts',(30.5101537410361,1.06991069848525,28.7149383113331));
#69779=CARTESIAN_POINT('Ctrl Pts',(30.2218612846042,1.16368326752433,28.7359662684601));
#69780=CARTESIAN_POINT('Ctrl Pts',(30.0727878905027,1.18239624374933,28.7452765661691));
#69781=CARTESIAN_POINT('Ctrl Pts',(29.7685724316717,1.16273575029291,28.764654767797));
#69782=CARTESIAN_POINT('Ctrl Pts',(29.6165255150965,1.12180125661046,28.7754428960271));
#69783=CARTESIAN_POINT('Ctrl Pts',(29.3404632117996,0.984593855919108,28.797259754998));
#69784=CARTESIAN_POINT('Ctrl Pts',(29.2184662863885,0.890859052794272,28.8080745514575));
#69785=CARTESIAN_POINT('Ctrl Pts',(29.0185031029016,0.663646825495766,28.8284093479536));
#69786=CARTESIAN_POINT('Ctrl Pts',(28.9418083423014,0.532910081337728,28.8372126922591));
#69787=CARTESIAN_POINT('Ctrl Pts',(28.8396688119263,0.243593095049782,28.8577274289443));
#69788=CARTESIAN_POINT('Ctrl Pts',(28.8175791014781,0.0870303940346913,
28.8688288945971));
#69789=CARTESIAN_POINT('Ctrl Pts',(28.8356734059559,-0.219589451967425,
28.8905705333577));
#69790=CARTESIAN_POINT('Ctrl Pts',(28.8733703746263,-0.366880393585839,
28.9010145619721));
#69791=CARTESIAN_POINT('Ctrl Pts',(29.0040267448551,-0.642739671975603,
28.9205750465844));
#69792=CARTESIAN_POINT('Ctrl Pts',(29.0970828699605,-0.768007510288218,
28.9301160290222));
#69793=CARTESIAN_POINT('Ctrl Pts',(29.3264450160403,-0.975407631545752,
28.9515537342264));
#69794=CARTESIAN_POINT('Ctrl Pts',(29.4604715589085,-1.05546393671967,28.9626222876417));
#69795=CARTESIAN_POINT('Ctrl Pts',(29.7327334190531,-1.15230702146743,28.9827747043974));
#69796=CARTESIAN_POINT('Ctrl Pts',(29.8659356312532,-1.17524047358086,28.9917674189746));
#69797=CARTESIAN_POINT('Ctrl Pts',(30.0000000000001,-1.17524047358085,29.));
#69798=CARTESIAN_POINT('Origin',(30.,-1.21864324187371E-14,15.78125));
#69799=CARTESIAN_POINT('',(29.9999999999999,-1.17524047358085,29.5625));
#69800=CARTESIAN_POINT('',(30.,-1.17524047358085,29.5));
#69801=CARTESIAN_POINT('',(30.,-1.17524047358085,15.78125));
#69802=CARTESIAN_POINT('Ctrl Pts',(29.9999999999998,-1.17524047358085,29.5625));
#69803=CARTESIAN_POINT('Ctrl Pts',(29.9467973546619,-1.17524047358085,29.5592329493093));
#69804=CARTESIAN_POINT('Ctrl Pts',(29.8935499193759,-1.17162840400865,29.5558350868076));
#69805=CARTESIAN_POINT('Ctrl Pts',(29.6905156464705,-1.14383638937277,29.5423818936273));
#69806=CARTESIAN_POINT('Ctrl Pts',(29.5458229652857,-1.09446322181842,29.531746189361));
#69807=CARTESIAN_POINT('Ctrl Pts',(29.2779882672223,-0.940574047774209,
29.5098431372833));
#69808=CARTESIAN_POINT('Ctrl Pts',(29.1585890601641,-0.835479489994527,
29.4987851149112));
#69809=CARTESIAN_POINT('Ctrl Pts',(28.9732889450876,-0.591037021395749,
29.4787398668936));
#69810=CARTESIAN_POINT('Ctrl Pts',(28.9066211123554,-0.456058910232785,
29.4698379853235));
#69811=CARTESIAN_POINT('Ctrl Pts',(28.8262612459225,-0.164388119091858,
29.4491563462818));
#69812=CARTESIAN_POINT('Ctrl Pts',(28.8148509180816,-0.0100732314283097,
29.4382142673958));
#69813=CARTESIAN_POINT('Ctrl Pts',(28.852213214805,0.296739305134607,29.4164589654342));
#69814=CARTESIAN_POINT('Ctrl Pts',(28.9016274703356,0.446176311860775,29.405862764764));
#69815=CARTESIAN_POINT('Ctrl Pts',(29.0526565417776,0.711342976877612,29.3870604663565));
#69816=CARTESIAN_POINT('Ctrl Pts',(29.1506118786123,0.825870653466757,29.3770454144149));
#69817=CARTESIAN_POINT('Ctrl Pts',(29.3887681357508,1.01569990993121,29.3556906361267));
#69818=CARTESIAN_POINT('Ctrl Pts',(29.5280199399709,1.08742345397384,29.3445966390884));
#69819=CARTESIAN_POINT('Ctrl Pts',(29.8244665773462,1.17210985589585,29.3233900912571));
#69820=CARTESIAN_POINT('Ctrl Pts',(29.9785058773413,1.18498177307898,29.3141652695437));
#69821=CARTESIAN_POINT('Ctrl Pts',(30.2808965556073,1.15114217787766,29.2943964213012));
#69822=CARTESIAN_POINT('Ctrl Pts',(30.4264177470889,1.1055232193301,29.2838429408837));
#69823=CARTESIAN_POINT('Ctrl Pts',(30.697402601783,0.95889535591386,29.2620038856125));
#69824=CARTESIAN_POINT('Ctrl Pts',(30.819169348162,0.85722095894767,29.2509217356401));
#69825=CARTESIAN_POINT('Ctrl Pts',(31.0108714255578,0.617827319896978,29.2306623578836));
#69826=CARTESIAN_POINT('Ctrl Pts',(31.0812140757987,0.48430476852144,29.221840827786));
#69827=CARTESIAN_POINT('Ctrl Pts',(31.1690224491511,0.194817477900372,29.2013140152506));
#69828=CARTESIAN_POINT('Ctrl Pts',(31.1844226308274,0.0412543787619307,
29.1904252437899));
#69829=CARTESIAN_POINT('Ctrl Pts',(31.1552826086302,-0.266085347349785,
29.1686325601491));
#69830=CARTESIAN_POINT('Ctrl Pts',(31.1098513200658,-0.416814367038074,
29.1579447461033));
#69831=CARTESIAN_POINT('Ctrl Pts',(30.9660264712179,-0.685700945491834,
29.1388786780306));
#69832=CARTESIAN_POINT('Ctrl Pts',(30.8713728192914,-0.802582950873403,
29.1292210796557));
#69833=CARTESIAN_POINT('Ctrl Pts',(30.6390456070483,-0.99836896334456,29.1080130601942));
#69834=CARTESIAN_POINT('Ctrl Pts',(30.5022270643229,-1.07372697770931,29.0969396285291));
#69835=CARTESIAN_POINT('Ctrl Pts',(30.2397868247199,-1.15682002769535,29.0778778247601));
#69836=CARTESIAN_POINT('Ctrl Pts',(30.1201628836901,-1.17524047358085,29.0698789231656));
#69837=CARTESIAN_POINT('Ctrl Pts',(29.9999999999995,-1.17524047358085,29.0625));
#69838=CARTESIAN_POINT('Ctrl Pts',(30.0000000000001,-1.17524047358085,29.));
#69839=CARTESIAN_POINT('Ctrl Pts',(30.0146960045521,-1.17524047358085,29.0009024474538));
#69840=CARTESIAN_POINT('Ctrl Pts',(30.0294011894743,-1.17496482224357,29.0018152315228));
#69841=CARTESIAN_POINT('Ctrl Pts',(30.199932441124,-1.16856010735523,29.0125142300756));
#69842=CARTESIAN_POINT('Ctrl Pts',(30.353002562887,-1.13175546267305,29.0232187723758));
#69843=CARTESIAN_POINT('Ctrl Pts',(30.6330116689674,-1.00191414666784,29.0450168400954));
#69844=CARTESIAN_POINT('Ctrl Pts',(30.7577840016447,-0.911212372347243,
29.0558945356534));
#69845=CARTESIAN_POINT('Ctrl Pts',(30.9634990803743,-0.689398439003151,
29.0763911529622));
#69846=CARTESIAN_POINT('Ctrl Pts',(31.0433641152287,-0.561238966842274,
29.0852039625465));
#69847=CARTESIAN_POINT('Ctrl Pts',(31.1533625468904,-0.274946500315461,
29.1055042381753));
#69848=CARTESIAN_POINT('Ctrl Pts',(31.1797284184379,-0.118602529514694,
29.1165901942211));
#69849=CARTESIAN_POINT('Ctrl Pts',(31.1696998210424,0.189193535485508,29.1384152356998));
#69850=CARTESIAN_POINT('Ctrl Pts',(31.1357401287962,0.337792934955289,29.1489520437553));
#69851=CARTESIAN_POINT('Ctrl Pts',(31.0124667812232,0.616132121424454,29.1686883723852));
#69852=CARTESIAN_POINT('Ctrl Pts',(30.9235367823029,0.742831293967475,29.1779572331897));
#69853=CARTESIAN_POINT('Ctrl Pts',(30.7007442503466,0.956131495282673,29.1992006935594));
#69854=CARTESIAN_POINT('Ctrl Pts',(30.5686344749746,1.04013508390185,29.2102914886907));
#69855=CARTESIAN_POINT('Ctrl Pts',(30.2847340927663,1.14996876391647,29.231619165161));
#69856=CARTESIAN_POINT('Ctrl Pts',(30.1365034722987,1.17678287240203,29.241562955497));
#69857=CARTESIAN_POINT('Ctrl Pts',(29.8314130542368,1.17348866622216,29.2604146402912));
#69858=CARTESIAN_POINT('Ctrl Pts',(29.6774432972388,1.14080144691636,29.271028448982));
#69859=CARTESIAN_POINT('Ctrl Pts',(29.3937190869037,1.01837161158084,29.2927918879254));
#69860=CARTESIAN_POINT('Ctrl Pts',(29.2662697773694,0.930754504522398,29.3037246074232));
#69861=CARTESIAN_POINT('Ctrl Pts',(29.0548960664095,0.714326580132712,29.3243777540292));
#69862=CARTESIAN_POINT('Ctrl Pts',(28.9719101496403,0.588650269969742,29.3332602962825));
#69863=CARTESIAN_POINT('Ctrl Pts',(28.8542643011592,0.305390771595589,29.3533455118009));
#69864=CARTESIAN_POINT('Ctrl Pts',(28.8237155837947,0.14936986715794,29.3644085600269));
#69865=CARTESIAN_POINT('Ctrl Pts',(28.8258171170069,-0.159374372506235,
29.386300834176));
#69866=CARTESIAN_POINT('Ctrl Pts',(28.8560851449643,-0.309160959864127,
29.3969218227258));
#69867=CARTESIAN_POINT('Ctrl Pts',(28.9721608102066,-0.589863983624277,
29.416825765087));
#69868=CARTESIAN_POINT('Ctrl Pts',(29.0571584178456,-0.717947603677171,
29.4258895505263));
#69869=CARTESIAN_POINT('Ctrl Pts',(29.2735722711375,-0.936836489269234,
29.4469394508198));
#69870=CARTESIAN_POINT('Ctrl Pts',(29.4037270862843,-1.02460346918986,29.4580436226767));
#69871=CARTESIAN_POINT('Ctrl Pts',(29.6852328519168,-1.14214540943397,29.4794975379443));
#69872=CARTESIAN_POINT('Ctrl Pts',(29.8330783756557,-1.1729174993834,29.4896673732243));
#69873=CARTESIAN_POINT('Ctrl Pts',(29.9885051427478,-1.17519832475183,29.4992926332218));
#69874=CARTESIAN_POINT('Ctrl Pts',(29.9942534046712,-1.17524047358085,29.4996471149485));
#69875=CARTESIAN_POINT('Ctrl Pts',(30.,-1.17524047358085,29.5));
#69876=CARTESIAN_POINT('Origin',(30.,-1.21864324187371E-14,15.78125));
#69877=CARTESIAN_POINT('',(30.,-1.17524047358085,30.0625));
#69878=CARTESIAN_POINT('',(29.9999999999998,-1.17524047358085,29.9999999999999));
#69879=CARTESIAN_POINT('',(30.,-1.17524047358085,15.78125));
#69880=CARTESIAN_POINT('Ctrl Pts',(30.,-1.17524047358085,30.0625));
#69881=CARTESIAN_POINT('Ctrl Pts',(29.9263916760993,-1.17524047358085,30.0579798840563));
#69882=CARTESIAN_POINT('Ctrl Pts',(29.8527927358329,-1.1683271801588,30.0532152422529));
#69883=CARTESIAN_POINT('Ctrl Pts',(29.6305589174408,-1.12600740432272,30.0380679862212));
#69884=CARTESIAN_POINT('Ctrl Pts',(29.4879403212856,-1.06872004039491,30.0272790588551));
#69885=CARTESIAN_POINT('Ctrl Pts',(29.229459906818,-0.900978381114361,30.0054593092048));
#69886=CARTESIAN_POINT('Ctrl Pts',(29.1168411945232,-0.790914788798306,
29.9946414903997));
#69887=CARTESIAN_POINT('Ctrl Pts',(28.9451007627829,-0.539025681180781,
29.975164899812));
#69888=CARTESIAN_POINT('Ctrl Pts',(28.885353566283,-0.401177024850609,29.9659464494622));
#69889=CARTESIAN_POINT('Ctrl Pts',(28.8194073352897,-0.10544306552401,29.944976701428));
#69890=CARTESIAN_POINT('Ctrl Pts',(28.8157651951869,0.0500317181756064,
29.9339523772439));
#69891=CARTESIAN_POINT('Ctrl Pts',(28.8690807484143,0.355959077177534,29.9122598409872));
#69892=CARTESIAN_POINT('Ctrl Pts',(28.9264649062036,0.503164977506288,29.9022508807468));
#69893=CARTESIAN_POINT('Ctrl Pts',(29.0920593097175,0.761174070029624,29.8829347271204));
#69894=CARTESIAN_POINT('Ctrl Pts',(29.1966290016669,0.870813111888444,29.8726262318314));
#69895=CARTESIAN_POINT('Ctrl Pts',(29.4460717811045,1.04817985046692,29.851020217295));
#69896=CARTESIAN_POINT('Ctrl Pts',(29.5899284156368,1.11237046788542,29.8399105187383));
#69897=CARTESIAN_POINT('Ctrl Pts',(29.8896511606184,1.17977836078127,29.8191153804746));
#69898=CARTESIAN_POINT('Ctrl Pts',(30.042143785172,1.18417711729498,29.810228885603));
#69899=CARTESIAN_POINT('Ctrl Pts',(30.3412103985985,1.13483145488925,29.7901144124214));
#69900=CARTESIAN_POINT('Ctrl Pts',(30.484863334991,1.08127741540018,29.7793943289302));
#69901=CARTESIAN_POINT('Ctrl Pts',(30.7472520600478,0.920389087318013,29.7575775552199));
#69902=CARTESIAN_POINT('Ctrl Pts',(30.8626628342488,0.813224513564577,29.7466910634298));
#69903=CARTESIAN_POINT('Ctrl Pts',(31.0408533066038,0.565701034414209,29.7269731686955));
#69904=CARTESIAN_POINT('Ctrl Pts',(31.1041185100332,0.42933329828376,29.7179429396888));
#69905=CARTESIAN_POINT('Ctrl Pts',(31.1774532864279,0.13565521801398,29.6971189688454));
#69906=CARTESIAN_POINT('Ctrl Pts',(31.185083485025,-0.0192736961984122,
29.6861333508878));
#69907=CARTESIAN_POINT('Ctrl Pts',(31.1399640096901,-0.325574493297471,
29.6644143350789));
#69908=CARTESIAN_POINT('Ctrl Pts',(31.0867572532099,-0.473736864086508,
29.654106159393));
#69909=CARTESIAN_POINT('Ctrl Pts',(30.9288924580137,-0.735375844574816,
29.6351359699395));
#69910=CARTESIAN_POINT('Ctrl Pts',(30.827743660758,-0.847605887956935,29.6249456831495));
#69911=CARTESIAN_POINT('Ctrl Pts',(30.5841967794232,-1.03154789843284,29.6034686040399));
#69912=CARTESIAN_POINT('Ctrl Pts',(30.4427060183441,-1.0997249484081,29.5923628543371));
#69913=CARTESIAN_POINT('Ctrl Pts',(30.1964052482032,-1.16291170221409,29.5749978904338));
#69914=CARTESIAN_POINT('Ctrl Pts',(30.0983061450535,-1.17524047358085,29.5685367516888));
#69915=CARTESIAN_POINT('Ctrl Pts',(29.9999999999998,-1.17524047358085,29.5625));
#69916=CARTESIAN_POINT('Ctrl Pts',(30.,-1.17524047358085,29.5));
#69917=CARTESIAN_POINT('Ctrl Pts',(30.1499565209686,-1.17524047358085,29.5092084811251));
#69918=CARTESIAN_POINT('Ctrl Pts',(30.2986551183888,-1.14654165825818,29.5193571963421));
#69919=CARTESIAN_POINT('Ctrl Pts',(30.5805418737435,-1.03331719508937,29.5406814366056));
#69920=CARTESIAN_POINT('Ctrl Pts',(30.7104602238272,-0.948696043146186,
29.5516595563353));
#69921=CARTESIAN_POINT('Ctrl Pts',(30.9271652336418,-0.73741304903825,29.5724576785973));
#69922=CARTESIAN_POINT('Ctrl Pts',(31.0130985609625,-0.614031092469691,
29.5814606062707));
#69923=CARTESIAN_POINT('Ctrl Pts',(31.1371264539894,-0.335358891062759,
29.6012205481486));
#69924=CARTESIAN_POINT('Ctrl Pts',(31.1715373282526,-0.181667965902616,
29.6121183834297));
#69925=CARTESIAN_POINT('Ctrl Pts',(31.1782875351469,0.125982959094587,29.6339331333974));
#69926=CARTESIAN_POINT('Ctrl Pts',(31.1521830035108,0.27698654047903,29.6446404159195));
#69927=CARTESIAN_POINT('Ctrl Pts',(31.0441268483734,0.560261316579686,29.6647267147429));
#69928=CARTESIAN_POINT('Ctrl Pts',(30.9634093757068,0.689883113720223,29.6736315391227));
#69929=CARTESIAN_POINT('Ctrl Pts',(30.7540662315648,0.914815989860588,29.6944615256665));
#69930=CARTESIAN_POINT('Ctrl Pts',(30.6261826944801,1.0066730037076,29.7055712306082));
#69931=CARTESIAN_POINT('Ctrl Pts',(30.3474095969538,1.1326991331979,29.7271581352984));
#69932=CARTESIAN_POINT('Ctrl Pts',(30.2000827038505,1.16777128079541,29.7374485757904));
#69933=CARTESIAN_POINT('Ctrl Pts',(29.8935937537322,1.18085135992657,29.7567330869508));
#69934=CARTESIAN_POINT('Ctrl Pts',(29.7372662628443,1.15617395643532,29.7668098469142));
#69935=CARTESIAN_POINT('Ctrl Pts',(29.4460305983855,1.04785975410839,29.7885340948419));
#69936=CARTESIAN_POINT('Ctrl Pts',(29.3136703421255,0.966357190577468,29.7995516007362));
#69937=CARTESIAN_POINT('Ctrl Pts',(29.091570241583,0.760352988788506,29.8204938700552));
#69938=CARTESIAN_POINT('Ctrl Pts',(29.0026423680915,0.639251124272773,29.8296723175212));
#69939=CARTESIAN_POINT('Ctrl Pts',(28.8716938065568,0.363925746310141,29.8491949446027));
#69940=CARTESIAN_POINT('Ctrl Pts',(28.8334229675251,0.211172023558316,29.8600263252283));
#69941=CARTESIAN_POINT('Ctrl Pts',(28.8188892259004,-0.0965571382164996,
29.8818466227683));
#69942=CARTESIAN_POINT('Ctrl Pts',(28.8412989000486,-0.248535346834791,
29.8926230136456));
#69943=CARTESIAN_POINT('Ctrl Pts',(28.942312504556,-0.5340148591211,29.9128656447428));
#69944=CARTESIAN_POINT('Ctrl Pts',(29.0193556498266,-0.664990211735325,
29.9216906330323));
#69945=CARTESIAN_POINT('Ctrl Pts',(29.2225255933627,-0.895077676800941,
29.9423242871271));
#69946=CARTESIAN_POINT('Ctrl Pts',(29.3483400060408,-0.990433515042349,
29.9534309783521));
#69947=CARTESIAN_POINT('Ctrl Pts',(29.6245422330139,-1.1237624473258,29.9751189235115));
#69948=CARTESIAN_POINT('Ctrl Pts',(29.7713190573348,-1.16255586776877,29.985507518588));
#69949=CARTESIAN_POINT('Ctrl Pts',(29.9476315409713,-1.1743662864253,29.9967531815485));
#69950=CARTESIAN_POINT('Ctrl Pts',(29.9738286104226,-1.17524047358085,29.9983928758457));
#69951=CARTESIAN_POINT('Ctrl Pts',(29.9999999999996,-1.17524047358085,29.9999999999999));
#69952=CARTESIAN_POINT('Origin',(30.,-1.21864324187371E-14,15.78125));
#69953=CARTESIAN_POINT('',(30.,-1.17524047358085,30.5625));
#69954=CARTESIAN_POINT('',(29.9999999999998,-1.17524047358085,30.4999999999999));
#69955=CARTESIAN_POINT('',(30.,-1.17524047358085,15.78125));
#69956=CARTESIAN_POINT('Ctrl Pts',(29.9999999999999,-1.17524047358085,30.5625));
#69957=CARTESIAN_POINT('Ctrl Pts',(29.87859718881,-1.17524047358085,30.555044935771));
#69958=CARTESIAN_POINT('Ctrl Pts',(29.7578462794256,-1.15643017462348,30.5469630079231));
#69959=CARTESIAN_POINT('Ctrl Pts',(29.5223698659242,-1.08113291221706,30.5298333797947));
#69960=CARTESIAN_POINT('Ctrl Pts',(29.4096002088597,-1.02391620699781,30.5208799114591));
#69961=CARTESIAN_POINT('Ctrl Pts',(29.1820826863431,-0.858187725726655,
30.5010328956616));
#69962=CARTESIAN_POINT('Ctrl Pts',(29.0755864711026,-0.74226695058618,30.4903833861391));
#69963=CARTESIAN_POINT('Ctrl Pts',(28.9175541454242,-0.481384400712606,
30.4714297273205));
#69964=CARTESIAN_POINT('Ctrl Pts',(28.8652363337421,-0.340257481842474,
30.4616267985498));
#69965=CARTESIAN_POINT('Ctrl Pts',(28.815283295232,-0.0402726424447981,
30.4403556313474));
#69966=CARTESIAN_POINT('Ctrl Pts',(28.8202904087434,0.116033016014593,30.4292723919329));
#69967=CARTESIAN_POINT('Ctrl Pts',(28.8903942350679,0.41669295482916,30.4079533551363));
#69968=CARTESIAN_POINT('Ctrl Pts',(28.9543854043788,0.558153128819785,30.3985868124474));
#69969=CARTESIAN_POINT('Ctrl Pts',(29.1315478521803,0.806074678810529,30.3789179332106));
#69970=CARTESIAN_POINT('Ctrl Pts',(29.2421055811419,0.910792536064214,30.3684162008828));
#69971=CARTESIAN_POINT('Ctrl Pts',(29.5017160718709,1.07586594659562,30.3466216552675));
#69972=CARTESIAN_POINT('Ctrl Pts',(29.6495548172672,1.13268560353193,30.3355287526402));
#69973=CARTESIAN_POINT('Ctrl Pts',(29.9519945282947,1.1837871612187,30.3151448923318));
#69974=CARTESIAN_POINT('Ctrl Pts',(30.1031613914609,1.18026105601431,30.3063430973327));
#69975=CARTESIAN_POINT('Ctrl Pts',(30.3988201345177,1.11599305235349,30.2859088407808));
#69976=CARTESIAN_POINT('Ctrl Pts',(30.5402500629299,1.05480717912897,30.2750546900124));
#69977=CARTESIAN_POINT('Ctrl Pts',(30.7944347031296,0.879976451319597,30.2532473998958));
#69978=CARTESIAN_POINT('Ctrl Pts',(30.9040431118398,0.766951615348157,30.2425094496776));
#69979=CARTESIAN_POINT('Ctrl Pts',(31.0689753458081,0.510549117592882,30.223290918131));
#69980=CARTESIAN_POINT('Ctrl Pts',(31.1250271192607,0.371095429137332,30.2138134394961));
#69981=CARTESIAN_POINT('Ctrl Pts',(31.1830815580213,0.0732292938782705,
30.1926925042524));
#69982=CARTESIAN_POINT('Ctrl Pts',(31.1824563525586,-0.0827153416037653,
30.1816348640652));
#69983=CARTESIAN_POINT('Ctrl Pts',(31.1207993480439,-0.386085590380016,
30.1601236460354));
#69984=CARTESIAN_POINT('Ctrl Pts',(31.0601308144882,-0.530428613118422,
30.1504611573687));
#69985=CARTESIAN_POINT('Ctrl Pts',(30.8888193562276,-0.783487027384905,
30.1309694527541));
#69986=CARTESIAN_POINT('Ctrl Pts',(30.7812795445953,-0.890749011015136,
30.1205628449218));
#69987=CARTESIAN_POINT('Ctrl Pts',(30.5267682373962,-1.06214794901788,30.0988571647179));
#69988=CARTESIAN_POINT('Ctrl Pts',(30.3809100882996,-1.12274761000244,30.0877518706328));
#69989=CARTESIAN_POINT('Ctrl Pts',(30.1523604876879,-1.16783357423751,30.0721187053907));
#69990=CARTESIAN_POINT('Ctrl Pts',(30.0761915030069,-1.17524047358085,30.0671787429637));
#69991=CARTESIAN_POINT('Ctrl Pts',(30.,-1.17524047358085,30.0625));
#69992=CARTESIAN_POINT('Ctrl Pts',(29.9999999999996,-1.17524047358085,29.9999999999999));
#69993=CARTESIAN_POINT('Ctrl Pts',(30.1287289986958,-1.17524047358085,30.0079049483617));
#69994=CARTESIAN_POINT('Ctrl Pts',(30.2567455299606,-1.1540988796436,30.0165156942669));
#69995=CARTESIAN_POINT('Ctrl Pts',(30.5250941977629,-1.06268366593765,30.0362353726713));
#69996=CARTESIAN_POINT('Ctrl Pts',(30.659989580509,-0.984598569323181,30.0472873928126));
#69997=CARTESIAN_POINT('Ctrl Pts',(30.8878392789542,-0.78430373476697,30.0683803131598));
#69998=CARTESIAN_POINT('Ctrl Pts',(30.9799768519055,-0.665589512740196,
30.0778047289255));
#69999=CARTESIAN_POINT('Ctrl Pts',(31.1182025022512,-0.393869611947964,
30.0970717007283));
#70000=CARTESIAN_POINT('Ctrl Pts',(31.16052513775,-0.242215229337512,30.1078251299214));
#70001=CARTESIAN_POINT('Ctrl Pts',(31.183296750852,0.0653802899747305,30.1296359512119));
#70002=CARTESIAN_POINT('Ctrl Pts',(31.1648281646971,0.218291541355271,30.1404785017947));
#70003=CARTESIAN_POINT('Ctrl Pts',(31.0712608350547,0.506051914399227,30.1608828629668));
#70004=CARTESIAN_POINT('Ctrl Pts',(30.9980258995704,0.638460005209143,30.1696826775517));
#70005=CARTESIAN_POINT('Ctrl Pts',(30.8013405043472,0.873851821952036,30.1901061897083));
#70006=CARTESIAN_POINT('Ctrl Pts',(30.6777833777517,0.972810187954768,30.2012019893176));
#70007=CARTESIAN_POINT('Ctrl Pts',(30.4044625790663,1.11370354858798,30.222981179922));
#70008=CARTESIAN_POINT('Ctrl Pts',(30.2583590845709,1.15637148267232,30.2334657933678));
#70009=CARTESIAN_POINT('Ctrl Pts',(29.9547860481489,1.18442751029054,30.2531021983901));
#70010=CARTESIAN_POINT('Ctrl Pts',(29.8001302980418,1.16832333064129,30.2625187720286));
#70011=CARTESIAN_POINT('Ctrl Pts',(29.5050358022508,1.07710916045235,30.2838737217699));
#70012=CARTESIAN_POINT('Ctrl Pts',(29.3676216445827,1.00262104003874,30.2949528877718));
#70013=CARTESIAN_POINT('Ctrl Pts',(29.133885390368,0.808265735464436,30.3161967092816));
#70014=CARTESIAN_POINT('Ctrl Pts',(29.0384365029953,0.691955856048158,30.3259351581227));
#70015=CARTESIAN_POINT('Ctrl Pts',(28.8928615291795,0.423965303949737,30.3449376912299));
#70016=CARTESIAN_POINT('Ctrl Pts',(28.8464607134353,0.273539680594875,30.3556039922081));
#70017=CARTESIAN_POINT('Ctrl Pts',(28.8153257979048,-0.0336925494769084,
30.3773890535762));
#70018=CARTESIAN_POINT('Ctrl Pts',(28.8297608924994,-0.187447360914171,
30.3882914188718));
#70019=CARTESIAN_POINT('Ctrl Pts',(28.915763813331,-0.477469105343294,30.4088561281766));
#70020=CARTESIAN_POINT('Ctrl Pts',(28.9852090680907,-0.611342914279369,
30.4176917737044));
#70021=CARTESIAN_POINT('Ctrl Pts',(29.1753547758778,-0.851973319195576,
30.4378994263954));
#70022=CARTESIAN_POINT('Ctrl Pts',(29.296552814894,-0.954486386260336,30.4489763873607));
#70023=CARTESIAN_POINT('Ctrl Pts',(29.5667870728762,-1.10289061661543,30.4708323290802));
#70024=CARTESIAN_POINT('Ctrl Pts',(29.7121150852083,-1.14942616389095,30.4814064433112));
#70025=CARTESIAN_POINT('Ctrl Pts',(29.9080894843003,-1.17254804864973,30.4942605325068));
#70026=CARTESIAN_POINT('Ctrl Pts',(29.9540678655128,-1.17524047358085,30.497179414468));
#70027=CARTESIAN_POINT('Ctrl Pts',(29.9999999999996,-1.17524047358085,30.4999999999999));
#70028=CARTESIAN_POINT('Origin',(30.,-1.21864324187371E-14,15.78125));
#70029=CARTESIAN_POINT('',(30.8234078741651,-0.838564036615812,30.5625));
#70030=CARTESIAN_POINT('Ctrl Pts',(29.9999999999996,-1.17524047358085,30.4999999999999));
#70031=CARTESIAN_POINT('Ctrl Pts',(30.1063627165445,-1.17524047358085,30.506531487003));
#70032=CARTESIAN_POINT('Ctrl Pts',(30.2124142608556,-1.16080842479057,30.5135555357051));
#70033=CARTESIAN_POINT('Ctrl Pts',(30.4106617155444,-1.10559796456395,30.5276868678729));
#70034=CARTESIAN_POINT('Ctrl Pts',(30.5022820820407,-1.06709869288998,30.5346780045058));
#70035=CARTESIAN_POINT('Ctrl Pts',(30.673678737238,-0.968061456707972,30.5487143145253));
#70036=CARTESIAN_POINT('Ctrl Pts',(30.7527765496958,-0.90791877422844,30.555703810039));
#70037=CARTESIAN_POINT('Ctrl Pts',(30.823407874166,-0.83856403661491,30.5625000000001));
#70038=CARTESIAN_POINT('Origin',(30.,-1.56558793706907E-14,30.5625000000001));
#70039=CARTESIAN_POINT('Origin',(30.,-1.32966554433622E-14,16.));
#70040=CARTESIAN_POINT('Origin',(30.,-1.32966554433622E-14,16.));
#70041=CARTESIAN_POINT('',(31.2041934952953,-0.894381364904537,16.3247595264192));
#70042=CARTESIAN_POINT('Ctrl Pts',(29.1765921258349,-0.838564036615844,
16.));
#70043=CARTESIAN_POINT('Ctrl Pts',(29.2487520159976,-0.936812680701164,
16.0195455809545));
#70044=CARTESIAN_POINT('Ctrl Pts',(29.3353435467743,-1.0235639347367,16.039234228078));
#70045=CARTESIAN_POINT('Ctrl Pts',(29.5376779891223,-1.17276771461038,16.0788670880384));
#70046=CARTESIAN_POINT('Ctrl Pts',(29.6536089107031,-1.23245734148137,16.0985110228563));
#70047=CARTESIAN_POINT('Ctrl Pts',(29.9561347058367,-1.33132329595442,16.1436679915754));
#70048=CARTESIAN_POINT('Ctrl Pts',(30.1342881765676,-1.34356937043143,16.1651272257976));
#70049=CARTESIAN_POINT('Ctrl Pts',(30.4639364648848,-1.31596498262617,16.2103767681647));
#70050=CARTESIAN_POINT('Ctrl Pts',(30.6256204275016,-1.27296147517128,16.233574208582));
#70051=CARTESIAN_POINT('Ctrl Pts',(30.9367837613818,-1.12785658919505,16.2803666131763));
#70052=CARTESIAN_POINT('Ctrl Pts',(31.0819753809162,-1.0232586553723,16.3034869854933));
#70053=CARTESIAN_POINT('Ctrl Pts',(31.2041934952953,-0.894381364904556,
16.3247595264192));
#70054=CARTESIAN_POINT('',(30.2433378840047,-1.48013062741372,16.3247595264192));
#70055=CARTESIAN_POINT('Origin',(30.,-1.32966554433622E-14,16.3247595264192));
#70056=CARTESIAN_POINT('Ctrl Pts',(30.0000000000046,1.33373412263454,16.1584936490537));
#70057=CARTESIAN_POINT('Ctrl Pts',(29.9229566197526,1.33637706265986,16.161136589079));
#70058=CARTESIAN_POINT('Ctrl Pts',(29.8544450638259,1.33215454753135,16.163603109717));
#70059=CARTESIAN_POINT('Ctrl Pts',(29.6282514683273,1.30599264999734,16.1719556820851));
#70060=CARTESIAN_POINT('Ctrl Pts',(29.4645017898244,1.25493599443995,16.1785525854589));
#70061=CARTESIAN_POINT('Ctrl Pts',(29.1556314965168,1.0904442613039,16.1921322573206));
#70062=CARTESIAN_POINT('Ctrl Pts',(29.0151927695643,0.975180135374777,16.1989814826418));
#70063=CARTESIAN_POINT('Ctrl Pts',(28.7777605589636,0.68493937081347,16.2122079855113));
#70064=CARTESIAN_POINT('Ctrl Pts',(28.6970848553023,0.520026749838233,16.218047438772));
#70065=CARTESIAN_POINT('Ctrl Pts',(28.5955913245901,0.191124499754384,16.2305887595464));
#70066=CARTESIAN_POINT('Ctrl Pts',(28.5759298114947,0.010043627653028,16.2373963058958));
#70067=CARTESIAN_POINT('Ctrl Pts',(28.6063542045486,-0.355647637044131,
16.2509482038391));
#70068=CARTESIAN_POINT('Ctrl Pts',(28.6584675525716,-0.536586390481523,
16.2575508938686));
#70069=CARTESIAN_POINT('Ctrl Pts',(28.804769485922,-0.819110586341092,16.2677424893791));
#70070=CARTESIAN_POINT('Ctrl Pts',(28.9031317119719,-0.969713974958467,
16.273653025791));
#70071=CARTESIAN_POINT('Ctrl Pts',(29.199410976174,-1.23941646392093,16.2879449223019));
#70072=CARTESIAN_POINT('Ctrl Pts',(29.3637987944395,-1.33889148571261,16.2948596529243));
#70073=CARTESIAN_POINT('Ctrl Pts',(29.6508112528307,-1.44362228182862,16.3055460935814));
#70074=CARTESIAN_POINT('Ctrl Pts',(29.7632922636866,-1.47020844863719,16.3094443635539));
#70075=CARTESIAN_POINT('Ctrl Pts',(29.9994132050485,-1.49732183809384,16.3170683877131));
#70076=CARTESIAN_POINT('Ctrl Pts',(30.1229027402064,-1.49587628373705,16.3207589898335));
#70077=CARTESIAN_POINT('Ctrl Pts',(30.2433378840021,-1.48013062741405,16.3247595264191));
#70078=CARTESIAN_POINT('Origin',(30.,-1.32966554433622E-14,16.));
#70079=CARTESIAN_POINT('Ctrl Pts',(30.0000000000002,-1.50000000000001,16.8125));
#70080=CARTESIAN_POINT('Ctrl Pts',(29.8374309170617,-1.50000000000001,16.8046783913503));
#70081=CARTESIAN_POINT('Ctrl Pts',(29.6757197620765,-1.47357729444258,16.7961640957352));
#70082=CARTESIAN_POINT('Ctrl Pts',(29.3345753610171,-1.35867108066285,16.7765589388149));
#70083=CARTESIAN_POINT('Ctrl Pts',(29.1621497524653,-1.25967607222118,16.7655132465099));
#70084=CARTESIAN_POINT('Ctrl Pts',(28.8706191056789,-1.00528518925076,16.7444205583108));
#70085=CARTESIAN_POINT('Ctrl Pts',(28.7525289442937,-0.85433413605806,16.7349630075588));
#70086=CARTESIAN_POINT('Ctrl Pts',(28.5748830688675,-0.508513347476126,
16.7157507415264));
#70087=CARTESIAN_POINT('Ctrl Pts',(28.5201083225798,-0.315342861227666,
16.705019047846));
#70088=CARTESIAN_POINT('Ctrl Pts',(28.4893812381258,0.0768796360488758,
16.6832289091084));
#70089=CARTESIAN_POINT('Ctrl Pts',(28.5120877046559,0.272040866827356,16.6723866185096));
#70090=CARTESIAN_POINT('Ctrl Pts',(28.6297398561329,0.63947572665909,16.6519735707412));
#70091=CARTESIAN_POINT('Ctrl Pts',(28.7222788636186,0.808683440996407,16.6431776245867));
#70092=CARTESIAN_POINT('Ctrl Pts',(28.9715826684579,1.11011928821307,16.6228097717056));
#70093=CARTESIAN_POINT('Ctrl Pts',(29.1285972489479,1.2371944826493,16.6117255376675));
#70094=CARTESIAN_POINT('Ctrl Pts',(29.4764211128784,1.41875808710319,16.5899474207545));
#70095=CARTESIAN_POINT('Ctrl Pts',(29.6625283053455,1.47415762233606,16.5794544583034));
#70096=CARTESIAN_POINT('Ctrl Pts',(30.0492497355351,1.51196727264003,16.5597980467542));
#70097=CARTESIAN_POINT('Ctrl Pts',(30.2463054645629,1.49258742024928,16.5504437178179));
#70098=CARTESIAN_POINT('Ctrl Pts',(30.6231564270347,1.37865583779414,16.529147701253));
#70099=CARTESIAN_POINT('Ctrl Pts',(30.7990856424485,1.28470816478719,16.5180736453463));
#70100=CARTESIAN_POINT('Ctrl Pts',(31.0988336211311,1.03864170876325,16.4968168346638));
#70101=CARTESIAN_POINT('Ctrl Pts',(31.2215556301223,0.891049402060874,16.4870027445589));
#70102=CARTESIAN_POINT('Ctrl Pts',(31.4094506590971,0.550436181771672,16.4680797878762));
#70103=CARTESIAN_POINT('Ctrl Pts',(31.4699049158396,0.359005410515039,16.4574447450286));
#70104=CARTESIAN_POINT('Ctrl Pts',(31.5122933091642,-0.0326520383467692,
16.4356859978696));
#70105=CARTESIAN_POINT('Ctrl Pts',(31.4952196858866,-0.228959953862231,
16.4247800025632));
#70106=CARTESIAN_POINT('Ctrl Pts',(31.3881172406464,-0.599526626811694,
16.4041929651771));
#70107=CARTESIAN_POINT('Ctrl Pts',(31.300844426577,-0.770779121647004,16.3953430421646));
#70108=CARTESIAN_POINT('Ctrl Pts',(31.0690211851343,-1.06871793972269,16.3759133629805));
#70109=CARTESIAN_POINT('Ctrl Pts',(30.9276174608134,-1.1935139431374,16.3656435174717));
#70110=CARTESIAN_POINT('Ctrl Pts',(30.6058972740411,-1.3849221656676,16.3448478526983));
#70111=CARTESIAN_POINT('Ctrl Pts',(30.4282952255496,-1.44972308953241,16.3345029444933));
#70112=CARTESIAN_POINT('Ctrl Pts',(30.2433378840032,-1.48013062741398,16.3247595264191));
#70113=CARTESIAN_POINT('Ctrl Pts',(31.2041934952953,-0.894381364904531,
16.3247595264192));
#70114=CARTESIAN_POINT('Ctrl Pts',(31.2978308567217,-0.768308186313297,
16.33276668881));
#70115=CARTESIAN_POINT('Ctrl Pts',(31.3710758402094,-0.628345765505124,
16.3400919019164));
#70116=CARTESIAN_POINT('Ctrl Pts',(31.4735871865681,-0.324510524004584,
16.3569716375553));
#70117=CARTESIAN_POINT('Ctrl Pts',(31.5001727925959,-0.161986730686535,
16.3660007371841));
#70118=CARTESIAN_POINT('Ctrl Pts',(31.4997859079869,0.202485940247452,16.3862492189027));
#70119=CARTESIAN_POINT('Ctrl Pts',(31.4592164909323,0.401327421311596,16.3972959678507));
#70120=CARTESIAN_POINT('Ctrl Pts',(31.3063109849155,0.761415726638002,16.4173008737022));
#70121=CARTESIAN_POINT('Ctrl Pts',(31.1993149527403,0.920789441682028,16.4262087502572));
#70122=CARTESIAN_POINT('Ctrl Pts',(30.927737201713,1.19478997630558,16.4468861668575));
#70123=CARTESIAN_POINT('Ctrl Pts',(30.7642938567671,1.30539963746525,16.4578223290454));
#70124=CARTESIAN_POINT('Ctrl Pts',(30.4012071029328,1.45894804482998,16.4795565821721));
#70125=CARTESIAN_POINT('Ctrl Pts',(30.2045613271838,1.49922584611532,16.4901365342825));
#70126=CARTESIAN_POINT('Ctrl Pts',(29.8153532439137,1.50071981302521,16.5089038160006));
#70127=CARTESIAN_POINT('Ctrl Pts',(29.6264615866043,1.46518905889,16.5189388458803));
#70128=CARTESIAN_POINT('Ctrl Pts',(29.2652001883276,1.32257698188105,16.5402814895924));
#70129=CARTESIAN_POINT('Ctrl Pts',(29.0973517156097,1.21423683760981,16.5513665514533));
#70130=CARTESIAN_POINT('Ctrl Pts',(28.8152158635768,0.940440031832944,16.5725462857904));
#70131=CARTESIAN_POINT('Ctrl Pts',(28.7029935775965,0.778399491568193,16.5817555838018));
#70132=CARTESIAN_POINT('Ctrl Pts',(28.5479560175053,0.422736814401416,16.6015146214222));
#70133=CARTESIAN_POINT('Ctrl Pts',(28.5057189580682,0.232905312381588,16.6120608159788));
#70134=CARTESIAN_POINT('Ctrl Pts',(28.4951590610144,-0.159927799856357,
16.6338848777698));
#70135=CARTESIAN_POINT('Ctrl Pts',(28.5299387266544,-0.359247208886169,
16.6449581782715));
#70136=CARTESIAN_POINT('Ctrl Pts',(28.6722713443677,-0.723556115441905,
16.665197561969));
#70137=CARTESIAN_POINT('Ctrl Pts',(28.7749427214916,-0.886360478602884,
16.6740138619457));
#70138=CARTESIAN_POINT('Ctrl Pts',(29.0386829229376,-1.16785093047933,16.6945222475229));
#70139=CARTESIAN_POINT('Ctrl Pts',(29.1984334219549,-1.28276611305493,16.7054003353954));
#70140=CARTESIAN_POINT('Ctrl Pts',(29.5564186818177,-1.44663336596446,16.7271757773774));
#70141=CARTESIAN_POINT('Ctrl Pts',(29.7518446854206,-1.49263399091841,16.7378560104973));
#70142=CARTESIAN_POINT('Ctrl Pts',(29.9670564156215,-1.49972884223086,16.7484074688974));
#70143=CARTESIAN_POINT('Ctrl Pts',(29.9835330897433,-1.50000000000001,16.7492077354109));
#70144=CARTESIAN_POINT('Ctrl Pts',(30.,-1.50000000000001,16.75));
#70145=CARTESIAN_POINT('Origin',(27.4975425688509,1.03655180724329,15.7235432561772));
#70146=CARTESIAN_POINT('',(27.507537153458,1.0459948352816,31.5905494329235));
#70147=CARTESIAN_POINT('',(27.4979325782409,1.02280733953167,31.5905494329235));
#70148=CARTESIAN_POINT('Origin',(27.4975191258909,1.03656151763528,31.5962151370756));
#70149=CARTESIAN_POINT('',(27.4979325782409,1.02280733953167,33.8969505670765));
#70150=CARTESIAN_POINT('',(27.4979325782409,1.02280733953167,15.7235432561772));
#70151=CARTESIAN_POINT('',(27.507537153458,1.0459948352816,33.8969505670765));
#70152=CARTESIAN_POINT('Origin',(27.4975191258914,1.03656151763504,33.891284862925));
#70153=CARTESIAN_POINT('',(27.507537153458,1.0459948352816,15.7235432561772));
#70154=CARTESIAN_POINT('Origin',(27.4239298924869,0.837015916807854,15.7235432561772));
#70155=CARTESIAN_POINT('',(27.4331527756843,0.847214001212616,31.5905494329235));
#70156=CARTESIAN_POINT('',(27.4253970781159,0.823344418487269,31.5905494329235));
#70157=CARTESIAN_POINT('Origin',(27.4239057599253,0.837023757952457,31.5962151370753));
#70158=CARTESIAN_POINT('',(27.4253970781159,0.823344418487269,33.8969505670765));
#70159=CARTESIAN_POINT('',(27.4253970781159,0.823344418487269,15.7235432561772));
#70160=CARTESIAN_POINT('',(27.4331527756843,0.847214001212616,33.8969505670765));
#70161=CARTESIAN_POINT('Origin',(27.4239057599256,0.837023757952334,33.8912848629251));
#70162=CARTESIAN_POINT('',(27.4331527756843,0.847214001212616,15.7235432561772));
#70163=CARTESIAN_POINT('Origin',(27.3661995449658,0.632319544909263,15.7235432561772));
#70164=CARTESIAN_POINT('',(27.3745938646118,0.643209811098917,31.5905494329235));
#70165=CARTESIAN_POINT('',(27.3687348611468,0.618805305313091,31.5905494329235));
#70166=CARTESIAN_POINT('Origin',(27.3661748715877,0.632325468463276,31.5962151370755));
#70167=CARTESIAN_POINT('',(27.3687348611468,0.618805305313091,33.8969505670765));
#70168=CARTESIAN_POINT('',(27.3687348611468,0.618805305313091,15.7235432561772));
#70169=CARTESIAN_POINT('',(27.3745938646118,0.643209811098917,33.8969505670765));
#70170=CARTESIAN_POINT('Origin',(27.3661748715881,0.632325468463155,33.891284862925));
#70171=CARTESIAN_POINT('',(27.3745938646118,0.643209811098917,15.7235432561772));
#70172=CARTESIAN_POINT('Origin',(27.3247074530776,0.423724712748722,15.7235432561772));
#70173=CARTESIAN_POINT('',(27.3322214554001,0.435240018610828,31.5905494329235));
#70174=CARTESIAN_POINT('',(27.328295268743,0.410451051658016,31.5905494329235));
#70175=CARTESIAN_POINT('Origin',(27.3246823910025,0.423728682191457,31.5962151370754));
#70176=CARTESIAN_POINT('',(27.328295268743,0.410451051658016,33.8969505670765));
#70177=CARTESIAN_POINT('',(27.328295268743,0.410451051658016,15.7235432561772));
#70178=CARTESIAN_POINT('',(27.3322214554001,0.435240018610828,33.8969505670765));
#70179=CARTESIAN_POINT('Origin',(27.3246823910029,0.423728682191396,33.891284862925));
#70180=CARTESIAN_POINT('',(27.3322214554001,0.435240018610828,15.7235432561772));
#70181=CARTESIAN_POINT('Origin',(27.2997094293662,0.212517476831317,15.7235432561772));
#70182=CARTESIAN_POINT('',(27.3062967880422,0.224586826676008,31.5905494329235));
#70183=CARTESIAN_POINT('',(27.3043276244395,0.199566230780642,31.5905494329235));
#70184=CARTESIAN_POINT('Origin',(27.2996841331102,0.212519467689854,31.5962151370755));
#70185=CARTESIAN_POINT('',(27.3043276244395,0.199566230780642,33.8969505670765));
#70186=CARTESIAN_POINT('',(27.3043276244395,0.199566230780642,15.7235432561772));
#70187=CARTESIAN_POINT('',(27.3062967880422,0.224586826676008,33.8969505670765));
#70188=CARTESIAN_POINT('Origin',(27.2996841331108,0.212519467689809,33.8912848629251));
#70189=CARTESIAN_POINT('',(27.3062967880422,0.224586826676008,15.7235432561772));
#70190=CARTESIAN_POINT('Origin',(27.2913595949605,1.54398896472578E-14,
15.7235432561772));
#70191=CARTESIAN_POINT('',(27.2969796967333,0.0125489822720319,31.5905494329235));
#70192=CARTESIAN_POINT('',(27.2969796967333,-0.0125489822720016,31.5905494329235));
#70193=CARTESIAN_POINT('Origin',(27.2913342204835,1.66533453693773E-14,
31.5962151370755));
#70194=CARTESIAN_POINT('',(27.2969796967333,-0.0125489822720016,33.8969505670765));
#70195=CARTESIAN_POINT('',(27.2969796967333,-0.0125489822720016,15.7235432561772));
#70196=CARTESIAN_POINT('',(27.2969796967333,0.0125489822720319,33.8969505670765));
#70197=CARTESIAN_POINT('Origin',(27.2913342204839,1.44047100636424E-14,
33.891284862925));
#70198=CARTESIAN_POINT('',(27.2969796967333,0.0125489822720319,15.7235432561772));
#70199=CARTESIAN_POINT('Origin',(27.5865837274296,1.22969701109861,15.7235432561772));
#70200=CARTESIAN_POINT('',(27.5972883935087,1.23832676336248,31.5905494329235));
#70201=CARTESIAN_POINT('',(27.5858941560429,1.2159643132099,31.5905494329235));
#70202=CARTESIAN_POINT('Origin',(27.586561118605,1.22970853087013,31.5962151370754));
#70203=CARTESIAN_POINT('',(27.5858941560429,1.2159643132099,33.8969505670765));
#70204=CARTESIAN_POINT('',(27.5858941560429,1.2159643132099,15.7235432561772));
#70205=CARTESIAN_POINT('',(27.5972883935087,1.23832676336248,33.8969505670765));
#70206=CARTESIAN_POINT('Origin',(27.5865611186055,1.22970853086989,33.891284862925));
#70207=CARTESIAN_POINT('',(27.5972883935087,1.23832676336248,15.7235432561772));
#70208=CARTESIAN_POINT('Origin',(27.690504399871,1.41526072396476,15.7235432561772));
#70209=CARTESIAN_POINT('',(27.701853149596,1.42302399516181,31.5905494329235));
#70210=CARTESIAN_POINT('',(27.6887394991445,1.40162446254803,31.5905494329235));
#70211=CARTESIAN_POINT('Origin',(27.6904827645727,1.41527398209261,31.5962151370755));
#70212=CARTESIAN_POINT('',(27.6887394991445,1.40162446254803,33.8969505670765));
#70213=CARTESIAN_POINT('',(27.6887394991445,1.40162446254803,15.7235432561772));
#70214=CARTESIAN_POINT('',(27.701853149596,1.42302399516181,33.8969505670765));
#70215=CARTESIAN_POINT('Origin',(27.6904827645732,1.41527398209234,33.891284862925));
#70216=CARTESIAN_POINT('',(27.701853149596,1.42302399516181,15.7235432561772));
#70217=CARTESIAN_POINT('Origin',(27.8086638806724,1.59209888384573,15.7235432561772));
#70218=CARTESIAN_POINT('',(27.8205867452275,1.59894781082746,31.5905494329235));
#70219=CARTESIAN_POINT('',(27.805834531806,1.57864313098712,31.5905494329235));
#70220=CARTESIAN_POINT('Origin',(27.8086433522893,1.59211379858911,31.5962151370755));
#70221=CARTESIAN_POINT('',(27.805834531806,1.57864313098712,33.8969505670765));
#70222=CARTESIAN_POINT('',(27.805834531806,1.57864313098712,15.7235432561772));
#70223=CARTESIAN_POINT('',(27.8205867452275,1.59894781082746,33.8969505670765));
#70224=CARTESIAN_POINT('Origin',(27.8086433522896,1.59211379858882,33.8912848629251));
#70225=CARTESIAN_POINT('',(27.8205867452275,1.59894781082746,15.7235432561772));
#70226=CARTESIAN_POINT('Origin',(27.9403336773427,1.75912122468118,15.7235432561772));
#70227=CARTESIAN_POINT('',(27.9527571483031,1.76501358153527,31.5905494329235));
#70228=CARTESIAN_POINT('',(27.9364573242129,1.74592893957157,31.5905494329235));
#70229=CARTESIAN_POINT('Origin',(27.9403143824389,1.75913770408581,31.5962151370755));
#70230=CARTESIAN_POINT('',(27.9364573242129,1.74592893957157,33.8969505670765));
#70231=CARTESIAN_POINT('',(27.9364573242129,1.74592893957157,15.7235432561772));
#70232=CARTESIAN_POINT('',(27.9527571483031,1.76501358153527,33.8969505670765));
#70233=CARTESIAN_POINT('Origin',(27.9403143824393,1.75913770408551,33.891284862925));
#70234=CARTESIAN_POINT('',(27.9527571483031,1.76501358153527,15.7235432561772));
#70235=CARTESIAN_POINT('Origin',(28.0847020018007,1.9152979981993,15.7235432561772));
#70236=CARTESIAN_POINT('',(28.0975494843367,1.92019745658633,31.5905494329235));
#70237=CARTESIAN_POINT('',(28.0798025434137,1.90245051566326,31.5905494329235));
#70238=CARTESIAN_POINT('Origin',(28.0846840593359,1.9153159406641,31.5962151370755));
#70239=CARTESIAN_POINT('',(28.0798025434137,1.90245051566326,33.8969505670765));
#70240=CARTESIAN_POINT('',(28.0798025434137,1.90245051566326,15.7235432561772));
#70241=CARTESIAN_POINT('',(28.0975494843367,1.92019745658633,33.8969505670765));
#70242=CARTESIAN_POINT('Origin',(28.0846840593363,1.91531594066375,33.891284862925));
#70243=CARTESIAN_POINT('',(28.0975494843367,1.92019745658633,15.7235432561772));
#70244=CARTESIAN_POINT('Origin',(28.2408787753188,2.05966632265731,15.7235432561772));
#70245=CARTESIAN_POINT('',(28.2540710604285,2.06354267578708,31.5905494329235));
#70246=CARTESIAN_POINT('',(28.2349864184648,2.0472428516969,31.5905494329235));
#70247=CARTESIAN_POINT('Origin',(28.2408622959143,2.05968561756092,31.5962151370754));
#70248=CARTESIAN_POINT('',(28.2349864184648,2.0472428516969,33.8969505670765));
#70249=CARTESIAN_POINT('',(28.2349864184648,2.0472428516969,15.7235432561772));
#70250=CARTESIAN_POINT('',(28.2540710604285,2.06354267578708,33.8969505670765));
#70251=CARTESIAN_POINT('Origin',(28.2408622959145,2.05968561756065,33.891284862925));
#70252=CARTESIAN_POINT('',(28.2540710604285,2.06354267578708,15.7235432561772));
#70253=CARTESIAN_POINT('Origin',(28.4079011161543,2.19133611932758,15.7235432561772));
#70254=CARTESIAN_POINT('',(28.4213568690129,2.19416546819404,31.5905494329235));
#70255=CARTESIAN_POINT('',(28.4010521891726,2.1794132547725,31.5905494329235));
#70256=CARTESIAN_POINT('Origin',(28.407886201411,2.19135664771063,31.5962151370753));
#70257=CARTESIAN_POINT('',(28.4010521891726,2.1794132547725,33.8969505670765));
#70258=CARTESIAN_POINT('',(28.4010521891726,2.1794132547725,15.7235432561772));
#70259=CARTESIAN_POINT('',(28.4213568690129,2.19416546819404,33.8969505670765));
#70260=CARTESIAN_POINT('Origin',(28.4078862014112,2.19135664771024,33.8912848629252));
#70261=CARTESIAN_POINT('',(28.4213568690129,2.19416546819404,15.7235432561772));
#70262=CARTESIAN_POINT('Origin',(28.5847392760353,2.309495600129,15.7235432561772));
#70263=CARTESIAN_POINT('',(28.598375537452,2.31126050085552,31.5905494329235));
#70264=CARTESIAN_POINT('',(28.5769760048382,2.29814685040398,31.5905494329235));
#70265=CARTESIAN_POINT('Origin',(28.5847260179075,2.30951723542729,31.5962151370754));
#70266=CARTESIAN_POINT('',(28.5769760048382,2.29814685040398,33.8969505670765));
#70267=CARTESIAN_POINT('',(28.5769760048382,2.29814685040398,15.7235432561772));
#70268=CARTESIAN_POINT('',(28.598375537452,2.31126050085552,33.8969505670765));
#70269=CARTESIAN_POINT('Origin',(28.5847260179077,2.30951723542689,33.891284862925));
#70270=CARTESIAN_POINT('',(28.598375537452,2.31126050085552,15.7235432561772));
#70271=CARTESIAN_POINT('Origin',(28.7703029889014,2.4134162725704,15.7235432561772));
#70272=CARTESIAN_POINT('',(28.7840356867901,2.41410584395713,31.5905494329235));
#70273=CARTESIAN_POINT('',(28.7616732366375,2.40271160649133,31.5905494329235));
#70274=CARTESIAN_POINT('Origin',(28.7702914691299,2.41343888139489,31.5962151370753));
#70275=CARTESIAN_POINT('',(28.7616732366375,2.40271160649133,33.8969505670765));
#70276=CARTESIAN_POINT('',(28.7616732366375,2.40271160649133,15.7235432561772));
#70277=CARTESIAN_POINT('',(28.7840356867901,2.41410584395713,33.8969505670765));
#70278=CARTESIAN_POINT('Origin',(28.7702914691301,2.41343888139455,33.8912848629251));
#70279=CARTESIAN_POINT('',(28.7840356867901,2.41410584395713,15.7235432561772));
#70280=CARTESIAN_POINT('Origin',(30.,-1.32966554433622E-14,34.));
#70281=CARTESIAN_POINT('',(28.75,0.721687836487017,33.8917468245269));
#70282=CARTESIAN_POINT('',(28.75,-1.44824191072421E-14,33.6983711515529));
#70283=CARTESIAN_POINT('Ctrl Pts',(28.75,0.72168783648698,33.8917468245269));
#70284=CARTESIAN_POINT('Ctrl Pts',(28.75,0.334936490538873,33.6983711515529));
#70285=CARTESIAN_POINT('Ctrl Pts',(28.75,-1.55145598201422E-14,33.6983711515529));
#70286=CARTESIAN_POINT('',(30.,1.44337567297405,33.8917468245269));
#70287=CARTESIAN_POINT('Ctrl Pts',(30.,1.44337567297404,33.8917468245269));
#70288=CARTESIAN_POINT('Ctrl Pts',(29.375,1.08253175473053,33.5309029062834));
#70289=CARTESIAN_POINT('Ctrl Pts',(28.75,0.721687836487025,33.8917468245269));
#70290=CARTESIAN_POINT('',(31.25,0.721687836487017,33.891746824527));
#70291=CARTESIAN_POINT('Ctrl Pts',(31.25,0.721687836487027,33.8917468245269));
#70292=CARTESIAN_POINT('Ctrl Pts',(30.625,1.08253175473053,33.5309029062834));
#70293=CARTESIAN_POINT('Ctrl Pts',(30.,1.44337567297404,33.8917468245269));
#70294=CARTESIAN_POINT('',(31.25,-0.72168783648704,33.8917468245269));
#70295=CARTESIAN_POINT('Ctrl Pts',(31.25,-0.721687836487026,33.8917468245269));
#70296=CARTESIAN_POINT('Ctrl Pts',(31.25,-1.26287869051112E-14,33.5309029062834));
#70297=CARTESIAN_POINT('Ctrl Pts',(31.25,0.721687836487001,33.8917468245269));
#70298=CARTESIAN_POINT('',(30.,-1.44337567297407,33.8917468245269));
#70299=CARTESIAN_POINT('Ctrl Pts',(30.,-1.44337567297406,33.8917468245269));
#70300=CARTESIAN_POINT('Ctrl Pts',(30.625,-1.08253175473056,33.5309029062834));
#70301=CARTESIAN_POINT('Ctrl Pts',(31.25,-0.721687836487049,33.8917468245269));
#70302=CARTESIAN_POINT('',(28.75,-0.721687836487044,33.8917468245269));
#70303=CARTESIAN_POINT('Ctrl Pts',(28.75,-0.721687836487053,33.8917468245269));
#70304=CARTESIAN_POINT('Ctrl Pts',(29.375,-1.08253175473056,33.5309029062834));
#70305=CARTESIAN_POINT('Ctrl Pts',(30.,-1.44337567297406,33.8917468245269));
#70306=CARTESIAN_POINT('Ctrl Pts',(28.75,-1.55145598201422E-14,33.6983711515529));
#70307=CARTESIAN_POINT('Ctrl Pts',(28.75,-0.334936490538901,33.6983711515529));
#70308=CARTESIAN_POINT('Ctrl Pts',(28.75,-0.721687836487005,33.8917468245269));
#70309=CARTESIAN_POINT('',(28.4483711515529,-1.34873480853811E-14,34.));
#70310=CARTESIAN_POINT('',(28.4483711515529,-1.34873480853811E-14,34.));
#70311=CARTESIAN_POINT('Origin',(30.,-1.32966554433622E-14,34.));
#70312=CARTESIAN_POINT('Origin',(30.,-1.32966554433622E-14,33.953125));
#70313=CARTESIAN_POINT('',(30.,-2.6137293696319,33.9862706303681));
#70314=CARTESIAN_POINT('Origin',(30.,-1.32966554433622E-14,33.9862706303681));
#70315=CARTESIAN_POINT('',(30.,-2.58058373926378,34.));
#70316=CARTESIAN_POINT('Origin',(30.,-2.58058373926378,33.953125));
#70317=CARTESIAN_POINT('Origin',(30.,-1.32966554433622E-14,34.));
#70318=CARTESIAN_POINT('Origin',(30.,-1.32966554433622E-14,33.8637293696319));
#70319=CARTESIAN_POINT('',(30.012548982272,-2.70302030326669,33.8969505670765));
#70320=CARTESIAN_POINT('',(30.,-2.69489040503949,33.9051095949605));
#70321=CARTESIAN_POINT('Ctrl Pts',(30.012548982272,-2.70302030326672,33.8969505670765));
#70322=CARTESIAN_POINT('Ctrl Pts',(30.0117595027242,-2.70125749446881,33.8987170220581));
#70323=CARTESIAN_POINT('Ctrl Pts',(30.0105608813139,-2.69960157002983,33.9003782103613));
#70324=CARTESIAN_POINT('Ctrl Pts',(30.0079476416933,-2.69733049287042,33.9026580100842));
#70325=CARTESIAN_POINT('Ctrl Pts',(30.0065751610721,-2.69644647069985,33.9035459832655));
#70326=CARTESIAN_POINT('Ctrl Pts',(30.0034509360646,-2.69522714758869,33.9047710768107));
#70327=CARTESIAN_POINT('Ctrl Pts',(30.0017003028408,-2.69489040503949,33.9051095949605));
#70328=CARTESIAN_POINT('Ctrl Pts',(30.,-2.69489040503949,33.9051095949605));
#70329=CARTESIAN_POINT('',(30.027378900953,-2.73613365141358,33.8637293696319));
#70330=CARTESIAN_POINT('Ctrl Pts',(30.0273789009518,-2.73613365141079,33.8637293696347));
#70331=CARTESIAN_POINT('Ctrl Pts',(30.019918653996,-2.71947585577342,33.8804609779984));
#70332=CARTESIAN_POINT('Ctrl Pts',(30.0125489822686,-2.70302030325915,33.8969505670841));
#70333=CARTESIAN_POINT('',(30.1873800711417,-2.72984718831552,33.8637293696319));
#70334=CARTESIAN_POINT('Origin',(30.,-1.32966554433622E-14,33.8637293696319));
#70335=CARTESIAN_POINT('',(30.1995662307806,-2.69567237556051,33.8969505670765));
#70336=CARTESIAN_POINT('Ctrl Pts',(30.1995662307834,-2.69567237555272,33.8969505670841));
#70337=CARTESIAN_POINT('Ctrl Pts',(30.1935103650644,-2.71265541886991,33.8804609779983));
#70338=CARTESIAN_POINT('Ctrl Pts',(30.1873800711428,-2.72984718831265,33.8637293696347));
#70339=CARTESIAN_POINT('',(30.224586826676,-2.69370321195777,33.8969505670765));
#70340=CARTESIAN_POINT('Origin',(30.2125187883694,-2.70030745889015,33.8912937927563));
#70341=CARTESIAN_POINT('',(30.241969073019,-2.72555094069392,33.8637293696319));
#70342=CARTESIAN_POINT('Ctrl Pts',(30.2419690730176,-2.72555094069121,33.8637293696347));
#70343=CARTESIAN_POINT('Ctrl Pts',(30.233224867931,-2.70952981970859,33.8804609779984));
#70344=CARTESIAN_POINT('Ctrl Pts',(30.2245868266721,-2.69370321195052,33.8969505670841));
#70345=CARTESIAN_POINT('',(30.4009837827878,-2.70673030953518,33.8637293696319));
#70346=CARTESIAN_POINT('Origin',(30.,-1.32966554433622E-14,33.8637293696319));
#70347=CARTESIAN_POINT('',(30.410451051658,-2.67170473125697,33.8969505670765));
#70348=CARTESIAN_POINT('Ctrl Pts',(30.4104510516601,-2.67170473124899,33.8969505670841));
#70349=CARTESIAN_POINT('Ctrl Pts',(30.4057463283755,-2.68911055925959,33.8804609779983));
#70350=CARTESIAN_POINT('Ctrl Pts',(30.4009837827886,-2.70673030953223,33.8637293696347));
#70351=CARTESIAN_POINT('',(30.4352400186108,-2.66777854459992,33.8969505670765));
#70352=CARTESIAN_POINT('Origin',(30.4237273077484,-2.67530902338216,33.8912940899387));
#70353=CARTESIAN_POINT('',(30.455067425287,-2.69816430208722,33.8637293696319));
#70354=CARTESIAN_POINT('Ctrl Pts',(30.4550674252854,-2.69816430208464,33.8637293696347));
#70355=CARTESIAN_POINT('Ctrl Pts',(30.445093173,-2.68287863129519,33.8804609779983));
#70356=CARTESIAN_POINT('Ctrl Pts',(30.4352400186063,-2.667778544593,33.8969505670841));
#70357=CARTESIAN_POINT('',(30.6121152960723,-2.66692553831739,33.8637293696319));
#70358=CARTESIAN_POINT('Origin',(30.,-1.32966554433622E-14,33.8637293696319));
#70359=CARTESIAN_POINT('',(30.618805305313,-2.63126513885325,33.8969505670765));
#70360=CARTESIAN_POINT('Ctrl Pts',(30.6188053053145,-2.63126513884514,33.8969505670841));
#70361=CARTESIAN_POINT('Ctrl Pts',(30.6154807306477,-2.64898643883144,33.8804609779984));
#70362=CARTESIAN_POINT('Ctrl Pts',(30.6121152960728,-2.66692553831439,33.8637293696347));
#70363=CARTESIAN_POINT('',(30.6432098110989,-2.62540613538822,33.8969505670765));
#70364=CARTESIAN_POINT('Origin',(30.6323233823986,-2.63381649164655,33.8912943077151));
#70365=CARTESIAN_POINT('',(30.6653601355529,-2.65414258332748,33.8637293696319));
#70366=CARTESIAN_POINT('Ctrl Pts',(30.665360135551,-2.65414258332505,33.8637293696347));
#70367=CARTESIAN_POINT('Ctrl Pts',(30.6542173306489,-2.63968660397218,33.8804609779983));
#70368=CARTESIAN_POINT('Ctrl Pts',(30.6432098110939,-2.62540613538168,33.8969505670841));
#70369=CARTESIAN_POINT('',(30.8194729150075,-2.61067828431314,33.8637293696319));
#70370=CARTESIAN_POINT('Origin',(30.,-1.32966554433622E-14,33.8637293696319));
#70371=CARTESIAN_POINT('',(30.8233444184872,-2.57460292188405,33.8969505670765));
#70372=CARTESIAN_POINT('Ctrl Pts',(30.8233444184881,-2.57460292187584,33.8969505670841));
#70373=CARTESIAN_POINT('Ctrl Pts',(30.8214204895475,-2.59253043613051,33.8804609779984));
#70374=CARTESIAN_POINT('Ctrl Pts',(30.8194729150079,-2.61067828431011,33.8637293696347));
#70375=CARTESIAN_POINT('',(30.8472140012126,-2.56684722431573,33.8969505670765));
#70376=CARTESIAN_POINT('Origin',(30.837020957759,-2.57608565616367,33.891294472568));
#70377=CARTESIAN_POINT('',(30.8715506793283,-2.59375719294955,33.8637293696319));
#70378=CARTESIAN_POINT('Ctrl Pts',(30.8715506793263,-2.59375719294726,33.8637293696347));
#70379=CARTESIAN_POINT('Ctrl Pts',(30.8593080209051,-2.58022003095079,33.8804609779983));
#70380=CARTESIAN_POINT('Ctrl Pts',(30.8472140012071,-2.5668472243096,33.8969505670841));
#70381=CARTESIAN_POINT('',(31.0217782109194,-2.53833533054748,33.8637293696319));
#70382=CARTESIAN_POINT('Origin',(30.,-1.32966554433622E-14,33.8637293696319));
#70383=CARTESIAN_POINT('',(31.0228073395316,-2.5020674217591,33.8969505670765));
#70384=CARTESIAN_POINT('Ctrl Pts',(31.0228073395319,-2.50206742175084,33.8969505670841));
#70385=CARTESIAN_POINT('Ctrl Pts',(31.0222959179792,-2.52009062118698,33.8804609779983));
#70386=CARTESIAN_POINT('Ctrl Pts',(31.0217782109195,-2.53833533054442,33.8637293696347));
#70387=CARTESIAN_POINT('',(31.0459948352815,-2.49246284654201,33.8969505670765));
#70388=CARTESIAN_POINT('Origin',(31.0365580110689,-2.50247243285094,33.8912946002427));
#70389=CARTESIAN_POINT('',(31.0723678233457,-2.51738042696529,33.8637293696319));
#70390=CARTESIAN_POINT('Ctrl Pts',(31.0723678233435,-2.51738042696321,33.8637293696347));
#70391=CARTESIAN_POINT('Ctrl Pts',(31.0591007914634,-2.5048455434284,33.8804609779984));
#70392=CARTESIAN_POINT('Ctrl Pts',(31.0459948352755,-2.49246284653634,33.8969505670841));
#70393=CARTESIAN_POINT('',(31.2177839043851,-2.45034269538684,33.8637293696319));
#70394=CARTESIAN_POINT('Origin',(30.,-1.32966554433622E-14,33.8637293696319));
#70395=CARTESIAN_POINT('',(31.2159643132098,-2.41410584395714,33.8969505670765));
#70396=CARTESIAN_POINT('Ctrl Pts',(31.2159643132094,-2.4141058439489,33.8969505670841));
#70397=CARTESIAN_POINT('Ctrl Pts',(31.2168685521286,-2.43211360954869,33.8804609779984));
#70398=CARTESIAN_POINT('Ctrl Pts',(31.2177839043849,-2.4503426953838,33.8637293696347));
#70399=CARTESIAN_POINT('',(31.2383267633624,-2.40271160649135,33.8969505670765));
#70400=CARTESIAN_POINT('Origin',(31.2297043338602,-2.41343066267494,33.891294700665));
#70401=CARTESIAN_POINT('',(31.2665734631337,-2.42548317353486,33.8637293696319));
#70402=CARTESIAN_POINT('Ctrl Pts',(31.2665734631313,-2.42548317353296,33.8637293696347));
#70403=CARTESIAN_POINT('Ctrl Pts',(31.2523638534557,-2.41402785018508,33.8804609779983));
#70404=CARTESIAN_POINT('Ctrl Pts',(31.238326763356,-2.40271160648617,33.8969505670841));
#70405=CARTESIAN_POINT('',(31.4062815551261,-2.34724288268751,33.8637293696319));
#70406=CARTESIAN_POINT('Origin',(30.,-1.32966554433622E-14,33.8637293696319));
#70407=CARTESIAN_POINT('',(31.401624462548,-2.31126050085554,33.8969505670765));
#70408=CARTESIAN_POINT('Ctrl Pts',(31.4016244625469,-2.31126050084735,33.8969505670841));
#70409=CARTESIAN_POINT('Ctrl Pts',(31.4039387870044,-2.32914180874765,33.8804609779983));
#70410=CARTESIAN_POINT('Ctrl Pts',(31.4062815551258,-2.34724288268448,33.8637293696347));
#70411=CARTESIAN_POINT('',(31.4230239951618,-2.29814685040399,33.8969505670765));
#70412=CARTESIAN_POINT('Origin',(31.4152691174526,-2.30950931155476,33.8912947803757));
#70413=CARTESIAN_POINT('',(31.452970256343,-2.31863200978458,33.8637293696319));
#70414=CARTESIAN_POINT('Ctrl Pts',(31.4529702563405,-2.31863200978284,33.8637293696347));
#70415=CARTESIAN_POINT('Ctrl Pts',(31.4379056758382,-2.30832687249962,33.8804609779984));
#70416=CARTESIAN_POINT('Ctrl Pts',(31.423023995155,-2.29814685039932,33.8969505670841));
#70417=CARTESIAN_POINT('',(31.5861090124437,-2.22967153707895,33.8637293696319));
#70418=CARTESIAN_POINT('Origin',(30.,-1.32966554433622E-14,33.8637293696319));
#70419=CARTESIAN_POINT('',(31.5786431309871,-2.19416546819406,33.8969505670765));
#70420=CARTESIAN_POINT('Ctrl Pts',(31.5786431309854,-2.19416546818597,33.8969505670841));
#70421=CARTESIAN_POINT('Ctrl Pts',(31.5823532724012,-2.21181007417745,33.8804609779984));
#70422=CARTESIAN_POINT('Ctrl Pts',(31.5861090124431,-2.22967153707596,33.8637293696347));
#70423=CARTESIAN_POINT('',(31.5989478108274,-2.17941325477251,33.8969505670765));
#70424=CARTESIAN_POINT('Origin',(31.5921082951429,-2.19134908471607,33.891294843835));
#70425=CARTESIAN_POINT('',(31.6304090047603,-2.1974857086706,33.8637293696319));
#70426=CARTESIAN_POINT('Ctrl Pts',(31.6304090047577,-2.19748570866908,33.8637293696347));
#70427=CARTESIAN_POINT('Ctrl Pts',(31.6145823315769,-2.18839429204867,33.8804609779984));
#70428=CARTESIAN_POINT('Ctrl Pts',(31.5989478108202,-2.1794132547684,33.8969505670841));
#70429=CARTESIAN_POINT('',(31.7561575802648,-2.09835352500328,33.8637293696319));
#70430=CARTESIAN_POINT('Origin',(30.,-1.32966554433622E-14,33.8637293696319));
#70431=CARTESIAN_POINT('',(31.7459289395715,-2.0635426757871,33.8969505670765));
#70432=CARTESIAN_POINT('Ctrl Pts',(31.7459289395692,-2.06354267577917,33.8969505670841));
#70433=CARTESIAN_POINT('Ctrl Pts',(31.7510120236878,-2.08084179499847,33.8804609779983));
#70434=CARTESIAN_POINT('Ctrl Pts',(31.7561575802639,-2.09835352500035,33.8637293696347));
#70435=CARTESIAN_POINT('',(31.7650135815352,-2.04724285169692,33.8969505670765));
#70436=CARTESIAN_POINT('Origin',(31.7591315960217,-2.05967847590834,33.8912948941586));
#70437=CARTESIAN_POINT('',(31.7977957394973,-2.06279117742452,33.8637293696319));
#70438=CARTESIAN_POINT('Ctrl Pts',(31.7977957394945,-2.06279117742322,33.8637293696347));
#70439=CARTESIAN_POINT('Ctrl Pts',(31.7813045503384,-2.05496953307228,33.8804609779984));
#70440=CARTESIAN_POINT('Ctrl Pts',(31.7650135815277,-2.04724285169338,33.8969505670841));
#70441=CARTESIAN_POINT('',(31.9153788526219,-1.9540984656726,33.8637293696319));
#70442=CARTESIAN_POINT('Origin',(30.,-1.32966554433622E-14,33.8637293696319));
#70443=CARTESIAN_POINT('',(31.9024505156632,-1.92019745658634,33.8969505670765));
#70444=CARTESIAN_POINT('Ctrl Pts',(31.9024505156603,-1.92019745657863,33.8969505670841));
#70445=CARTESIAN_POINT('Ctrl Pts',(31.9088752035777,-1.93704443420321,33.8804609779984));
#70446=CARTESIAN_POINT('Ctrl Pts',(31.9153788526208,-1.95409846566976,33.8637293696347));
#70447=CARTESIAN_POINT('',(31.9201974565863,-1.90245051566327,33.8969505670765));
#70448=CARTESIAN_POINT('Origin',(31.9153092670123,-1.91530927561705,33.891294933562));
#70449=CARTESIAN_POINT('',(31.9540984656725,-1.91537885262194,33.8637293696319));
#70450=CARTESIAN_POINT('Ctrl Pts',(31.9540984656697,-1.91537885262084,33.8637293696347));
#70451=CARTESIAN_POINT('Ctrl Pts',(31.9370444342032,-1.90887520357777,33.8804609779984));
#70452=CARTESIAN_POINT('Ctrl Pts',(31.9201974565786,-1.90245051566033,33.8969505670841));
#70453=CARTESIAN_POINT('',(32.0627911774245,-1.79779573949737,33.8637293696319));
#70454=CARTESIAN_POINT('Origin',(30.,-1.32966554433622E-14,33.8637293696319));
#70455=CARTESIAN_POINT('',(32.0472428516969,-1.76501358153528,33.8969505670765));
#70456=CARTESIAN_POINT('Ctrl Pts',(32.0472428516934,-1.76501358152781,33.8969505670841));
#70457=CARTESIAN_POINT('Ctrl Pts',(32.0549695330723,-1.78130455033843,33.8804609779983));
#70458=CARTESIAN_POINT('Ctrl Pts',(32.0627911774232,-1.7977957394946,33.8637293696347));
#70459=CARTESIAN_POINT('',(32.063542675787,-1.74592893957158,33.8969505670765));
#70460=CARTESIAN_POINT('Origin',(32.0596784217459,-1.75913156587025,33.8912949636253));
#70461=CARTESIAN_POINT('',(32.0983535250032,-1.75615758026484,33.8637293696319));
#70462=CARTESIAN_POINT('Ctrl Pts',(32.0983535250003,-1.75615758026399,33.8637293696347));
#70463=CARTESIAN_POINT('Ctrl Pts',(32.0808417949984,-1.75101202368781,33.8804609779984));
#70464=CARTESIAN_POINT('Ctrl Pts',(32.0635426757791,-1.74592893956926,33.8969505670841));
#70465=CARTESIAN_POINT('',(32.1974857086705,-1.63040900476039,33.8637293696319));
#70466=CARTESIAN_POINT('Origin',(30.,-1.32966554433622E-14,33.8637293696319));
#70467=CARTESIAN_POINT('',(32.1794132547725,-1.59894781082747,33.8969505670765));
#70468=CARTESIAN_POINT('Ctrl Pts',(32.1794132547683,-1.59894781082035,33.8969505670841));
#70469=CARTESIAN_POINT('Ctrl Pts',(32.1883942920486,-1.61458233157699,33.8804609779984));
#70470=CARTESIAN_POINT('Ctrl Pts',(32.197485708669,-1.63040900475776,33.8637293696347));
#70471=CARTESIAN_POINT('',(32.194165468194,-1.57864313098713,33.8969505670765));
#70472=CARTESIAN_POINT('Origin',(32.1913489771416,-1.59210823242541,33.8912949854673));
#70473=CARTESIAN_POINT('',(32.2296715370789,-1.58610901244375,33.8637293696319));
#70474=CARTESIAN_POINT('Ctrl Pts',(32.2296715370759,-1.58610901244313,33.8637293696347));
#70475=CARTESIAN_POINT('Ctrl Pts',(32.2118100741774,-1.58235327240121,33.8804609779984));
#70476=CARTESIAN_POINT('Ctrl Pts',(32.1941654681859,-1.57864313098543,33.8969505670841));
#70477=CARTESIAN_POINT('',(32.3186320097845,-1.45297025634306,33.8637293696319));
#70478=CARTESIAN_POINT('Origin',(30.,-1.32966554433622E-14,33.8637293696319));
#70479=CARTESIAN_POINT('',(32.2981468504039,-1.42302399516182,33.8969505670765));
#70480=CARTESIAN_POINT('Ctrl Pts',(32.2981468503993,-1.42302399515499,33.8969505670841));
#70481=CARTESIAN_POINT('Ctrl Pts',(32.3083268724996,-1.4379056758382,33.8804609779984));
#70482=CARTESIAN_POINT('Ctrl Pts',(32.3186320097828,-1.45297025634053,33.8637293696347));
#70483=CARTESIAN_POINT('',(32.3112605008555,-1.40162446254804,33.8969505670765));
#70484=CARTESIAN_POINT('Origin',(32.3095091411127,-1.41526902814879,33.891294999854));
#70485=CARTESIAN_POINT('',(32.3472428826875,-1.40628155512619,33.8637293696319));
#70486=CARTESIAN_POINT('Ctrl Pts',(32.3472428826845,-1.4062815551258,33.8637293696347));
#70487=CARTESIAN_POINT('Ctrl Pts',(32.3291418087476,-1.4039387870044,33.8804609779983));
#70488=CARTESIAN_POINT('Ctrl Pts',(32.3112605008473,-1.40162446254698,33.8969505670841));
#70489=CARTESIAN_POINT('',(32.4254831735348,-1.26657346313373,33.8637293696319));
#70490=CARTESIAN_POINT('Origin',(30.,-1.32966554433622E-14,33.8637293696319));
#70491=CARTESIAN_POINT('',(32.4027116064913,-1.2383267633625,33.8969505670765));
#70492=CARTESIAN_POINT('Ctrl Pts',(32.4027116064861,-1.23832676335608,33.8969505670841));
#70493=CARTESIAN_POINT('Ctrl Pts',(32.414027850185,-1.25236385345577,33.8804609779983));
#70494=CARTESIAN_POINT('Ctrl Pts',(32.4254831735329,-1.26657346313137,33.8637293696347));
#70495=CARTESIAN_POINT('',(32.4141058439571,-1.21596431320991,33.8969505670765));
#70496=CARTESIAN_POINT('Origin',(32.4134304175703,-1.22970422416536,33.8912950072666));
#70497=CARTESIAN_POINT('',(32.4503426953868,-1.21778390438519,33.8637293696319));
#70498=CARTESIAN_POINT('Ctrl Pts',(32.4503426953838,-1.21778390438504,33.8637293696347));
#70499=CARTESIAN_POINT('Ctrl Pts',(32.4321136095486,-1.21686855212869,33.8804609779984));
#70500=CARTESIAN_POINT('Ctrl Pts',(32.4141058439489,-1.2159643132095,33.8969505670841));
#70501=CARTESIAN_POINT('',(32.5173804269652,-1.07236782334576,33.8637293696319));
#70502=CARTESIAN_POINT('Origin',(30.,-1.32966554433622E-14,33.8637293696319));
#70503=CARTESIAN_POINT('',(32.492462846542,-1.0459948352816,33.8969505670765));
#70504=CARTESIAN_POINT('Ctrl Pts',(32.4924628465363,-1.04599483527564,33.8969505670841));
#70505=CARTESIAN_POINT('Ctrl Pts',(32.5048455434283,-1.05910079146353,33.8804609779984));
#70506=CARTESIAN_POINT('Ctrl Pts',(32.5173804269631,-1.07236782334356,33.8637293696347));
#70507=CARTESIAN_POINT('',(32.5020674217591,-1.02280733953168,33.8969505670765));
#70508=CARTESIAN_POINT('Origin',(32.5024720978725,-1.03655788791108,33.8912950079413));
#70509=CARTESIAN_POINT('',(32.5383353305474,-1.02177821091943,33.8637293696319));
#70510=CARTESIAN_POINT('Ctrl Pts',(32.5383353305444,-1.02177821091952,33.8637293696347));
#70511=CARTESIAN_POINT('Ctrl Pts',(32.5200906211869,-1.02229591797926,33.8804609779983));
#70512=CARTESIAN_POINT('Ctrl Pts',(32.5020674217508,-1.02280733953191,33.8969505670841));
#70513=CARTESIAN_POINT('',(32.5937571929495,-0.871550679328387,33.8637293696319));
#70514=CARTESIAN_POINT('Origin',(30.,-1.32966554433622E-14,33.8637293696319));
#70515=CARTESIAN_POINT('',(32.5668472243157,-0.847214001212625,33.8969505670765));
#70516=CARTESIAN_POINT('Ctrl Pts',(32.5668472243096,-0.847214001207098,
33.8969505670841));
#70517=CARTESIAN_POINT('Ctrl Pts',(32.5802200309508,-0.859308020905142,
33.8804609779983));
#70518=CARTESIAN_POINT('Ctrl Pts',(32.5937571929472,-0.871550679326345,
33.8637293696347));
#70519=CARTESIAN_POINT('',(32.574602921884,-0.823344418487278,33.8969505670765));
#70520=CARTESIAN_POINT('Origin',(32.5760852110325,-0.837020829522246,33.8912950018862));
#70521=CARTESIAN_POINT('',(32.6106782843131,-0.819472915007605,33.8637293696319));
#70522=CARTESIAN_POINT('Ctrl Pts',(32.6106782843101,-0.819472915007929,
33.8637293696347));
#70523=CARTESIAN_POINT('Ctrl Pts',(32.5925304361305,-0.821420489547588,
33.8804609779984));
#70524=CARTESIAN_POINT('Ctrl Pts',(32.5746029218758,-0.823344418488157,
33.8969505670841));
#70525=CARTESIAN_POINT('',(32.6541425833274,-0.665360135552938,33.8637293696319));
#70526=CARTESIAN_POINT('Origin',(30.,-1.32966554433622E-14,33.8637293696319));
#70527=CARTESIAN_POINT('',(32.6254061353882,-0.643209811098926,33.8969505670765));
#70528=CARTESIAN_POINT('Ctrl Pts',(32.6254061353816,-0.643209811093906,
33.8969505670841));
#70529=CARTESIAN_POINT('Ctrl Pts',(32.6396866039721,-0.65421733064898,33.8804609779984));
#70530=CARTESIAN_POINT('Ctrl Pts',(32.654142583325,-0.665360135551083,33.8637293696347));
#70531=CARTESIAN_POINT('',(32.6312651388532,-0.6188053053131,33.8969505670765));
#70532=CARTESIAN_POINT('Origin',(32.633815908334,-0.632323260043048,33.8912949888765));
#70533=CARTESIAN_POINT('',(32.6669255383174,-0.612115296072366,33.8637293696319));
#70534=CARTESIAN_POINT('Ctrl Pts',(32.6669255383144,-0.612115296072921,
33.8637293696347));
#70535=CARTESIAN_POINT('Ctrl Pts',(32.6489864388314,-0.615480730647825,
33.8804609779983));
#70536=CARTESIAN_POINT('Ctrl Pts',(32.6312651388451,-0.618805305314621,
33.8969505670841));
#70537=CARTESIAN_POINT('',(32.6981643020872,-0.455067425287109,33.8637293696319));
#70538=CARTESIAN_POINT('Origin',(30.,-1.32966554433622E-14,33.8637293696319));
#70539=CARTESIAN_POINT('',(32.6677785445999,-0.435240018610835,33.8969505670765));
#70540=CARTESIAN_POINT('Ctrl Pts',(32.667778544593,-0.43524001860635,33.8969505670841));
#70541=CARTESIAN_POINT('Ctrl Pts',(32.6828786312952,-0.445093173000037,
33.8804609779984));
#70542=CARTESIAN_POINT('Ctrl Pts',(32.6981643020846,-0.45506742528547,33.8637293696347));
#70543=CARTESIAN_POINT('',(32.6717047312569,-0.410451051658023,33.8969505670765));
#70544=CARTESIAN_POINT('Origin',(32.6753082614924,-0.423727206709312,33.8912949684251));
#70545=CARTESIAN_POINT('',(32.7067303095351,-0.400983782787849,33.8637293696319));
#70546=CARTESIAN_POINT('Ctrl Pts',(32.7067303095322,-0.400983782788643,
33.8637293696347));
#70547=CARTESIAN_POINT('Ctrl Pts',(32.6891105592595,-0.405746328375509,
33.8804609779984));
#70548=CARTESIAN_POINT('Ctrl Pts',(32.6717047312489,-0.410451051660171,
33.8969505670841));
#70549=CARTESIAN_POINT('',(32.7255509406939,-0.241969073019109,33.8637293696319));
#70550=CARTESIAN_POINT('Origin',(30.,-1.32966554433622E-14,33.8637293696319));
#70551=CARTESIAN_POINT('',(32.6937032119577,-0.224586826676015,33.8969505670765));
#70552=CARTESIAN_POINT('Ctrl Pts',(32.6937032119505,-0.224586826672072,
33.8969505670841));
#70553=CARTESIAN_POINT('Ctrl Pts',(32.7095298197086,-0.233224867931026,
33.8804609779984));
#70554=CARTESIAN_POINT('Ctrl Pts',(32.7255509406912,-0.241969073017673,
33.8637293696347));
#70555=CARTESIAN_POINT('',(32.6956723755605,-0.199566230780649,33.8969505670765));
#70556=CARTESIAN_POINT('Origin',(32.7003064571198,-0.212518732061269,33.8912949397143));
#70557=CARTESIAN_POINT('',(32.7298471883155,-0.187380071141808,33.8637293696319));
#70558=CARTESIAN_POINT('Ctrl Pts',(32.7298471883126,-0.187380071142835,
33.8637293696347));
#70559=CARTESIAN_POINT('Ctrl Pts',(32.7126554188699,-0.19351036506442,33.8804609779983));
#70560=CARTESIAN_POINT('Ctrl Pts',(32.6956723755527,-0.199566230783424,
33.8969505670841));
#70561=CARTESIAN_POINT('',(32.7361336514135,-0.0273789009530657,33.8637293696319));
#70562=CARTESIAN_POINT('Origin',(30.,-1.32966554433622E-14,33.8637293696319));
#70563=CARTESIAN_POINT('',(32.7030203032667,-0.0125489822720396,33.8969505670765));
#70564=CARTESIAN_POINT('Ctrl Pts',(32.7030203032592,-0.0125489822686859,
33.8969505670841));
#70565=CARTESIAN_POINT('Ctrl Pts',(32.7194758557734,-0.0199186539960853,
33.8804609779984));
#70566=CARTESIAN_POINT('Ctrl Pts',(32.7361336514107,-0.0273789009518218,
33.8637293696347));
#70567=CARTESIAN_POINT('',(32.7030203032667,0.0125489822719939,33.8969505670765));
#70568=CARTESIAN_POINT('Origin',(32.7086563646857,-6.24428584025816E-9,
33.8912949140187));
#70569=CARTESIAN_POINT('',(32.7361336514135,0.0273789009530202,33.8637293696319));
#70570=CARTESIAN_POINT('Ctrl Pts',(32.7361336514108,0.027378900951751,33.8637293696347));
#70571=CARTESIAN_POINT('Ctrl Pts',(32.7194758557734,0.0199186539960142,
33.8804609779984));
#70572=CARTESIAN_POINT('Ctrl Pts',(32.7030203032592,0.0125489822686146,
33.8969505670841));
#70573=CARTESIAN_POINT('',(32.7298471883155,0.187380071141762,33.8637293696319));
#70574=CARTESIAN_POINT('Origin',(30.,-1.32966554433622E-14,33.8637293696319));
#70575=CARTESIAN_POINT('',(32.6956723755605,0.199566230780603,33.8969505670765));
#70576=CARTESIAN_POINT('Ctrl Pts',(32.6956723755527,0.199566230783364,33.8969505670841));
#70577=CARTESIAN_POINT('Ctrl Pts',(32.7126554188699,0.193510365064359,33.8804609779983));
#70578=CARTESIAN_POINT('Ctrl Pts',(32.7298471883126,0.187380071142775,33.8637293696347));
#70579=CARTESIAN_POINT('',(32.6937032119577,0.224586826675969,33.8969505670765));
#70580=CARTESIAN_POINT('Origin',(32.7003074588901,0.212518788369426,33.8912937927563));
#70581=CARTESIAN_POINT('',(32.7255509406939,0.241969073019064,33.8637293696319));
#70582=CARTESIAN_POINT('Ctrl Pts',(32.7255509406912,0.241969073017624,33.8637293696347));
#70583=CARTESIAN_POINT('Ctrl Pts',(32.7095298197086,0.233224867930978,33.8804609779984));
#70584=CARTESIAN_POINT('Ctrl Pts',(32.6937032119505,0.224586826672025,33.8969505670841));
#70585=CARTESIAN_POINT('',(32.7067303095351,0.400983782787804,33.8637293696319));
#70586=CARTESIAN_POINT('Origin',(30.,-1.32966554433622E-14,33.8637293696319));
#70587=CARTESIAN_POINT('',(32.6717047312569,0.410451051657977,33.8969505670765));
#70588=CARTESIAN_POINT('Ctrl Pts',(32.6717047312489,0.410451051660138,33.8969505670841));
#70589=CARTESIAN_POINT('Ctrl Pts',(32.6891105592595,0.405746328375475,33.8804609779984));
#70590=CARTESIAN_POINT('Ctrl Pts',(32.7067303095322,0.400983782788608,33.8637293696347));
#70591=CARTESIAN_POINT('',(32.6677785445999,0.435240018610789,33.8969505670765));
#70592=CARTESIAN_POINT('Origin',(32.6753090233822,0.423727307748461,33.8912940899386));
#70593=CARTESIAN_POINT('',(32.6981643020872,0.455067425287063,33.8637293696319));
#70594=CARTESIAN_POINT('Ctrl Pts',(32.6981643020846,0.455067425285395,33.8637293696347));
#70595=CARTESIAN_POINT('Ctrl Pts',(32.6828786312952,0.445093172999962,33.8804609779983));
#70596=CARTESIAN_POINT('Ctrl Pts',(32.667778544593,0.435240018606276,33.8969505670841));
#70597=CARTESIAN_POINT('',(32.6669255383174,0.61211529607232,33.8637293696319));
#70598=CARTESIAN_POINT('Origin',(30.,-1.32966554433622E-14,33.8637293696319));
#70599=CARTESIAN_POINT('',(32.6312651388532,0.618805305313054,33.8969505670765));
#70600=CARTESIAN_POINT('Ctrl Pts',(32.6312651388451,0.618805305314574,33.8969505670841));
#70601=CARTESIAN_POINT('Ctrl Pts',(32.6489864388314,0.615480730647778,33.8804609779983));
#70602=CARTESIAN_POINT('Ctrl Pts',(32.6669255383144,0.612115296072874,33.8637293696347));
#70603=CARTESIAN_POINT('',(32.6254061353882,0.64320981109888,33.8969505670765));
#70604=CARTESIAN_POINT('Origin',(32.6338164916465,0.632323382398585,33.8912943077151));
#70605=CARTESIAN_POINT('',(32.6541425833274,0.665360135552893,33.8637293696319));
#70606=CARTESIAN_POINT('Ctrl Pts',(32.654142583325,0.665360135551018,33.8637293696347));
#70607=CARTESIAN_POINT('Ctrl Pts',(32.6396866039721,0.654217330648915,33.8804609779984));
#70608=CARTESIAN_POINT('Ctrl Pts',(32.6254061353817,0.643209811093841,33.8969505670841));
#70609=CARTESIAN_POINT('',(32.6106782843131,0.81947291500756,33.8637293696319));
#70610=CARTESIAN_POINT('Origin',(30.,-1.32966554433622E-14,33.8637293696319));
#70611=CARTESIAN_POINT('',(32.574602921884,0.823344418487232,33.8969505670765));
#70612=CARTESIAN_POINT('Ctrl Pts',(32.5746029218758,0.823344418488117,33.8969505670841));
#70613=CARTESIAN_POINT('Ctrl Pts',(32.5925304361305,0.821420489547548,33.8804609779984));
#70614=CARTESIAN_POINT('Ctrl Pts',(32.6106782843101,0.819472915007888,33.8637293696347));
#70615=CARTESIAN_POINT('',(32.5668472243157,0.84721400121258,33.8969505670765));
#70616=CARTESIAN_POINT('Origin',(32.5760856561636,0.83702095775897,33.891294472568));
#70617=CARTESIAN_POINT('',(32.5937571929495,0.871550679328342,33.8637293696319));
#70618=CARTESIAN_POINT('Ctrl Pts',(32.5937571929473,0.871550679326287,33.8637293696347));
#70619=CARTESIAN_POINT('Ctrl Pts',(32.5802200309508,0.859308020905083,33.8804609779984));
#70620=CARTESIAN_POINT('Ctrl Pts',(32.5668472243096,0.847214001207037,33.8969505670841));
#70621=CARTESIAN_POINT('',(32.5383353305474,1.02177821091938,33.8637293696319));
#70622=CARTESIAN_POINT('Origin',(30.,-1.32966554433622E-14,33.8637293696319));
#70623=CARTESIAN_POINT('',(32.5020674217591,1.02280733953163,33.8969505670765));
#70624=CARTESIAN_POINT('Ctrl Pts',(32.5020674217508,1.02280733953187,33.8969505670841));
#70625=CARTESIAN_POINT('Ctrl Pts',(32.520090621187,1.02229591797922,33.8804609779984));
#70626=CARTESIAN_POINT('Ctrl Pts',(32.5383353305444,1.02177821091947,33.8637293696347));
#70627=CARTESIAN_POINT('',(32.492462846542,1.04599483528156,33.8969505670765));
#70628=CARTESIAN_POINT('Origin',(32.5024724328509,1.03655801106889,33.8912946002427));
#70629=CARTESIAN_POINT('',(32.5173804269653,1.07236782334572,33.8637293696319));
#70630=CARTESIAN_POINT('Ctrl Pts',(32.5173804269632,1.0723678233435,33.8637293696347));
#70631=CARTESIAN_POINT('Ctrl Pts',(32.5048455434284,1.05910079146346,33.8804609779983));
#70632=CARTESIAN_POINT('Ctrl Pts',(32.4924628465363,1.04599483527555,33.8969505670841));
#70633=CARTESIAN_POINT('',(32.4503426953868,1.21778390438515,33.8637293696319));
#70634=CARTESIAN_POINT('Origin',(30.,-1.32966554433622E-14,33.8637293696319));
#70635=CARTESIAN_POINT('',(32.4141058439571,1.21596431320987,33.8969505670765));
#70636=CARTESIAN_POINT('Ctrl Pts',(32.4141058439489,1.21596431320946,33.8969505670841));
#70637=CARTESIAN_POINT('Ctrl Pts',(32.4321136095487,1.21686855212866,33.8804609779984));
#70638=CARTESIAN_POINT('Ctrl Pts',(32.4503426953838,1.217783904385,33.8637293696347));
#70639=CARTESIAN_POINT('',(32.4027116064913,1.23832676336245,33.8969505670765));
#70640=CARTESIAN_POINT('Origin',(32.4134306626749,1.22970433386022,33.891294700665));
#70641=CARTESIAN_POINT('',(32.4254831735348,1.26657346313369,33.8637293696319));
#70642=CARTESIAN_POINT('Ctrl Pts',(32.4254831735329,1.26657346313132,33.8637293696347));
#70643=CARTESIAN_POINT('Ctrl Pts',(32.414027850185,1.25236385345572,33.8804609779984));
#70644=CARTESIAN_POINT('Ctrl Pts',(32.4027116064861,1.23832676335603,33.8969505670841));
#70645=CARTESIAN_POINT('',(32.3472428826875,1.40628155512614,33.8637293696319));
#70646=CARTESIAN_POINT('Origin',(30.,-1.32966554433622E-14,33.8637293696319));
#70647=CARTESIAN_POINT('',(32.3112605008555,1.401624462548,33.8969505670765));
#70648=CARTESIAN_POINT('Ctrl Pts',(32.3112605008473,1.40162446254694,33.8969505670841));
#70649=CARTESIAN_POINT('Ctrl Pts',(32.3291418087476,1.40393878700437,33.8804609779984));
#70650=CARTESIAN_POINT('Ctrl Pts',(32.3472428826845,1.40628155512576,33.8637293696347));
#70651=CARTESIAN_POINT('',(32.298146850404,1.42302399516178,33.8969505670765));
#70652=CARTESIAN_POINT('Origin',(32.3095093115547,1.41526911745259,33.8912947803757));
#70653=CARTESIAN_POINT('',(32.3186320097845,1.45297025634302,33.8637293696319));
#70654=CARTESIAN_POINT('Ctrl Pts',(32.3186320097828,1.45297025634046,33.8637293696347));
#70655=CARTESIAN_POINT('Ctrl Pts',(32.3083268724996,1.43790567583815,33.8804609779983));
#70656=CARTESIAN_POINT('Ctrl Pts',(32.2981468503993,1.42302399515495,33.8969505670841));
#70657=CARTESIAN_POINT('',(32.2296715370789,1.58610901244371,33.8637293696319));
#70658=CARTESIAN_POINT('Origin',(30.,-1.32966554433622E-14,33.8637293696319));
#70659=CARTESIAN_POINT('',(32.194165468194,1.57864313098709,33.8969505670765));
#70660=CARTESIAN_POINT('Ctrl Pts',(32.1941654681859,1.57864313098539,33.8969505670841));
#70661=CARTESIAN_POINT('Ctrl Pts',(32.2118100741774,1.58235327240116,33.8804609779984));
#70662=CARTESIAN_POINT('Ctrl Pts',(32.2296715370759,1.58610901244308,33.8637293696347));
#70663=CARTESIAN_POINT('',(32.1794132547725,1.59894781082743,33.8969505670765));
#70664=CARTESIAN_POINT('Origin',(32.191349084716,1.59210829514292,33.891294843835));
#70665=CARTESIAN_POINT('',(32.1974857086706,1.63040900476035,33.8637293696319));
#70666=CARTESIAN_POINT('Ctrl Pts',(32.1974857086691,1.6304090047577,33.8637293696347));
#70667=CARTESIAN_POINT('Ctrl Pts',(32.1883942920486,1.61458233157692,33.8804609779983));
#70668=CARTESIAN_POINT('Ctrl Pts',(32.1794132547684,1.59894781082026,33.8969505670841));
#70669=CARTESIAN_POINT('',(32.0983535250032,1.7561575802648,33.8637293696319));
#70670=CARTESIAN_POINT('Origin',(30.,-1.32966554433622E-14,33.8637293696319));
#70671=CARTESIAN_POINT('',(32.0635426757871,1.74592893957153,33.8969505670765));
#70672=CARTESIAN_POINT('Ctrl Pts',(32.0635426757792,1.74592893956921,33.8969505670841));
#70673=CARTESIAN_POINT('Ctrl Pts',(32.0808417949984,1.75101202368776,33.8804609779983));
#70674=CARTESIAN_POINT('Ctrl Pts',(32.0983535250003,1.75615758026393,33.8637293696347));
#70675=CARTESIAN_POINT('',(32.0472428516969,1.76501358153524,33.8969505670765));
#70676=CARTESIAN_POINT('Origin',(32.0596784759083,1.75913159602166,33.8912948941586));
#70677=CARTESIAN_POINT('',(32.0627911774245,1.79779573949733,33.8637293696319));
#70678=CARTESIAN_POINT('Ctrl Pts',(32.0627911774232,1.79779573949457,33.8637293696347));
#70679=CARTESIAN_POINT('Ctrl Pts',(32.0549695330723,1.78130455033839,33.8804609779984));
#70680=CARTESIAN_POINT('Ctrl Pts',(32.0472428516934,1.76501358152777,33.8969505670841));
#70681=CARTESIAN_POINT('',(31.9540984656726,1.9153788526219,33.8637293696319));
#70682=CARTESIAN_POINT('Origin',(30.,-1.32966554433622E-14,33.8637293696319));
#70683=CARTESIAN_POINT('',(31.9201974565863,1.90245051566323,33.8969505670765));
#70684=CARTESIAN_POINT('Ctrl Pts',(31.9201974565786,1.90245051566028,33.8969505670841));
#70685=CARTESIAN_POINT('Ctrl Pts',(31.9370444342032,1.90887520357773,33.8804609779983));
#70686=CARTESIAN_POINT('Ctrl Pts',(31.9540984656697,1.91537885262081,33.8637293696347));
#70687=CARTESIAN_POINT('',(31.9024505156632,1.9201974565863,33.8969505670765));
#70688=CARTESIAN_POINT('Origin',(31.915309275617,1.91530926701235,33.891294933562));
#70689=CARTESIAN_POINT('',(31.9153788526219,1.95409846567256,33.8637293696319));
#70690=CARTESIAN_POINT('Ctrl Pts',(31.9153788526208,1.95409846566973,33.8637293696347));
#70691=CARTESIAN_POINT('Ctrl Pts',(31.9088752035777,1.93704443420319,33.8804609779984));
#70692=CARTESIAN_POINT('Ctrl Pts',(31.9024505156603,1.9201974565786,33.8969505670841));
#70693=CARTESIAN_POINT('',(31.7977957394973,2.06279117742448,33.8637293696319));
#70694=CARTESIAN_POINT('Origin',(30.,-1.32966554433622E-14,33.8637293696319));
#70695=CARTESIAN_POINT('',(31.7650135815352,2.04724285169688,33.8969505670765));
#70696=CARTESIAN_POINT('Ctrl Pts',(31.7650135815278,2.04724285169333,33.8969505670841));
#70697=CARTESIAN_POINT('Ctrl Pts',(31.7813045503384,2.05496953307223,33.8804609779984));
#70698=CARTESIAN_POINT('Ctrl Pts',(31.7977957394946,2.06279117742316,33.8637293696347));
#70699=CARTESIAN_POINT('',(31.7459289395715,2.06354267578706,33.8969505670765));
#70700=CARTESIAN_POINT('Origin',(31.7591315658702,2.05967842174595,33.8912949636253));
#70701=CARTESIAN_POINT('',(31.7561575802648,2.09835352500324,33.8637293696319));
#70702=CARTESIAN_POINT('Ctrl Pts',(31.7561575802639,2.09835352500033,33.8637293696347));
#70703=CARTESIAN_POINT('Ctrl Pts',(31.7510120236877,2.08084179499845,33.8804609779984));
#70704=CARTESIAN_POINT('Ctrl Pts',(31.7459289395692,2.06354267577915,33.8969505670841));
#70705=CARTESIAN_POINT('',(31.6304090047604,2.19748570867057,33.8637293696319));
#70706=CARTESIAN_POINT('Origin',(30.,-1.32966554433622E-14,33.8637293696319));
#70707=CARTESIAN_POINT('',(31.5989478108274,2.17941325477248,33.8969505670765));
#70708=CARTESIAN_POINT('Ctrl Pts',(31.5989478108202,2.17941325476838,33.8969505670841));
#70709=CARTESIAN_POINT('Ctrl Pts',(31.6145823315769,2.18839429204865,33.8804609779983));
#70710=CARTESIAN_POINT('Ctrl Pts',(31.6304090047577,2.19748570866908,33.8637293696347));
#70711=CARTESIAN_POINT('',(31.5786431309871,2.19416546819402,33.8969505670765));
#70712=CARTESIAN_POINT('Origin',(31.5921082324254,2.19134897714166,33.8912949854673));
#70713=CARTESIAN_POINT('',(31.5861090124437,2.22967153707891,33.8637293696319));
#70714=CARTESIAN_POINT('Ctrl Pts',(31.5861090124431,2.22967153707593,33.8637293696347));
#70715=CARTESIAN_POINT('Ctrl Pts',(31.5823532724012,2.21181007417742,33.8804609779984));
#70716=CARTESIAN_POINT('Ctrl Pts',(31.5786431309854,2.19416546818594,33.8969505670841));
#70717=CARTESIAN_POINT('',(31.452970256343,2.31863200978455,33.8637293696319));
#70718=CARTESIAN_POINT('Origin',(30.,-1.32966554433622E-14,33.8637293696319));
#70719=CARTESIAN_POINT('',(31.4230239951618,2.29814685040396,33.8969505670765));
#70720=CARTESIAN_POINT('Ctrl Pts',(31.423023995155,2.29814685039929,33.8969505670841));
#70721=CARTESIAN_POINT('Ctrl Pts',(31.4379056758382,2.30832687249959,33.8804609779983));
#70722=CARTESIAN_POINT('Ctrl Pts',(31.4529702563405,2.31863200978281,33.8637293696347));
#70723=CARTESIAN_POINT('',(31.401624462548,2.3112605008555,33.8969505670765));
#70724=CARTESIAN_POINT('Origin',(31.4152690281487,2.30950914111275,33.891294999854));
#70725=CARTESIAN_POINT('',(31.4062815551261,2.34724288268748,33.8637293696319));
#70726=CARTESIAN_POINT('Ctrl Pts',(31.4062815551258,2.34724288268445,33.8637293696347));
#70727=CARTESIAN_POINT('Ctrl Pts',(31.4039387870044,2.32914180874762,33.8804609779983));
#70728=CARTESIAN_POINT('Ctrl Pts',(31.4016244625469,2.31126050084732,33.8969505670841));
#70729=CARTESIAN_POINT('',(31.2665734631337,2.42548317353483,33.8637293696319));
#70730=CARTESIAN_POINT('Origin',(30.,-1.32966554433622E-14,33.8637293696319));
#70731=CARTESIAN_POINT('',(31.2383267633625,2.40271160649132,33.8969505670765));
#70732=CARTESIAN_POINT('Ctrl Pts',(31.2383267633561,2.40271160648613,33.8969505670841));
#70733=CARTESIAN_POINT('Ctrl Pts',(31.2523638534557,2.41402785018503,33.8804609779983));
#70734=CARTESIAN_POINT('Ctrl Pts',(31.2665734631313,2.4254831735329,33.8637293696347));
#70735=CARTESIAN_POINT('',(31.2159643132099,2.41410584395711,33.8969505670765));
#70736=CARTESIAN_POINT('Origin',(31.2297042241653,2.41343041757031,33.8912950072666));
#70737=CARTESIAN_POINT('',(31.2177839043851,2.45034269538681,33.8637293696319));
#70738=CARTESIAN_POINT('Ctrl Pts',(31.217783904385,2.45034269538375,33.8637293696347));
#70739=CARTESIAN_POINT('Ctrl Pts',(31.2168685521287,2.43211360954864,33.8804609779984));
#70740=CARTESIAN_POINT('Ctrl Pts',(31.2159643132095,2.41410584394886,33.8969505670841));
#70741=CARTESIAN_POINT('',(31.0723678233457,2.51738042696526,33.8637293696319));
#70742=CARTESIAN_POINT('Origin',(30.,-1.32966554433622E-14,33.8637293696319));
#70743=CARTESIAN_POINT('',(31.0459948352816,2.49246284654197,33.8969505670765));
#70744=CARTESIAN_POINT('Ctrl Pts',(31.0459948352756,2.4924628465363,33.8969505670841));
#70745=CARTESIAN_POINT('Ctrl Pts',(31.0591007914635,2.50484554342835,33.8804609779983));
#70746=CARTESIAN_POINT('Ctrl Pts',(31.0723678233435,2.51738042696315,33.8637293696347));
#70747=CARTESIAN_POINT('',(31.0228073395316,2.50206742175906,33.8969505670765));
#70748=CARTESIAN_POINT('Origin',(31.036557887911,2.50247209787251,33.8912950079413));
#70749=CARTESIAN_POINT('',(31.0217782109194,2.53833533054745,33.8637293696319));
#70750=CARTESIAN_POINT('Ctrl Pts',(31.0217782109194,2.5383353305444,33.8637293696347));
#70751=CARTESIAN_POINT('Ctrl Pts',(31.0222959179792,2.52009062118696,33.8804609779984));
#70752=CARTESIAN_POINT('Ctrl Pts',(31.0228073395318,2.50206742175081,33.8969505670841));
#70753=CARTESIAN_POINT('',(30.8715506793283,2.59375719294951,33.8637293696319));
#70754=CARTESIAN_POINT('Origin',(30.,-1.32966554433622E-14,33.8637293696319));
#70755=CARTESIAN_POINT('',(30.8472140012126,2.5668472243157,33.8969505670765));
#70756=CARTESIAN_POINT('Ctrl Pts',(30.847214001207,2.56684722430959,33.8969505670841));
#70757=CARTESIAN_POINT('Ctrl Pts',(30.8593080209051,2.58022003095078,33.8804609779984));
#70758=CARTESIAN_POINT('Ctrl Pts',(30.8715506793263,2.59375719294725,33.8637293696347));
#70759=CARTESIAN_POINT('',(30.8233444184872,2.57460292188402,33.8969505670765));
#70760=CARTESIAN_POINT('Origin',(30.8370208295222,2.57608521103255,33.8912950018862));
#70761=CARTESIAN_POINT('',(30.8194729150076,2.61067828431311,33.8637293696319));
#70762=CARTESIAN_POINT('Ctrl Pts',(30.8194729150079,2.61067828431008,33.8637293696347));
#70763=CARTESIAN_POINT('Ctrl Pts',(30.8214204895475,2.59253043613048,33.8804609779984));
#70764=CARTESIAN_POINT('Ctrl Pts',(30.8233444184881,2.57460292187581,33.8969505670841));
#70765=CARTESIAN_POINT('',(30.6653601355529,2.65414258332745,33.8637293696319));
#70766=CARTESIAN_POINT('Origin',(30.,-1.32966554433622E-14,33.8637293696319));
#70767=CARTESIAN_POINT('',(30.6432098110989,2.62540613538819,33.8969505670765));
#70768=CARTESIAN_POINT('Ctrl Pts',(30.6432098110938,2.62540613538167,33.8969505670841));
#70769=CARTESIAN_POINT('Ctrl Pts',(30.6542173306489,2.63968660397217,33.8804609779983));
#70770=CARTESIAN_POINT('Ctrl Pts',(30.665360135551,2.65414258332504,33.8637293696347));
#70771=CARTESIAN_POINT('',(30.6188053053131,2.63126513885322,33.8969505670765));
#70772=CARTESIAN_POINT('Origin',(30.632323260043,2.633815908334,33.8912949888765));
#70773=CARTESIAN_POINT('',(30.6121152960723,2.66692553831736,33.8637293696319));
#70774=CARTESIAN_POINT('Ctrl Pts',(30.6121152960729,2.66692553831437,33.8637293696347));
#70775=CARTESIAN_POINT('Ctrl Pts',(30.6154807306478,2.6489864388314,33.8804609779983));
#70776=CARTESIAN_POINT('Ctrl Pts',(30.6188053053146,2.63126513884509,33.8969505670841));
#70777=CARTESIAN_POINT('',(30.4550674252871,2.69816430208719,33.8637293696319));
#70778=CARTESIAN_POINT('Origin',(30.,-1.32966554433622E-14,33.8637293696319));
#70779=CARTESIAN_POINT('',(30.4352400186108,2.66777854459989,33.8969505670765));
#70780=CARTESIAN_POINT('Ctrl Pts',(30.4352400186063,2.66777854459299,33.8969505670841));
#70781=CARTESIAN_POINT('Ctrl Pts',(30.4450931729999,2.68287863129519,33.8804609779983));
#70782=CARTESIAN_POINT('Ctrl Pts',(30.4550674252854,2.69816430208465,33.8637293696347));
#70783=CARTESIAN_POINT('',(30.410451051658,2.67170473125694,33.8969505670765));
#70784=CARTESIAN_POINT('Origin',(30.4237272067093,2.67530826149246,33.891294968425));
#70785=CARTESIAN_POINT('',(30.4009837827878,2.70673030953515,33.8637293696319));
#70786=CARTESIAN_POINT('Ctrl Pts',(30.4009837827886,2.7067303095322,33.8637293696347));
#70787=CARTESIAN_POINT('Ctrl Pts',(30.4057463283755,2.68911055925956,33.8804609779984));
#70788=CARTESIAN_POINT('Ctrl Pts',(30.4104510516602,2.67170473124897,33.8969505670841));
#70789=CARTESIAN_POINT('',(30.2419690730191,2.72555094069389,33.8637293696319));
#70790=CARTESIAN_POINT('Origin',(30.,-1.32966554433622E-14,33.8637293696319));
#70791=CARTESIAN_POINT('',(30.224586826676,2.69370321195774,33.8969505670765));
#70792=CARTESIAN_POINT('Ctrl Pts',(30.224586826672,2.6937032119505,33.8969505670841));
#70793=CARTESIAN_POINT('Ctrl Pts',(30.233224867931,2.70952981970859,33.8804609779983));
#70794=CARTESIAN_POINT('Ctrl Pts',(30.2419690730176,2.72555094069122,33.8637293696347));
#70795=CARTESIAN_POINT('',(30.1995662307806,2.69567237556048,33.8969505670765));
#70796=CARTESIAN_POINT('Origin',(30.2125187320612,2.70030645711979,33.8912949397143));
#70797=CARTESIAN_POINT('',(30.1873800711418,2.72984718831549,33.8637293696319));
#70798=CARTESIAN_POINT('Ctrl Pts',(30.1873800711428,2.7298471883126,33.8637293696347));
#70799=CARTESIAN_POINT('Ctrl Pts',(30.1935103650644,2.71265541886987,33.8804609779983));
#70800=CARTESIAN_POINT('Ctrl Pts',(30.1995662307834,2.6956723755527,33.8969505670841));
#70801=CARTESIAN_POINT('',(30.027378900953,2.73613365141356,33.8637293696319));
#70802=CARTESIAN_POINT('Origin',(30.,-1.32966554433622E-14,33.8637293696319));
#70803=CARTESIAN_POINT('',(30.012548982272,2.70302030326666,33.8969505670765));
#70804=CARTESIAN_POINT('Ctrl Pts',(30.0125489822686,2.70302030325912,33.8969505670841));
#70805=CARTESIAN_POINT('Ctrl Pts',(30.019918653996,2.71947585577339,33.8804609779983));
#70806=CARTESIAN_POINT('Ctrl Pts',(30.0273789009518,2.73613365141076,33.8637293696347));
#70807=CARTESIAN_POINT('',(29.987451017728,2.70302030326666,33.8969505670765));
#70808=CARTESIAN_POINT('Origin',(30.,2.70866577951602,33.891284862925));
#70809=CARTESIAN_POINT('',(29.9726210990469,2.73613365141356,33.8637293696319));
#70810=CARTESIAN_POINT('Ctrl Pts',(29.9726210990482,2.73613365141079,33.8637293696347));
#70811=CARTESIAN_POINT('Ctrl Pts',(29.980081346004,2.7194758557734,33.8804609779983));
#70812=CARTESIAN_POINT('Ctrl Pts',(29.9874510177314,2.70302030325912,33.8969505670841));
#70813=CARTESIAN_POINT('',(29.8126199288582,2.72984718831549,33.8637293696319));
#70814=CARTESIAN_POINT('Origin',(30.,-1.32966554433622E-14,33.8637293696319));
#70815=CARTESIAN_POINT('',(29.8004337692194,2.69567237556048,33.8969505670765));
#70816=CARTESIAN_POINT('Ctrl Pts',(29.8004337692166,2.6956723755527,33.8969505670841));
#70817=CARTESIAN_POINT('Ctrl Pts',(29.8064896349356,2.71265541886987,33.8804609779983));
#70818=CARTESIAN_POINT('Ctrl Pts',(29.8126199288572,2.7298471883126,33.8637293696347));
#70819=CARTESIAN_POINT('',(29.775413173324,2.69370321195775,33.8969505670765));
#70820=CARTESIAN_POINT('Origin',(29.7874812116306,2.70030745889017,33.8912937927563));
#70821=CARTESIAN_POINT('',(29.7580309269809,2.72555094069389,33.8637293696319));
#70822=CARTESIAN_POINT('Ctrl Pts',(29.7580309269824,2.72555094069121,33.8637293696347));
#70823=CARTESIAN_POINT('Ctrl Pts',(29.766775132069,2.70952981970858,33.8804609779983));
#70824=CARTESIAN_POINT('Ctrl Pts',(29.775413173328,2.69370321195049,33.8969505670841));
#70825=CARTESIAN_POINT('',(29.5990162172122,2.70673030953515,33.8637293696319));
#70826=CARTESIAN_POINT('Origin',(30.,-1.32966554433622E-14,33.8637293696319));
#70827=CARTESIAN_POINT('',(29.589548948342,2.67170473125694,33.8969505670765));
#70828=CARTESIAN_POINT('Ctrl Pts',(29.5895489483398,2.67170473124897,33.8969505670841));
#70829=CARTESIAN_POINT('Ctrl Pts',(29.5942536716245,2.68911055925956,33.8804609779983));
#70830=CARTESIAN_POINT('Ctrl Pts',(29.5990162172114,2.7067303095322,33.8637293696347));
#70831=CARTESIAN_POINT('',(29.5647599813892,2.6677785445999,33.8969505670765));
#70832=CARTESIAN_POINT('Origin',(29.5762726922515,2.67530902338217,33.8912940899386));
#70833=CARTESIAN_POINT('',(29.5449325747129,2.6981643020872,33.8637293696319));
#70834=CARTESIAN_POINT('Ctrl Pts',(29.5449325747146,2.69816430208465,33.8637293696347));
#70835=CARTESIAN_POINT('Ctrl Pts',(29.554906827,2.68287863129518,33.8804609779983));
#70836=CARTESIAN_POINT('Ctrl Pts',(29.5647599813937,2.66777854459298,33.8969505670841));
#70837=CARTESIAN_POINT('',(29.3878847039277,2.66692553831737,33.8637293696319));
#70838=CARTESIAN_POINT('Origin',(30.,-1.32966554433622E-14,33.8637293696319));
#70839=CARTESIAN_POINT('',(29.3811946946869,2.63126513885323,33.8969505670765));
#70840=CARTESIAN_POINT('Ctrl Pts',(29.3811946946854,2.6312651388451,33.8969505670841));
#70841=CARTESIAN_POINT('Ctrl Pts',(29.3845192693522,2.64898643883141,33.8804609779983));
#70842=CARTESIAN_POINT('Ctrl Pts',(29.3878847039271,2.66692553831437,33.8637293696347));
#70843=CARTESIAN_POINT('',(29.3567901889011,2.6254061353882,33.8969505670765));
#70844=CARTESIAN_POINT('Origin',(29.3676766176014,2.6338164916465,33.8912943077151));
#70845=CARTESIAN_POINT('',(29.3346398644471,2.65414258332745,33.8637293696319));
#70846=CARTESIAN_POINT('Ctrl Pts',(29.334639864449,2.65414258332502,33.8637293696347));
#70847=CARTESIAN_POINT('Ctrl Pts',(29.3457826693511,2.63968660397215,33.8804609779983));
#70848=CARTESIAN_POINT('Ctrl Pts',(29.3567901889061,2.62540613538165,33.8969505670841));
#70849=CARTESIAN_POINT('',(29.1805270849924,2.61067828431312,33.8637293696319));
#70850=CARTESIAN_POINT('Origin',(30.,-1.32966554433622E-14,33.8637293696319));
#70851=CARTESIAN_POINT('',(29.1766555815128,2.57460292188403,33.8969505670765));
#70852=CARTESIAN_POINT('Ctrl Pts',(29.1766555815118,2.57460292187581,33.8969505670841));
#70853=CARTESIAN_POINT('Ctrl Pts',(29.1785795104524,2.59253043613048,33.8804609779983));
#70854=CARTESIAN_POINT('Ctrl Pts',(29.1805270849921,2.61067828431008,33.8637293696347));
#70855=CARTESIAN_POINT('',(29.1527859987874,2.56684722431571,33.8969505670765));
#70856=CARTESIAN_POINT('Origin',(29.162979042241,2.57608565616365,33.891294472568));
#70857=CARTESIAN_POINT('',(29.1284493206716,2.59375719294953,33.8637293696319));
#70858=CARTESIAN_POINT('Ctrl Pts',(29.1284493206737,2.59375719294727,33.8637293696347));
#70859=CARTESIAN_POINT('Ctrl Pts',(29.1406919790949,2.58022003095078,33.8804609779983));
#70860=CARTESIAN_POINT('Ctrl Pts',(29.1527859987929,2.56684722430958,33.8969505670841));
#70861=CARTESIAN_POINT('',(28.9782217890806,2.53833533054746,33.8637293696319));
#70862=CARTESIAN_POINT('Origin',(30.,-1.32966554433622E-14,33.8637293696319));
#70863=CARTESIAN_POINT('',(28.9771926604684,2.50206742175908,33.8969505670765));
#70864=CARTESIAN_POINT('Ctrl Pts',(28.9771926604681,2.50206742175082,33.8969505670841));
#70865=CARTESIAN_POINT('Ctrl Pts',(28.9777040820208,2.52009062118696,33.8804609779983));
#70866=CARTESIAN_POINT('Ctrl Pts',(28.9782217890805,2.5383353305444,33.8637293696347));
#70867=CARTESIAN_POINT('',(28.9540051647184,2.49246284654199,33.8969505670765));
#70868=CARTESIAN_POINT('Origin',(28.9634419889311,2.50247243285091,33.8912946002427));
#70869=CARTESIAN_POINT('',(28.9276321766543,2.51738042696527,33.8637293696319));
#70870=CARTESIAN_POINT('Ctrl Pts',(28.9276321766565,2.51738042696315,33.8637293696347));
#70871=CARTESIAN_POINT('Ctrl Pts',(28.9408992085365,2.50484554342835,33.8804609779983));
#70872=CARTESIAN_POINT('Ctrl Pts',(28.9540051647244,2.49246284653631,33.8969505670841));
#70873=CARTESIAN_POINT('',(28.7822160956148,2.45034269538683,33.8637293696319));
#70874=CARTESIAN_POINT('Origin',(30.,-1.32966554433622E-14,33.8637293696319));
#70875=CARTESIAN_POINT('Ctrl Pts',(28.7840356867905,2.41410584394887,33.8969505670841));
#70876=CARTESIAN_POINT('Ctrl Pts',(28.7831314478713,2.43211360954865,33.8804609779983));
#70877=CARTESIAN_POINT('Ctrl Pts',(28.782216095615,2.45034269538377,33.8637293696347));
#70878=CARTESIAN_POINT('',(28.7334265368663,2.42548317353484,33.8637293696319));
#70879=CARTESIAN_POINT('Ctrl Pts',(28.7334265368687,2.42548317353291,33.8637293696347));
#70880=CARTESIAN_POINT('Ctrl Pts',(28.7476361465443,2.41402785018503,33.8804609779983));
#70881=CARTESIAN_POINT('Ctrl Pts',(28.7616732366439,2.40271160648614,33.8969505670841));
#70882=CARTESIAN_POINT('',(28.5937184448738,2.3472428826875,33.8637293696319));
#70883=CARTESIAN_POINT('Origin',(30.,-1.32966554433622E-14,33.8637293696319));
#70884=CARTESIAN_POINT('Ctrl Pts',(28.5983755374531,2.31126050084732,33.8969505670841));
#70885=CARTESIAN_POINT('Ctrl Pts',(28.5960612129956,2.32914180874763,33.8804609779983));
#70886=CARTESIAN_POINT('Ctrl Pts',(28.5937184448742,2.34724288268447,33.8637293696347));
#70887=CARTESIAN_POINT('',(28.547029743657,2.31863200978457,33.8637293696319));
#70888=CARTESIAN_POINT('Ctrl Pts',(28.5470297436595,2.31863200978283,33.8637293696347));
#70889=CARTESIAN_POINT('Ctrl Pts',(28.5620943241618,2.30832687249961,33.8804609779983));
#70890=CARTESIAN_POINT('Ctrl Pts',(28.576976004845,2.29814685039931,33.8969505670841));
#70891=CARTESIAN_POINT('',(28.4138909875563,2.22967153707894,33.8637293696319));
#70892=CARTESIAN_POINT('Origin',(30.,-1.32966554433622E-14,33.8637293696319));
#70893=CARTESIAN_POINT('Ctrl Pts',(28.4213568690146,2.19416546818595,33.8969505670841));
#70894=CARTESIAN_POINT('Ctrl Pts',(28.4176467275988,2.21181007417744,33.8804609779983));
#70895=CARTESIAN_POINT('Ctrl Pts',(28.4138909875569,2.22967153707594,33.8637293696347));
#70896=CARTESIAN_POINT('',(28.3695909952396,2.19748570867059,33.8637293696319));
#70897=CARTESIAN_POINT('Ctrl Pts',(28.3695909952423,2.19748570866909,33.8637293696347));
#70898=CARTESIAN_POINT('Ctrl Pts',(28.3854176684231,2.18839429204867,33.8804609779983));
#70899=CARTESIAN_POINT('Ctrl Pts',(28.4010521891798,2.17941325476839,33.8969505670841));
#70900=CARTESIAN_POINT('',(28.2438424197352,2.09835352500326,33.8637293696319));
#70901=CARTESIAN_POINT('Origin',(30.,-1.32966554433622E-14,33.8637293696319));
#70902=CARTESIAN_POINT('Ctrl Pts',(28.2540710604308,2.06354267577915,33.8969505670841));
#70903=CARTESIAN_POINT('Ctrl Pts',(28.2489879763122,2.08084179499845,33.8804609779983));
#70904=CARTESIAN_POINT('Ctrl Pts',(28.2438424197361,2.09835352500033,33.8637293696347));
#70905=CARTESIAN_POINT('',(28.2022042605027,2.0627911774245,33.8637293696319));
#70906=CARTESIAN_POINT('Ctrl Pts',(28.2022042605055,2.0627911774232,33.8637293696347));
#70907=CARTESIAN_POINT('Ctrl Pts',(28.2186954496616,2.05496953307227,33.8804609779984));
#70908=CARTESIAN_POINT('Ctrl Pts',(28.2349864184722,2.04724285169337,33.8969505670841));
#70909=CARTESIAN_POINT('',(28.0846211473781,1.95409846567259,33.8637293696319));
#70910=CARTESIAN_POINT('Origin',(30.,-1.32966554433622E-14,33.8637293696319));
#70911=CARTESIAN_POINT('Ctrl Pts',(28.0975494843397,1.92019745657863,33.8969505670841));
#70912=CARTESIAN_POINT('Ctrl Pts',(28.0911247964223,1.9370444342032,33.8804609779983));
#70913=CARTESIAN_POINT('Ctrl Pts',(28.0846211473792,1.95409846566974,33.8637293696347));
#70914=CARTESIAN_POINT('',(28.0459015343274,1.91537885262192,33.8637293696319));
#70915=CARTESIAN_POINT('Ctrl Pts',(28.0459015343303,1.91537885262084,33.8637293696347));
#70916=CARTESIAN_POINT('Ctrl Pts',(28.0629555657968,1.90887520357776,33.8804609779983));
#70917=CARTESIAN_POINT('Ctrl Pts',(28.0798025434214,1.90245051566032,33.8969505670841));
#70918=CARTESIAN_POINT('',(27.9372088225755,1.79779573949736,33.8637293696319));
#70919=CARTESIAN_POINT('Origin',(30.,-1.32966554433622E-14,33.8637293696319));
#70920=CARTESIAN_POINT('Ctrl Pts',(27.9527571483066,1.76501358152779,33.8969505670841));
#70921=CARTESIAN_POINT('Ctrl Pts',(27.9450304669277,1.78130455033841,33.8804609779983));
#70922=CARTESIAN_POINT('Ctrl Pts',(27.9372088225768,1.79779573949458,33.8637293696347));
#70923=CARTESIAN_POINT('',(27.9016464749967,1.75615758026483,33.8637293696319));
#70924=CARTESIAN_POINT('Ctrl Pts',(27.9016464749997,1.75615758026397,33.8637293696347));
#70925=CARTESIAN_POINT('Ctrl Pts',(27.9191582050016,1.75101202368779,33.8804609779983));
#70926=CARTESIAN_POINT('Ctrl Pts',(27.9364573242208,1.74592893956924,33.8969505670841));
#70927=CARTESIAN_POINT('',(27.8025142913294,1.63040900476038,33.8637293696319));
#70928=CARTESIAN_POINT('Origin',(30.,-1.32966554433622E-14,33.8637293696319));
#70929=CARTESIAN_POINT('Ctrl Pts',(27.8205867452316,1.59894781082027,33.8969505670841));
#70930=CARTESIAN_POINT('Ctrl Pts',(27.8116057079513,1.61458233157693,33.8804609779983));
#70931=CARTESIAN_POINT('Ctrl Pts',(27.8025142913309,1.63040900475771,33.8637293696347));
#70932=CARTESIAN_POINT('',(27.7703284629211,1.58610901244374,33.8637293696319));
#70933=CARTESIAN_POINT('Ctrl Pts',(27.7703284629241,1.58610901244311,33.8637293696347));
#70934=CARTESIAN_POINT('Ctrl Pts',(27.7881899258226,1.5823532724012,33.8804609779984));
#70935=CARTESIAN_POINT('Ctrl Pts',(27.8058345318141,1.57864313098542,33.8969505670841));
#70936=CARTESIAN_POINT('',(27.6813679902154,1.45297025634305,33.8637293696319));
#70937=CARTESIAN_POINT('Origin',(30.,-1.32966554433622E-14,33.8637293696319));
#70938=CARTESIAN_POINT('Ctrl Pts',(27.7018531496007,1.423023995155,33.8969505670841));
#70939=CARTESIAN_POINT('Ctrl Pts',(27.6916731275004,1.43790567583821,33.8804609779983));
#70940=CARTESIAN_POINT('Ctrl Pts',(27.6813679902172,1.45297025634054,33.8637293696347));
#70941=CARTESIAN_POINT('',(27.6527571173125,1.40628155512618,33.8637293696319));
#70942=CARTESIAN_POINT('Ctrl Pts',(27.6527571173155,1.40628155512578,33.8637293696347));
#70943=CARTESIAN_POINT('Ctrl Pts',(27.6708581912524,1.40393878700439,33.8804609779983));
#70944=CARTESIAN_POINT('Ctrl Pts',(27.6887394991527,1.40162446254697,33.8969505670841));
#70945=CARTESIAN_POINT('',(27.5745168264652,1.26657346313372,33.8637293696319));
#70946=CARTESIAN_POINT('Origin',(30.,-1.32966554433622E-14,33.8637293696319));
#70947=CARTESIAN_POINT('Ctrl Pts',(27.5972883935138,1.23832676335601,33.8969505670841));
#70948=CARTESIAN_POINT('Ctrl Pts',(27.5859721498149,1.2523638534557,33.8804609779984));
#70949=CARTESIAN_POINT('Ctrl Pts',(27.5745168264671,1.26657346313129,33.8637293696347));
#70950=CARTESIAN_POINT('',(27.5496573046132,1.21778390438518,33.8637293696319));
#70951=CARTESIAN_POINT('Ctrl Pts',(27.5496573046163,1.21778390438503,33.8637293696347));
#70952=CARTESIAN_POINT('Ctrl Pts',(27.5678863904514,1.21686855212868,33.8804609779984));
#70953=CARTESIAN_POINT('Ctrl Pts',(27.5858941560511,1.21596431320949,33.8969505670841));
#70954=CARTESIAN_POINT('',(27.4826195730347,1.07236782334576,33.8637293696319));
#70955=CARTESIAN_POINT('Origin',(30.,-1.32966554433622E-14,33.8637293696319));
#70956=CARTESIAN_POINT('Ctrl Pts',(27.5075371534637,1.04599483527557,33.8969505670841));
#70957=CARTESIAN_POINT('Ctrl Pts',(27.4951544565716,1.05910079146348,33.8804609779983));
#70958=CARTESIAN_POINT('Ctrl Pts',(27.4826195730368,1.07236782334352,33.8637293696347));
#70959=CARTESIAN_POINT('',(27.4616646694525,1.02177821091942,33.8637293696319));
#70960=CARTESIAN_POINT('Ctrl Pts',(27.4616646694556,1.0217782109195,33.8637293696347));
#70961=CARTESIAN_POINT('Ctrl Pts',(27.479909378813,1.02229591797925,33.8804609779983));
#70962=CARTESIAN_POINT('Ctrl Pts',(27.4979325782492,1.0228073395319,33.8969505670841));
#70963=CARTESIAN_POINT('',(27.4062428070505,0.871550679328378,33.8637293696319));
#70964=CARTESIAN_POINT('Origin',(30.,-1.32966554433622E-14,33.8637293696319));
#70965=CARTESIAN_POINT('Ctrl Pts',(27.4331527756904,0.847214001207086,33.8969505670841));
#70966=CARTESIAN_POINT('Ctrl Pts',(27.4197799690492,0.859308020905129,33.8804609779984));
#70967=CARTESIAN_POINT('Ctrl Pts',(27.4062428070528,0.871550679326332,33.8637293696347));
#70968=CARTESIAN_POINT('',(27.3893217156869,0.819472915007596,33.8637293696319));
#70969=CARTESIAN_POINT('Ctrl Pts',(27.3893217156899,0.819472915007932,33.8637293696347));
#70970=CARTESIAN_POINT('Ctrl Pts',(27.4074695638695,0.821420489547589,33.8804609779983));
#70971=CARTESIAN_POINT('Ctrl Pts',(27.4253970781241,0.823344418488154,33.8969505670841));
#70972=CARTESIAN_POINT('',(27.3458574166725,0.665360135552929,33.8637293696319));
#70973=CARTESIAN_POINT('Origin',(30.,-1.32966554433622E-14,33.8637293696319));
#70974=CARTESIAN_POINT('Ctrl Pts',(27.3745938646183,0.643209811093841,33.8969505670841));
#70975=CARTESIAN_POINT('Ctrl Pts',(27.3603133960278,0.654217330648928,33.8804609779983));
#70976=CARTESIAN_POINT('Ctrl Pts',(27.3458574166749,0.665360135551045,33.8637293696347));
#70977=CARTESIAN_POINT('',(27.3330744616826,0.612115296072357,33.8637293696319));
#70978=CARTESIAN_POINT('Ctrl Pts',(27.3330744616856,0.612115296072913,33.8637293696347));
#70979=CARTESIAN_POINT('Ctrl Pts',(27.3510135611686,0.615480730647817,33.8804609779983));
#70980=CARTESIAN_POINT('Ctrl Pts',(27.3687348611549,0.618805305314613,33.8969505670841));
#70981=CARTESIAN_POINT('',(27.3018356979128,0.455067425287102,33.8637293696319));
#70982=CARTESIAN_POINT('Origin',(30.,-1.32966554433622E-14,33.8637293696319));
#70983=CARTESIAN_POINT('Ctrl Pts',(27.332221455407,0.435240018606297,33.8969505670841));
#70984=CARTESIAN_POINT('Ctrl Pts',(27.3171213687048,0.445093172999983,33.8804609779983));
#70985=CARTESIAN_POINT('Ctrl Pts',(27.3018356979154,0.455067425285416,33.8637293696347));
#70986=CARTESIAN_POINT('',(27.2932696904648,0.400983782787843,33.8637293696319));
#70987=CARTESIAN_POINT('Ctrl Pts',(27.2932696904678,0.40098378278865,33.8637293696347));
#70988=CARTESIAN_POINT('Ctrl Pts',(27.3108894407404,0.405746328375518,33.8804609779983));
#70989=CARTESIAN_POINT('Ctrl Pts',(27.328295268751,0.410451051660182,33.8969505670841));
#70990=CARTESIAN_POINT('',(27.2744490593061,0.241969073019103,33.8637293696319));
#70991=CARTESIAN_POINT('Origin',(30.,-1.32966554433622E-14,33.8637293696319));
#70992=CARTESIAN_POINT('Ctrl Pts',(27.3062967880495,0.224586826672042,33.8969505670841));
#70993=CARTESIAN_POINT('Ctrl Pts',(27.2904701802914,0.233224867930985,33.8804609779983));
#70994=CARTESIAN_POINT('Ctrl Pts',(27.2744490593088,0.24196907301762,33.8637293696347));
#70995=CARTESIAN_POINT('',(27.2701528116845,0.1873800711418,33.8637293696319));
#70996=CARTESIAN_POINT('Ctrl Pts',(27.2701528116874,0.187380071142834,33.8637293696347));
#70997=CARTESIAN_POINT('Ctrl Pts',(27.2873445811301,0.193510365064418,33.8804609779983));
#70998=CARTESIAN_POINT('Ctrl Pts',(27.3043276244473,0.199566230783421,33.8969505670841));
#70999=CARTESIAN_POINT('',(27.2638663485864,0.0273789009530583,33.8637293696319));
#71000=CARTESIAN_POINT('Origin',(30.,-1.32966554433622E-14,33.8637293696319));
#71001=CARTESIAN_POINT('Ctrl Pts',(27.2969796967408,0.0125489822686371,
33.8969505670841));
#71002=CARTESIAN_POINT('Ctrl Pts',(27.2805241442266,0.0199186539960461,
33.8804609779983));
#71003=CARTESIAN_POINT('Ctrl Pts',(27.2638663485892,0.0273789009517924,
33.8637293696347));
#71004=CARTESIAN_POINT('',(27.2638663485864,-0.0273789009530277,33.8637293696319));
#71005=CARTESIAN_POINT('Ctrl Pts',(27.2638663485892,-0.0273789009517733,
33.8637293696347));
#71006=CARTESIAN_POINT('Ctrl Pts',(27.2805241442266,-0.0199186539960275,
33.8804609779983));
#71007=CARTESIAN_POINT('Ctrl Pts',(27.2969796967409,-0.012548982268619,
33.8969505670841));
#71008=CARTESIAN_POINT('',(27.2701528116845,-0.18738007114177,33.8637293696319));
#71009=CARTESIAN_POINT('Origin',(30.,-1.32966554433622E-14,33.8637293696319));
#71010=CARTESIAN_POINT('',(27.3043276244395,-0.199566230780611,33.8969505670765));
#71011=CARTESIAN_POINT('Ctrl Pts',(27.3043276244473,-0.199566230783401,
33.8969505670841));
#71012=CARTESIAN_POINT('Ctrl Pts',(27.2873445811301,-0.193510365064398,
33.8804609779983));
#71013=CARTESIAN_POINT('Ctrl Pts',(27.2701528116874,-0.187380071142813,
33.8637293696347));
#71014=CARTESIAN_POINT('',(27.3062967880422,-0.224586826675978,33.8969505670765));
#71015=CARTESIAN_POINT('Origin',(27.2996925411099,-0.212518788369432,33.8912937927564));
#71016=CARTESIAN_POINT('',(27.2744490593061,-0.241969073019072,33.8637293696319));
#71017=CARTESIAN_POINT('Ctrl Pts',(27.2744490593088,-0.241969073017592,
33.8637293696347));
#71018=CARTESIAN_POINT('Ctrl Pts',(27.2904701802914,-0.233224867930958,
33.8804609779983));
#71019=CARTESIAN_POINT('Ctrl Pts',(27.3062967880495,-0.224586826672017,
33.8969505670841));
#71020=CARTESIAN_POINT('',(27.2932696904648,-0.400983782787811,33.8637293696319));
#71021=CARTESIAN_POINT('Origin',(30.,-1.32966554433622E-14,33.8637293696319));
#71022=CARTESIAN_POINT('',(27.328295268743,-0.410451051657984,33.8969505670765));
#71023=CARTESIAN_POINT('Ctrl Pts',(27.328295268751,-0.410451051660133,33.8969505670841));
#71024=CARTESIAN_POINT('Ctrl Pts',(27.3108894407404,-0.40574632837547,33.8804609779983));
#71025=CARTESIAN_POINT('Ctrl Pts',(27.2932696904678,-0.400983782788603,
33.8637293696347));
#71026=CARTESIAN_POINT('',(27.3322214554001,-0.435240018610796,33.8969505670765));
#71027=CARTESIAN_POINT('Origin',(27.3246909766178,-0.423727307748468,33.8912940899386));
#71028=CARTESIAN_POINT('',(27.3018356979128,-0.45506742528707,33.8637293696319));
#71029=CARTESIAN_POINT('Ctrl Pts',(27.3018356979154,-0.455067425285398,
33.8637293696347));
#71030=CARTESIAN_POINT('Ctrl Pts',(27.3171213687048,-0.445093172999969,
33.8804609779984));
#71031=CARTESIAN_POINT('Ctrl Pts',(27.332221455407,-0.435240018606285,33.8969505670841));
#71032=CARTESIAN_POINT('',(27.3330744616826,-0.612115296072328,33.8637293696319));
#71033=CARTESIAN_POINT('Origin',(30.,-1.32966554433622E-14,33.8637293696319));
#71034=CARTESIAN_POINT('',(27.3687348611467,-0.618805305313063,33.8969505670765));
#71035=CARTESIAN_POINT('Ctrl Pts',(27.3687348611549,-0.618805305314591,
33.8969505670841));
#71036=CARTESIAN_POINT('Ctrl Pts',(27.3510135611686,-0.615480730647799,
33.8804609779983));
#71037=CARTESIAN_POINT('Ctrl Pts',(27.3330744616856,-0.6121152960729,33.8637293696347));
#71038=CARTESIAN_POINT('',(27.3745938646118,-0.643209811098888,33.8969505670765));
#71039=CARTESIAN_POINT('Origin',(27.3661835083535,-0.632323382398592,33.8912943077151));
#71040=CARTESIAN_POINT('',(27.3458574166725,-0.665360135552901,33.8637293696319));
#71041=CARTESIAN_POINT('Ctrl Pts',(27.345857416675,-0.665360135551053,33.8637293696347));
#71042=CARTESIAN_POINT('Ctrl Pts',(27.3603133960278,-0.654217330648938,
33.8804609779984));
#71043=CARTESIAN_POINT('Ctrl Pts',(27.3745938646183,-0.643209811093851,
33.8969505670841));
#71044=CARTESIAN_POINT('',(27.3893217156868,-0.819472915007569,33.8637293696319));
#71045=CARTESIAN_POINT('Origin',(30.,-1.32966554433622E-14,33.8637293696319));
#71046=CARTESIAN_POINT('',(27.4253970781159,-0.823344418487241,33.8969505670765));
#71047=CARTESIAN_POINT('Ctrl Pts',(27.4253970781241,-0.823344418488121,
33.8969505670841));
#71048=CARTESIAN_POINT('Ctrl Pts',(27.4074695638695,-0.821420489547552,
33.8804609779983));
#71049=CARTESIAN_POINT('Ctrl Pts',(27.3893217156899,-0.819472915007892,
33.8637293696347));
#71050=CARTESIAN_POINT('',(27.4331527756843,-0.847214001212589,33.8969505670765));
#71051=CARTESIAN_POINT('Origin',(27.4239143438363,-0.837020957758988,33.8912944725679));
#71052=CARTESIAN_POINT('',(27.4062428070504,-0.871550679328351,33.8637293696319));
#71053=CARTESIAN_POINT('Ctrl Pts',(27.4062428070527,-0.871550679326329,
33.8637293696347));
#71054=CARTESIAN_POINT('Ctrl Pts',(27.4197799690492,-0.859308020905111,
33.8804609779983));
#71055=CARTESIAN_POINT('Ctrl Pts',(27.4331527756904,-0.847214001207053,
33.8969505670841));
#71056=CARTESIAN_POINT('',(27.4616646694525,-1.02177821091939,33.8637293696319));
#71057=CARTESIAN_POINT('Origin',(30.,-1.32966554433622E-14,33.8637293696319));
#71058=CARTESIAN_POINT('',(27.4979325782409,-1.02280733953164,33.8969505670765));
#71059=CARTESIAN_POINT('Ctrl Pts',(27.4979325782492,-1.02280733953187,33.8969505670841));
#71060=CARTESIAN_POINT('Ctrl Pts',(27.479909378813,-1.02229591797922,33.8804609779983));
#71061=CARTESIAN_POINT('Ctrl Pts',(27.4616646694556,-1.02177821091947,33.8637293696347));
#71062=CARTESIAN_POINT('',(27.507537153458,-1.04599483528157,33.8969505670765));
#71063=CARTESIAN_POINT('Origin',(27.4975275671491,-1.03655801106889,33.8912946002427));
#71064=CARTESIAN_POINT('',(27.4826195730347,-1.07236782334573,33.8637293696319));
#71065=CARTESIAN_POINT('Ctrl Pts',(27.4826195730368,-1.07236782334351,33.8637293696347));
#71066=CARTESIAN_POINT('Ctrl Pts',(27.4951544565716,-1.05910079146347,33.8804609779983));
#71067=CARTESIAN_POINT('Ctrl Pts',(27.5075371534637,-1.04599483527557,33.8969505670841));
#71068=CARTESIAN_POINT('',(27.5496573046131,-1.21778390438516,33.8637293696319));
#71069=CARTESIAN_POINT('Origin',(30.,-1.32966554433622E-14,33.8637293696319));
#71070=CARTESIAN_POINT('',(27.5858941560428,-1.21596431320988,33.8969505670765));
#71071=CARTESIAN_POINT('Ctrl Pts',(27.5858941560511,-1.21596431320946,33.8969505670841));
#71072=CARTESIAN_POINT('Ctrl Pts',(27.5678863904513,-1.21686855212866,33.8804609779983));
#71073=CARTESIAN_POINT('Ctrl Pts',(27.5496573046162,-1.217783904385,33.8637293696347));
#71074=CARTESIAN_POINT('',(27.5972883935086,-1.23832676336246,33.8969505670765));
#71075=CARTESIAN_POINT('Origin',(27.5865693373251,-1.22970433386023,33.891294700665));
#71076=CARTESIAN_POINT('',(27.5745168264651,-1.2665734631337,33.8637293696319));
#71077=CARTESIAN_POINT('Ctrl Pts',(27.574516826467,-1.26657346313129,33.8637293696347));
#71078=CARTESIAN_POINT('Ctrl Pts',(27.5859721498149,-1.2523638534557,33.8804609779983));
#71079=CARTESIAN_POINT('Ctrl Pts',(27.5972883935138,-1.23832676335601,33.8969505670841));
#71080=CARTESIAN_POINT('',(27.6527571173125,-1.40628155512615,33.8637293696319));
#71081=CARTESIAN_POINT('Origin',(30.,-1.32966554433622E-14,33.8637293696319));
#71082=CARTESIAN_POINT('',(27.6887394991444,-1.40162446254801,33.8969505670765));
#71083=CARTESIAN_POINT('Ctrl Pts',(27.6887394991526,-1.40162446254695,33.8969505670841));
#71084=CARTESIAN_POINT('Ctrl Pts',(27.6708581912523,-1.40393878700437,33.8804609779983));
#71085=CARTESIAN_POINT('Ctrl Pts',(27.6527571173155,-1.40628155512576,33.8637293696347));
#71086=CARTESIAN_POINT('',(27.701853149596,-1.42302399516179,33.8969505670765));
#71087=CARTESIAN_POINT('Origin',(27.6904906884452,-1.4152691174526,33.8912947803756));
#71088=CARTESIAN_POINT('',(27.6813679902154,-1.45297025634303,33.8637293696319));
#71089=CARTESIAN_POINT('Ctrl Pts',(27.6813679902171,-1.4529702563405,33.8637293696347));
#71090=CARTESIAN_POINT('Ctrl Pts',(27.6916731275004,-1.43790567583818,33.8804609779983));
#71091=CARTESIAN_POINT('Ctrl Pts',(27.7018531496007,-1.42302399515497,33.8969505670841));
#71092=CARTESIAN_POINT('',(27.770328462921,-1.58610901244372,33.8637293696319));
#71093=CARTESIAN_POINT('Origin',(30.,-1.32966554433622E-14,33.8637293696319));
#71094=CARTESIAN_POINT('',(27.8058345318059,-1.5786431309871,33.8969505670765));
#71095=CARTESIAN_POINT('Ctrl Pts',(27.805834531814,-1.5786431309854,33.8969505670841));
#71096=CARTESIAN_POINT('Ctrl Pts',(27.7881899258225,-1.58235327240118,33.8804609779983));
#71097=CARTESIAN_POINT('Ctrl Pts',(27.770328462924,-1.5861090124431,33.8637293696347));
#71098=CARTESIAN_POINT('',(27.8205867452275,-1.59894781082744,33.8969505670765));
#71099=CARTESIAN_POINT('Origin',(27.8086509152839,-1.59210829514295,33.8912948438349));
#71100=CARTESIAN_POINT('',(27.8025142913294,-1.63040900476036,33.8637293696319));
#71101=CARTESIAN_POINT('Ctrl Pts',(27.8025142913309,-1.63040900475772,33.8637293696347));
#71102=CARTESIAN_POINT('Ctrl Pts',(27.8116057079513,-1.61458233157693,33.8804609779984));
#71103=CARTESIAN_POINT('Ctrl Pts',(27.8205867452316,-1.59894781082027,33.8969505670841));
#71104=CARTESIAN_POINT('',(27.9016464749967,-1.75615758026481,33.8637293696319));
#71105=CARTESIAN_POINT('Origin',(30.,-1.32966554433622E-14,33.8637293696319));
#71106=CARTESIAN_POINT('',(27.9364573242129,-1.74592893957155,33.8969505670765));
#71107=CARTESIAN_POINT('Ctrl Pts',(27.9364573242208,-1.74592893956922,33.8969505670841));
#71108=CARTESIAN_POINT('Ctrl Pts',(27.9191582050015,-1.75101202368778,33.8804609779983));
#71109=CARTESIAN_POINT('Ctrl Pts',(27.9016464749996,-1.75615758026396,33.8637293696347));
#71110=CARTESIAN_POINT('',(27.9527571483031,-1.76501358153525,33.8969505670765));
#71111=CARTESIAN_POINT('Origin',(27.9403215240917,-1.75913159602167,33.8912948941586));
#71112=CARTESIAN_POINT('',(27.9372088225755,-1.79779573949734,33.8637293696319));
#71113=CARTESIAN_POINT('Ctrl Pts',(27.9372088225768,-1.79779573949458,33.8637293696347));
#71114=CARTESIAN_POINT('Ctrl Pts',(27.9450304669278,-1.78130455033841,33.8804609779984));
#71115=CARTESIAN_POINT('Ctrl Pts',(27.9527571483066,-1.76501358152779,33.8969505670841));
#71116=CARTESIAN_POINT('',(28.0459015343274,-1.91537885262191,33.8637293696319));
#71117=CARTESIAN_POINT('Origin',(30.,-1.32966554433622E-14,33.8637293696319));
#71118=CARTESIAN_POINT('',(28.0798025434136,-1.90245051566325,33.8969505670765));
#71119=CARTESIAN_POINT('Ctrl Pts',(28.0798025434214,-1.90245051566032,33.8969505670841));
#71120=CARTESIAN_POINT('Ctrl Pts',(28.0629555657968,-1.90887520357775,33.8804609779983));
#71121=CARTESIAN_POINT('Ctrl Pts',(28.0459015343303,-1.91537885262082,33.8637293696347));
#71122=CARTESIAN_POINT('',(28.0975494843367,-1.92019745658631,33.8969505670765));
#71123=CARTESIAN_POINT('Origin',(28.0846907243829,-1.91530926701236,33.891294933562));
#71124=CARTESIAN_POINT('',(28.084621147378,-1.95409846567257,33.8637293696319));
#71125=CARTESIAN_POINT('Ctrl Pts',(28.0846211473791,-1.9540984656697,33.8637293696347));
#71126=CARTESIAN_POINT('Ctrl Pts',(28.0911247964222,-1.93704443420316,33.8804609779983));
#71127=CARTESIAN_POINT('Ctrl Pts',(28.0975494843396,-1.92019745657857,33.8969505670841));
#71128=CARTESIAN_POINT('',(28.2022042605026,-2.06279117742449,33.8637293696319));
#71129=CARTESIAN_POINT('Origin',(30.,-1.32966554433622E-14,33.8637293696319));
#71130=CARTESIAN_POINT('',(28.2349864184647,-2.04724285169689,33.8969505670765));
#71131=CARTESIAN_POINT('Ctrl Pts',(28.2349864184722,-2.04724285169334,33.8969505670841));
#71132=CARTESIAN_POINT('Ctrl Pts',(28.2186954496616,-2.05496953307223,33.8804609779983));
#71133=CARTESIAN_POINT('Ctrl Pts',(28.2022042605054,-2.06279117742317,33.8637293696347));
#71134=CARTESIAN_POINT('',(28.2540710604284,-2.06354267578707,33.8969505670765));
#71135=CARTESIAN_POINT('Origin',(28.2408684341297,-2.05967842174595,33.8912949636253));
#71136=CARTESIAN_POINT('',(28.2438424197351,-2.09835352500325,33.8637293696319));
#71137=CARTESIAN_POINT('Ctrl Pts',(28.243842419736,-2.09835352500031,33.8637293696347));
#71138=CARTESIAN_POINT('Ctrl Pts',(28.2489879763122,-2.08084179499844,33.8804609779983));
#71139=CARTESIAN_POINT('Ctrl Pts',(28.2540710604307,-2.06354267577914,33.8969505670841));
#71140=CARTESIAN_POINT('',(28.3695909952396,-2.19748570867058,33.8637293696319));
#71141=CARTESIAN_POINT('Origin',(30.,-1.32966554433622E-14,33.8637293696319));
#71142=CARTESIAN_POINT('',(28.4010521891725,-2.17941325477249,33.8969505670765));
#71143=CARTESIAN_POINT('Ctrl Pts',(28.4010521891797,-2.17941325476838,33.8969505670841));
#71144=CARTESIAN_POINT('Ctrl Pts',(28.385417668423,-2.18839429204864,33.8804609779983));
#71145=CARTESIAN_POINT('Ctrl Pts',(28.3695909952423,-2.19748570866905,33.8637293696347));
#71146=CARTESIAN_POINT('',(28.4213568690129,-2.19416546819403,33.8969505670765));
#71147=CARTESIAN_POINT('Origin',(28.4078917675746,-2.19134897714168,33.8912949854673));
#71148=CARTESIAN_POINT('',(28.4138909875562,-2.22967153707893,33.8637293696319));
#71149=CARTESIAN_POINT('Ctrl Pts',(28.4138909875569,-2.22967153707595,33.8637293696347));
#71150=CARTESIAN_POINT('Ctrl Pts',(28.4176467275988,-2.21181007417744,33.8804609779984));
#71151=CARTESIAN_POINT('Ctrl Pts',(28.4213568690146,-2.19416546818595,33.8969505670841));
#71152=CARTESIAN_POINT('',(28.5470297436569,-2.31863200978456,33.8637293696319));
#71153=CARTESIAN_POINT('Origin',(30.,-1.32966554433622E-14,33.8637293696319));
#71154=CARTESIAN_POINT('',(28.5769760048382,-2.29814685040397,33.8969505670765));
#71155=CARTESIAN_POINT('Ctrl Pts',(28.576976004845,-2.29814685039931,33.8969505670841));
#71156=CARTESIAN_POINT('Ctrl Pts',(28.5620943241618,-2.30832687249962,33.8804609779983));
#71157=CARTESIAN_POINT('Ctrl Pts',(28.5470297436595,-2.31863200978285,33.8637293696347));
#71158=CARTESIAN_POINT('',(28.5983755374519,-2.31126050085552,33.8969505670765));
#71159=CARTESIAN_POINT('Origin',(28.5847309718512,-2.30950914111276,33.891294999854));
#71160=CARTESIAN_POINT('',(28.5937184448738,-2.3472428826875,33.8637293696319));
#71161=CARTESIAN_POINT('Ctrl Pts',(28.5937184448742,-2.34724288268445,33.8637293696347));
#71162=CARTESIAN_POINT('Ctrl Pts',(28.5960612129955,-2.32914180874762,33.8804609779983));
#71163=CARTESIAN_POINT('Ctrl Pts',(28.598375537453,-2.31126050084731,33.8969505670841));
#71164=CARTESIAN_POINT('',(28.7334265368663,-2.42548317353484,33.8637293696319));
#71165=CARTESIAN_POINT('Origin',(30.,-1.32966554433622E-14,33.8637293696319));
#71166=CARTESIAN_POINT('',(28.7616732366375,-2.40271160649133,33.8969505670765));
#71167=CARTESIAN_POINT('Ctrl Pts',(28.761673236644,-2.40271160648615,33.8969505670841));
#71168=CARTESIAN_POINT('Ctrl Pts',(28.7476361465443,-2.41402785018505,33.8804609779983));
#71169=CARTESIAN_POINT('Ctrl Pts',(28.7334265368687,-2.42548317353292,33.8637293696347));
#71170=CARTESIAN_POINT('',(28.7840356867901,-2.41410584395713,33.8969505670765));
#71171=CARTESIAN_POINT('Origin',(28.7702957758346,-2.41343041757033,33.8912950072666));
#71172=CARTESIAN_POINT('',(28.7822160956148,-2.45034269538683,33.8637293696319));
#71173=CARTESIAN_POINT('Ctrl Pts',(28.782216095615,-2.45034269538378,33.8637293696347));
#71174=CARTESIAN_POINT('Ctrl Pts',(28.7831314478713,-2.43211360954867,33.8804609779983));
#71175=CARTESIAN_POINT('Ctrl Pts',(28.7840356867905,-2.41410584394888,33.8969505670841));
#71176=CARTESIAN_POINT('',(28.9276321766542,-2.51738042696528,33.8637293696319));
#71177=CARTESIAN_POINT('Origin',(30.,-1.32966554433622E-14,33.8637293696319));
#71178=CARTESIAN_POINT('',(28.9540051647184,-2.49246284654199,33.8969505670765));
#71179=CARTESIAN_POINT('Ctrl Pts',(28.9540051647244,-2.49246284653629,33.8969505670841));
#71180=CARTESIAN_POINT('Ctrl Pts',(28.9408992085365,-2.50484554342835,33.8804609779984));
#71181=CARTESIAN_POINT('Ctrl Pts',(28.9276321766564,-2.51738042696316,33.8637293696347));
#71182=CARTESIAN_POINT('',(28.9771926604683,-2.50206742175908,33.8969505670765));
#71183=CARTESIAN_POINT('Origin',(28.9634421120889,-2.50247209787259,33.8912950079413));
#71184=CARTESIAN_POINT('',(28.9782217890806,-2.53833533054747,33.8637293696319));
#71185=CARTESIAN_POINT('Ctrl Pts',(28.9782217890805,-2.53833533054441,33.8637293696347));
#71186=CARTESIAN_POINT('Ctrl Pts',(28.9777040820207,-2.52009062118697,33.8804609779983));
#71187=CARTESIAN_POINT('Ctrl Pts',(28.9771926604681,-2.50206742175082,33.8969505670841));
#71188=CARTESIAN_POINT('',(29.1284493206716,-2.59375719294953,33.8637293696319));
#71189=CARTESIAN_POINT('Origin',(30.,-1.32966554433622E-14,33.8637293696319));
#71190=CARTESIAN_POINT('',(29.1527859987874,-2.56684722431572,33.8969505670765));
#71191=CARTESIAN_POINT('Ctrl Pts',(29.1527859987929,-2.56684722430957,33.8969505670841));
#71192=CARTESIAN_POINT('Ctrl Pts',(29.1406919790949,-2.58022003095078,33.8804609779984));
#71193=CARTESIAN_POINT('Ctrl Pts',(29.1284493206736,-2.59375719294726,33.8637293696347));
#71194=CARTESIAN_POINT('',(29.1766555815127,-2.57460292188404,33.8969505670765));
#71195=CARTESIAN_POINT('Origin',(29.1629791704777,-2.57608521103258,33.8912950018861));
#71196=CARTESIAN_POINT('',(29.1805270849924,-2.61067828431313,33.8637293696319));
#71197=CARTESIAN_POINT('Ctrl Pts',(29.1805270849921,-2.61067828431009,33.8637293696347));
#71198=CARTESIAN_POINT('Ctrl Pts',(29.1785795104524,-2.59253043613049,33.8804609779983));
#71199=CARTESIAN_POINT('Ctrl Pts',(29.1766555815118,-2.57460292187582,33.8969505670841));
#71200=CARTESIAN_POINT('',(29.334639864447,-2.65414258332747,33.8637293696319));
#71201=CARTESIAN_POINT('Origin',(30.,-1.32966554433622E-14,33.8637293696319));
#71202=CARTESIAN_POINT('',(29.3567901889011,-2.62540613538822,33.8969505670765));
#71203=CARTESIAN_POINT('Ctrl Pts',(29.3567901889061,-2.62540613538166,33.8969505670841));
#71204=CARTESIAN_POINT('Ctrl Pts',(29.345782669351,-2.63968660397217,33.8804609779983));
#71205=CARTESIAN_POINT('Ctrl Pts',(29.3346398644489,-2.65414258332506,33.8637293696347));
#71206=CARTESIAN_POINT('',(29.3811946946869,-2.63126513885324,33.8969505670765));
#71207=CARTESIAN_POINT('Origin',(29.3676767399569,-2.63381590833404,33.8912949888765));
#71208=CARTESIAN_POINT('',(29.3878847039276,-2.66692553831738,33.8637293696319));
#71209=CARTESIAN_POINT('Ctrl Pts',(29.3878847039271,-2.66692553831437,33.8637293696347));
#71210=CARTESIAN_POINT('Ctrl Pts',(29.3845192693522,-2.64898643883142,33.8804609779983));
#71211=CARTESIAN_POINT('Ctrl Pts',(29.3811946946854,-2.63126513884512,33.8969505670841));
#71212=CARTESIAN_POINT('',(29.5449325747129,-2.69816430208721,33.8637293696319));
#71213=CARTESIAN_POINT('Origin',(30.,-1.32966554433622E-14,33.8637293696319));
#71214=CARTESIAN_POINT('',(29.5647599813891,-2.66777854459992,33.8969505670765));
#71215=CARTESIAN_POINT('Ctrl Pts',(29.5647599813936,-2.667778544593,33.8969505670841));
#71216=CARTESIAN_POINT('Ctrl Pts',(29.554906827,-2.68287863129519,33.8804609779983));
#71217=CARTESIAN_POINT('Ctrl Pts',(29.5449325747145,-2.69816430208464,33.8637293696347));
#71218=CARTESIAN_POINT('',(29.589548948342,-2.67170473125696,33.8969505670765));
#71219=CARTESIAN_POINT('Origin',(29.5762727932907,-2.67530826149246,33.8912949684251));
#71220=CARTESIAN_POINT('',(29.5990162172121,-2.70673030953517,33.8637293696319));
#71221=CARTESIAN_POINT('Ctrl Pts',(29.5990162172114,-2.70673030953221,33.8637293696347));
#71222=CARTESIAN_POINT('Ctrl Pts',(29.5942536716245,-2.68911055925957,33.8804609779984));
#71223=CARTESIAN_POINT('Ctrl Pts',(29.5895489483398,-2.67170473124899,33.8969505670841));
#71224=CARTESIAN_POINT('',(29.7580309269809,-2.72555094069392,33.8637293696319));
#71225=CARTESIAN_POINT('Origin',(30.,-1.32966554433622E-14,33.8637293696319));
#71226=CARTESIAN_POINT('',(29.775413173324,-2.69370321195777,33.8969505670765));
#71227=CARTESIAN_POINT('Ctrl Pts',(29.7754131733279,-2.6937032119505,33.8969505670841));
#71228=CARTESIAN_POINT('Ctrl Pts',(29.766775132069,-2.70952981970859,33.8804609779984));
#71229=CARTESIAN_POINT('Ctrl Pts',(29.7580309269823,-2.72555094069122,33.8637293696347));
#71230=CARTESIAN_POINT('',(29.8004337692193,-2.6956723755605,33.8969505670765));
#71231=CARTESIAN_POINT('Origin',(29.7874812679387,-2.70030645711978,33.8912949397144));
#71232=CARTESIAN_POINT('',(29.8126199288582,-2.72984718831551,33.8637293696319));
#71233=CARTESIAN_POINT('Ctrl Pts',(29.8126199288571,-2.72984718831264,33.8637293696347));
#71234=CARTESIAN_POINT('Ctrl Pts',(29.8064896349355,-2.7126554188699,33.8804609779983));
#71235=CARTESIAN_POINT('Ctrl Pts',(29.8004337692165,-2.69567237555272,33.8969505670841));
#71236=CARTESIAN_POINT('',(29.9726210990469,-2.73613365141358,33.8637293696319));
#71237=CARTESIAN_POINT('Origin',(30.,-1.32966554433622E-14,33.8637293696319));
#71238=CARTESIAN_POINT('',(29.987451017728,-2.70302030326669,33.8969505670765));
#71239=CARTESIAN_POINT('Ctrl Pts',(29.9874510177314,-2.70302030325915,33.8969505670841));
#71240=CARTESIAN_POINT('Ctrl Pts',(29.980081346004,-2.71947585577343,33.8804609779983));
#71241=CARTESIAN_POINT('Ctrl Pts',(29.9726210990482,-2.73613365141081,33.8637293696347));
#71242=CARTESIAN_POINT('Ctrl Pts',(30.,-2.69489040503949,33.9051095949605));
#71243=CARTESIAN_POINT('Ctrl Pts',(29.9982996971592,-2.69489040503949,33.9051095949605));
#71244=CARTESIAN_POINT('Ctrl Pts',(29.9965490639354,-2.69522714758869,33.9047710768107));
#71245=CARTESIAN_POINT('Ctrl Pts',(29.9934248389279,-2.69644647069985,33.9035459832655));
#71246=CARTESIAN_POINT('Ctrl Pts',(29.9920523583067,-2.69733049287042,33.9026580100842));
#71247=CARTESIAN_POINT('Ctrl Pts',(29.9894391186861,-2.69960157002983,33.9003782103613));
#71248=CARTESIAN_POINT('Ctrl Pts',(29.9882404972758,-2.7012574944688,33.8987170220582));
#71249=CARTESIAN_POINT('Ctrl Pts',(29.987451017728,-2.7030203032667,33.8969505670765));
#71250=CARTESIAN_POINT('',(30.,-2.73627063036813,33.8637293696319));
#71251=CARTESIAN_POINT('Origin',(30.,-1.32966554433622E-14,31.5762293696319));
#71252=CARTESIAN_POINT('',(30.012548982272,2.70302030326666,31.5905494329235));
#71253=CARTESIAN_POINT('',(30.,2.69489040503946,31.5823904050395));
#71254=CARTESIAN_POINT('Ctrl Pts',(30.012548982272,2.70302030326668,31.5905494329235));
#71255=CARTESIAN_POINT('Ctrl Pts',(30.0117595027242,2.70125749446877,31.5887829779419));
#71256=CARTESIAN_POINT('Ctrl Pts',(30.0105608813139,2.6996015700298,31.5871217896387));
#71257=CARTESIAN_POINT('Ctrl Pts',(30.0079476416933,2.69733049287039,31.5848419899159));
#71258=CARTESIAN_POINT('Ctrl Pts',(30.0065751610721,2.69644647069982,31.5839540167345));
#71259=CARTESIAN_POINT('Ctrl Pts',(30.0034509360646,2.69522714758867,31.5827289231894));
#71260=CARTESIAN_POINT('Ctrl Pts',(30.0017003028408,2.69489040503946,31.5823904050395));
#71261=CARTESIAN_POINT('Ctrl Pts',(30.,2.69489040503946,31.5823904050395));
#71262=CARTESIAN_POINT('',(30.0273789009535,2.73613365141461,31.6237706303691));
#71263=CARTESIAN_POINT('Ctrl Pts',(30.0273789009505,2.73613365140797,31.6237706303625));
#71264=CARTESIAN_POINT('Ctrl Pts',(30.0199186539932,2.71947585576695,31.6070390219952));
#71265=CARTESIAN_POINT('Ctrl Pts',(30.0125489822642,2.70302030324912,31.5905494329059));
#71266=CARTESIAN_POINT('',(30.1873800711414,2.72984718831658,31.6237706303691));
#71267=CARTESIAN_POINT('Origin',(30.,-1.32966554433622E-14,31.6237706303681));
#71268=CARTESIAN_POINT('',(30.1995662307806,2.69567237556048,31.5905494329235));
#71269=CARTESIAN_POINT('Ctrl Pts',(30.1995662307774,2.69567237556935,31.5905494329321));
#71270=CARTESIAN_POINT('Ctrl Pts',(30.1935103650619,2.71265541887687,31.6070390220085));
#71271=CARTESIAN_POINT('Ctrl Pts',(30.1873800711438,2.72984718830972,31.6237706303625));
#71272=CARTESIAN_POINT('',(30.224586826676,2.69370321195774,31.5905494329235));
#71273=CARTESIAN_POINT('Origin',(30.2125187883694,2.70030745889013,31.5962062072437));
#71274=CARTESIAN_POINT('',(30.2419690730196,2.72555094069491,31.6237706303691));
#71275=CARTESIAN_POINT('Ctrl Pts',(30.2419690730161,2.72555094068852,31.6237706303625));
#71276=CARTESIAN_POINT('Ctrl Pts',(30.2332248679276,2.70952981970239,31.6070390219952));
#71277=CARTESIAN_POINT('Ctrl Pts',(30.2245868266668,2.69370321194088,31.5905494329059));
#71278=CARTESIAN_POINT('',(30.4009837827875,2.70673030953627,31.6237706303691));
#71279=CARTESIAN_POINT('Origin',(30.,-1.32966554433622E-14,31.6237706303681));
#71280=CARTESIAN_POINT('',(30.410451051658,2.67170473125694,31.5905494329235));
#71281=CARTESIAN_POINT('Ctrl Pts',(30.4104510516555,2.67170473126603,31.5905494329321));
#71282=CARTESIAN_POINT('Ctrl Pts',(30.4057463283736,2.68911055926674,31.6070390220085));
#71283=CARTESIAN_POINT('Ctrl Pts',(30.4009837827894,2.70673030952925,31.6237706303625));
#71284=CARTESIAN_POINT('',(30.4352400186108,2.66777854459989,31.5905494329235));
#71285=CARTESIAN_POINT('Origin',(30.4237273077485,2.6753090233822,31.5962059100614));
#71286=CARTESIAN_POINT('',(30.4550674252877,2.69816430208816,31.6237706303691));
#71287=CARTESIAN_POINT('Ctrl Pts',(30.4550674252837,2.69816430208208,31.6237706303625));
#71288=CARTESIAN_POINT('Ctrl Pts',(30.4450931729961,2.68287863128927,31.6070390219952));
#71289=CARTESIAN_POINT('Ctrl Pts',(30.4352400186003,2.66777854458381,31.5905494329059));
#71290=CARTESIAN_POINT('',(30.6121152960721,2.6669255383185,31.6237706303691));
#71291=CARTESIAN_POINT('Origin',(30.,-1.32966554433622E-14,31.6237706303681));
#71292=CARTESIAN_POINT('',(30.6188053053131,2.63126513885322,31.5905494329235));
#71293=CARTESIAN_POINT('Ctrl Pts',(30.6188053053114,2.63126513886247,31.5905494329321));
#71294=CARTESIAN_POINT('Ctrl Pts',(30.6154807306465,2.64898643883871,31.6070390220085));
#71295=CARTESIAN_POINT('Ctrl Pts',(30.6121152960735,2.66692553831135,31.6237706303626));
#71296=CARTESIAN_POINT('',(30.6432098110989,2.62540613538819,31.5905494329235));
#71297=CARTESIAN_POINT('Origin',(30.6323233823986,2.63381649164648,31.5962056922849));
#71298=CARTESIAN_POINT('',(30.6653601355536,2.65414258332836,31.6237706303691));
#71299=CARTESIAN_POINT('Ctrl Pts',(30.6653601355491,2.65414258332261,31.6237706303625));
#71300=CARTESIAN_POINT('Ctrl Pts',(30.6542173306446,2.63968660396658,31.6070390219952));
#71301=CARTESIAN_POINT('Ctrl Pts',(30.6432098110871,2.62540613537299,31.5905494329059));
#71302=CARTESIAN_POINT('',(30.8194729150074,2.61067828431427,31.6237706303691));
#71303=CARTESIAN_POINT('Origin',(30.,-1.32966554433622E-14,31.6237706303681));
#71304=CARTESIAN_POINT('',(30.8233444184872,2.57460292188402,31.5905494329235));
#71305=CARTESIAN_POINT('Ctrl Pts',(30.8233444184862,2.57460292189339,31.5905494329321));
#71306=CARTESIAN_POINT('Ctrl Pts',(30.8214204895467,2.59253043613788,31.6070390220085));
#71307=CARTESIAN_POINT('Ctrl Pts',(30.8194729150082,2.61067828430704,31.6237706303625));
#71308=CARTESIAN_POINT('',(30.8472140012126,2.5668472243157,31.5905494329235));
#71309=CARTESIAN_POINT('Origin',(30.837020957759,2.57608565616362,31.596205527432));
#71310=CARTESIAN_POINT('',(30.8715506793291,2.59375719295037,31.6237706303691));
#71311=CARTESIAN_POINT('Ctrl Pts',(30.8715506793242,2.59375719294498,31.6237706303625));
#71312=CARTESIAN_POINT('Ctrl Pts',(30.8593080209003,2.58022003094555,31.6070390219952));
#71313=CARTESIAN_POINT('Ctrl Pts',(30.8472140011997,2.56684722430147,31.5905494329059));
#71314=CARTESIAN_POINT('',(31.0217782109193,2.53833533054861,31.6237706303691));
#71315=CARTESIAN_POINT('Origin',(30.,-1.32966554433622E-14,31.6237706303681));
#71316=CARTESIAN_POINT('',(31.0228073395316,2.50206742175906,31.5905494329235));
#71317=CARTESIAN_POINT('Ctrl Pts',(31.0228073395313,2.50206742176848,31.5905494329321));
#71318=CARTESIAN_POINT('Ctrl Pts',(31.022295917979,2.52009062119439,31.6070390220085));
#71319=CARTESIAN_POINT('Ctrl Pts',(31.0217782109195,2.53833533054134,31.6237706303625));
#71320=CARTESIAN_POINT('',(31.0459948352816,2.49246284654197,31.5905494329235));
#71321=CARTESIAN_POINT('Origin',(31.0365580110689,2.5024724328509,31.5962053997573));
#71322=CARTESIAN_POINT('',(31.0723678233466,2.51738042696606,31.6237706303691));
#71323=CARTESIAN_POINT('Ctrl Pts',(31.0723678233413,2.51738042696106,31.6237706303625));
#71324=CARTESIAN_POINT('Ctrl Pts',(31.0591007914584,2.50484554342351,31.6070390219952));
#71325=CARTESIAN_POINT('Ctrl Pts',(31.0459948352676,2.49246284652878,31.5905494329059));
#71326=CARTESIAN_POINT('',(31.2177839043852,2.45034269538797,31.6237706303691));
#71327=CARTESIAN_POINT('Origin',(30.,-1.32966554433622E-14,31.6237706303681));
#71328=CARTESIAN_POINT('',(31.2159643132099,2.41410584395711,31.5905494329235));
#71329=CARTESIAN_POINT('Ctrl Pts',(31.2159643132104,2.41410584396651,31.5905494329321));
#71330=CARTESIAN_POINT('Ctrl Pts',(31.216868552129,2.43211360955606,31.6070390220085));
#71331=CARTESIAN_POINT('Ctrl Pts',(31.2177839043849,2.4503426953807,31.6237706303625));
#71332=CARTESIAN_POINT('',(31.2383267633625,2.40271160649132,31.5905494329235));
#71333=CARTESIAN_POINT('Origin',(31.2297043338602,2.41343066267493,31.5962052993351));
#71334=CARTESIAN_POINT('',(31.2665734631346,2.42548317353555,31.6237706303691));
#71335=CARTESIAN_POINT('Ctrl Pts',(31.266573463129,2.42548317353098,31.6237706303625));
#71336=CARTESIAN_POINT('Ctrl Pts',(31.2523638534503,2.4140278501806,31.6070390219952));
#71337=CARTESIAN_POINT('Ctrl Pts',(31.2383267633475,2.40271160647926,31.5905494329059));
#71338=CARTESIAN_POINT('',(31.4062815551263,2.34724288268863,31.6237706303691));
#71339=CARTESIAN_POINT('Origin',(30.,-1.32966554433622E-14,31.6237706303681));
#71340=CARTESIAN_POINT('',(31.401624462548,2.3112605008555,31.5905494329235));
#71341=CARTESIAN_POINT('Ctrl Pts',(31.4016244625492,2.31126050086484,31.5905494329321));
#71342=CARTESIAN_POINT('Ctrl Pts',(31.4039387870053,2.32914180875499,31.6070390220085));
#71343=CARTESIAN_POINT('Ctrl Pts',(31.4062815551254,2.34724288268141,31.6237706303625));
#71344=CARTESIAN_POINT('',(31.4230239951618,2.29814685040396,31.5905494329235));
#71345=CARTESIAN_POINT('Origin',(31.4152691174526,2.30950931155475,31.5962052196244));
#71346=CARTESIAN_POINT('',(31.452970256344,2.3186320097852,31.6237706303691));
#71347=CARTESIAN_POINT('Ctrl Pts',(31.452970256338,2.31863200978109,31.6237706303625));
#71348=CARTESIAN_POINT('Ctrl Pts',(31.4379056758324,2.30832687249561,31.6070390219952));
#71349=CARTESIAN_POINT('Ctrl Pts',(31.4230239951459,2.2981468503931,31.5905494329059));
#71350=CARTESIAN_POINT('',(31.5861090124439,2.22967153708005,31.6237706303691));
#71351=CARTESIAN_POINT('Origin',(30.,-1.32966554433622E-14,31.6237706303681));
#71352=CARTESIAN_POINT('',(31.5786431309871,2.19416546819402,31.5905494329235));
#71353=CARTESIAN_POINT('Ctrl Pts',(31.578643130989,2.19416546820324,31.5905494329321));
#71354=CARTESIAN_POINT('Ctrl Pts',(31.5823532724027,2.21181007418469,31.6070390220085));
#71355=CARTESIAN_POINT('Ctrl Pts',(31.5861090124425,2.22967153707293,31.6237706303625));
#71356=CARTESIAN_POINT('',(31.5989478108274,2.17941325477248,31.5905494329235));
#71357=CARTESIAN_POINT('Origin',(31.5921082951429,2.19134908471604,31.596205156165));
#71358=CARTESIAN_POINT('',(31.6304090047614,2.19748570867114,31.6237706303691));
#71359=CARTESIAN_POINT('Ctrl Pts',(31.6304090047551,2.19748570866755,31.6237706303626));
#71360=CARTESIAN_POINT('Ctrl Pts',(31.6145823315708,2.18839429204514,31.6070390219952));
#71361=CARTESIAN_POINT('Ctrl Pts',(31.5989478108108,2.17941325476293,31.5905494329059));
#71362=CARTESIAN_POINT('',(31.7561575802651,2.09835352500435,31.6237706303691));
#71363=CARTESIAN_POINT('Origin',(30.,-1.32966554433622E-14,31.6237706303681));
#71364=CARTESIAN_POINT('',(31.7459289395715,2.06354267578706,31.5905494329235));
#71365=CARTESIAN_POINT('Ctrl Pts',(31.7459289395742,2.06354267579611,31.5905494329321));
#71366=CARTESIAN_POINT('Ctrl Pts',(31.7510120236898,2.08084179500558,31.6070390220085));
#71367=CARTESIAN_POINT('Ctrl Pts',(31.7561575802631,2.09835352499738,31.6237706303625));
#71368=CARTESIAN_POINT('',(31.7650135815352,2.04724285169688,31.5905494329235));
#71369=CARTESIAN_POINT('Origin',(31.7591315960216,2.05967847590828,31.5962051058414));
#71370=CARTESIAN_POINT('',(31.7977957394984,2.06279117742498,31.6237706303691));
#71371=CARTESIAN_POINT('Ctrl Pts',(31.7977957394918,2.06279117742187,31.6237706303625));
#71372=CARTESIAN_POINT('Ctrl Pts',(31.781304550332,2.05496953306921,31.6070390219952));
#71373=CARTESIAN_POINT('Ctrl Pts',(31.7650135815179,2.04724285168864,31.5905494329059));
#71374=CARTESIAN_POINT('',(31.9153788526223,1.95409846567364,31.6237706303691));
#71375=CARTESIAN_POINT('Origin',(30.,-1.32966554433622E-14,31.6237706303681));
#71376=CARTESIAN_POINT('',(31.9024505156632,1.9201974565863,31.5905494329235));
#71377=CARTESIAN_POINT('Ctrl Pts',(31.9024505156666,1.92019745659511,31.5905494329321));
#71378=CARTESIAN_POINT('Ctrl Pts',(31.9088752035804,1.93704443421013,31.6070390220085));
#71379=CARTESIAN_POINT('Ctrl Pts',(31.9153788526197,1.95409846566686,31.6237706303625));
#71380=CARTESIAN_POINT('',(31.9201974565863,1.90245051566323,31.5905494329235));
#71381=CARTESIAN_POINT('Origin',(31.9153092670123,1.91530927561703,31.596205066438));
#71382=CARTESIAN_POINT('',(31.9540984656736,1.91537885262231,31.6237706303691));
#71383=CARTESIAN_POINT('Ctrl Pts',(31.9540984656668,1.9153788526197,31.6237706303625));
#71384=CARTESIAN_POINT('Ctrl Pts',(31.9370444341966,1.90887520357521,31.6070390219952));
#71385=CARTESIAN_POINT('Ctrl Pts',(31.9201974565683,1.90245051565638,31.5905494329059));
#71386=CARTESIAN_POINT('',(32.062791177425,1.79779573949838,31.6237706303691));
#71387=CARTESIAN_POINT('Origin',(30.,-1.32966554433622E-14,31.6237706303681));
#71388=CARTESIAN_POINT('',(32.0472428516969,1.76501358153524,31.5905494329235));
#71389=CARTESIAN_POINT('Ctrl Pts',(32.0472428517009,1.76501358154374,31.5905494329321));
#71390=CARTESIAN_POINT('Ctrl Pts',(32.0549695330754,1.78130455034511,31.6070390220085));
#71391=CARTESIAN_POINT('Ctrl Pts',(32.0627911774219,1.7977957394918,31.6237706303625));
#71392=CARTESIAN_POINT('',(32.0635426757871,1.74592893957153,31.5905494329235));
#71393=CARTESIAN_POINT('Origin',(32.059678421746,1.75913156587022,31.5962050363748));
#71394=CARTESIAN_POINT('',(32.0983535250043,1.75615758026513,31.6237706303691));
#71395=CARTESIAN_POINT('Ctrl Pts',(32.0983535249974,1.75615758026307,31.6237706303625));
#71396=CARTESIAN_POINT('Ctrl Pts',(32.0808417949917,1.75101202368577,31.6070390219952));
#71397=CARTESIAN_POINT('Ctrl Pts',(32.0635426757687,1.74592893956612,31.5905494329059));
#71398=CARTESIAN_POINT('',(32.1974857086711,1.63040900476136,31.6237706303691));
#71399=CARTESIAN_POINT('Origin',(30.,-1.32966554433622E-14,31.6237706303681));
#71400=CARTESIAN_POINT('',(32.1794132547725,1.59894781082743,31.5905494329235));
#71401=CARTESIAN_POINT('Ctrl Pts',(32.1794132547772,1.59894781083559,31.5905494329321));
#71402=CARTESIAN_POINT('Ctrl Pts',(32.1883942920524,1.61458233158336,31.6070390220085));
#71403=CARTESIAN_POINT('Ctrl Pts',(32.1974857086675,1.63040900475503,31.6237706303625));
#71404=CARTESIAN_POINT('',(32.194165468194,1.57864313098709,31.5905494329235));
#71405=CARTESIAN_POINT('Origin',(32.1913489771416,1.59210823242537,31.5962050145327));
#71406=CARTESIAN_POINT('',(32.22967153708,1.58610901244395,31.6237706303691));
#71407=CARTESIAN_POINT('Ctrl Pts',(32.2296715370729,1.58610901244245,31.6237706303625));
#71408=CARTESIAN_POINT('Ctrl Pts',(32.2118100741705,1.58235327239971,31.6070390219952));
#71409=CARTESIAN_POINT('Ctrl Pts',(32.1941654681752,1.57864313098313,31.5905494329059));
#71410=CARTESIAN_POINT('',(32.3186320097852,1.45297025634397,31.6237706303691));
#71411=CARTESIAN_POINT('Origin',(30.,-1.32966554433622E-14,31.6237706303681));
#71412=CARTESIAN_POINT('',(32.298146850404,1.42302399516178,31.5905494329235));
#71413=CARTESIAN_POINT('Ctrl Pts',(32.2981468504093,1.42302399516954,31.5905494329321));
#71414=CARTESIAN_POINT('Ctrl Pts',(32.3083268725038,1.43790567584429,31.6070390220085));
#71415=CARTESIAN_POINT('Ctrl Pts',(32.3186320097811,1.45297025633794,31.6237706303625));
#71416=CARTESIAN_POINT('',(32.3112605008555,1.401624462548,31.5905494329235));
#71417=CARTESIAN_POINT('Origin',(32.3095091411128,1.41526902814876,31.596205000146));
#71418=CARTESIAN_POINT('',(32.3472428826886,1.40628155512629,31.6237706303691));
#71419=CARTESIAN_POINT('Ctrl Pts',(32.3472428826814,1.40628155512536,31.6237706303625));
#71420=CARTESIAN_POINT('Ctrl Pts',(32.3291418087406,1.40393878700346,31.6070390219952));
#71421=CARTESIAN_POINT('Ctrl Pts',(32.3112605008365,1.40162446254554,31.5905494329059));
#71422=CARTESIAN_POINT('',(32.4254831735355,1.26657346313459,31.6237706303691));
#71423=CARTESIAN_POINT('Origin',(30.,-1.32966554433622E-14,31.6237706303681));
#71424=CARTESIAN_POINT('',(32.4027116064913,1.23832676336245,31.5905494329235));
#71425=CARTESIAN_POINT('Ctrl Pts',(32.4027116064972,1.23832676336979,31.5905494329321));
#71426=CARTESIAN_POINT('Ctrl Pts',(32.4140278501897,1.2523638534615,31.6070390220085));
#71427=CARTESIAN_POINT('Ctrl Pts',(32.425483173531,1.26657346312893,31.6237706303625));
#71428=CARTESIAN_POINT('',(32.4141058439571,1.21596431320987,31.5905494329235));
#71429=CARTESIAN_POINT('Origin',(32.4134304175703,1.22970422416531,31.5962049927334));
#71430=CARTESIAN_POINT('',(32.450342695388,1.21778390438521,31.6237706303691));
#71431=CARTESIAN_POINT('Ctrl Pts',(32.4503426953807,1.21778390438485,31.6237706303625));
#71432=CARTESIAN_POINT('Ctrl Pts',(32.4321136095416,1.2168685521283,31.6070390219952));
#71433=CARTESIAN_POINT('Ctrl Pts',(32.4141058439379,1.21596431320891,31.5905494329059));
#71434=CARTESIAN_POINT('',(32.517380426966,1.07236782334656,31.6237706303691));
#71435=CARTESIAN_POINT('Origin',(30.,-1.32966554433622E-14,31.6237706303681));
#71436=CARTESIAN_POINT('',(32.492462846542,1.04599483528156,31.5905494329235));
#71437=CARTESIAN_POINT('Ctrl Pts',(32.4924628465485,1.04599483528841,31.5905494329321));
#71438=CARTESIAN_POINT('Ctrl Pts',(32.5048455434335,1.05910079146886,31.6070390220085));
#71439=CARTESIAN_POINT('Ctrl Pts',(32.5173804269611,1.07236782334125,31.6237706303625));
#71440=CARTESIAN_POINT('',(32.5020674217591,1.02280733953163,31.5905494329235));
#71441=CARTESIAN_POINT('Origin',(32.5024720978725,1.03655788791103,31.5962049920587));
#71442=CARTESIAN_POINT('',(32.5383353305486,1.02177821091935,31.6237706303691));
#71443=CARTESIAN_POINT('Ctrl Pts',(32.5383353305413,1.02177821091956,31.6237706303625));
#71444=CARTESIAN_POINT('Ctrl Pts',(32.5200906211799,1.02229591797942,31.6070390219952));
#71445=CARTESIAN_POINT('Ctrl Pts',(32.5020674217399,1.02280733953218,31.5905494329059));
#71446=CARTESIAN_POINT('',(32.5937571929504,0.87155067932912,31.6237706303691));
#71447=CARTESIAN_POINT('Origin',(30.,-1.32966554433622E-14,31.6237706303681));
#71448=CARTESIAN_POINT('',(32.5668472243157,0.84721400121258,31.5905494329235));
#71449=CARTESIAN_POINT('Ctrl Pts',(32.5668472243227,0.847214001218895,31.5905494329321));
#71450=CARTESIAN_POINT('Ctrl Pts',(32.5802200309563,0.859308020910075,31.6070390220085));
#71451=CARTESIAN_POINT('Ctrl Pts',(32.593757192945,0.871550679324244,31.6237706303625));
#71452=CARTESIAN_POINT('',(32.574602921884,0.823344418487232,31.5905494329235));
#71453=CARTESIAN_POINT('Origin',(32.5760852110325,0.837020829522203,31.5962049981138));
#71454=CARTESIAN_POINT('',(32.6106782843143,0.819472915007436,31.6237706303691));
#71455=CARTESIAN_POINT('Ctrl Pts',(32.6106782843071,0.819472915008212,31.6237706303625));
#71456=CARTESIAN_POINT('Ctrl Pts',(32.5925304361235,0.8214204895483,31.6070390219952));
#71457=CARTESIAN_POINT('Ctrl Pts',(32.5746029218649,0.823344418489286,31.5905494329059));
#71458=CARTESIAN_POINT('',(32.6541425833284,0.665360135553601,31.6237706303691));
#71459=CARTESIAN_POINT('Origin',(30.,-1.32966554433622E-14,31.6237706303681));
#71460=CARTESIAN_POINT('',(32.6254061353882,0.64320981109888,31.5905494329235));
#71461=CARTESIAN_POINT('Ctrl Pts',(32.6254061353957,0.643209811104633,31.5905494329321));
#71462=CARTESIAN_POINT('Ctrl Pts',(32.639686603978,0.654217330653466,31.6070390220085));
#71463=CARTESIAN_POINT('Ctrl Pts',(32.6541425833226,0.665360135549173,31.6237706303625));
#71464=CARTESIAN_POINT('',(32.6312651388532,0.618805305313054,31.5905494329235));
#71465=CARTESIAN_POINT('Origin',(32.633815908334,0.632323260043002,31.5962050111235));
#71466=CARTESIAN_POINT('',(32.6669255383185,0.612115296072106,31.6237706303691));
#71467=CARTESIAN_POINT('Ctrl Pts',(32.6669255383114,0.61211529607344,31.6237706303625));
#71468=CARTESIAN_POINT('Ctrl Pts',(32.6489864388245,0.61548073064908,31.6070390219952));
#71469=CARTESIAN_POINT('Ctrl Pts',(32.6312651388343,0.618805305316593,31.5905494329059));
#71470=CARTESIAN_POINT('',(32.6981643020882,0.455067425287697,31.6237706303691));
#71471=CARTESIAN_POINT('Origin',(30.,-1.32966554433622E-14,31.6237706303681));
#71472=CARTESIAN_POINT('',(32.6677785445999,0.435240018610789,31.5905494329235));
#71473=CARTESIAN_POINT('Ctrl Pts',(32.6677785446078,0.435240018615936,31.5905494329321));
#71474=CARTESIAN_POINT('Ctrl Pts',(32.6828786313014,0.44509317300403,31.6070390220085));
#71475=CARTESIAN_POINT('Ctrl Pts',(32.6981643020821,0.455067425283731,31.6237706303625));
#71476=CARTESIAN_POINT('',(32.6717047312569,0.410451051657977,31.5905494329235));
#71477=CARTESIAN_POINT('Origin',(32.6753082614925,0.423727206709275,31.596205031575));
#71478=CARTESIAN_POINT('',(32.7067303095363,0.400983782787501,31.6237706303691));
#71479=CARTESIAN_POINT('Ctrl Pts',(32.7067303095293,0.400983782789396,31.6237706303625));
#71480=CARTESIAN_POINT('Ctrl Pts',(32.6891105592528,0.405746328377311,31.6070390219952));
#71481=CARTESIAN_POINT('Ctrl Pts',(32.6717047312384,0.410451051662997,31.5905494329059));
#71482=CARTESIAN_POINT('',(32.7255509406949,0.24196907301962,31.6237706303691));
#71483=CARTESIAN_POINT('Origin',(30.,-1.32966554433622E-14,31.6237706303681));
#71484=CARTESIAN_POINT('',(32.6937032119577,0.224586826675969,31.5905494329235));
#71485=CARTESIAN_POINT('Ctrl Pts',(32.693703211966,0.224586826680493,31.5905494329321));
#71486=CARTESIAN_POINT('Ctrl Pts',(32.7095298197151,0.233224867934539,31.6070390220085));
#71487=CARTESIAN_POINT('Ctrl Pts',(32.7255509406885,0.241969073016156,31.6237706303625));
#71488=CARTESIAN_POINT('',(32.6956723755605,0.199566230780603,31.5905494329235));
#71489=CARTESIAN_POINT('Origin',(32.7003064571198,0.212518732061222,31.5962050602857));
#71490=CARTESIAN_POINT('',(32.7298471883166,0.187380071141372,31.6237706303691));
#71491=CARTESIAN_POINT('Ctrl Pts',(32.7298471883097,0.187380071143799,31.6237706303625));
#71492=CARTESIAN_POINT('Ctrl Pts',(32.7126554188632,0.193510365066728,31.6070390219952));
#71493=CARTESIAN_POINT('Ctrl Pts',(32.6956723755424,0.199566230787043,31.5905494329059));
#71494=CARTESIAN_POINT('',(32.7361336514146,0.0273789009534945,31.6237706303691));
#71495=CARTESIAN_POINT('Origin',(30.,-1.32966554433622E-14,31.6237706303681));
#71496=CARTESIAN_POINT('',(32.7030203032667,0.0125489822719939,31.5905494329235));
#71497=CARTESIAN_POINT('Ctrl Pts',(32.7030203032753,0.0125489822758371,
31.5905494329321));
#71498=CARTESIAN_POINT('Ctrl Pts',(32.7194758557802,0.0199186539990537,
31.6070390220085));
#71499=CARTESIAN_POINT('Ctrl Pts',(32.736133651408,0.0273789009505039,31.6237706303625));
#71500=CARTESIAN_POINT('',(32.7030203032667,-0.0125489822720396,31.5905494329235));
#71501=CARTESIAN_POINT('Origin',(32.7086563646858,6.24424376688964E-9,31.5962050859813));
#71502=CARTESIAN_POINT('',(32.7361336514146,-0.02737890095354,31.6237706303691));
#71503=CARTESIAN_POINT('Ctrl Pts',(32.736133651408,-0.0273789009505768,
31.6237706303625));
#71504=CARTESIAN_POINT('Ctrl Pts',(32.719475855767,-0.0199186539932038,
31.6070390219952));
#71505=CARTESIAN_POINT('Ctrl Pts',(32.7030203032491,-0.0125489822642076,
31.5905494329059));
#71506=CARTESIAN_POINT('',(32.7298471883166,-0.187380071141418,31.6237706303691));
#71507=CARTESIAN_POINT('Origin',(30.,-1.32966554433622E-14,31.6237706303681));
#71508=CARTESIAN_POINT('',(32.6956723755605,-0.199566230780649,31.5905494329235));
#71509=CARTESIAN_POINT('Ctrl Pts',(32.6956723755694,-0.199566230777489,
31.5905494329321));
#71510=CARTESIAN_POINT('Ctrl Pts',(32.7126554188769,-0.193510365061924,
31.6070390220085));
#71511=CARTESIAN_POINT('Ctrl Pts',(32.7298471883097,-0.187380071143864,
31.6237706303625));
#71512=CARTESIAN_POINT('',(32.6937032119577,-0.224586826676015,31.5905494329235));
#71513=CARTESIAN_POINT('Origin',(32.7003074588902,-0.212518788369472,31.5962062072437));
#71514=CARTESIAN_POINT('',(32.7255509406949,-0.241969073019665,31.6237706303691));
#71515=CARTESIAN_POINT('Ctrl Pts',(32.7255509406885,-0.241969073016199,
31.6237706303625));
#71516=CARTESIAN_POINT('Ctrl Pts',(32.7095298197024,-0.23322486792764,31.6070390219952));
#71517=CARTESIAN_POINT('Ctrl Pts',(32.6937032119408,-0.22458682666682,31.5905494329059));
#71518=CARTESIAN_POINT('',(32.7067303095363,-0.400983782787547,31.6237706303691));
#71519=CARTESIAN_POINT('Origin',(30.,-1.32966554433622E-14,31.6237706303681));
#71520=CARTESIAN_POINT('',(32.6717047312569,-0.410451051658023,31.5905494329235));
#71521=CARTESIAN_POINT('Ctrl Pts',(32.671704731266,-0.41045105165556,31.5905494329321));
#71522=CARTESIAN_POINT('Ctrl Pts',(32.6891105592667,-0.405746328373564,
31.6070390220085));
#71523=CARTESIAN_POINT('Ctrl Pts',(32.7067303095293,-0.40098378278943,31.6237706303625));
#71524=CARTESIAN_POINT('',(32.6677785445999,-0.435240018610835,31.5905494329235));
#71525=CARTESIAN_POINT('Origin',(32.6753090233822,-0.42372730774851,31.5962059100614));
#71526=CARTESIAN_POINT('',(32.6981643020882,-0.455067425287743,31.6237706303691));
#71527=CARTESIAN_POINT('Ctrl Pts',(32.6981643020821,-0.455067425283808,
31.6237706303625));
#71528=CARTESIAN_POINT('Ctrl Pts',(32.6828786312893,-0.445093172996188,
31.6070390219952));
#71529=CARTESIAN_POINT('Ctrl Pts',(32.6677785445838,-0.435240018600367,
31.5905494329059));
#71530=CARTESIAN_POINT('',(32.6669255383185,-0.612115296072152,31.6237706303691));
#71531=CARTESIAN_POINT('Origin',(30.,-1.32966554433622E-14,31.6237706303681));
#71532=CARTESIAN_POINT('',(32.6312651388532,-0.6188053053131,31.5905494329235));
#71533=CARTESIAN_POINT('Ctrl Pts',(32.6312651388625,-0.618805305311361,
31.5905494329321));
#71534=CARTESIAN_POINT('Ctrl Pts',(32.6489864388387,-0.615480730646455,
31.6070390220085));
#71535=CARTESIAN_POINT('Ctrl Pts',(32.6669255383114,-0.612115296073488,
31.6237706303625));
#71536=CARTESIAN_POINT('',(32.6254061353882,-0.643209811098926,31.5905494329235));
#71537=CARTESIAN_POINT('Origin',(32.6338164916465,-0.632323382398633,31.5962056922849));
#71538=CARTESIAN_POINT('',(32.6541425833284,-0.665360135553646,31.6237706303691));
#71539=CARTESIAN_POINT('Ctrl Pts',(32.6541425833226,-0.665360135549238,
31.6237706303625));
#71540=CARTESIAN_POINT('Ctrl Pts',(32.6396866039666,-0.654217330644686,
31.6070390219952));
#71541=CARTESIAN_POINT('Ctrl Pts',(32.625406135373,-0.643209811087222,31.5905494329059));
#71542=CARTESIAN_POINT('',(32.6106782843143,-0.819472915007481,31.6237706303691));
#71543=CARTESIAN_POINT('Origin',(30.,-1.32966554433622E-14,31.6237706303681));
#71544=CARTESIAN_POINT('',(32.574602921884,-0.823344418487278,31.5905494329235));
#71545=CARTESIAN_POINT('Ctrl Pts',(32.5746029218934,-0.823344418486272,
31.5905494329321));
#71546=CARTESIAN_POINT('Ctrl Pts',(32.5925304361379,-0.821420489546795,
31.6070390220085));
#71547=CARTESIAN_POINT('Ctrl Pts',(32.610678284307,-0.819472915008254,31.6237706303626));
#71548=CARTESIAN_POINT('',(32.5668472243157,-0.847214001212625,31.5905494329235));
#71549=CARTESIAN_POINT('Origin',(32.5760856561636,-0.837020957759021,31.596205527432));
#71550=CARTESIAN_POINT('',(32.5937571929504,-0.871550679329165,31.6237706303691));
#71551=CARTESIAN_POINT('Ctrl Pts',(32.593757192945,-0.871550679324299,31.6237706303625));
#71552=CARTESIAN_POINT('Ctrl Pts',(32.5802200309455,-0.859308020900409,
31.6070390219952));
#71553=CARTESIAN_POINT('Ctrl Pts',(32.5668472243014,-0.847214001199744,
31.5905494329059));
#71554=CARTESIAN_POINT('',(32.5383353305486,-1.02177821091939,31.6237706303691));
#71555=CARTESIAN_POINT('Origin',(30.,-1.32966554433622E-14,31.6237706303681));
#71556=CARTESIAN_POINT('',(32.5020674217591,-1.02280733953168,31.5905494329235));
#71557=CARTESIAN_POINT('Ctrl Pts',(32.5020674217685,-1.02280733953141,31.5905494329321));
#71558=CARTESIAN_POINT('Ctrl Pts',(32.5200906211944,-1.02229591797905,31.6070390220085));
#71559=CARTESIAN_POINT('Ctrl Pts',(32.5383353305413,-1.0217782109196,31.6237706303625));
#71560=CARTESIAN_POINT('',(32.492462846542,-1.0459948352816,31.5905494329235));
#71561=CARTESIAN_POINT('Origin',(32.5024724328509,-1.03655801106895,31.5962053997573));
#71562=CARTESIAN_POINT('',(32.517380426966,-1.07236782334661,31.6237706303691));
#71563=CARTESIAN_POINT('Ctrl Pts',(32.517380426961,-1.07236782334134,31.6237706303625));
#71564=CARTESIAN_POINT('Ctrl Pts',(32.5048455434235,-1.0591007914584,31.6070390219952));
#71565=CARTESIAN_POINT('Ctrl Pts',(32.4924628465288,-1.04599483526767,31.5905494329059));
#71566=CARTESIAN_POINT('',(32.450342695388,-1.21778390438525,31.6237706303691));
#71567=CARTESIAN_POINT('Origin',(30.,-1.32966554433622E-14,31.6237706303681));
#71568=CARTESIAN_POINT('',(32.4141058439571,-1.21596431320991,31.5905494329235));
#71569=CARTESIAN_POINT('Ctrl Pts',(32.4141058439665,-1.21596431321038,31.5905494329321));
#71570=CARTESIAN_POINT('Ctrl Pts',(32.4321136095561,-1.21686855212907,31.6070390220085));
#71571=CARTESIAN_POINT('Ctrl Pts',(32.4503426953807,-1.21778390438489,31.6237706303625));
#71572=CARTESIAN_POINT('',(32.4027116064913,-1.2383267633625,31.5905494329235));
#71573=CARTESIAN_POINT('Origin',(32.4134306626749,-1.2297043338603,31.5962052993351));
#71574=CARTESIAN_POINT('',(32.4254831735355,-1.26657346313463,31.6237706303691));
#71575=CARTESIAN_POINT('Ctrl Pts',(32.425483173531,-1.26657346312898,31.6237706303625));
#71576=CARTESIAN_POINT('Ctrl Pts',(32.4140278501806,-1.25236385345028,31.6070390219952));
#71577=CARTESIAN_POINT('Ctrl Pts',(32.4027116064792,-1.23832676334755,31.5905494329059));
#71578=CARTESIAN_POINT('',(32.3472428826886,-1.40628155512633,31.6237706303691));
#71579=CARTESIAN_POINT('Origin',(30.,-1.32966554433622E-14,31.6237706303681));
#71580=CARTESIAN_POINT('',(32.3112605008555,-1.40162446254804,31.5905494329235));
#71581=CARTESIAN_POINT('Ctrl Pts',(32.3112605008648,-1.40162446254925,31.5905494329321));
#71582=CARTESIAN_POINT('Ctrl Pts',(32.329141808755,-1.40393878700536,31.6070390220085));
#71583=CARTESIAN_POINT('Ctrl Pts',(32.3472428826814,-1.4062815551254,31.6237706303625));
#71584=CARTESIAN_POINT('',(32.2981468504039,-1.42302399516182,31.5905494329235));
#71585=CARTESIAN_POINT('Origin',(32.3095093115547,-1.41526911745265,31.5962052196244));
#71586=CARTESIAN_POINT('',(32.3186320097852,-1.45297025634402,31.6237706303691));
#71587=CARTESIAN_POINT('Ctrl Pts',(32.3186320097811,-1.45297025633802,31.6237706303625));
#71588=CARTESIAN_POINT('Ctrl Pts',(32.3083268724956,-1.43790567583238,31.6070390219952));
#71589=CARTESIAN_POINT('Ctrl Pts',(32.2981468503931,-1.42302399514595,31.5905494329059));
#71590=CARTESIAN_POINT('',(32.22967153708,-1.58610901244399,31.6237706303691));
#71591=CARTESIAN_POINT('Origin',(30.,-1.32966554433622E-14,31.6237706303681));
#71592=CARTESIAN_POINT('',(32.194165468194,-1.57864313098713,31.5905494329235));
#71593=CARTESIAN_POINT('Ctrl Pts',(32.1941654682032,-1.57864313098907,31.5905494329321));
#71594=CARTESIAN_POINT('Ctrl Pts',(32.2118100741847,-1.58235327240274,31.6070390220085));
#71595=CARTESIAN_POINT('Ctrl Pts',(32.2296715370729,-1.58610901244249,31.6237706303625));
#71596=CARTESIAN_POINT('',(32.1794132547725,-1.59894781082747,31.5905494329235));
#71597=CARTESIAN_POINT('Origin',(32.191349084716,-1.59210829514296,31.596205156165));
#71598=CARTESIAN_POINT('',(32.1974857086711,-1.6304090047614,31.6237706303691));
#71599=CARTESIAN_POINT('Ctrl Pts',(32.1974857086675,-1.63040900475512,31.6237706303625));
#71600=CARTESIAN_POINT('Ctrl Pts',(32.1883942920451,-1.61458233157088,31.6070390219952));
#71601=CARTESIAN_POINT('Ctrl Pts',(32.1794132547629,-1.59894781081085,31.5905494329059));
#71602=CARTESIAN_POINT('',(32.0983535250043,-1.75615758026517,31.6237706303691));
#71603=CARTESIAN_POINT('Origin',(30.,-1.32966554433622E-14,31.6237706303681));
#71604=CARTESIAN_POINT('',(32.063542675787,-1.74592893957158,31.5905494329235));
#71605=CARTESIAN_POINT('Ctrl Pts',(32.0635426757961,-1.74592893957424,31.5905494329321));
#71606=CARTESIAN_POINT('Ctrl Pts',(32.0808417950055,-1.75101202368991,31.6070390220085));
#71607=CARTESIAN_POINT('Ctrl Pts',(32.0983535249973,-1.75615758026313,31.6237706303625));
#71608=CARTESIAN_POINT('',(32.0472428516969,-1.76501358153528,31.5905494329235));
#71609=CARTESIAN_POINT('Origin',(32.0596784759083,-1.75913159602171,31.5962051058414));
#71610=CARTESIAN_POINT('',(32.062791177425,-1.79779573949842,31.6237706303691));
#71611=CARTESIAN_POINT('Ctrl Pts',(32.0627911774219,-1.79779573949184,31.6237706303625));
#71612=CARTESIAN_POINT('Ctrl Pts',(32.0549695330692,-1.78130455033205,31.6070390219952));
#71613=CARTESIAN_POINT('Ctrl Pts',(32.0472428516887,-1.76501358151791,31.5905494329059));
#71614=CARTESIAN_POINT('',(31.9540984656736,-1.91537885262235,31.6237706303691));
#71615=CARTESIAN_POINT('Origin',(30.,-1.32966554433622E-14,31.6237706303681));
#71616=CARTESIAN_POINT('',(31.9201974565863,-1.90245051566327,31.5905494329235));
#71617=CARTESIAN_POINT('Ctrl Pts',(31.9201974565951,-1.90245051566663,31.5905494329321));
#71618=CARTESIAN_POINT('Ctrl Pts',(31.9370444342101,-1.90887520358042,31.6070390220085));
#71619=CARTESIAN_POINT('Ctrl Pts',(31.9540984656668,-1.91537885261975,31.6237706303625));
#71620=CARTESIAN_POINT('',(31.9024505156632,-1.92019745658634,31.5905494329235));
#71621=CARTESIAN_POINT('Origin',(31.915309275617,-1.91530926701241,31.5962050664381));
#71622=CARTESIAN_POINT('',(31.9153788526223,-1.95409846567368,31.6237706303691));
#71623=CARTESIAN_POINT('Ctrl Pts',(31.9153788526197,-1.9540984656669,31.6237706303625));
#71624=CARTESIAN_POINT('Ctrl Pts',(31.9088752035752,-1.93704443419662,31.6070390219952));
#71625=CARTESIAN_POINT('Ctrl Pts',(31.9024505156564,-1.92019745656839,31.5905494329059));
#71626=CARTESIAN_POINT('',(31.7977957394984,-2.06279117742501,31.6237706303691));
#71627=CARTESIAN_POINT('Origin',(30.,-1.32966554433622E-14,31.6237706303681));
#71628=CARTESIAN_POINT('',(31.7650135815352,-2.04724285169692,31.5905494329235));
#71629=CARTESIAN_POINT('Ctrl Pts',(31.7650135815437,-2.04724285170096,31.5905494329321));
#71630=CARTESIAN_POINT('Ctrl Pts',(31.7813045503451,-2.05496953307547,31.6070390220085));
#71631=CARTESIAN_POINT('Ctrl Pts',(31.7977957394918,-2.06279117742192,31.6237706303625));
#71632=CARTESIAN_POINT('',(31.7459289395715,-2.0635426757871,31.5905494329235));
#71633=CARTESIAN_POINT('Origin',(31.7591315658702,-2.05967842174604,31.5962050363748));
#71634=CARTESIAN_POINT('',(31.7561575802651,-2.09835352500439,31.6237706303691));
#71635=CARTESIAN_POINT('Ctrl Pts',(31.7561575802631,-2.09835352499741,31.6237706303625));
#71636=CARTESIAN_POINT('Ctrl Pts',(31.7510120236858,-2.08084179499169,31.6070390219952));
#71637=CARTESIAN_POINT('Ctrl Pts',(31.7459289395661,-2.06354267576866,31.5905494329059));
#71638=CARTESIAN_POINT('',(31.6304090047613,-2.19748570867118,31.6237706303691));
#71639=CARTESIAN_POINT('Origin',(30.,-1.32966554433622E-14,31.6237706303681));
#71640=CARTESIAN_POINT('',(31.5989478108274,-2.17941325477251,31.5905494329235));
#71641=CARTESIAN_POINT('Ctrl Pts',(31.5989478108356,-2.17941325477721,31.5905494329321));
#71642=CARTESIAN_POINT('Ctrl Pts',(31.6145823315833,-2.18839429205237,31.6070390220085));
#71643=CARTESIAN_POINT('Ctrl Pts',(31.630409004755,-2.19748570866756,31.6237706303625));
#71644=CARTESIAN_POINT('',(31.5786431309871,-2.19416546819406,31.5905494329235));
#71645=CARTESIAN_POINT('Origin',(31.5921082324253,-2.19134897714169,31.5962050145327));
#71646=CARTESIAN_POINT('',(31.5861090124439,-2.22967153708009,31.6237706303691));
#71647=CARTESIAN_POINT('Ctrl Pts',(31.5861090124425,-2.22967153707296,31.6237706303625));
#71648=CARTESIAN_POINT('Ctrl Pts',(31.5823532723997,-2.21181007417054,31.6070390219952));
#71649=CARTESIAN_POINT('Ctrl Pts',(31.5786431309832,-2.19416546817524,31.5905494329059));
#71650=CARTESIAN_POINT('',(31.452970256344,-2.31863200978524,31.6237706303691));
#71651=CARTESIAN_POINT('Origin',(30.,-1.32966554433622E-14,31.6237706303681));
#71652=CARTESIAN_POINT('',(31.4230239951618,-2.29814685040399,31.5905494329235));
#71653=CARTESIAN_POINT('Ctrl Pts',(31.4230239951696,-2.2981468504093,31.5905494329321));
#71654=CARTESIAN_POINT('Ctrl Pts',(31.4379056758443,-2.30832687250383,31.6070390220085));
#71655=CARTESIAN_POINT('Ctrl Pts',(31.452970256338,-2.31863200978113,31.6237706303625));
#71656=CARTESIAN_POINT('',(31.401624462548,-2.31126050085554,31.5905494329235));
#71657=CARTESIAN_POINT('Origin',(31.4152690281487,-2.30950914111279,31.596205000146));
#71658=CARTESIAN_POINT('',(31.4062815551263,-2.34724288268866,31.6237706303691));
#71659=CARTESIAN_POINT('Ctrl Pts',(31.4062815551254,-2.34724288268144,31.6237706303625));
#71660=CARTESIAN_POINT('Ctrl Pts',(31.4039387870035,-2.32914180874065,31.6070390219952));
#71661=CARTESIAN_POINT('Ctrl Pts',(31.4016244625455,-2.31126050083648,31.5905494329059));
#71662=CARTESIAN_POINT('',(31.2665734631346,-2.42548317353559,31.6237706303691));
#71663=CARTESIAN_POINT('Origin',(30.,-1.32966554433622E-14,31.6237706303681));
#71664=CARTESIAN_POINT('',(31.2383267633624,-2.40271160649135,31.5905494329235));
#71665=CARTESIAN_POINT('Ctrl Pts',(31.2383267633697,-2.40271160649727,31.5905494329321));
#71666=CARTESIAN_POINT('Ctrl Pts',(31.2523638534615,-2.41402785018975,31.6070390220085));
#71667=CARTESIAN_POINT('Ctrl Pts',(31.2665734631289,-2.42548317353104,31.6237706303625));
#71668=CARTESIAN_POINT('',(31.2159643132098,-2.41410584395714,31.5905494329235));
#71669=CARTESIAN_POINT('Origin',(31.2297042241653,-2.41343041757036,31.5962049927334));
#71670=CARTESIAN_POINT('',(31.2177839043852,-2.450342695388,31.6237706303691));
#71671=CARTESIAN_POINT('Ctrl Pts',(31.2177839043848,-2.45034269538075,31.6237706303625));
#71672=CARTESIAN_POINT('Ctrl Pts',(31.2168685521282,-2.43211360954164,31.6070390219952));
#71673=CARTESIAN_POINT('Ctrl Pts',(31.2159643132088,-2.41410584393796,31.5905494329059));
#71674=CARTESIAN_POINT('',(31.0723678233465,-2.51738042696609,31.6237706303691));
#71675=CARTESIAN_POINT('Origin',(30.,-1.32966554433622E-14,31.6237706303681));
#71676=CARTESIAN_POINT('',(31.0459948352815,-2.49246284654201,31.5905494329235));
#71677=CARTESIAN_POINT('Ctrl Pts',(31.0459948352884,-2.49246284654849,31.5905494329321));
#71678=CARTESIAN_POINT('Ctrl Pts',(31.0591007914688,-2.5048455434335,31.6070390220085));
#71679=CARTESIAN_POINT('Ctrl Pts',(31.0723678233412,-2.51738042696111,31.6237706303625));
#71680=CARTESIAN_POINT('',(31.0228073395316,-2.5020674217591,31.5905494329235));
#71681=CARTESIAN_POINT('Origin',(31.036557887911,-2.50247209787259,31.5962049920587));
#71682=CARTESIAN_POINT('',(31.0217782109193,-2.53833533054864,31.6237706303691));
#71683=CARTESIAN_POINT('Ctrl Pts',(31.0217782109196,-2.53833533054137,31.6237706303625));
#71684=CARTESIAN_POINT('Ctrl Pts',(31.0222959179794,-2.52009062117993,31.6070390219952));
#71685=CARTESIAN_POINT('Ctrl Pts',(31.0228073395322,-2.50206742173989,31.5905494329059));
#71686=CARTESIAN_POINT('',(30.8715506793291,-2.59375719295041,31.6237706303691));
#71687=CARTESIAN_POINT('Origin',(30.,-1.32966554433622E-14,31.6237706303681));
#71688=CARTESIAN_POINT('',(30.8472140012126,-2.56684722431573,31.5905494329235));
#71689=CARTESIAN_POINT('Ctrl Pts',(30.8472140012189,-2.56684722432271,31.5905494329321));
#71690=CARTESIAN_POINT('Ctrl Pts',(30.8593080209101,-2.58022003095631,31.6070390220085));
#71691=CARTESIAN_POINT('Ctrl Pts',(30.8715506793242,-2.593757192945,31.6237706303625));
#71692=CARTESIAN_POINT('',(30.8233444184872,-2.57460292188405,31.5905494329235));
#71693=CARTESIAN_POINT('Origin',(30.8370208295222,-2.5760852110326,31.5962049981139));
#71694=CARTESIAN_POINT('',(30.8194729150074,-2.6106782843143,31.6237706303691));
#71695=CARTESIAN_POINT('Ctrl Pts',(30.8194729150082,-2.61067828430707,31.6237706303625));
#71696=CARTESIAN_POINT('Ctrl Pts',(30.8214204895483,-2.5925304361235,31.6070390219952));
#71697=CARTESIAN_POINT('Ctrl Pts',(30.8233444184892,-2.57460292186495,31.5905494329059));
#71698=CARTESIAN_POINT('',(30.6653601355536,-2.65414258332839,31.6237706303691));
#71699=CARTESIAN_POINT('Origin',(30.,-1.32966554433622E-14,31.6237706303681));
#71700=CARTESIAN_POINT('',(30.6432098110989,-2.62540613538822,31.5905494329235));
#71701=CARTESIAN_POINT('Ctrl Pts',(30.6432098111046,-2.62540613539568,31.5905494329321));
#71702=CARTESIAN_POINT('Ctrl Pts',(30.6542173306535,-2.63968660397806,31.6070390220085));
#71703=CARTESIAN_POINT('Ctrl Pts',(30.6653601355492,-2.65414258332262,31.6237706303625));
#71704=CARTESIAN_POINT('',(30.618805305313,-2.63126513885325,31.5905494329235));
#71705=CARTESIAN_POINT('Origin',(30.632323260043,-2.63381590833404,31.5962050111235));
#71706=CARTESIAN_POINT('',(30.6121152960721,-2.66692553831853,31.6237706303691));
#71707=CARTESIAN_POINT('Ctrl Pts',(30.6121152960734,-2.66692553831138,31.6237706303625));
#71708=CARTESIAN_POINT('Ctrl Pts',(30.615480730649,-2.6489864388245,31.6070390219952));
#71709=CARTESIAN_POINT('Ctrl Pts',(30.6188053053166,-2.63126513883437,31.5905494329059));
#71710=CARTESIAN_POINT('',(30.4550674252877,-2.69816430208819,31.6237706303691));
#71711=CARTESIAN_POINT('Origin',(30.,-1.32966554433622E-14,31.6237706303681));
#71712=CARTESIAN_POINT('',(30.4352400186108,-2.66777854459992,31.5905494329235));
#71713=CARTESIAN_POINT('Ctrl Pts',(30.435240018616,-2.6677785446078,31.5905494329321));
#71714=CARTESIAN_POINT('Ctrl Pts',(30.445093173004,-2.68287863130142,31.6070390220085));
#71715=CARTESIAN_POINT('Ctrl Pts',(30.4550674252837,-2.69816430208209,31.6237706303625));
#71716=CARTESIAN_POINT('',(30.410451051658,-2.67170473125697,31.5905494329235));
#71717=CARTESIAN_POINT('Origin',(30.4237272067093,-2.67530826149246,31.5962050315749));
#71718=CARTESIAN_POINT('',(30.4009837827875,-2.7067303095363,31.6237706303691));
#71719=CARTESIAN_POINT('Ctrl Pts',(30.4009837827894,-2.70673030952928,31.6237706303625));
#71720=CARTESIAN_POINT('Ctrl Pts',(30.4057463283773,-2.68911055925278,31.6070390219952));
#71721=CARTESIAN_POINT('Ctrl Pts',(30.410451051663,-2.67170473123841,31.5905494329059));
#71722=CARTESIAN_POINT('',(30.2419690730196,-2.72555094069494,31.6237706303691));
#71723=CARTESIAN_POINT('Origin',(30.,-1.32966554433622E-14,31.6237706303681));
#71724=CARTESIAN_POINT('',(30.224586826676,-2.69370321195777,31.5905494329235));
#71725=CARTESIAN_POINT('Ctrl Pts',(30.2245868266805,-2.69370321196604,31.5905494329321));
#71726=CARTESIAN_POINT('Ctrl Pts',(30.2332248679346,-2.70952981971513,31.6070390220085));
#71727=CARTESIAN_POINT('Ctrl Pts',(30.2419690730162,-2.72555094068854,31.6237706303625));
#71728=CARTESIAN_POINT('',(30.1995662307806,-2.69567237556051,31.5905494329235));
#71729=CARTESIAN_POINT('Origin',(30.2125187320612,-2.70030645711985,31.5962050602857));
#71730=CARTESIAN_POINT('',(30.1873800711414,-2.72984718831661,31.6237706303691));
#71731=CARTESIAN_POINT('Ctrl Pts',(30.1873800711438,-2.72984718830975,31.6237706303625));
#71732=CARTESIAN_POINT('Ctrl Pts',(30.1935103650667,-2.71265541886325,31.6070390219952));
#71733=CARTESIAN_POINT('Ctrl Pts',(30.199566230787,-2.6956723755424,31.5905494329059));
#71734=CARTESIAN_POINT('',(30.0273789009535,-2.73613365141464,31.6237706303691));
#71735=CARTESIAN_POINT('Origin',(30.,-1.32966554433622E-14,31.6237706303681));
#71736=CARTESIAN_POINT('',(30.012548982272,-2.70302030326669,31.5905494329235));
#71737=CARTESIAN_POINT('Ctrl Pts',(30.0125489822759,-2.70302030327528,31.5905494329321));
#71738=CARTESIAN_POINT('Ctrl Pts',(30.0199186539991,-2.7194758557802,31.6070390220085));
#71739=CARTESIAN_POINT('Ctrl Pts',(30.0273789009505,-2.736133651408,31.6237706303625));
#71740=CARTESIAN_POINT('',(29.987451017728,-2.70302030326669,31.5905494329235));
#71741=CARTESIAN_POINT('Origin',(30.,-2.7086657795165,31.5962151370754));
#71742=CARTESIAN_POINT('',(29.9726210990465,-2.73613365141464,31.6237706303691));
#71743=CARTESIAN_POINT('Ctrl Pts',(29.9726210990495,-2.73613365140799,31.6237706303625));
#71744=CARTESIAN_POINT('Ctrl Pts',(29.9800813460068,-2.71947585576697,31.6070390219952));
#71745=CARTESIAN_POINT('Ctrl Pts',(29.9874510177359,-2.70302030324915,31.5905494329059));
#71746=CARTESIAN_POINT('',(29.8126199288586,-2.72984718831661,31.6237706303691));
#71747=CARTESIAN_POINT('Origin',(30.,-1.32966554433622E-14,31.6237706303681));
#71748=CARTESIAN_POINT('',(29.8004337692193,-2.6956723755605,31.5905494329235));
#71749=CARTESIAN_POINT('Ctrl Pts',(29.8004337692225,-2.69567237556937,31.5905494329321));
#71750=CARTESIAN_POINT('Ctrl Pts',(29.806489634938,-2.71265541887691,31.6070390220085));
#71751=CARTESIAN_POINT('Ctrl Pts',(29.8126199288561,-2.72984718830976,31.6237706303625));
#71752=CARTESIAN_POINT('',(29.775413173324,-2.69370321195777,31.5905494329235));
#71753=CARTESIAN_POINT('Origin',(29.7874812116305,-2.70030745889015,31.5962062072437));
#71754=CARTESIAN_POINT('',(29.7580309269803,-2.72555094069494,31.6237706303691));
#71755=CARTESIAN_POINT('Ctrl Pts',(29.7580309269838,-2.72555094068855,31.6237706303625));
#71756=CARTESIAN_POINT('Ctrl Pts',(29.7667751320723,-2.7095298197024,31.6070390219952));
#71757=CARTESIAN_POINT('Ctrl Pts',(29.7754131733332,-2.69370321194088,31.5905494329059));
#71758=CARTESIAN_POINT('',(29.5990162172124,-2.70673030953629,31.6237706303691));
#71759=CARTESIAN_POINT('Origin',(30.,-1.32966554433622E-14,31.6237706303681));
#71760=CARTESIAN_POINT('',(29.589548948342,-2.67170473125696,31.5905494329235));
#71761=CARTESIAN_POINT('Ctrl Pts',(29.5895489483445,-2.67170473126605,31.5905494329321));
#71762=CARTESIAN_POINT('Ctrl Pts',(29.5942536716264,-2.68911055926676,31.6070390220085));
#71763=CARTESIAN_POINT('Ctrl Pts',(29.5990162172106,-2.70673030952926,31.6237706303625));
#71764=CARTESIAN_POINT('',(29.5647599813891,-2.66777854459992,31.5905494329235));
#71765=CARTESIAN_POINT('Origin',(29.5762726922515,-2.67530902338218,31.5962059100614));
#71766=CARTESIAN_POINT('',(29.5449325747122,-2.69816430208819,31.6237706303691));
#71767=CARTESIAN_POINT('Ctrl Pts',(29.5449325747162,-2.6981643020821,31.6237706303625));
#71768=CARTESIAN_POINT('Ctrl Pts',(29.5549068270038,-2.68287863128929,31.6070390219952));
#71769=CARTESIAN_POINT('Ctrl Pts',(29.5647599813996,-2.66777854458383,31.5905494329059));
#71770=CARTESIAN_POINT('',(29.3878847039278,-2.66692553831852,31.6237706303691));
#71771=CARTESIAN_POINT('Origin',(30.,-1.32966554433622E-14,31.6237706303681));
#71772=CARTESIAN_POINT('',(29.3811946946869,-2.63126513885324,31.5905494329235));
#71773=CARTESIAN_POINT('Ctrl Pts',(29.3811946946886,-2.63126513886249,31.5905494329321));
#71774=CARTESIAN_POINT('Ctrl Pts',(29.3845192693535,-2.64898643883873,31.6070390220085));
#71775=CARTESIAN_POINT('Ctrl Pts',(29.3878847039265,-2.66692553831137,31.6237706303625));
#71776=CARTESIAN_POINT('',(29.3567901889011,-2.62540613538822,31.5905494329235));
#71777=CARTESIAN_POINT('Origin',(29.3676766176013,-2.63381649164654,31.5962056922849));
#71778=CARTESIAN_POINT('',(29.3346398644463,-2.65414258332839,31.6237706303691));
#71779=CARTESIAN_POINT('Ctrl Pts',(29.3346398644508,-2.65414258332263,31.6237706303626));
#71780=CARTESIAN_POINT('Ctrl Pts',(29.3457826693553,-2.63968660396658,31.6070390219952));
#71781=CARTESIAN_POINT('Ctrl Pts',(29.3567901889128,-2.62540613537299,31.5905494329059));
#71782=CARTESIAN_POINT('',(29.1805270849925,-2.61067828431429,31.6237706303691));
#71783=CARTESIAN_POINT('Origin',(30.,-1.32966554433622E-14,31.6237706303681));
#71784=CARTESIAN_POINT('',(29.1766555815127,-2.57460292188404,31.5905494329235));
#71785=CARTESIAN_POINT('Ctrl Pts',(29.1766555815137,-2.5746029218934,31.5905494329321));
#71786=CARTESIAN_POINT('Ctrl Pts',(29.1785795104532,-2.59253043613788,31.6070390220085));
#71787=CARTESIAN_POINT('Ctrl Pts',(29.1805270849917,-2.61067828430705,31.6237706303625));
#71788=CARTESIAN_POINT('',(29.1527859987874,-2.56684722431572,31.5905494329235));
#71789=CARTESIAN_POINT('Origin',(29.162979042241,-2.57608565616368,31.5962055274321));
#71790=CARTESIAN_POINT('',(29.1284493206708,-2.59375719295039,31.6237706303691));
#71791=CARTESIAN_POINT('Ctrl Pts',(29.1284493206757,-2.593757192945,31.6237706303625));
#71792=CARTESIAN_POINT('Ctrl Pts',(29.1406919790996,-2.58022003094555,31.6070390219952));
#71793=CARTESIAN_POINT('Ctrl Pts',(29.1527859988003,-2.56684722430145,31.5905494329059));
#71794=CARTESIAN_POINT('',(28.9782217890806,-2.53833533054863,31.6237706303691));
#71795=CARTESIAN_POINT('Origin',(30.,-1.32966554433622E-14,31.6237706303681));
#71796=CARTESIAN_POINT('',(28.9771926604683,-2.50206742175908,31.5905494329235));
#71797=CARTESIAN_POINT('Ctrl Pts',(28.9771926604686,-2.50206742176849,31.5905494329321));
#71798=CARTESIAN_POINT('Ctrl Pts',(28.9777040820209,-2.5200906211944,31.6070390220085));
#71799=CARTESIAN_POINT('Ctrl Pts',(28.9782217890804,-2.53833533054136,31.6237706303625));
#71800=CARTESIAN_POINT('',(28.9540051647184,-2.49246284654199,31.5905494329235));
#71801=CARTESIAN_POINT('Origin',(28.963441988931,-2.50247243285095,31.5962053997573));
#71802=CARTESIAN_POINT('',(28.9276321766534,-2.51738042696608,31.6237706303691));
#71803=CARTESIAN_POINT('Ctrl Pts',(28.9276321766587,-2.51738042696105,31.6237706303625));
#71804=CARTESIAN_POINT('Ctrl Pts',(28.9408992085416,-2.5048455434235,31.6070390219952));
#71805=CARTESIAN_POINT('Ctrl Pts',(28.9540051647323,-2.49246284652876,31.5905494329059));
#71806=CARTESIAN_POINT('',(28.7822160956147,-2.45034269538798,31.6237706303691));
#71807=CARTESIAN_POINT('Origin',(30.,-1.32966554433622E-14,31.6237706303681));
#71808=CARTESIAN_POINT('',(28.7840356867901,-2.41410584395713,31.5905494329235));
#71809=CARTESIAN_POINT('Ctrl Pts',(28.7840356867896,-2.41410584396654,31.5905494329321));
#71810=CARTESIAN_POINT('Ctrl Pts',(28.783131447871,-2.43211360955609,31.6070390220085));
#71811=CARTESIAN_POINT('Ctrl Pts',(28.7822160956151,-2.45034269538072,31.6237706303625));
#71812=CARTESIAN_POINT('',(28.7616732366375,-2.40271160649133,31.5905494329235));
#71813=CARTESIAN_POINT('Origin',(28.7702956661397,-2.41343066267495,31.5962052993351));
#71814=CARTESIAN_POINT('',(28.7334265368654,-2.42548317353557,31.6237706303691));
#71815=CARTESIAN_POINT('Ctrl Pts',(28.7334265368711,-2.425483173531,31.6237706303625));
#71816=CARTESIAN_POINT('Ctrl Pts',(28.7476361465498,-2.41402785018062,31.6070390219952));
#71817=CARTESIAN_POINT('Ctrl Pts',(28.7616732366525,-2.40271160647928,31.5905494329059));
#71818=CARTESIAN_POINT('',(28.5937184448736,-2.34724288268865,31.6237706303691));
#71819=CARTESIAN_POINT('Origin',(30.,-1.32966554433622E-14,31.6237706303681));
#71820=CARTESIAN_POINT('',(28.5983755374519,-2.31126050085552,31.5905494329235));
#71821=CARTESIAN_POINT('Ctrl Pts',(28.5983755374507,-2.31126050086484,31.5905494329321));
#71822=CARTESIAN_POINT('Ctrl Pts',(28.5960612129946,-2.32914180875499,31.6070390220085));
#71823=CARTESIAN_POINT('Ctrl Pts',(28.5937184448745,-2.34724288268142,31.6237706303625));
#71824=CARTESIAN_POINT('',(28.5769760048382,-2.29814685040397,31.5905494329235));
#71825=CARTESIAN_POINT('Origin',(28.5847308825473,-2.30950931155478,31.5962052196244));
#71826=CARTESIAN_POINT('',(28.547029743656,-2.31863200978522,31.6237706303691));
#71827=CARTESIAN_POINT('Ctrl Pts',(28.547029743662,-2.31863200978111,31.6237706303625));
#71828=CARTESIAN_POINT('Ctrl Pts',(28.5620943241676,-2.30832687249563,31.6070390219952));
#71829=CARTESIAN_POINT('Ctrl Pts',(28.5769760048541,-2.29814685039312,31.5905494329059));
#71830=CARTESIAN_POINT('',(28.413890987556,-2.22967153708007,31.6237706303691));
#71831=CARTESIAN_POINT('Origin',(30.,-1.32966554433622E-14,31.6237706303681));
#71832=CARTESIAN_POINT('',(28.4213568690129,-2.19416546819403,31.5905494329235));
#71833=CARTESIAN_POINT('Ctrl Pts',(28.421356869011,-2.19416546820326,31.5905494329321));
#71834=CARTESIAN_POINT('Ctrl Pts',(28.4176467275973,-2.21181007418472,31.6070390220085));
#71835=CARTESIAN_POINT('Ctrl Pts',(28.4138909875575,-2.22967153707296,31.6237706303625));
#71836=CARTESIAN_POINT('',(28.4010521891725,-2.17941325477249,31.5905494329235));
#71837=CARTESIAN_POINT('Origin',(28.407891704857,-2.19134908471608,31.596205156165));
#71838=CARTESIAN_POINT('',(28.3695909952386,-2.19748570867116,31.6237706303691));
#71839=CARTESIAN_POINT('Ctrl Pts',(28.3695909952449,-2.19748570866753,31.6237706303625));
#71840=CARTESIAN_POINT('Ctrl Pts',(28.3854176684292,-2.18839429204513,31.6070390219952));
#71841=CARTESIAN_POINT('Ctrl Pts',(28.4010521891892,-2.17941325476292,31.5905494329059));
#71842=CARTESIAN_POINT('',(28.2438424197348,-2.09835352500436,31.6237706303691));
#71843=CARTESIAN_POINT('Origin',(30.,-1.32966554433622E-14,31.6237706303681));
#71844=CARTESIAN_POINT('',(28.2540710604284,-2.06354267578707,31.5905494329235));
#71845=CARTESIAN_POINT('Ctrl Pts',(28.2540710604258,-2.0635426757961,31.5905494329321));
#71846=CARTESIAN_POINT('Ctrl Pts',(28.2489879763101,-2.08084179500557,31.6070390220085));
#71847=CARTESIAN_POINT('Ctrl Pts',(28.2438424197369,-2.09835352499738,31.6237706303625));
#71848=CARTESIAN_POINT('',(28.2349864184647,-2.04724285169689,31.5905494329235));
#71849=CARTESIAN_POINT('Origin',(28.2408684039783,-2.05967847590829,31.5962051058414));
#71850=CARTESIAN_POINT('',(28.2022042605016,-2.06279117742499,31.6237706303691));
#71851=CARTESIAN_POINT('Ctrl Pts',(28.2022042605082,-2.06279117742185,31.6237706303625));
#71852=CARTESIAN_POINT('Ctrl Pts',(28.2186954496679,-2.0549695330692,31.6070390219952));
#71853=CARTESIAN_POINT('Ctrl Pts',(28.2349864184821,-2.04724285168864,31.5905494329059));
#71854=CARTESIAN_POINT('',(28.0846211473776,-1.95409846567366,31.6237706303691));
#71855=CARTESIAN_POINT('Origin',(30.,-1.32966554433622E-14,31.6237706303681));
#71856=CARTESIAN_POINT('',(28.0975494843367,-1.92019745658631,31.5905494329235));
#71857=CARTESIAN_POINT('Ctrl Pts',(28.0975494843333,-1.92019745659509,31.5905494329321));
#71858=CARTESIAN_POINT('Ctrl Pts',(28.0911247964195,-1.93704443421011,31.6070390220085));
#71859=CARTESIAN_POINT('Ctrl Pts',(28.0846211473802,-1.95409846566685,31.6237706303626));
#71860=CARTESIAN_POINT('',(28.0798025434136,-1.90245051566325,31.5905494329235));
#71861=CARTESIAN_POINT('Origin',(28.0846907329876,-1.91530927561707,31.5962050664381));
#71862=CARTESIAN_POINT('',(28.0459015343263,-1.91537885262232,31.6237706303691));
#71863=CARTESIAN_POINT('Ctrl Pts',(28.0459015343331,-1.91537885261973,31.6237706303625));
#71864=CARTESIAN_POINT('Ctrl Pts',(28.0629555658034,-1.90887520357524,31.6070390219952));
#71865=CARTESIAN_POINT('Ctrl Pts',(28.0798025434316,-1.90245051565641,31.5905494329059));
#71866=CARTESIAN_POINT('',(27.937208822575,-1.79779573949839,31.6237706303691));
#71867=CARTESIAN_POINT('Origin',(30.,-1.32966554433622E-14,31.6237706303681));
#71868=CARTESIAN_POINT('',(27.9527571483031,-1.76501358153525,31.5905494329235));
#71869=CARTESIAN_POINT('Ctrl Pts',(27.9527571482991,-1.76501358154376,31.5905494329321));
#71870=CARTESIAN_POINT('Ctrl Pts',(27.9450304669246,-1.78130455034514,31.6070390220085));
#71871=CARTESIAN_POINT('Ctrl Pts',(27.9372088225781,-1.79779573949183,31.6237706303625));
#71872=CARTESIAN_POINT('',(27.9364573242129,-1.74592893957155,31.5905494329235));
#71873=CARTESIAN_POINT('Origin',(27.940321578254,-1.75913156587022,31.5962050363747));
#71874=CARTESIAN_POINT('',(27.9016464749956,-1.75615758026514,31.6237706303691));
#71875=CARTESIAN_POINT('Ctrl Pts',(27.9016464750026,-1.75615758026309,31.6237706303625));
#71876=CARTESIAN_POINT('Ctrl Pts',(27.9191582050083,-1.75101202368579,31.6070390219952));
#71877=CARTESIAN_POINT('Ctrl Pts',(27.9364573242313,-1.74592893956614,31.5905494329059));
#71878=CARTESIAN_POINT('',(27.8025142913288,-1.63040900476137,31.6237706303691));
#71879=CARTESIAN_POINT('Origin',(30.,-1.32966554433622E-14,31.6237706303681));
#71880=CARTESIAN_POINT('',(27.8205867452275,-1.59894781082744,31.5905494329235));
#71881=CARTESIAN_POINT('Ctrl Pts',(27.8205867452228,-1.59894781083561,31.5905494329321));
#71882=CARTESIAN_POINT('Ctrl Pts',(27.8116057079476,-1.61458233158338,31.6070390220085));
#71883=CARTESIAN_POINT('Ctrl Pts',(27.8025142913325,-1.63040900475507,31.6237706303625));
#71884=CARTESIAN_POINT('',(27.8058345318059,-1.5786431309871,31.5905494329235));
#71885=CARTESIAN_POINT('Origin',(27.8086510228583,-1.5921082324254,31.5962050145327));
#71886=CARTESIAN_POINT('',(27.7703284629199,-1.58610901244396,31.6237706303691));
#71887=CARTESIAN_POINT('Ctrl Pts',(27.770328462927,-1.58610901244246,31.6237706303625));
#71888=CARTESIAN_POINT('Ctrl Pts',(27.7881899258294,-1.58235327239973,31.6070390219952));
#71889=CARTESIAN_POINT('Ctrl Pts',(27.8058345318247,-1.57864313098315,31.5905494329059));
#71890=CARTESIAN_POINT('',(27.6813679902147,-1.45297025634398,31.6237706303691));
#71891=CARTESIAN_POINT('Origin',(30.,-1.32966554433622E-14,31.6237706303681));
#71892=CARTESIAN_POINT('',(27.701853149596,-1.42302399516179,31.5905494329235));
#71893=CARTESIAN_POINT('Ctrl Pts',(27.7018531495907,-1.42302399516956,31.5905494329321));
#71894=CARTESIAN_POINT('Ctrl Pts',(27.6916731274962,-1.43790567584432,31.6070390220085));
#71895=CARTESIAN_POINT('Ctrl Pts',(27.6813679902189,-1.45297025633799,31.6237706303626));
#71896=CARTESIAN_POINT('',(27.6887394991444,-1.40162446254801,31.5905494329235));
#71897=CARTESIAN_POINT('Origin',(27.6904908588872,-1.41526902814876,31.596205000146));
#71898=CARTESIAN_POINT('',(27.6527571173113,-1.4062815551263,31.6237706303691));
#71899=CARTESIAN_POINT('Ctrl Pts',(27.6527571173185,-1.40628155512537,31.6237706303626));
#71900=CARTESIAN_POINT('Ctrl Pts',(27.6708581912593,-1.40393878700346,31.6070390219953));
#71901=CARTESIAN_POINT('Ctrl Pts',(27.6887394991635,-1.40162446254554,31.5905494329059));
#71902=CARTESIAN_POINT('',(27.5745168264644,-1.2665734631346,31.6237706303691));
#71903=CARTESIAN_POINT('Origin',(30.,-1.32966554433622E-14,31.6237706303681));
#71904=CARTESIAN_POINT('',(27.5972883935086,-1.23832676336246,31.5905494329235));
#71905=CARTESIAN_POINT('Ctrl Pts',(27.5972883935027,-1.23832676336977,31.5905494329321));
#71906=CARTESIAN_POINT('Ctrl Pts',(27.5859721498102,-1.25236385346148,31.6070390220085));
#71907=CARTESIAN_POINT('Ctrl Pts',(27.574516826469,-1.2665734631289,31.6237706303626));
#71908=CARTESIAN_POINT('',(27.5858941560428,-1.21596431320988,31.5905494329235));
#71909=CARTESIAN_POINT('Origin',(27.5865695824296,-1.22970422416533,31.5962049927334));
#71910=CARTESIAN_POINT('',(27.549657304612,-1.21778390438522,31.6237706303691));
#71911=CARTESIAN_POINT('Ctrl Pts',(27.5496573046193,-1.21778390438485,31.6237706303625));
#71912=CARTESIAN_POINT('Ctrl Pts',(27.5678863904584,-1.2168685521283,31.6070390219952));
#71913=CARTESIAN_POINT('Ctrl Pts',(27.585894156062,-1.21596431320891,31.5905494329059));
#71914=CARTESIAN_POINT('',(27.4826195730339,-1.07236782334657,31.6237706303691));
#71915=CARTESIAN_POINT('Origin',(30.,-1.32966554433622E-14,31.6237706303681));
#71916=CARTESIAN_POINT('',(27.507537153458,-1.04599483528157,31.5905494329235));
#71917=CARTESIAN_POINT('Ctrl Pts',(27.5075371534515,-1.04599483528841,31.5905494329321));
#71918=CARTESIAN_POINT('Ctrl Pts',(27.4951544565665,-1.05910079146888,31.6070390220085));
#71919=CARTESIAN_POINT('Ctrl Pts',(27.4826195730389,-1.07236782334129,31.6237706303626));
#71920=CARTESIAN_POINT('',(27.4979325782409,-1.02280733953164,31.5905494329235));
#71921=CARTESIAN_POINT('Origin',(27.4975279021274,-1.03655788791105,31.5962049920587));
#71922=CARTESIAN_POINT('',(27.4616646694513,-1.02177821091936,31.6237706303691));
#71923=CARTESIAN_POINT('Ctrl Pts',(27.4616646694586,-1.02177821091956,31.6237706303626));
#71924=CARTESIAN_POINT('Ctrl Pts',(27.4799093788201,-1.02229591797942,31.6070390219952));
#71925=CARTESIAN_POINT('Ctrl Pts',(27.4979325782601,-1.02280733953218,31.5905494329059));
#71926=CARTESIAN_POINT('',(27.4062428070496,-0.871550679329129,31.6237706303691));
#71927=CARTESIAN_POINT('Origin',(30.,-1.32966554433622E-14,31.6237706303681));
#71928=CARTESIAN_POINT('',(27.4331527756843,-0.847214001212589,31.5905494329235));
#71929=CARTESIAN_POINT('Ctrl Pts',(27.4331527756773,-0.847214001218912,
31.5905494329321));
#71930=CARTESIAN_POINT('Ctrl Pts',(27.4197799690437,-0.859308020910092,
31.6070390220085));
#71931=CARTESIAN_POINT('Ctrl Pts',(27.406242807055,-0.871550679324261,31.6237706303625));
#71932=CARTESIAN_POINT('',(27.4253970781159,-0.823344418487241,31.5905494329235));
#71933=CARTESIAN_POINT('Origin',(27.4239147889674,-0.837020829522197,31.5962049981138));
#71934=CARTESIAN_POINT('',(27.3893217156857,-0.819472915007445,31.6237706303691));
#71935=CARTESIAN_POINT('Ctrl Pts',(27.3893217156929,-0.819472915008222,
31.6237706303625));
#71936=CARTESIAN_POINT('Ctrl Pts',(27.4074695638765,-0.821420489548307,
31.6070390219952));
#71937=CARTESIAN_POINT('Ctrl Pts',(27.425397078135,-0.823344418489291,31.590549432906));
#71938=CARTESIAN_POINT('',(27.3458574166716,-0.665360135553609,31.6237706303691));
#71939=CARTESIAN_POINT('Origin',(30.,-1.32966554433622E-14,31.6237706303681));
#71940=CARTESIAN_POINT('',(27.3745938646118,-0.643209811098888,31.5905494329235));
#71941=CARTESIAN_POINT('Ctrl Pts',(27.3745938646043,-0.643209811104637,
31.5905494329321));
#71942=CARTESIAN_POINT('Ctrl Pts',(27.3603133960219,-0.65421733065347,31.6070390220085));
#71943=CARTESIAN_POINT('Ctrl Pts',(27.3458574166774,-0.665360135549176,
31.6237706303625));
#71944=CARTESIAN_POINT('',(27.3687348611467,-0.618805305313063,31.5905494329235));
#71945=CARTESIAN_POINT('Origin',(27.3661840916659,-0.632323260043008,31.5962050111235));
#71946=CARTESIAN_POINT('',(27.3330744616815,-0.612115296072114,31.6237706303691));
#71947=CARTESIAN_POINT('Ctrl Pts',(27.3330744616886,-0.612115296073467,
31.6237706303625));
#71948=CARTESIAN_POINT('Ctrl Pts',(27.3510135611755,-0.615480730649101,
31.6070390219952));
#71949=CARTESIAN_POINT('Ctrl Pts',(27.3687348611656,-0.61880530531661,31.590549432906));
#71950=CARTESIAN_POINT('',(27.3018356979118,-0.455067425287704,31.6237706303691));
#71951=CARTESIAN_POINT('Origin',(30.,-1.32966554433622E-14,31.6237706303681));
#71952=CARTESIAN_POINT('',(27.3322214554001,-0.435240018610796,31.5905494329235));
#71953=CARTESIAN_POINT('Ctrl Pts',(27.3322214553922,-0.435240018615941,
31.5905494329321));
#71954=CARTESIAN_POINT('Ctrl Pts',(27.3171213686986,-0.445093173004034,
31.6070390220085));
#71955=CARTESIAN_POINT('Ctrl Pts',(27.3018356979179,-0.455067425283735,
31.6237706303625));
#71956=CARTESIAN_POINT('',(27.328295268743,-0.410451051657984,31.5905494329235));
#71957=CARTESIAN_POINT('Origin',(27.3246917385075,-0.423727206709274,31.5962050315749));
#71958=CARTESIAN_POINT('',(27.2932696904637,-0.400983782787508,31.6237706303691));
#71959=CARTESIAN_POINT('Ctrl Pts',(27.2932696904707,-0.400983782789399,
31.6237706303625));
#71960=CARTESIAN_POINT('Ctrl Pts',(27.3108894407472,-0.405746328377308,
31.6070390219952));
#71961=CARTESIAN_POINT('Ctrl Pts',(27.3282952687616,-0.410451051662988,
31.5905494329059));
#71962=CARTESIAN_POINT('',(27.274449059305,-0.241969073019628,31.6237706303691));
#71963=CARTESIAN_POINT('Origin',(30.,-1.32966554433622E-14,31.6237706303681));
#71964=CARTESIAN_POINT('',(27.3062967880422,-0.224586826675978,31.5905494329235));
#71965=CARTESIAN_POINT('Ctrl Pts',(27.306296788034,-0.224586826680481,31.5905494329321));
#71966=CARTESIAN_POINT('Ctrl Pts',(27.2904701802848,-0.233224867934527,
31.6070390220085));
#71967=CARTESIAN_POINT('Ctrl Pts',(27.2744490593114,-0.241969073016143,
31.6237706303626));
#71968=CARTESIAN_POINT('',(27.3043276244395,-0.199566230780611,31.5905494329235));
#71969=CARTESIAN_POINT('Origin',(27.2996935428802,-0.212518732061225,31.5962050602856));
#71970=CARTESIAN_POINT('',(27.2701528116834,-0.18738007114138,31.6237706303691));
#71971=CARTESIAN_POINT('Ctrl Pts',(27.2701528116903,-0.187380071143839,
31.6237706303625));
#71972=CARTESIAN_POINT('Ctrl Pts',(27.2873445811368,-0.193510365066767,
31.6070390219952));
#71973=CARTESIAN_POINT('Ctrl Pts',(27.3043276244576,-0.199566230787083,
31.5905494329059));
#71974=CARTESIAN_POINT('',(27.2638663485853,-0.027378900953502,31.6237706303691));
#71975=CARTESIAN_POINT('Origin',(30.,-1.32966554433622E-14,31.6237706303681));
#71976=CARTESIAN_POINT('Ctrl Pts',(27.2969796967247,-0.0125489822758455,
31.5905494329321));
#71977=CARTESIAN_POINT('Ctrl Pts',(27.2805241442198,-0.0199186539990725,
31.6070390220085));
#71978=CARTESIAN_POINT('Ctrl Pts',(27.263866348592,-0.0273789009505331,
31.6237706303626));
#71979=CARTESIAN_POINT('',(27.2638663485853,0.0273789009535324,31.6237706303691));
#71980=CARTESIAN_POINT('Ctrl Pts',(27.263866348592,0.0273789009505529,31.6237706303626));
#71981=CARTESIAN_POINT('Ctrl Pts',(27.280524144233,0.0199186539931685,31.6070390219952));
#71982=CARTESIAN_POINT('Ctrl Pts',(27.2969796967508,0.012548982264161,31.5905494329059));
#71983=CARTESIAN_POINT('',(27.2701528116834,0.187380071141411,31.6237706303691));
#71984=CARTESIAN_POINT('Origin',(30.,-1.32966554433622E-14,31.6237706303681));
#71985=CARTESIAN_POINT('Ctrl Pts',(27.3043276244306,0.199566230777481,31.5905494329321));
#71986=CARTESIAN_POINT('Ctrl Pts',(27.2873445811231,0.193510365061917,31.6070390220085));
#71987=CARTESIAN_POINT('Ctrl Pts',(27.2701528116902,0.187380071143857,31.6237706303625));
#71988=CARTESIAN_POINT('',(27.2744490593051,0.241969073019658,31.6237706303691));
#71989=CARTESIAN_POINT('Ctrl Pts',(27.2744490593115,0.241969073016152,31.6237706303625));
#71990=CARTESIAN_POINT('Ctrl Pts',(27.2904701802976,0.233224867927605,31.6070390219952));
#71991=CARTESIAN_POINT('Ctrl Pts',(27.3062967880591,0.224586826666795,31.5905494329059));
#71992=CARTESIAN_POINT('',(27.2932696904637,0.40098378278754,31.6237706303691));
#71993=CARTESIAN_POINT('Origin',(30.,-1.32966554433622E-14,31.6237706303681));
#71994=CARTESIAN_POINT('Ctrl Pts',(27.3282952687339,0.410451051655568,31.5905494329321));
#71995=CARTESIAN_POINT('Ctrl Pts',(27.3108894407332,0.405746328373579,31.6070390220085));
#71996=CARTESIAN_POINT('Ctrl Pts',(27.2932696904707,0.400983782789452,31.6237706303626));
#71997=CARTESIAN_POINT('',(27.3018356979118,0.455067425287736,31.6237706303691));
#71998=CARTESIAN_POINT('Ctrl Pts',(27.3018356979179,0.455067425283746,31.6237706303626));
#71999=CARTESIAN_POINT('Ctrl Pts',(27.3171213687107,0.445093172996126,31.6070390219952));
#72000=CARTESIAN_POINT('Ctrl Pts',(27.3322214554162,0.435240018600305,31.5905494329059));
#72001=CARTESIAN_POINT('',(27.3330744616815,0.612115296072143,31.6237706303691));
#72002=CARTESIAN_POINT('Origin',(30.,-1.32966554433622E-14,31.6237706303681));
#72003=CARTESIAN_POINT('Ctrl Pts',(27.3687348611375,0.618805305311351,31.5905494329321));
#72004=CARTESIAN_POINT('Ctrl Pts',(27.3510135611613,0.615480730646445,31.6070390220085));
#72005=CARTESIAN_POINT('Ctrl Pts',(27.3330744616886,0.612115296073478,31.6237706303625));
#72006=CARTESIAN_POINT('',(27.3458574166716,0.665360135553637,31.6237706303691));
#72007=CARTESIAN_POINT('Ctrl Pts',(27.3458574166774,0.665360135549173,31.6237706303626));
#72008=CARTESIAN_POINT('Ctrl Pts',(27.3603133960334,0.65421733064462,31.6070390219952));
#72009=CARTESIAN_POINT('Ctrl Pts',(27.374593864627,0.643209811087154,31.5905494329059));
#72010=CARTESIAN_POINT('',(27.3893217156857,0.819472915007473,31.6237706303691));
#72011=CARTESIAN_POINT('Origin',(30.,-1.32966554433622E-14,31.6237706303681));
#72012=CARTESIAN_POINT('Ctrl Pts',(27.4253970781066,0.823344418486268,31.5905494329322));
#72013=CARTESIAN_POINT('Ctrl Pts',(27.4074695638621,0.821420489546793,31.6070390220085));
#72014=CARTESIAN_POINT('Ctrl Pts',(27.3893217156929,0.819472915008255,31.6237706303625));
#72015=CARTESIAN_POINT('',(27.4062428070496,0.871550679329156,31.6237706303691));
#72016=CARTESIAN_POINT('Ctrl Pts',(27.406242807055,0.87155067932429,31.6237706303625));
#72017=CARTESIAN_POINT('Ctrl Pts',(27.4197799690545,0.8593080209004,31.6070390219952));
#72018=CARTESIAN_POINT('Ctrl Pts',(27.4331527756986,0.847214001199735,31.5905494329059));
#72019=CARTESIAN_POINT('',(27.4616646694514,1.02177821091938,31.6237706303691));
#72020=CARTESIAN_POINT('Origin',(30.,-1.32966554433622E-14,31.6237706303681));
#72021=CARTESIAN_POINT('Ctrl Pts',(27.4979325782315,1.0228073395314,31.5905494329321));
#72022=CARTESIAN_POINT('Ctrl Pts',(27.4799093788056,1.02229591797904,31.6070390220085));
#72023=CARTESIAN_POINT('Ctrl Pts',(27.4616646694587,1.02177821091959,31.6237706303625));
#72024=CARTESIAN_POINT('',(27.4826195730339,1.0723678233466,31.6237706303691));
#72025=CARTESIAN_POINT('Ctrl Pts',(27.4826195730389,1.0723678233413,31.6237706303626));
#72026=CARTESIAN_POINT('Ctrl Pts',(27.4951544565765,1.05910079145835,31.6070390219952));
#72027=CARTESIAN_POINT('Ctrl Pts',(27.5075371534712,1.04599483526761,31.5905494329059));
#72028=CARTESIAN_POINT('',(27.549657304612,1.21778390438524,31.6237706303691));
#72029=CARTESIAN_POINT('Origin',(30.,-1.32966554433622E-14,31.6237706303681));
#72030=CARTESIAN_POINT('Ctrl Pts',(27.5858941560335,1.21596431321037,31.5905494329321));
#72031=CARTESIAN_POINT('Ctrl Pts',(27.5678863904439,1.21686855212906,31.6070390220085));
#72032=CARTESIAN_POINT('Ctrl Pts',(27.5496573046193,1.21778390438488,31.6237706303626));
#72033=CARTESIAN_POINT('',(27.5745168264644,1.26657346313462,31.6237706303691));
#72034=CARTESIAN_POINT('Ctrl Pts',(27.574516826469,1.26657346312892,31.6237706303626));
#72035=CARTESIAN_POINT('Ctrl Pts',(27.5859721498194,1.25236385345021,31.6070390219952));
#72036=CARTESIAN_POINT('Ctrl Pts',(27.5972883935207,1.23832676334747,31.5905494329059));
#72037=CARTESIAN_POINT('',(27.6527571173114,1.40628155512632,31.6237706303691));
#72038=CARTESIAN_POINT('Origin',(30.,-1.32966554433622E-14,31.6237706303681));
#72039=CARTESIAN_POINT('Ctrl Pts',(27.6887394991352,1.40162446254924,31.5905494329321));
#72040=CARTESIAN_POINT('Ctrl Pts',(27.670858191245,1.40393878700535,31.6070390220085));
#72041=CARTESIAN_POINT('Ctrl Pts',(27.6527571173186,1.40628155512539,31.6237706303625));
#72042=CARTESIAN_POINT('',(27.6813679902148,1.45297025634401,31.6237706303691));
#72043=CARTESIAN_POINT('Ctrl Pts',(27.6813679902189,1.452970256338,31.6237706303625));
#72044=CARTESIAN_POINT('Ctrl Pts',(27.6916731275044,1.43790567583238,31.6070390219952));
#72045=CARTESIAN_POINT('Ctrl Pts',(27.7018531496069,1.42302399514596,31.5905494329059));
#72046=CARTESIAN_POINT('',(27.7703284629199,1.58610901244398,31.6237706303691));
#72047=CARTESIAN_POINT('Origin',(30.,-1.32966554433622E-14,31.6237706303681));
#72048=CARTESIAN_POINT('Ctrl Pts',(27.8058345317968,1.57864313098906,31.5905494329321));
#72049=CARTESIAN_POINT('Ctrl Pts',(27.7881899258153,1.58235327240273,31.6070390220085));
#72050=CARTESIAN_POINT('Ctrl Pts',(27.770328462927,1.58610901244249,31.6237706303626));
#72051=CARTESIAN_POINT('',(27.8025142913288,1.63040900476139,31.6237706303691));
#72052=CARTESIAN_POINT('Ctrl Pts',(27.8025142913324,1.63040900475507,31.6237706303626));
#72053=CARTESIAN_POINT('Ctrl Pts',(27.8116057079549,1.61458233157081,31.6070390219952));
#72054=CARTESIAN_POINT('Ctrl Pts',(27.8205867452371,1.59894781081078,31.5905494329059));
#72055=CARTESIAN_POINT('',(27.9016464749956,1.75615758026516,31.6237706303691));
#72056=CARTESIAN_POINT('Origin',(30.,-1.32966554433622E-14,31.6237706303681));
#72057=CARTESIAN_POINT('Ctrl Pts',(27.9364573242039,1.74592893957422,31.5905494329321));
#72058=CARTESIAN_POINT('Ctrl Pts',(27.9191582049944,1.75101202368989,31.6070390220085));
#72059=CARTESIAN_POINT('Ctrl Pts',(27.9016464750026,1.7561575802631,31.6237706303626));
#72060=CARTESIAN_POINT('',(27.937208822575,1.79779573949841,31.6237706303691));
#72061=CARTESIAN_POINT('Ctrl Pts',(27.9372088225781,1.79779573949182,31.6237706303625));
#72062=CARTESIAN_POINT('Ctrl Pts',(27.9450304669308,1.78130455033204,31.6070390219952));
#72063=CARTESIAN_POINT('Ctrl Pts',(27.9527571483113,1.76501358151789,31.5905494329059));
#72064=CARTESIAN_POINT('',(28.0459015343263,1.91537885262234,31.6237706303691));
#72065=CARTESIAN_POINT('Origin',(30.,-1.32966554433622E-14,31.6237706303681));
#72066=CARTESIAN_POINT('Ctrl Pts',(28.0798025434049,1.90245051566662,31.5905494329321));
#72067=CARTESIAN_POINT('Ctrl Pts',(28.0629555657899,1.90887520358041,31.6070390220085));
#72068=CARTESIAN_POINT('Ctrl Pts',(28.0459015343331,1.91537885261975,31.6237706303626));
#72069=CARTESIAN_POINT('',(28.0846211473777,1.95409846567367,31.6237706303691));
#72070=CARTESIAN_POINT('Ctrl Pts',(28.0846211473803,1.95409846566688,31.6237706303625));
#72071=CARTESIAN_POINT('Ctrl Pts',(28.0911247964248,1.93704443419661,31.6070390219952));
#72072=CARTESIAN_POINT('Ctrl Pts',(28.0975494843436,1.9201974565684,31.5905494329059));
#72073=CARTESIAN_POINT('',(28.2022042605016,2.062791177425,31.6237706303691));
#72074=CARTESIAN_POINT('Origin',(30.,-1.32966554433622E-14,31.6237706303681));
#72075=CARTESIAN_POINT('Ctrl Pts',(28.2349864184563,2.04724285170094,31.5905494329321));
#72076=CARTESIAN_POINT('Ctrl Pts',(28.2186954496549,2.05496953307545,31.6070390220085));
#72077=CARTESIAN_POINT('Ctrl Pts',(28.2022042605082,2.0627911774219,31.6237706303626));
#72078=CARTESIAN_POINT('',(28.2438424197349,2.09835352500437,31.6237706303691));
#72079=CARTESIAN_POINT('Ctrl Pts',(28.2438424197369,2.09835352499738,31.6237706303625));
#72080=CARTESIAN_POINT('Ctrl Pts',(28.2489879763142,2.08084179499167,31.6070390219952));
#72081=CARTESIAN_POINT('Ctrl Pts',(28.2540710604339,2.06354267576863,31.5905494329059));
#72082=CARTESIAN_POINT('',(28.3695909952386,2.19748570867117,31.6237706303691));
#72083=CARTESIAN_POINT('Origin',(30.,-1.32966554433622E-14,31.6237706303681));
#72084=CARTESIAN_POINT('Ctrl Pts',(28.4010521891644,2.17941325477719,31.5905494329321));
#72085=CARTESIAN_POINT('Ctrl Pts',(28.3854176684167,2.18839429205237,31.6070390220085));
#72086=CARTESIAN_POINT('Ctrl Pts',(28.369590995245,2.19748570866756,31.6237706303626));
#72087=CARTESIAN_POINT('',(28.413890987556,2.22967153708007,31.6237706303691));
#72088=CARTESIAN_POINT('Ctrl Pts',(28.4138909875575,2.22967153707294,31.6237706303625));
#72089=CARTESIAN_POINT('Ctrl Pts',(28.4176467276003,2.21181007417053,31.6070390219952));
#72090=CARTESIAN_POINT('Ctrl Pts',(28.4213568690169,2.19416546817523,31.5905494329059));
#72091=CARTESIAN_POINT('',(28.547029743656,2.31863200978522,31.6237706303691));
#72092=CARTESIAN_POINT('Origin',(30.,-1.32966554433622E-14,31.6237706303681));
#72093=CARTESIAN_POINT('Ctrl Pts',(28.5769760048304,2.29814685040929,31.5905494329321));
#72094=CARTESIAN_POINT('Ctrl Pts',(28.5620943241557,2.30832687250382,31.6070390220085));
#72095=CARTESIAN_POINT('Ctrl Pts',(28.547029743662,2.31863200978111,31.6237706303625));
#72096=CARTESIAN_POINT('',(28.5937184448737,2.34724288268865,31.6237706303691));
#72097=CARTESIAN_POINT('Ctrl Pts',(28.5937184448746,2.34724288268143,31.6237706303626));
#72098=CARTESIAN_POINT('Ctrl Pts',(28.5960612129965,2.32914180874063,31.6070390219952));
#72099=CARTESIAN_POINT('Ctrl Pts',(28.5983755374545,2.31126050083645,31.5905494329059));
#72100=CARTESIAN_POINT('',(28.7334265368654,2.42548317353557,31.6237706303691));
#72101=CARTESIAN_POINT('Origin',(30.,-1.32966554433622E-14,31.6237706303681));
#72102=CARTESIAN_POINT('Ctrl Pts',(28.7616732366302,2.40271160649724,31.5905494329321));
#72103=CARTESIAN_POINT('Ctrl Pts',(28.7476361465385,2.4140278501897,31.6070390220085));
#72104=CARTESIAN_POINT('Ctrl Pts',(28.7334265368711,2.42548317353099,31.6237706303625));
#72105=CARTESIAN_POINT('',(28.7822160956148,2.45034269538798,31.6237706303691));
#72106=CARTESIAN_POINT('Ctrl Pts',(28.7822160956151,2.45034269538071,31.6237706303626));
#72107=CARTESIAN_POINT('Ctrl Pts',(28.7831314478717,2.4321136095416,31.6070390219952));
#72108=CARTESIAN_POINT('Ctrl Pts',(28.7840356867911,2.41410584393792,31.5905494329059));
#72109=CARTESIAN_POINT('',(28.9276321766534,2.51738042696607,31.6237706303691));
#72110=CARTESIAN_POINT('Origin',(30.,-1.32966554433622E-14,31.6237706303681));
#72111=CARTESIAN_POINT('',(28.9540051647184,2.49246284654199,31.5905494329235));
#72112=CARTESIAN_POINT('Ctrl Pts',(28.9540051647116,2.49246284654845,31.5905494329321));
#72113=CARTESIAN_POINT('Ctrl Pts',(28.9408992085311,2.50484554343346,31.6070390220085));
#72114=CARTESIAN_POINT('Ctrl Pts',(28.9276321766587,2.51738042696107,31.6237706303625));
#72115=CARTESIAN_POINT('',(28.9771926604684,2.50206742175908,31.5905494329235));
#72116=CARTESIAN_POINT('Origin',(28.9634421120889,2.50247209787257,31.5962049920587));
#72117=CARTESIAN_POINT('',(28.9782217890806,2.53833533054862,31.6237706303691));
#72118=CARTESIAN_POINT('Ctrl Pts',(28.9782217890804,2.53833533054134,31.6237706303625));
#72119=CARTESIAN_POINT('Ctrl Pts',(28.9777040820206,2.52009062117991,31.6070390219952));
#72120=CARTESIAN_POINT('Ctrl Pts',(28.9771926604678,2.50206742173986,31.5905494329059));
#72121=CARTESIAN_POINT('',(29.1284493206709,2.59375719295039,31.6237706303691));
#72122=CARTESIAN_POINT('Origin',(30.,-1.32966554433622E-14,31.6237706303681));
#72123=CARTESIAN_POINT('',(29.1527859987874,2.56684722431571,31.5905494329235));
#72124=CARTESIAN_POINT('Ctrl Pts',(29.1527859987811,2.56684722432269,31.5905494329321));
#72125=CARTESIAN_POINT('Ctrl Pts',(29.1406919790899,2.58022003095629,31.6070390220085));
#72126=CARTESIAN_POINT('Ctrl Pts',(29.1284493206758,2.59375719294498,31.6237706303625));
#72127=CARTESIAN_POINT('',(29.1766555815128,2.57460292188403,31.5905494329235));
#72128=CARTESIAN_POINT('Origin',(29.1629791704778,2.57608521103256,31.5962049981139));
#72129=CARTESIAN_POINT('',(29.1805270849926,2.61067828431428,31.6237706303691));
#72130=CARTESIAN_POINT('Ctrl Pts',(29.1805270849917,2.61067828430704,31.6237706303626));
#72131=CARTESIAN_POINT('Ctrl Pts',(29.1785795104516,2.59253043612347,31.6070390219952));
#72132=CARTESIAN_POINT('Ctrl Pts',(29.1766555815107,2.57460292186492,31.5905494329059));
#72133=CARTESIAN_POINT('',(29.3346398644464,2.65414258332837,31.6237706303691));
#72134=CARTESIAN_POINT('Origin',(30.,-1.32966554433622E-14,31.6237706303681));
#72135=CARTESIAN_POINT('',(29.3567901889011,2.6254061353882,31.5905494329235));
#72136=CARTESIAN_POINT('Ctrl Pts',(29.3567901888954,2.62540613539565,31.5905494329321));
#72137=CARTESIAN_POINT('Ctrl Pts',(29.3457826693465,2.63968660397804,31.6070390220085));
#72138=CARTESIAN_POINT('Ctrl Pts',(29.3346398644508,2.6541425833226,31.6237706303625));
#72139=CARTESIAN_POINT('',(29.3811946946869,2.63126513885323,31.5905494329235));
#72140=CARTESIAN_POINT('Origin',(29.367676739957,2.63381590833401,31.5962050111235));
#72141=CARTESIAN_POINT('',(29.3878847039279,2.66692553831851,31.6237706303691));
#72142=CARTESIAN_POINT('Ctrl Pts',(29.3878847039265,2.66692553831136,31.6237706303626));
#72143=CARTESIAN_POINT('Ctrl Pts',(29.3845192693509,2.64898643882447,31.6070390219952));
#72144=CARTESIAN_POINT('Ctrl Pts',(29.3811946946833,2.63126513883434,31.5905494329059));
#72145=CARTESIAN_POINT('',(29.5449325747123,2.69816430208817,31.6237706303691));
#72146=CARTESIAN_POINT('Origin',(30.,-1.32966554433622E-14,31.6237706303681));
#72147=CARTESIAN_POINT('',(29.5647599813892,2.6677785445999,31.5905494329235));
#72148=CARTESIAN_POINT('Ctrl Pts',(29.5647599813841,2.66777854460778,31.5905494329321));
#72149=CARTESIAN_POINT('Ctrl Pts',(29.554906826996,2.6828786313014,31.6070390220085));
#72150=CARTESIAN_POINT('Ctrl Pts',(29.5449325747163,2.69816430208207,31.6237706303625));
#72151=CARTESIAN_POINT('',(29.589548948342,2.67170473125694,31.5905494329235));
#72152=CARTESIAN_POINT('Origin',(29.5762727932907,2.67530826149244,31.5962050315749));
#72153=CARTESIAN_POINT('',(29.5990162172125,2.70673030953627,31.6237706303691));
#72154=CARTESIAN_POINT('Ctrl Pts',(29.5990162172106,2.70673030952925,31.6237706303625));
#72155=CARTESIAN_POINT('Ctrl Pts',(29.5942536716227,2.68911055925274,31.6070390219952));
#72156=CARTESIAN_POINT('Ctrl Pts',(29.589548948337,2.67170473123838,31.5905494329059));
#72157=CARTESIAN_POINT('',(29.7580309269804,2.72555094069491,31.6237706303691));
#72158=CARTESIAN_POINT('Origin',(30.,-1.32966554433622E-14,31.6237706303681));
#72159=CARTESIAN_POINT('',(29.775413173324,2.69370321195775,31.5905494329235));
#72160=CARTESIAN_POINT('Ctrl Pts',(29.7754131733195,2.69370321196601,31.5905494329321));
#72161=CARTESIAN_POINT('Ctrl Pts',(29.7667751320655,2.7095298197151,31.6070390220085));
#72162=CARTESIAN_POINT('Ctrl Pts',(29.7580309269838,2.72555094068851,31.6237706303625));
#72163=CARTESIAN_POINT('',(29.8004337692194,2.69567237556048,31.5905494329235));
#72164=CARTESIAN_POINT('Origin',(29.7874812679388,2.70030645711977,31.5962050602857));
#72165=CARTESIAN_POINT('',(29.8126199288586,2.72984718831658,31.6237706303691));
#72166=CARTESIAN_POINT('Ctrl Pts',(29.8126199288562,2.72984718830972,31.6237706303625));
#72167=CARTESIAN_POINT('Ctrl Pts',(29.8064896349333,2.71265541886322,31.6070390219952));
#72168=CARTESIAN_POINT('Ctrl Pts',(29.800433769213,2.69567237554238,31.5905494329059));
#72169=CARTESIAN_POINT('',(29.9726210990465,2.73613365141461,31.6237706303691));
#72170=CARTESIAN_POINT('Origin',(30.,-1.32966554433622E-14,31.6237706303681));
#72171=CARTESIAN_POINT('',(29.987451017728,2.70302030326666,31.5905494329235));
#72172=CARTESIAN_POINT('Ctrl Pts',(29.9874510177241,2.70302030327525,31.5905494329321));
#72173=CARTESIAN_POINT('Ctrl Pts',(29.9800813460009,2.71947585578017,31.6070390220085));
#72174=CARTESIAN_POINT('Ctrl Pts',(29.9726210990495,2.73613365140797,31.6237706303625));
#72175=CARTESIAN_POINT('Ctrl Pts',(30.,2.69489040503946,31.5823904050395));
#72176=CARTESIAN_POINT('Ctrl Pts',(29.9982996971592,2.69489040503946,31.5823904050395));
#72177=CARTESIAN_POINT('Ctrl Pts',(29.9965490639354,2.69522714758866,31.5827289231894));
#72178=CARTESIAN_POINT('Ctrl Pts',(29.9934248389279,2.69644647069982,31.5839540167345));
#72179=CARTESIAN_POINT('Ctrl Pts',(29.9920523583067,2.69733049287039,31.5848419899159));
#72180=CARTESIAN_POINT('Ctrl Pts',(29.9894391186861,2.6996015700298,31.5871217896387));
#72181=CARTESIAN_POINT('Ctrl Pts',(29.9882404972758,2.70125749446876,31.5887829779419));
#72182=CARTESIAN_POINT('Ctrl Pts',(29.987451017728,2.70302030326666,31.5905494329235));
#72183=CARTESIAN_POINT('',(30.,2.68872936963187,31.5762293696319));
#72184=CARTESIAN_POINT('',(30.,2.68872936963187,31.5762293696319));
#72185=CARTESIAN_POINT('',(30.,-2.68872936963189,31.5762293696319));
#72186=CARTESIAN_POINT('Origin',(30.,-1.32966554433622E-14,31.5762293696319));
#72187=CARTESIAN_POINT('Origin',(30.,-1.32966554433622E-14,31.5762293696319));
#72188=CARTESIAN_POINT('Origin',(30.,-1.32966554433622E-14,31.5430837392638));
#72189=CARTESIAN_POINT('',(30.,-2.67500000000001,31.5430837392638));
#72190=CARTESIAN_POINT('Origin',(30.,-1.32966554433622E-14,31.5430837392638));
#72191=CARTESIAN_POINT('Origin',(30.,-2.72187500000001,31.5430837392638));
#72192=CARTESIAN_POINT('Origin',(30.,-1.32966554433622E-14,16.));
#72193=CARTESIAN_POINT('',(30.,-2.67500000000001,31.06875));
#72194=CARTESIAN_POINT('Origin',(30.,-1.32966554433622E-14,31.06875));
#72195=CARTESIAN_POINT('',(30.,-2.67500000000001,16.));
#72196=CARTESIAN_POINT('Origin',(30.,-1.32966554433622E-14,31.06875));
#72197=CARTESIAN_POINT('',(30.,-2.60625000000001,31.));
#72198=CARTESIAN_POINT('Origin',(30.,-1.32966554433622E-14,31.));
#72199=CARTESIAN_POINT('Origin',(30.,-2.60625000000001,31.06875));
#72200=CARTESIAN_POINT('Origin',(30.,-1.32966554433622E-14,30.85));
#72201=CARTESIAN_POINT('',(30.,-1.65000000000002,31.));
#72202=CARTESIAN_POINT('Origin',(30.,-1.65000000000001,30.85));
#72203=CARTESIAN_POINT('Origin',(30.,-1.32966554433622E-14,31.));
#72204=CARTESIAN_POINT('Origin',(30.,-1.32966554433622E-14,31.6569162607362));
#72205=CARTESIAN_POINT('',(27.4723387620945,1.08324912480478,31.6569162607362));
#72206=CARTESIAN_POINT('Origin',(27.5075595450194,1.04598613791953,31.6570432561871));
#72207=CARTESIAN_POINT('',(27.5347062454699,1.21853465435945,31.6569162607362));
#72208=CARTESIAN_POINT('Origin',(30.,-1.32966554433622E-14,31.6569162607362));
#72209=CARTESIAN_POINT('Origin',(27.5859112932463,1.21595145595199,31.6570220656254));
#72210=CARTESIAN_POINT('Origin',(30.,-1.32966554433622E-14,31.6569162607362));
#72211=CARTESIAN_POINT('',(27.4467007962708,1.0213536000015,31.6569162607362));
#72212=CARTESIAN_POINT('Origin',(27.4979506713832,1.02279586647784,31.6570220656247));
#72213=CARTESIAN_POINT('',(27.3951399513465,0.881591814236737,31.6569162607362));
#72214=CARTESIAN_POINT('Origin',(27.4331757806072,0.847207087483285,31.6570432561871));
#72215=CARTESIAN_POINT('Origin',(30.,-1.32966554433622E-14,31.6569162607362));
#72216=CARTESIAN_POINT('Origin',(30.,-1.32966554433622E-14,31.6569162607362));
#72217=CARTESIAN_POINT('',(27.3744372857209,0.817875561065013,31.6569162607362));
#72218=CARTESIAN_POINT('Origin',(27.4254160156494,0.82333440037271,31.6570220656251));
#72219=CARTESIAN_POINT('',(27.3340009690024,0.674499196974899,31.6569162607362));
#72220=CARTESIAN_POINT('Origin',(27.3746173410621,0.643204723628532,31.6570432561866));
#72221=CARTESIAN_POINT('Origin',(30.,-1.32966554433622E-14,31.6569162607362));
#72222=CARTESIAN_POINT('Origin',(30.,-1.32966554433622E-14,31.6569162607362));
#72223=CARTESIAN_POINT('',(27.3183612423927,0.609355047323335,31.6569162607362));
#72224=CARTESIAN_POINT('Origin',(27.3687545263143,0.61879680390278,31.6570220656251));
#72225=CARTESIAN_POINT('',(27.2892987572189,0.463248067869971,31.6569162607362));
#72226=CARTESIAN_POINT('Origin',(27.3322452586394,0.435236788764015,31.6570432561869));
#72227=CARTESIAN_POINT('Origin',(30.,-1.32966554433622E-14,31.6569162607362));
#72228=CARTESIAN_POINT('Origin',(30.,-1.32966554433622E-14,31.6569162607362));
#72229=CARTESIAN_POINT('',(27.2788183937405,0.397077657083795,31.6569162607362));
#72230=CARTESIAN_POINT('Origin',(27.3283155403022,0.41044411936593,31.6570220656249));
#72231=CARTESIAN_POINT('',(27.2613089199969,0.249140860381007,31.6569162607362));
#72232=CARTESIAN_POINT('Origin',(27.3063207713152,0.224585474366194,31.6570432561871));
#72233=CARTESIAN_POINT('Origin',(30.,-1.32966554433622E-14,31.6569162607362));
#72234=CARTESIAN_POINT('Origin',(30.,-1.32966554433622E-14,31.6569162607362));
#72235=CARTESIAN_POINT('',(27.2560525345756,0.182352151046611,31.6569162607362));
#72236=CARTESIAN_POINT('Origin',(27.3043483774102,0.199560910346922,31.6570220656251));
#72237=CARTESIAN_POINT('',(27.2502040239902,0.0334976166400503,31.6569162607362));
#72238=CARTESIAN_POINT('Origin',(27.2970037121761,0.0125495158363338,31.6570432561875));
#72239=CARTESIAN_POINT('Origin',(30.,-1.32966554433622E-14,31.6569162607362));
#72240=CARTESIAN_POINT('Origin',(30.,-1.32966554433622E-14,31.6569162607362));
#72241=CARTESIAN_POINT('',(27.2502040239902,-0.0334976166400194,31.6569162607362));
#72242=CARTESIAN_POINT('Origin',(27.297000803166,-0.0125526580452972,31.6570220656252));
#72243=CARTESIAN_POINT('',(27.2560525345756,-0.18235215104658,31.6569162607362));
#72244=CARTESIAN_POINT('Origin',(27.3043515239857,-0.199563814630509,31.6570432561868));
#72245=CARTESIAN_POINT('Origin',(30.,-1.32966554433622E-14,31.6569162607362));
#72246=CARTESIAN_POINT('Origin',(30.,-1.32966554433622E-14,31.6569162607362));
#72247=CARTESIAN_POINT('',(27.2613089199969,-0.249140860380976,31.6569162607362));
#72248=CARTESIAN_POINT('Origin',(27.3063181178117,-0.22458883512474,31.6570220656265));
#72249=CARTESIAN_POINT('',(27.2788183937405,-0.397077657083763,31.6569162607362));
#72250=CARTESIAN_POINT('Origin',(27.3283189050458,-0.410446767819208,31.6570432561867));
#72251=CARTESIAN_POINT('Origin',(30.,-1.32966554433622E-14,31.6569162607362));
#72252=CARTESIAN_POINT('Origin',(30.,-1.32966554433622E-14,31.6569162607362));
#72253=CARTESIAN_POINT('',(27.2892987572189,-0.463248067869938,31.6569162607362));
#72254=CARTESIAN_POINT('Origin',(27.3322428769935,-0.4352403473568,31.6570220656245));
#72255=CARTESIAN_POINT('',(27.3183612423927,-0.609355047323306,31.6569162607362));
#72256=CARTESIAN_POINT('Origin',(27.3687580884808,-0.618799180197033,31.6570432561867));
#72257=CARTESIAN_POINT('Origin',(30.,-1.32966554433622E-14,31.6569162607362));
#72258=CARTESIAN_POINT('Origin',(30.,-1.32966554433622E-14,31.6569162607362));
#72259=CARTESIAN_POINT('',(27.3340009690024,-0.674499196974871,31.6569162607362));
#72260=CARTESIAN_POINT('Origin',(27.3746152459701,-0.643208458106799,31.6570220656281));
#72261=CARTESIAN_POINT('',(27.3744372857209,-0.817875561064986,31.6569162607362));
#72262=CARTESIAN_POINT('Origin',(27.4254197532793,-0.823336489857566,31.6570432561877));
#72263=CARTESIAN_POINT('Origin',(30.,-1.32966554433622E-14,31.6569162607362));
#72264=CARTESIAN_POINT('Origin',(30.,-1.32966554433622E-14,31.6569162607362));
#72265=CARTESIAN_POINT('',(27.3951399513465,-0.88159181423671,31.6569162607362));
#72266=CARTESIAN_POINT('Origin',(27.4331739849698,-0.847210974835381,31.6570220656246));
#72267=CARTESIAN_POINT('',(27.4467007962708,-1.02135360000148,31.6569162607362));
#72268=CARTESIAN_POINT('Origin',(27.4979545614299,-1.02279765627042,31.6570432561873));
#72269=CARTESIAN_POINT('Origin',(30.,-1.32966554433622E-14,31.6569162607362));
#72270=CARTESIAN_POINT('Origin',(30.,-1.32966554433622E-14,31.6569162607362));
#72271=CARTESIAN_POINT('',(27.4723387620945,-1.08324912480475,31.6569162607362));
#72272=CARTESIAN_POINT('Origin',(27.5075580599161,-1.04599015417175,31.657022065625));
#72273=CARTESIAN_POINT('',(27.5347062454699,-1.21853465435942,31.6569162607362));
#72274=CARTESIAN_POINT('Origin',(27.5859153117243,-1.21595293501783,31.6570432561869));
#72275=CARTESIAN_POINT('Origin',(30.,-1.32966554433622E-14,31.6569162607362));
#72276=CARTESIAN_POINT('Origin',(30.,-1.32966554433622E-14,31.6569162607362));
#72277=CARTESIAN_POINT('',(27.5651214449068,-1.27822784430149,31.6569162607362));
#72278=CARTESIAN_POINT('Origin',(27.5973088682438,-1.23832045638074,31.6570220656251));
#72279=CARTESIAN_POINT('',(27.637911050459,-1.40820303736935,31.6569162607362));
#72280=CARTESIAN_POINT('Origin',(27.6887596968882,-1.40161145957539,31.6570432561872));
#72281=CARTESIAN_POINT('Origin',(30.,-1.32966554433622E-14,31.6569162607362));
#72282=CARTESIAN_POINT('Origin',(30.,-1.32966554433622E-14,31.6569162607362));
#72283=CARTESIAN_POINT('',(27.6729159636906,-1.46532586408421,31.6569162607362));
#72284=CARTESIAN_POINT('Origin',(27.7018730663766,-1.42301610118967,31.6570220656267));
#72285=CARTESIAN_POINT('',(27.7556789192963,-1.58918938037887,31.6569162607362));
#72286=CARTESIAN_POINT('Origin',(27.8058536470839,-1.57862858340189,31.6570432561867));
#72287=CARTESIAN_POINT('Origin',(30.,-1.32966554433622E-14,31.6569162607362));
#72288=CARTESIAN_POINT('Origin',(30.,-1.32966554433622E-14,31.6569162607362));
#72289=CARTESIAN_POINT('',(27.7950577293922,-1.64338966264456,31.6569162607362));
#72290=CARTESIAN_POINT('Origin',(27.8206059812726,-1.59893837851,31.6570220656387));
#72291=CARTESIAN_POINT('',(27.8872837739086,-1.76037784239926,31.6569162607362));
#72292=CARTESIAN_POINT('Origin',(27.9364752391763,-1.7459129370637,31.6570432561874));
#72293=CARTESIAN_POINT('Origin',(30.,-1.32966554433622E-14,31.6569162607362));
#72294=CARTESIAN_POINT('Origin',(30.,-1.32966554433622E-14,31.6569162607362));
#72295=CARTESIAN_POINT('',(27.9307936974098,-1.81132141745219,31.6569162607362));
#72296=CARTESIAN_POINT('Origin',(27.9527755849842,-1.76500266908356,31.6570220656253));
#72297=CARTESIAN_POINT('',(28.0319142266042,-1.92071298963622,31.6569162607362));
#72298=CARTESIAN_POINT('Origin',(28.0798191476078,-1.90243315689441,31.657043256187));
#72299=CARTESIAN_POINT('Origin',(30.,-1.32966554433622E-14,31.6569162607362));
#72300=CARTESIAN_POINT('Origin',(30.,-1.32966554433622E-14,31.6569162607362));
#72301=CARTESIAN_POINT('',(28.0792870103637,-1.96808577339573,31.6569162607362));
#72302=CARTESIAN_POINT('Origin',(28.097567008002,-1.92018513125043,31.6570220656245));
#72303=CARTESIAN_POINT('',(28.1886785825478,-2.06920630259019,31.6569162607362));
#72304=CARTESIAN_POINT('Origin',(28.2350016095212,-2.0472242436889,31.6570432561873));
#72305=CARTESIAN_POINT('Origin',(30.,-1.32966554433622E-14,31.6569162607362));
#72306=CARTESIAN_POINT('Origin',(30.,-1.32966554433622E-14,31.6569162607362));
#72307=CARTESIAN_POINT('',(28.2396221576007,-2.11271622609136,31.6569162607362));
#72308=CARTESIAN_POINT('Origin',(28.2540875630401,-2.06352901355267,31.6570220656256));
#72309=CARTESIAN_POINT('',(28.3566103373554,-2.20494227060778,31.6569162607362));
#72310=CARTESIAN_POINT('Origin',(28.4010658734316,-2.17939351225073,31.6570432561869));
#72311=CARTESIAN_POINT('Origin',(30.,-1.32966554433622E-14,31.6569162607362));
#72312=CARTESIAN_POINT('Origin',(30.,-1.32966554433622E-14,31.6569162607362));
#72313=CARTESIAN_POINT('',(28.4108106196211,-2.2443210807037,31.6569162607362));
#72314=CARTESIAN_POINT('Origin',(28.4213722488256,-2.19415055329735,31.6570220656249));
#72315=CARTESIAN_POINT('',(28.5346741359157,-2.32708403630936,31.6569162607362));
#72316=CARTESIAN_POINT('Origin',(28.5769880979323,-2.29812609508764,31.6570432561867));
#72317=CARTESIAN_POINT('Origin',(30.,-1.32966554433622E-14,31.6569162607362));
#72318=CARTESIAN_POINT('Origin',(30.,-1.32966554433622E-14,31.6569162607362));
#72319=CARTESIAN_POINT('',(28.5917969626306,-2.362088949541,31.6569162607362));
#72320=CARTESIAN_POINT('Origin',(28.5983896996446,-2.31124442525031,31.6570220656249));
#72321=CARTESIAN_POINT('',(28.7217721556985,-2.43487855509312,31.6569162607362));
#72322=CARTESIAN_POINT('Origin',(28.7616836640096,-2.40268996634326,31.6570432561868));
#72323=CARTESIAN_POINT('Origin',(30.,-1.32966554433622E-14,31.6569162607362));
#72324=CARTESIAN_POINT('Origin',(30.,-1.32966554433622E-14,31.6569162607362));
#72325=CARTESIAN_POINT('',(28.7814653456405,-2.46529375453011,31.6569162607362));
#72326=CARTESIAN_POINT('Origin',(28.784048544048,-2.41408870675338,31.6570220656255));
#72327=CARTESIAN_POINT('',(28.9167508751952,-2.52766123790546,31.6569162607362));
#72328=CARTESIAN_POINT('Origin',(28.9540138620808,-2.49244045498024,31.6570432561872));
#72329=CARTESIAN_POINT('Origin',(30.,-1.32966554433622E-14,31.6569162607362));
#72330=CARTESIAN_POINT('Origin',(30.,-1.32966554433622E-14,31.6569162607362));
#72331=CARTESIAN_POINT('',(28.9786463999985,-2.55329920372917,31.6569162607362));
#72332=CARTESIAN_POINT('Origin',(28.9772041335221,-2.50204932861609,31.657022065625));
#72333=CARTESIAN_POINT('',(29.1184081857632,-2.60486004865345,31.6569162607362));
#72334=CARTESIAN_POINT('Origin',(29.1527929125168,-2.56682421939275,31.6570432561872));
#72335=CARTESIAN_POINT('Origin',(30.,-1.32966554433622E-14,31.6569162607362));
#72336=CARTESIAN_POINT('Origin',(30.,-1.32966554433622E-14,31.6569162607362));
#72337=CARTESIAN_POINT('',(29.182124438935,-2.6255627142791,31.6569162607362));
#72338=CARTESIAN_POINT('Origin',(29.1766655996274,-2.57458398435135,31.6570220656246));
#72339=CARTESIAN_POINT('',(29.3255008030251,-2.66599903099763,31.6569162607362));
#72340=CARTESIAN_POINT('Origin',(29.3567952763715,-2.62538265893786,31.6570432561866));
#72341=CARTESIAN_POINT('Origin',(30.,-1.32966554433622E-14,31.6569162607362));
#72342=CARTESIAN_POINT('Origin',(30.,-1.32966554433622E-14,31.6569162607362));
#72343=CARTESIAN_POINT('',(29.3906449526766,-2.6816387576073,31.6569162607362));
#72344=CARTESIAN_POINT('Origin',(29.3812031960972,-2.63124547368565,31.6570220656251));
#72345=CARTESIAN_POINT('',(29.53675193213,-2.71070124278106,31.6569162607362));
#72346=CARTESIAN_POINT('Origin',(29.5647632112362,-2.66775474136028,31.6570432561871));
#72347=CARTESIAN_POINT('Origin',(30.,-1.32966554433622E-14,31.6569162607362));
#72348=CARTESIAN_POINT('Origin',(30.,-1.32966554433622E-14,31.6569162607362));
#72349=CARTESIAN_POINT('',(29.6029223429162,-2.72118160625948,31.6569162607362));
#72350=CARTESIAN_POINT('Origin',(29.5895558806344,-2.67168445969898,31.6570220656245));
#72351=CARTESIAN_POINT('',(29.750859139619,-2.73869108000313,31.6569162607362));
#72352=CARTESIAN_POINT('Origin',(29.7754145256345,-2.69367922868347,31.6570432561876));
#72353=CARTESIAN_POINT('Origin',(30.,-1.32966554433622E-14,31.6569162607362));
#72354=CARTESIAN_POINT('Origin',(30.,-1.32966554433622E-14,31.6569162607362));
#72355=CARTESIAN_POINT('',(29.8176478489534,-2.74394746542436,31.6569162607362));
#72356=CARTESIAN_POINT('Origin',(29.800439089653,-2.69565162258972,31.6570220656252));
#72357=CARTESIAN_POINT('',(29.9665023833599,-2.74979597600977,31.6569162607362));
#72358=CARTESIAN_POINT('Origin',(29.9874504841626,-2.70299628782621,31.6570432561866));
#72359=CARTESIAN_POINT('Origin',(30.,-1.32966554433622E-14,31.6569162607362));
#72360=CARTESIAN_POINT('Origin',(30.,-1.32966554433622E-14,31.6569162607362));
#72361=CARTESIAN_POINT('',(30.03349761664,-2.74979597600977,31.6569162607362));
#72362=CARTESIAN_POINT('Origin',(30.0125526580435,-2.70299919683014,31.6570220656269));
#72363=CARTESIAN_POINT('',(30.1823521510466,-2.74394746542436,31.6569162607362));
#72364=CARTESIAN_POINT('Origin',(30.1995638146306,-2.69564847601399,31.6570432561868));
#72365=CARTESIAN_POINT('Origin',(30.,-1.32966554433622E-14,31.6569162607362));
#72366=CARTESIAN_POINT('Origin',(30.,-1.32966554433622E-14,31.6569162607362));
#72367=CARTESIAN_POINT('',(30.2491408603809,-2.73869108000313,31.6569162607362));
#72368=CARTESIAN_POINT('Origin',(30.2245888351274,-2.69368188219317,31.6570220656245));
#72369=CARTESIAN_POINT('',(30.3970776570837,-2.72118160625948,31.6569162607362));
#72370=CARTESIAN_POINT('Origin',(30.4104467678196,-2.67168109495285,31.6570432561872));
#72371=CARTESIAN_POINT('Origin',(30.,-1.32966554433622E-14,31.6569162607362));
#72372=CARTESIAN_POINT('Origin',(30.,-1.32966554433622E-14,31.6569162607362));
#72373=CARTESIAN_POINT('',(30.4632480678699,-2.71070124278107,31.6569162607362));
#72374=CARTESIAN_POINT('Origin',(30.4352403473562,-2.66775712300563,31.6570220656249));
#72375=CARTESIAN_POINT('',(30.6093550473233,-2.68163875760731,31.6569162607362));
#72376=CARTESIAN_POINT('Origin',(30.6187991801974,-2.63124191151731,31.6570432561874));
#72377=CARTESIAN_POINT('Origin',(30.,-1.32966554433622E-14,31.6569162607362));
#72378=CARTESIAN_POINT('Origin',(30.,-1.32966554433622E-14,31.6569162607362));
#72379=CARTESIAN_POINT('',(30.6744991969748,-2.66599903099764,31.6569162607362));
#72380=CARTESIAN_POINT('Origin',(30.6432084581108,-2.62538475403506,31.6570220656255));
#72381=CARTESIAN_POINT('',(30.817875561065,-2.62556271427912,31.6569162607362));
#72382=CARTESIAN_POINT('Origin',(30.8233364898573,-2.57458024672293,31.6570432561868));
#72383=CARTESIAN_POINT('Origin',(30.,-1.32966554433622E-14,31.6569162607362));
#72384=CARTESIAN_POINT('Origin',(30.,-1.32966554433622E-14,31.6569162607362));
#72385=CARTESIAN_POINT('',(30.8815918142367,-2.60486004865346,31.6569162607362));
#72386=CARTESIAN_POINT('Origin',(30.8472109748348,-2.56682601502956,31.6570220656249));
#72387=CARTESIAN_POINT('',(31.0213536000014,-2.55329920372919,31.6569162607362));
#72388=CARTESIAN_POINT('Origin',(31.0227976562703,-2.50204543857134,31.6570432561867));
#72389=CARTESIAN_POINT('Origin',(30.,-1.32966554433622E-14,31.6569162607362));
#72390=CARTESIAN_POINT('Origin',(30.,-1.32966554433622E-14,31.6569162607362));
#72391=CARTESIAN_POINT('',(31.0832491248047,-2.52766123790547,31.6569162607362));
#72392=CARTESIAN_POINT('Origin',(31.0459901541642,-2.49244194007693,31.6570220656289));
#72393=CARTESIAN_POINT('',(31.2185346543594,-2.46529375453013,31.6569162607362));
#72394=CARTESIAN_POINT('Origin',(31.2159529350178,-2.41408468827489,31.6570432561872));
#72395=CARTESIAN_POINT('Origin',(30.,-1.32966554433622E-14,31.6569162607362));
#72396=CARTESIAN_POINT('Origin',(30.,-1.32966554433622E-14,31.6569162607362));
#72397=CARTESIAN_POINT('',(31.2782278443015,-2.43487855509314,31.6569162607362));
#72398=CARTESIAN_POINT('Origin',(31.238320456382,-2.40269113175716,31.6570220656245));
#72399=CARTESIAN_POINT('',(31.4082030373693,-2.36208894954102,31.6569162607362));
#72400=CARTESIAN_POINT('Origin',(31.4016114595753,-2.31124030311134,31.6570432561875));
#72401=CARTESIAN_POINT('Origin',(30.,-1.32966554433622E-14,31.6569162607362));
#72402=CARTESIAN_POINT('Origin',(30.,-1.32966554433622E-14,31.6569162607362));
#72403=CARTESIAN_POINT('',(31.4653258640842,-2.32708403630938,31.6569162607362));
#72404=CARTESIAN_POINT('Origin',(31.4230161011935,-2.29812693362589,31.657022065625));
#72405=CARTESIAN_POINT('',(31.5891893803788,-2.24432108070372,31.6569162607362));
#72406=CARTESIAN_POINT('Origin',(31.5786285834021,-2.1941463529175,31.6570432561862));
#72407=CARTESIAN_POINT('Origin',(30.,-1.32966554433622E-14,31.6569162607362));
#72408=CARTESIAN_POINT('Origin',(30.,-1.32966554433622E-14,31.6569162607362));
#72409=CARTESIAN_POINT('',(31.6433896626445,-2.2049422706078,31.6569162607362));
#72410=CARTESIAN_POINT('Origin',(31.5989383785409,-2.17939401874466,31.6570220656252));
#72411=CARTESIAN_POINT('',(31.7603778423992,-2.11271622609138,31.6569162607362));
#72412=CARTESIAN_POINT('Origin',(31.7459129370641,-2.0635247608251,31.6570432561869));
#72413=CARTESIAN_POINT('Origin',(30.,-1.32966554433622E-14,31.6569162607362));
#72414=CARTESIAN_POINT('Origin',(30.,-1.32966554433622E-14,31.6569162607362));
#72415=CARTESIAN_POINT('',(31.8113214174522,-2.06920630259022,31.6569162607362));
#72416=CARTESIAN_POINT('Origin',(31.7650026690826,-2.04722441501533,31.6570220656257));
#72417=CARTESIAN_POINT('',(31.9207129896362,-1.96808577339576,31.6569162607362));
#72418=CARTESIAN_POINT('Origin',(31.9024331568943,-1.92018085239205,31.657043256187));
#72419=CARTESIAN_POINT('Origin',(30.,-1.32966554433622E-14,31.6569162607362));
#72420=CARTESIAN_POINT('Origin',(30.,-1.32966554433622E-14,31.6569162607362));
#72421=CARTESIAN_POINT('',(31.9680857733957,-1.92071298963625,31.6569162607362));
#72422=CARTESIAN_POINT('Origin',(31.9201851312437,-1.90243299199549,31.6570220656273));
#72423=CARTESIAN_POINT('',(32.0692063025902,-1.81132141745222,31.6569162607362));
#72424=CARTESIAN_POINT('Origin',(32.0472242436891,-1.76499839047944,31.6570432561871));
#72425=CARTESIAN_POINT('Origin',(30.,-1.32966554433622E-14,31.6569162607362));
#72426=CARTESIAN_POINT('Origin',(30.,-1.32966554433622E-14,31.6569162607362));
#72427=CARTESIAN_POINT('',(32.1127162260913,-1.76037784239929,31.6569162607362));
#72428=CARTESIAN_POINT('Origin',(32.0635290135546,-1.74591243696045,31.6570220656248));
#72429=CARTESIAN_POINT('',(32.2049422706077,-1.64338966264459,31.6569162607362));
#72430=CARTESIAN_POINT('Origin',(32.1793935122505,-1.59893412656801,31.6570432561871));
#72431=CARTESIAN_POINT('Origin',(30.,-1.32966554433622E-14,31.6569162607362));
#72432=CARTESIAN_POINT('Origin',(30.,-1.32966554433622E-14,31.6569162607362));
#72433=CARTESIAN_POINT('',(32.2443210807037,-1.5891893803789,31.6569162607362));
#72434=CARTESIAN_POINT('Origin',(32.1941505532956,-1.57862775117404,31.6570220656256));
#72435=CARTESIAN_POINT('',(32.3270840363093,-1.46532586408424,31.6569162607362));
#72436=CARTESIAN_POINT('Origin',(32.2981260950875,-1.42301190206755,31.6570432561867));
#72437=CARTESIAN_POINT('Origin',(30.,-1.32966554433622E-14,31.6569162607362));
#72438=CARTESIAN_POINT('Origin',(30.,-1.32966554433622E-14,31.6569162607362));
#72439=CARTESIAN_POINT('',(32.362088949541,-1.40820303736938,31.6569162607362));
#72440=CARTESIAN_POINT('Origin',(32.3112444252322,-1.40161030035328,31.657022065632));
#72441=CARTESIAN_POINT('',(32.4348785550931,-1.27822784430152,31.6569162607362));
#72442=CARTESIAN_POINT('Origin',(32.4026899663432,-1.23831633599041,31.6570432561868));
#72443=CARTESIAN_POINT('Origin',(30.,-1.32966554433622E-14,31.6569162607362));
#72444=CARTESIAN_POINT('Origin',(30.,-1.32966554433622E-14,31.6569162607362));
#72445=CARTESIAN_POINT('',(32.4652937545301,-1.21853465435946,31.6569162607362));
#72446=CARTESIAN_POINT('Origin',(32.414088706754,-1.21595145595202,31.6570220656252));
#72447=CARTESIAN_POINT('',(32.5276612379054,-1.08324912480479,31.6569162607362));
#72448=CARTESIAN_POINT('Origin',(32.4924404549811,-1.04598613792014,31.6570432561868));
#72449=CARTESIAN_POINT('Origin',(30.,-1.32966554433622E-14,31.6569162607362));
#72450=CARTESIAN_POINT('Origin',(30.,-1.32966554433622E-14,31.6569162607362));
#72451=CARTESIAN_POINT('',(32.5532992037291,-1.02135360000151,31.6569162607362));
#72452=CARTESIAN_POINT('Origin',(32.5020493286151,-1.0227958664779,31.6570220656254));
#72453=CARTESIAN_POINT('',(32.6048600486534,-0.881591814236746,31.6569162607362));
#72454=CARTESIAN_POINT('Origin',(32.5668242193914,-0.847207087482045,31.6570432561878));
#72455=CARTESIAN_POINT('Origin',(30.,-1.32966554433622E-14,31.6569162607362));
#72456=CARTESIAN_POINT('Origin',(30.,-1.32966554433622E-14,31.6569162607362));
#72457=CARTESIAN_POINT('',(32.6255627142791,-0.817875561065022,31.6569162607362));
#72458=CARTESIAN_POINT('Origin',(32.5745839843496,-0.82333440037284,31.6570220656255));
#72459=CARTESIAN_POINT('',(32.6659990309976,-0.674499196974908,31.6569162607362));
#72460=CARTESIAN_POINT('Origin',(32.6253826589374,-0.643204723628158,31.6570432561868));
#72461=CARTESIAN_POINT('Origin',(30.,-1.32966554433622E-14,31.6569162607362));
#72462=CARTESIAN_POINT('Origin',(30.,-1.32966554433622E-14,31.6569162607362));
#72463=CARTESIAN_POINT('',(32.6816387576073,-0.609355047323343,31.6569162607362));
#72464=CARTESIAN_POINT('Origin',(32.6312454736857,-0.618796803902764,31.657022065625));
#72465=CARTESIAN_POINT('',(32.710701242781,-0.463248067869977,31.6569162607362));
#72466=CARTESIAN_POINT('Origin',(32.6677547413593,-0.435236788763208,31.6570432561875));
#72467=CARTESIAN_POINT('Origin',(30.,-1.32966554433622E-14,31.6569162607362));
#72468=CARTESIAN_POINT('Origin',(30.,-1.32966554433622E-14,31.6569162607362));
#72469=CARTESIAN_POINT('',(32.7211816062594,-0.397077657083801,31.6569162607362));
#72470=CARTESIAN_POINT('Origin',(32.6716844596186,-0.410444119388296,31.6570220656567));
#72471=CARTESIAN_POINT('',(32.7386910800031,-0.249140860381013,31.6569162607362));
#72472=CARTESIAN_POINT('Origin',(32.6936792286845,-0.224585474366052,31.6570432561872));
#72473=CARTESIAN_POINT('Origin',(30.,-1.32966554433622E-14,31.6569162607362));
#72474=CARTESIAN_POINT('Origin',(30.,-1.32966554433622E-14,31.6569162607362));
#72475=CARTESIAN_POINT('',(32.7439474654243,-0.182352151046618,31.6569162607362));
#72476=CARTESIAN_POINT('Origin',(32.695651622591,-0.19956091034649,31.6570220656247));
#72477=CARTESIAN_POINT('',(32.7497959760097,-0.0334976166400576,31.6569162607362));
#72478=CARTESIAN_POINT('Origin',(32.702996287825,-0.0125495158368562,31.657043256187));
#72479=CARTESIAN_POINT('Origin',(30.,-1.32966554433622E-14,31.6569162607362));
#72480=CARTESIAN_POINT('Origin',(30.,-1.32966554433622E-14,31.6569162607362));
#72481=CARTESIAN_POINT('',(32.7497959760097,0.0334976166400122,31.6569162607362));
#72482=CARTESIAN_POINT('Origin',(32.7029991968315,0.0125526580441019,31.6570220656263));
#72483=CARTESIAN_POINT('',(32.7439474654243,0.182352151046572,31.6569162607362));
#72484=CARTESIAN_POINT('Origin',(32.695648476013,0.199563814630937,31.6570432561873));
#72485=CARTESIAN_POINT('Origin',(30.,-1.32966554433622E-14,31.6569162607362));
#72486=CARTESIAN_POINT('Origin',(30.,-1.32966554433622E-14,31.6569162607362));
#72487=CARTESIAN_POINT('',(32.7386910800031,0.249140860380968,31.6569162607362));
#72488=CARTESIAN_POINT('Origin',(32.6936818821912,0.224588835126342,31.6570220656253));
#72489=CARTESIAN_POINT('',(32.7211816062594,0.397077657083756,31.6569162607362));
#72490=CARTESIAN_POINT('Origin',(32.6716810949533,0.410446767819417,31.657043256187));
#72491=CARTESIAN_POINT('Origin',(30.,-1.32966554433622E-14,31.6569162607362));
#72492=CARTESIAN_POINT('Origin',(30.,-1.32966554433622E-14,31.6569162607362));
#72493=CARTESIAN_POINT('',(32.710701242781,0.463248067869931,31.6569162607362));
#72494=CARTESIAN_POINT('Origin',(32.6677571230054,0.435240347356078,31.6570220656249));
#72495=CARTESIAN_POINT('',(32.6816387576073,0.609355047323298,31.6569162607362));
#72496=CARTESIAN_POINT('Origin',(32.6312419115184,0.618799180197174,31.657043256187));
#72497=CARTESIAN_POINT('Origin',(30.,-1.32966554433622E-14,31.6569162607362));
#72498=CARTESIAN_POINT('Origin',(30.,-1.32966554433622E-14,31.6569162607362));
#72499=CARTESIAN_POINT('',(32.6659990309976,0.674499196974863,31.6569162607362));
#72500=CARTESIAN_POINT('Origin',(32.6253847539863,0.643208458072405,31.6570220656495));
#72501=CARTESIAN_POINT('',(32.6255627142791,0.817875561064977,31.6569162607362));
#72502=CARTESIAN_POINT('Origin',(32.574580246722,0.823336489857403,31.6570432561872));
#72503=CARTESIAN_POINT('Origin',(30.,-1.32966554433622E-14,31.6569162607362));
#72504=CARTESIAN_POINT('Origin',(30.,-1.32966554433622E-14,31.6569162607362));
#72505=CARTESIAN_POINT('',(32.6048600486534,0.881591814236701,31.6569162607362));
#72506=CARTESIAN_POINT('Origin',(32.5668260150295,0.847210974834854,31.6570220656249));
#72507=CARTESIAN_POINT('',(32.5532992037291,1.02135360000147,31.6569162607362));
#72508=CARTESIAN_POINT('Origin',(32.5020454385711,1.02279765627039,31.6570432561869));
#72509=CARTESIAN_POINT('Origin',(30.,-1.32966554433622E-14,31.6569162607362));
#72510=CARTESIAN_POINT('Origin',(30.,-1.32966554433622E-14,31.6569162607362));
#72511=CARTESIAN_POINT('',(32.5276612379054,1.08324912480474,31.6569162607362));
#72512=CARTESIAN_POINT('Origin',(32.4924419400839,1.04599015417185,31.6570220656248));
#72513=CARTESIAN_POINT('',(32.4652937545301,1.21853465435941,31.6569162607362));
#72514=CARTESIAN_POINT('Origin',(32.4140846882753,1.2159529350178,31.657043256187));
#72515=CARTESIAN_POINT('Origin',(30.,-1.32966554433622E-14,31.6569162607362));
#72516=CARTESIAN_POINT('Origin',(30.,-1.32966554433622E-14,31.6569162607362));
#72517=CARTESIAN_POINT('',(32.4348785550931,1.27822784430148,31.6569162607362));
#72518=CARTESIAN_POINT('Origin',(32.4026911317566,1.23832045638126,31.6570220656248));
#72519=CARTESIAN_POINT('',(32.362088949541,1.40820303736934,31.6569162607362));
#72520=CARTESIAN_POINT('Origin',(32.3112403031114,1.40161145957535,31.6570432561874));
#72521=CARTESIAN_POINT('Origin',(30.,-1.32966554433622E-14,31.6569162607362));
#72522=CARTESIAN_POINT('Origin',(30.,-1.32966554433622E-14,31.6569162607362));
#72523=CARTESIAN_POINT('',(32.3270840363093,1.4653258640842,31.6569162607362));
#72524=CARTESIAN_POINT('Origin',(32.2981269336259,1.42301610119356,31.657022065625));
#72525=CARTESIAN_POINT('',(32.2443210807037,1.58918938037886,31.6569162607362));
#72526=CARTESIAN_POINT('Origin',(32.1941463529162,1.57862858340189,31.6570432561866));
#72527=CARTESIAN_POINT('Origin',(30.,-1.32966554433622E-14,31.6569162607362));
#72528=CARTESIAN_POINT('Origin',(30.,-1.32966554433622E-14,31.6569162607362));
#72529=CARTESIAN_POINT('',(32.2049422706078,1.64338966264455,31.6569162607362));
#72530=CARTESIAN_POINT('Origin',(32.1793940187453,1.59893837854221,31.6570220656245));
#72531=CARTESIAN_POINT('',(32.1127162260913,1.76037784239925,31.6569162607362));
#72532=CARTESIAN_POINT('Origin',(32.0635247608241,1.74591293706383,31.6570432561872));
#72533=CARTESIAN_POINT('Origin',(30.,-1.32966554433622E-14,31.6569162607362));
#72534=CARTESIAN_POINT('Origin',(30.,-1.32966554433622E-14,31.6569162607362));
#72535=CARTESIAN_POINT('',(32.0692063025902,1.81132141745218,31.6569162607362));
#72536=CARTESIAN_POINT('Origin',(32.0472244150162,1.76500266908448,31.6570220656248));
#72537=CARTESIAN_POINT('',(31.9680857733957,1.92071298963621,31.6569162607362));
#72538=CARTESIAN_POINT('Origin',(31.9201808523931,1.90243315689474,31.6570432561866));
#72539=CARTESIAN_POINT('Origin',(30.,-1.32966554433622E-14,31.6569162607362));
#72540=CARTESIAN_POINT('Origin',(30.,-1.32966554433622E-14,31.6569162607362));
#72541=CARTESIAN_POINT('',(31.9207129896362,1.96808577339572,31.6569162607362));
#72542=CARTESIAN_POINT('Origin',(31.9024329919958,1.92018513124459,31.657022065627));
#72543=CARTESIAN_POINT('',(31.8113214174522,2.06920630259018,31.6569162607362));
#72544=CARTESIAN_POINT('Origin',(31.7649983904793,2.04722424368911,31.6570432561871));
#72545=CARTESIAN_POINT('Origin',(30.,-1.32966554433622E-14,31.6569162607362));
#72546=CARTESIAN_POINT('Origin',(30.,-1.32966554433622E-14,31.6569162607362));
#72547=CARTESIAN_POINT('',(31.7603778423992,2.11271622609134,31.6569162607362));
#72548=CARTESIAN_POINT('Origin',(31.7459124369604,2.06352901355459,31.6570220656248));
#72549=CARTESIAN_POINT('',(31.6433896626445,2.20494227060776,31.6569162607362));
#72550=CARTESIAN_POINT('Origin',(31.5989341265682,2.17939351225069,31.657043256187));
#72551=CARTESIAN_POINT('Origin',(30.,-1.32966554433622E-14,31.6569162607362));
#72552=CARTESIAN_POINT('Origin',(30.,-1.32966554433622E-14,31.6569162607362));
#72553=CARTESIAN_POINT('',(31.5891893803789,2.24432108070368,31.6569162607362));
#72554=CARTESIAN_POINT('Origin',(31.5786277511742,2.19415055329685,31.6570220656251));
#72555=CARTESIAN_POINT('',(31.4653258640842,2.32708403630934,31.6569162607362));
#72556=CARTESIAN_POINT('Origin',(31.4230119020666,2.29812609508688,31.6570432561872));
#72557=CARTESIAN_POINT('Origin',(30.,-1.32966554433622E-14,31.6569162607362));
#72558=CARTESIAN_POINT('Origin',(30.,-1.32966554433622E-14,31.6569162607362));
#72559=CARTESIAN_POINT('',(31.4082030373693,2.36208894954099,31.6569162607362));
#72560=CARTESIAN_POINT('Origin',(31.4016103003533,2.31124442523252,31.6570220656319));
#72561=CARTESIAN_POINT('',(31.2782278443015,2.4348785550931,31.6569162607362));
#72562=CARTESIAN_POINT('Origin',(31.2383163359906,2.4026899663434,31.6570432561867));
#72563=CARTESIAN_POINT('Origin',(30.,-1.32966554433622E-14,31.6569162607362));
#72564=CARTESIAN_POINT('Origin',(30.,-1.32966554433622E-14,31.6569162607362));
#72565=CARTESIAN_POINT('',(31.2185346543594,2.46529375453009,31.6569162607362));
#72566=CARTESIAN_POINT('Origin',(31.215951455952,2.4140887067551,31.6570220656248));
#72567=CARTESIAN_POINT('',(31.0832491248047,2.52766123790544,31.6569162607362));
#72568=CARTESIAN_POINT('Origin',(31.045986137919,2.49244045498011,31.6570432561873));
#72569=CARTESIAN_POINT('Origin',(30.,-1.32966554433622E-14,31.6569162607362));
#72570=CARTESIAN_POINT('Origin',(30.,-1.32966554433622E-14,31.6569162607362));
#72571=CARTESIAN_POINT('',(31.0213536000015,2.55329920372915,31.6569162607362));
#72572=CARTESIAN_POINT('Origin',(31.0227958664779,2.50204932861496,31.6570220656254));
#72573=CARTESIAN_POINT('',(30.8815918142367,2.60486004865343,31.6569162607362));
#72574=CARTESIAN_POINT('Origin',(30.8472070874836,2.56682421939316,31.6570432561869));
#72575=CARTESIAN_POINT('Origin',(30.,-1.32966554433622E-14,31.6569162607362));
#72576=CARTESIAN_POINT('Origin',(30.,-1.32966554433622E-14,31.6569162607362));
#72577=CARTESIAN_POINT('',(30.817875561065,2.62556271427908,31.6569162607362));
#72578=CARTESIAN_POINT('Origin',(30.8233344003728,2.5745839843498,31.6570220656254));
#72579=CARTESIAN_POINT('',(30.6744991969749,2.6659990309976,31.6569162607362));
#72580=CARTESIAN_POINT('Origin',(30.6432047236281,2.62538265893739,31.6570432561868));
#72581=CARTESIAN_POINT('Origin',(30.,-1.32966554433622E-14,31.6569162607362));
#72582=CARTESIAN_POINT('Origin',(30.,-1.32966554433622E-14,31.6569162607362));
#72583=CARTESIAN_POINT('',(30.6093550473233,2.68163875760728,31.6569162607362));
#72584=CARTESIAN_POINT('Origin',(30.6187968039028,2.63124547368537,31.6570220656252));
#72585=CARTESIAN_POINT('',(30.4632480678699,2.71070124278104,31.6569162607362));
#72586=CARTESIAN_POINT('Origin',(30.4352367887645,2.66775474136143,31.6570432561865));
#72587=CARTESIAN_POINT('Origin',(30.,-1.32966554433622E-14,31.6569162607362));
#72588=CARTESIAN_POINT('Origin',(30.,-1.32966554433622E-14,31.6569162607362));
#72589=CARTESIAN_POINT('',(27.5651214449069,1.27822784430151,31.6569162607362));
#72590=CARTESIAN_POINT('Origin',(27.5973100336575,1.23831633598946,31.6570432561873));
#72591=CARTESIAN_POINT('',(27.637911050459,1.40820303736937,31.6569162607362));
#72592=CARTESIAN_POINT('Origin',(30.,-1.32966554433622E-14,31.6569162607362));
#72593=CARTESIAN_POINT('Origin',(27.6887555747495,1.40161030035545,31.6570220656248));
#72594=CARTESIAN_POINT('Origin',(30.,-1.32966554433622E-14,31.6569162607362));
#72595=CARTESIAN_POINT('',(27.6729159636906,1.46532586408423,31.6569162607362));
#72596=CARTESIAN_POINT('Origin',(27.7018739049127,1.42301190206727,31.6570432561868));
#72597=CARTESIAN_POINT('',(27.7556789192963,1.58918938037889,31.6569162607362));
#72598=CARTESIAN_POINT('Origin',(30.,-1.32966554433622E-14,31.6569162607362));
#72599=CARTESIAN_POINT('Origin',(27.805849446702,1.5786277511745,31.6570220656247));
#72600=CARTESIAN_POINT('Origin',(30.,-1.32966554433622E-14,31.6569162607362));
#72601=CARTESIAN_POINT('',(27.7950577293922,1.64338966264458,31.6569162607362));
#72602=CARTESIAN_POINT('Origin',(27.8206064877494,1.59893412656804,31.6570432561871));
#72603=CARTESIAN_POINT('',(27.8872837739086,1.76037784239928,31.6569162607362));
#72604=CARTESIAN_POINT('Origin',(30.,-1.32966554433622E-14,31.6569162607362));
#72605=CARTESIAN_POINT('Origin',(27.936470986445,1.74591243696058,31.6570220656246));
#72606=CARTESIAN_POINT('Origin',(30.,-1.32966554433622E-14,31.6569162607362));
#72607=CARTESIAN_POINT('',(27.9307936974098,1.81132141745221,31.6569162607362));
#72608=CARTESIAN_POINT('Origin',(27.9527757563104,1.76499839048029,31.6570432561867));
#72609=CARTESIAN_POINT('',(28.0319142266043,1.92071298963623,31.6569162607362));
#72610=CARTESIAN_POINT('Origin',(30.,-1.32966554433622E-14,31.6569162607362));
#72611=CARTESIAN_POINT('Origin',(28.0798148687497,1.90243299199796,31.6570220656246));
#72612=CARTESIAN_POINT('Origin',(30.,-1.32966554433622E-14,31.6569162607362));
#72613=CARTESIAN_POINT('',(28.0792870103638,1.96808577339574,31.6569162607362));
#72614=CARTESIAN_POINT('Origin',(28.0975668431059,1.92018085239124,31.6570432561874));
#72615=CARTESIAN_POINT('',(28.1886785825478,2.0692063025902,31.6569162607362));
#72616=CARTESIAN_POINT('Origin',(30.,-1.32966554433622E-14,31.6569162607362));
#72617=CARTESIAN_POINT('Origin',(28.2349973309159,2.04722441501599,31.657022065625));
#72618=CARTESIAN_POINT('Origin',(30.,-1.32966554433622E-14,31.6569162607362));
#72619=CARTESIAN_POINT('',(28.2396221576007,2.11271622609137,31.6569162607362));
#72620=CARTESIAN_POINT('Origin',(28.2540870629359,2.06352476082518,31.6570432561869));
#72621=CARTESIAN_POINT('',(28.3566103373554,2.20494227060779,31.6569162607362));
#72622=CARTESIAN_POINT('Origin',(30.,-1.32966554433622E-14,31.6569162607362));
#72623=CARTESIAN_POINT('Origin',(28.4010616214895,2.17939401872761,31.6570220656385));
#72624=CARTESIAN_POINT('Origin',(30.,-1.32966554433622E-14,31.6569162607362));
#72625=CARTESIAN_POINT('',(28.4108106196211,2.2443210807037,31.6569162607362));
#72626=CARTESIAN_POINT('Origin',(28.4213714165984,2.19414635291463,31.6570432561873));
#72627=CARTESIAN_POINT('',(28.5346741359158,2.32708403630936,31.6569162607362));
#72628=CARTESIAN_POINT('Origin',(30.,-1.32966554433622E-14,31.6569162607362));
#72629=CARTESIAN_POINT('Origin',(28.5769838988101,2.29812693362349,31.6570220656266));
#72630=CARTESIAN_POINT('Origin',(30.,-1.32966554433622E-14,31.6569162607362));
#72631=CARTESIAN_POINT('',(28.5917969626306,2.36208894954101,31.6569162607362));
#72632=CARTESIAN_POINT('Origin',(28.5983885404246,2.31124030311217,31.6570432561871));
#72633=CARTESIAN_POINT('',(28.7217721556985,2.43487855509312,31.6569162607362));
#72634=CARTESIAN_POINT('Origin',(30.,-1.32966554433622E-14,31.6569162607362));
#72635=CARTESIAN_POINT('Origin',(28.7616795436181,2.40269113175706,31.6570220656245));
#72636=CARTESIAN_POINT('Origin',(30.,-1.32966554433622E-14,31.6569162607362));
#72637=CARTESIAN_POINT('',(28.7814653456406,2.46529375453011,31.6569162607362));
#72638=CARTESIAN_POINT('Origin',(28.7840470649822,2.41408468827519,31.6570432561871));
#72639=CARTESIAN_POINT('',(28.9167508751953,2.52766123790545,31.6569162607362));
#72640=CARTESIAN_POINT('Origin',(30.,-1.32966554433622E-14,31.6569162607362));
#72641=CARTESIAN_POINT('Origin',(28.9540098458282,2.49244194008388,31.6570220656249));
#72642=CARTESIAN_POINT('Origin',(30.,-1.32966554433622E-14,31.6569162607362));
#72643=CARTESIAN_POINT('',(28.9786463999985,2.55329920372917,31.6569162607362));
#72644=CARTESIAN_POINT('Origin',(28.9772023437296,2.50204543857058,31.657043256187));
#72645=CARTESIAN_POINT('',(29.1184081857633,2.60486004865344,31.6569162607362));
#72646=CARTESIAN_POINT('Origin',(30.,-1.32966554433622E-14,31.6569162607362));
#72647=CARTESIAN_POINT('Origin',(29.1527890251647,2.56682601503002,31.6570220656247));
#72648=CARTESIAN_POINT('Origin',(30.,-1.32966554433622E-14,31.6569162607362));
#72649=CARTESIAN_POINT('',(29.182124438935,2.62556271427909,31.6569162607362));
#72650=CARTESIAN_POINT('Origin',(29.1766635101426,2.57458024672254,31.657043256187));
#72651=CARTESIAN_POINT('',(29.3255008030251,2.66599903099761,31.6569162607362));
#72652=CARTESIAN_POINT('Origin',(30.,-1.32966554433622E-14,31.6569162607362));
#72653=CARTESIAN_POINT('Origin',(29.356791541893,2.62538475403008,31.657022065628));
#72654=CARTESIAN_POINT('Origin',(30.,-1.32966554433622E-14,31.6569162607362));
#72655=CARTESIAN_POINT('',(29.3906449526767,2.68163875760729,31.6569162607362));
#72656=CARTESIAN_POINT('Origin',(29.3812008198028,2.6312419115181,31.6570432561872));
#72657=CARTESIAN_POINT('',(29.5367519321301,2.71070124278105,31.6569162607362));
#72658=CARTESIAN_POINT('Origin',(30.,-1.32966554433622E-14,31.6569162607362));
#72659=CARTESIAN_POINT('Origin',(29.5647596526443,2.66775712300484,31.6570220656252));
#72660=CARTESIAN_POINT('Origin',(30.,-1.32966554433622E-14,31.6569162607362));
#72661=CARTESIAN_POINT('',(29.6029223429162,2.72118160625946,31.6569162607362));
#72662=CARTESIAN_POINT('Origin',(29.5895532321803,2.67168109495224,31.6570432561874));
#72663=CARTESIAN_POINT('',(29.750859139619,2.7386910800031,31.6569162607362));
#72664=CARTESIAN_POINT('Origin',(30.,-1.32966554433622E-14,31.6569162607362));
#72665=CARTESIAN_POINT('Origin',(29.7754111648735,2.69368188219135,31.6570220656252));
#72666=CARTESIAN_POINT('Origin',(30.,-1.32966554433622E-14,31.6569162607362));
#72667=CARTESIAN_POINT('',(29.8176478489534,2.74394746542433,31.6569162607362));
#72668=CARTESIAN_POINT('Origin',(29.8004361853695,2.6956484760142,31.6570432561868));
#72669=CARTESIAN_POINT('',(29.9665023833599,2.74979597600974,31.6569162607362));
#72670=CARTESIAN_POINT('Origin',(30.,-1.32966554433622E-14,31.6569162607362));
#72671=CARTESIAN_POINT('Origin',(29.9874473419551,2.70299919683309,31.6570220656256));
#72672=CARTESIAN_POINT('Origin',(30.,-1.32966554433622E-14,31.6569162607362));
#72673=CARTESIAN_POINT('',(30.3970776570838,2.72118160625945,31.6569162607362));
#72674=CARTESIAN_POINT('Origin',(30.4104441193885,2.67168445961759,31.6570220656571));
#72675=CARTESIAN_POINT('',(30.249140860381,2.7386910800031,31.6569162607362));
#72676=CARTESIAN_POINT('Origin',(30.2245854743662,2.69367922868485,31.657043256187));
#72677=CARTESIAN_POINT('Origin',(30.,-1.32966554433622E-14,31.6569162607362));
#72678=CARTESIAN_POINT('Origin',(30.,-1.32966554433622E-14,16.));
#72679=CARTESIAN_POINT('',(27.4723387620945,1.08324912480478,33.8305837392638));
#72680=CARTESIAN_POINT('',(27.4723387620945,1.08324912480478,16.));
#72681=CARTESIAN_POINT('',(27.5347062454699,1.21853465435945,33.8305837392638));
#72682=CARTESIAN_POINT('Origin',(30.,-1.32966554433622E-14,33.8305837392638));
#72683=CARTESIAN_POINT('',(27.5347062454699,1.21853465435945,16.));
#72684=CARTESIAN_POINT('Origin',(30.,-1.32966554433622E-14,16.));
#72685=CARTESIAN_POINT('',(27.4467007962708,1.0213536000015,33.8305837392638));
#72686=CARTESIAN_POINT('',(27.4467007962708,1.0213536000015,16.));
#72687=CARTESIAN_POINT('',(27.3951399513465,0.881591814236741,33.8305837392638));
#72688=CARTESIAN_POINT('',(27.3951399513465,0.881591814236737,16.));
#72689=CARTESIAN_POINT('Origin',(30.,-1.32966554433622E-14,33.8305837392638));
#72690=CARTESIAN_POINT('Origin',(30.,-1.32966554433622E-14,16.));
#72691=CARTESIAN_POINT('',(27.3744372857209,0.817875561065013,33.8305837392638));
#72692=CARTESIAN_POINT('',(27.3744372857209,0.817875561065013,16.));
#72693=CARTESIAN_POINT('',(27.3340009690024,0.674499196974903,33.8305837392638));
#72694=CARTESIAN_POINT('',(27.3340009690024,0.674499196974899,16.));
#72695=CARTESIAN_POINT('Origin',(30.,-1.32966554433622E-14,33.8305837392638));
#72696=CARTESIAN_POINT('Origin',(30.,-1.32966554433622E-14,16.));
#72697=CARTESIAN_POINT('',(27.3183612423927,0.609355047323334,33.8305837392638));
#72698=CARTESIAN_POINT('',(27.3183612423927,0.609355047323335,16.));
#72699=CARTESIAN_POINT('',(27.2892987572189,0.463248067869974,33.8305837392638));
#72700=CARTESIAN_POINT('',(27.2892987572189,0.463248067869971,16.));
#72701=CARTESIAN_POINT('Origin',(30.,-1.32966554433622E-14,33.8305837392638));
#72702=CARTESIAN_POINT('Origin',(30.,-1.32966554433622E-14,16.));
#72703=CARTESIAN_POINT('',(27.2788183937405,0.397077657083793,33.8305837392638));
#72704=CARTESIAN_POINT('',(27.2788183937405,0.397077657083795,16.));
#72705=CARTESIAN_POINT('',(27.2613089199969,0.24914086038101,33.8305837392638));
#72706=CARTESIAN_POINT('',(27.2613089199969,0.249140860381007,16.));
#72707=CARTESIAN_POINT('Origin',(30.,-1.32966554433622E-14,33.8305837392638));
#72708=CARTESIAN_POINT('Origin',(30.,-1.32966554433622E-14,16.));
#72709=CARTESIAN_POINT('',(27.2560525345756,0.182352151046609,33.8305837392638));
#72710=CARTESIAN_POINT('',(27.2560525345756,0.182352151046611,16.));
#72711=CARTESIAN_POINT('',(27.2502040239902,0.0334976166400525,33.8305837392638));
#72712=CARTESIAN_POINT('',(27.2502040239902,0.0334976166400503,16.));
#72713=CARTESIAN_POINT('Origin',(30.,-1.32966554433622E-14,33.8305837392638));
#72714=CARTESIAN_POINT('Origin',(30.,-1.32966554433622E-14,16.));
#72715=CARTESIAN_POINT('',(27.2502040239902,-0.0334976166400219,33.8305837392638));
#72716=CARTESIAN_POINT('',(27.2502040239902,-0.0334976166400194,16.));
#72717=CARTESIAN_POINT('',(27.2560525345756,-0.182352151046578,33.8305837392638));
#72718=CARTESIAN_POINT('',(27.2560525345756,-0.18235215104658,16.));
#72719=CARTESIAN_POINT('Origin',(30.,-1.32966554433622E-14,33.8305837392638));
#72720=CARTESIAN_POINT('Origin',(30.,-1.32966554433622E-14,16.));
#72721=CARTESIAN_POINT('',(27.2613089199969,-0.249140860380979,33.8305837392638));
#72722=CARTESIAN_POINT('',(27.2613089199969,-0.249140860380976,16.));
#72723=CARTESIAN_POINT('',(27.2788183937405,-0.397077657083761,33.8305837392638));
#72724=CARTESIAN_POINT('',(27.2788183937405,-0.397077657083763,16.));
#72725=CARTESIAN_POINT('Origin',(30.,-1.32966554433622E-14,33.8305837392638));
#72726=CARTESIAN_POINT('Origin',(30.,-1.32966554433622E-14,16.));
#72727=CARTESIAN_POINT('',(27.2892987572189,-0.463248067869942,33.8305837392638));
#72728=CARTESIAN_POINT('',(27.2892987572189,-0.463248067869938,16.));
#72729=CARTESIAN_POINT('',(27.3183612423927,-0.609355047323305,33.8305837392638));
#72730=CARTESIAN_POINT('',(27.3183612423927,-0.609355047323306,16.));
#72731=CARTESIAN_POINT('Origin',(30.,-1.32966554433622E-14,33.8305837392638));
#72732=CARTESIAN_POINT('Origin',(30.,-1.32966554433622E-14,16.));
#72733=CARTESIAN_POINT('',(27.3340009690023,-0.674499196974875,33.8305837392638));
#72734=CARTESIAN_POINT('',(27.3340009690024,-0.674499196974871,16.));
#72735=CARTESIAN_POINT('',(27.3744372857209,-0.817875561064985,33.8305837392638));
#72736=CARTESIAN_POINT('',(27.3744372857209,-0.817875561064986,16.));
#72737=CARTESIAN_POINT('Origin',(30.,-1.32966554433622E-14,33.8305837392638));
#72738=CARTESIAN_POINT('Origin',(30.,-1.32966554433622E-14,16.));
#72739=CARTESIAN_POINT('',(27.3951399513465,-0.881591814236714,33.8305837392638));
#72740=CARTESIAN_POINT('',(27.3951399513465,-0.88159181423671,16.));
#72741=CARTESIAN_POINT('',(27.4467007962708,-1.02135360000148,33.8305837392638));
#72742=CARTESIAN_POINT('',(27.4467007962708,-1.02135360000148,16.));
#72743=CARTESIAN_POINT('Origin',(30.,-1.32966554433622E-14,33.8305837392638));
#72744=CARTESIAN_POINT('Origin',(30.,-1.32966554433622E-14,16.));
#72745=CARTESIAN_POINT('',(27.4723387620945,-1.08324912480476,33.8305837392638));
#72746=CARTESIAN_POINT('',(27.4723387620945,-1.08324912480475,16.));
#72747=CARTESIAN_POINT('',(27.5347062454699,-1.21853465435942,33.8305837392638));
#72748=CARTESIAN_POINT('',(27.5347062454699,-1.21853465435942,16.));
#72749=CARTESIAN_POINT('Origin',(30.,-1.32966554433622E-14,33.8305837392638));
#72750=CARTESIAN_POINT('Origin',(30.,-1.32966554433622E-14,16.));
#72751=CARTESIAN_POINT('',(27.5651214449068,-1.27822784430149,33.8305837392638));
#72752=CARTESIAN_POINT('',(27.5651214449068,-1.27822784430149,16.));
#72753=CARTESIAN_POINT('',(27.637911050459,-1.40820303736935,33.8305837392638));
#72754=CARTESIAN_POINT('',(27.637911050459,-1.40820303736935,16.));
#72755=CARTESIAN_POINT('Origin',(30.,-1.32966554433622E-14,33.8305837392638));
#72756=CARTESIAN_POINT('Origin',(30.,-1.32966554433622E-14,16.));
#72757=CARTESIAN_POINT('',(27.6729159636906,-1.46532586408422,33.8305837392638));
#72758=CARTESIAN_POINT('',(27.6729159636906,-1.46532586408421,16.));
#72759=CARTESIAN_POINT('',(27.7556789192963,-1.58918938037887,33.8305837392638));
#72760=CARTESIAN_POINT('',(27.7556789192963,-1.58918938037887,16.));
#72761=CARTESIAN_POINT('Origin',(30.,-1.32966554433622E-14,33.8305837392638));
#72762=CARTESIAN_POINT('Origin',(30.,-1.32966554433622E-14,16.));
#72763=CARTESIAN_POINT('',(27.7950577293922,-1.64338966264456,33.8305837392638));
#72764=CARTESIAN_POINT('',(27.7950577293922,-1.64338966264456,16.));
#72765=CARTESIAN_POINT('',(27.8872837739086,-1.76037784239926,33.8305837392638));
#72766=CARTESIAN_POINT('',(27.8872837739086,-1.76037784239926,16.));
#72767=CARTESIAN_POINT('Origin',(30.,-1.32966554433622E-14,33.8305837392638));
#72768=CARTESIAN_POINT('Origin',(30.,-1.32966554433622E-14,16.));
#72769=CARTESIAN_POINT('',(27.9307936974098,-1.81132141745219,33.8305837392638));
#72770=CARTESIAN_POINT('',(27.9307936974098,-1.81132141745219,16.));
#72771=CARTESIAN_POINT('',(28.0319142266042,-1.92071298963622,33.8305837392638));
#72772=CARTESIAN_POINT('',(28.0319142266042,-1.92071298963622,16.));
#72773=CARTESIAN_POINT('Origin',(30.,-1.32966554433622E-14,33.8305837392638));
#72774=CARTESIAN_POINT('Origin',(30.,-1.32966554433622E-14,16.));
#72775=CARTESIAN_POINT('',(28.0792870103637,-1.96808577339574,33.8305837392638));
#72776=CARTESIAN_POINT('',(28.0792870103637,-1.96808577339573,16.));
#72777=CARTESIAN_POINT('',(28.1886785825478,-2.06920630259019,33.8305837392638));
#72778=CARTESIAN_POINT('',(28.1886785825478,-2.06920630259019,16.));
#72779=CARTESIAN_POINT('Origin',(30.,-1.32966554433622E-14,33.8305837392638));
#72780=CARTESIAN_POINT('Origin',(30.,-1.32966554433622E-14,16.));
#72781=CARTESIAN_POINT('',(28.2396221576007,-2.11271622609136,33.8305837392638));
#72782=CARTESIAN_POINT('',(28.2396221576007,-2.11271622609136,16.));
#72783=CARTESIAN_POINT('',(28.3566103373554,-2.20494227060778,33.8305837392638));
#72784=CARTESIAN_POINT('',(28.3566103373554,-2.20494227060778,16.));
#72785=CARTESIAN_POINT('Origin',(30.,-1.32966554433622E-14,33.8305837392638));
#72786=CARTESIAN_POINT('Origin',(30.,-1.32966554433622E-14,16.));
#72787=CARTESIAN_POINT('',(28.4108106196211,-2.2443210807037,33.8305837392638));
#72788=CARTESIAN_POINT('',(28.4108106196211,-2.2443210807037,16.));
#72789=CARTESIAN_POINT('',(28.5346741359157,-2.32708403630936,33.8305837392638));
#72790=CARTESIAN_POINT('',(28.5346741359157,-2.32708403630936,16.));
#72791=CARTESIAN_POINT('Origin',(30.,-1.32966554433622E-14,33.8305837392638));
#72792=CARTESIAN_POINT('Origin',(30.,-1.32966554433622E-14,16.));
#72793=CARTESIAN_POINT('',(28.5917969626306,-2.36208894954101,33.8305837392638));
#72794=CARTESIAN_POINT('',(28.5917969626306,-2.362088949541,16.));
#72795=CARTESIAN_POINT('',(28.7217721556985,-2.43487855509313,33.8305837392638));
#72796=CARTESIAN_POINT('',(28.7217721556985,-2.43487855509312,16.));
#72797=CARTESIAN_POINT('Origin',(30.,-1.32966554433622E-14,33.8305837392638));
#72798=CARTESIAN_POINT('Origin',(30.,-1.32966554433622E-14,16.));
#72799=CARTESIAN_POINT('',(28.7814653456405,-2.46529375453011,33.8305837392638));
#72800=CARTESIAN_POINT('',(28.7814653456405,-2.46529375453011,16.));
#72801=CARTESIAN_POINT('',(28.9167508751952,-2.52766123790546,33.8305837392638));
#72802=CARTESIAN_POINT('',(28.9167508751952,-2.52766123790546,16.));
#72803=CARTESIAN_POINT('Origin',(30.,-1.32966554433622E-14,33.8305837392638));
#72804=CARTESIAN_POINT('Origin',(30.,-1.32966554433622E-14,16.));
#72805=CARTESIAN_POINT('',(28.9786463999985,-2.55329920372918,33.8305837392638));
#72806=CARTESIAN_POINT('',(28.9786463999985,-2.55329920372917,16.));
#72807=CARTESIAN_POINT('',(29.1184081857632,-2.60486004865345,33.8305837392638));
#72808=CARTESIAN_POINT('',(29.1184081857632,-2.60486004865345,16.));
#72809=CARTESIAN_POINT('Origin',(30.,-1.32966554433622E-14,33.8305837392638));
#72810=CARTESIAN_POINT('Origin',(30.,-1.32966554433622E-14,16.));
#72811=CARTESIAN_POINT('',(29.182124438935,-2.62556271427911,33.8305837392638));
#72812=CARTESIAN_POINT('',(29.182124438935,-2.6255627142791,16.));
#72813=CARTESIAN_POINT('',(29.3255008030251,-2.66599903099763,33.8305837392638));
#72814=CARTESIAN_POINT('',(29.3255008030251,-2.66599903099763,16.));
#72815=CARTESIAN_POINT('Origin',(30.,-1.32966554433622E-14,33.8305837392638));
#72816=CARTESIAN_POINT('Origin',(30.,-1.32966554433622E-14,16.));
#72817=CARTESIAN_POINT('',(29.3906449526766,-2.68163875760731,33.8305837392638));
#72818=CARTESIAN_POINT('',(29.3906449526766,-2.6816387576073,16.));
#72819=CARTESIAN_POINT('',(29.53675193213,-2.71070124278107,33.8305837392638));
#72820=CARTESIAN_POINT('',(29.53675193213,-2.71070124278106,16.));
#72821=CARTESIAN_POINT('Origin',(30.,-1.32966554433622E-14,33.8305837392638));
#72822=CARTESIAN_POINT('Origin',(30.,-1.32966554433622E-14,16.));
#72823=CARTESIAN_POINT('',(29.6029223429162,-2.72118160625948,33.8305837392638));
#72824=CARTESIAN_POINT('',(29.6029223429162,-2.72118160625948,16.));
#72825=CARTESIAN_POINT('',(29.750859139619,-2.73869108000313,33.8305837392638));
#72826=CARTESIAN_POINT('',(29.750859139619,-2.73869108000313,16.));
#72827=CARTESIAN_POINT('Origin',(30.,-1.32966554433622E-14,33.8305837392638));
#72828=CARTESIAN_POINT('Origin',(30.,-1.32966554433622E-14,16.));
#72829=CARTESIAN_POINT('',(29.8176478489534,-2.74394746542436,33.8305837392638));
#72830=CARTESIAN_POINT('',(29.8176478489534,-2.74394746542436,16.));
#72831=CARTESIAN_POINT('',(29.9665023833599,-2.74979597600977,33.8305837392638));
#72832=CARTESIAN_POINT('',(29.9665023833599,-2.74979597600977,16.));
#72833=CARTESIAN_POINT('Origin',(30.,-1.32966554433622E-14,33.8305837392638));
#72834=CARTESIAN_POINT('Origin',(30.,-1.32966554433622E-14,16.));
#72835=CARTESIAN_POINT('',(30.03349761664,-2.74979597600977,33.8305837392638));
#72836=CARTESIAN_POINT('',(30.03349761664,-2.74979597600977,16.));
#72837=CARTESIAN_POINT('',(30.1823521510466,-2.74394746542436,33.8305837392638));
#72838=CARTESIAN_POINT('',(30.1823521510466,-2.74394746542436,16.));
#72839=CARTESIAN_POINT('Origin',(30.,-1.32966554433622E-14,33.8305837392638));
#72840=CARTESIAN_POINT('Origin',(30.,-1.32966554433622E-14,16.));
#72841=CARTESIAN_POINT('',(30.249140860381,-2.73869108000313,33.8305837392638));
#72842=CARTESIAN_POINT('',(30.2491408603809,-2.73869108000313,16.));
#72843=CARTESIAN_POINT('',(30.3970776570837,-2.72118160625949,33.8305837392638));
#72844=CARTESIAN_POINT('',(30.3970776570837,-2.72118160625948,16.));
#72845=CARTESIAN_POINT('Origin',(30.,-1.32966554433622E-14,33.8305837392638));
#72846=CARTESIAN_POINT('Origin',(30.,-1.32966554433622E-14,16.));
#72847=CARTESIAN_POINT('',(30.4632480678699,-2.71070124278108,33.8305837392638));
#72848=CARTESIAN_POINT('',(30.4632480678699,-2.71070124278107,16.));
#72849=CARTESIAN_POINT('',(30.6093550473233,-2.68163875760732,33.8305837392638));
#72850=CARTESIAN_POINT('',(30.6093550473233,-2.68163875760731,16.));
#72851=CARTESIAN_POINT('Origin',(30.,-1.32966554433622E-14,33.8305837392638));
#72852=CARTESIAN_POINT('Origin',(30.,-1.32966554433622E-14,16.));
#72853=CARTESIAN_POINT('',(30.6744991969748,-2.66599903099764,33.8305837392638));
#72854=CARTESIAN_POINT('',(30.6744991969748,-2.66599903099764,16.));
#72855=CARTESIAN_POINT('',(30.817875561065,-2.62556271427912,33.8305837392638));
#72856=CARTESIAN_POINT('',(30.817875561065,-2.62556271427912,16.));
#72857=CARTESIAN_POINT('Origin',(30.,-1.32966554433622E-14,33.8305837392638));
#72858=CARTESIAN_POINT('Origin',(30.,-1.32966554433622E-14,16.));
#72859=CARTESIAN_POINT('',(30.8815918142367,-2.60486004865346,33.8305837392638));
#72860=CARTESIAN_POINT('',(30.8815918142367,-2.60486004865346,16.));
#72861=CARTESIAN_POINT('',(31.0213536000014,-2.55329920372919,33.8305837392638));
#72862=CARTESIAN_POINT('',(31.0213536000014,-2.55329920372919,16.));
#72863=CARTESIAN_POINT('Origin',(30.,-1.32966554433622E-14,33.8305837392638));
#72864=CARTESIAN_POINT('Origin',(30.,-1.32966554433622E-14,16.));
#72865=CARTESIAN_POINT('',(31.0832491248047,-2.52766123790547,33.8305837392638));
#72866=CARTESIAN_POINT('',(31.0832491248047,-2.52766123790547,16.));
#72867=CARTESIAN_POINT('',(31.2185346543594,-2.46529375453013,33.8305837392638));
#72868=CARTESIAN_POINT('',(31.2185346543594,-2.46529375453013,16.));
#72869=CARTESIAN_POINT('Origin',(30.,-1.32966554433622E-14,33.8305837392638));
#72870=CARTESIAN_POINT('Origin',(30.,-1.32966554433622E-14,16.));
#72871=CARTESIAN_POINT('',(31.2782278443015,-2.43487855509314,33.8305837392638));
#72872=CARTESIAN_POINT('',(31.2782278443015,-2.43487855509314,16.));
#72873=CARTESIAN_POINT('',(31.4082030373693,-2.36208894954103,33.8305837392638));
#72874=CARTESIAN_POINT('',(31.4082030373693,-2.36208894954102,16.));
#72875=CARTESIAN_POINT('Origin',(30.,-1.32966554433622E-14,33.8305837392638));
#72876=CARTESIAN_POINT('Origin',(30.,-1.32966554433622E-14,16.));
#72877=CARTESIAN_POINT('',(31.4653258640842,-2.32708403630938,33.8305837392638));
#72878=CARTESIAN_POINT('',(31.4653258640842,-2.32708403630938,16.));
#72879=CARTESIAN_POINT('',(31.5891893803788,-2.24432108070372,33.8305837392638));
#72880=CARTESIAN_POINT('',(31.5891893803788,-2.24432108070372,16.));
#72881=CARTESIAN_POINT('Origin',(30.,-1.32966554433622E-14,33.8305837392638));
#72882=CARTESIAN_POINT('Origin',(30.,-1.32966554433622E-14,16.));
#72883=CARTESIAN_POINT('',(31.6433896626445,-2.2049422706078,33.8305837392638));
#72884=CARTESIAN_POINT('',(31.6433896626445,-2.2049422706078,16.));
#72885=CARTESIAN_POINT('',(31.7603778423992,-2.11271622609139,33.8305837392638));
#72886=CARTESIAN_POINT('',(31.7603778423992,-2.11271622609138,16.));
#72887=CARTESIAN_POINT('Origin',(30.,-1.32966554433622E-14,33.8305837392638));
#72888=CARTESIAN_POINT('Origin',(30.,-1.32966554433622E-14,16.));
#72889=CARTESIAN_POINT('',(31.8113214174522,-2.06920630259022,33.8305837392638));
#72890=CARTESIAN_POINT('',(31.8113214174522,-2.06920630259022,16.));
#72891=CARTESIAN_POINT('',(31.9207129896362,-1.96808577339576,33.8305837392638));
#72892=CARTESIAN_POINT('',(31.9207129896362,-1.96808577339576,16.));
#72893=CARTESIAN_POINT('Origin',(30.,-1.32966554433622E-14,33.8305837392638));
#72894=CARTESIAN_POINT('Origin',(30.,-1.32966554433622E-14,16.));
#72895=CARTESIAN_POINT('',(31.9680857733957,-1.92071298963625,33.8305837392638));
#72896=CARTESIAN_POINT('',(31.9680857733957,-1.92071298963625,16.));
#72897=CARTESIAN_POINT('',(32.0692063025902,-1.81132141745222,33.8305837392638));
#72898=CARTESIAN_POINT('',(32.0692063025902,-1.81132141745222,16.));
#72899=CARTESIAN_POINT('Origin',(30.,-1.32966554433622E-14,33.8305837392638));
#72900=CARTESIAN_POINT('Origin',(30.,-1.32966554433622E-14,16.));
#72901=CARTESIAN_POINT('',(32.1127162260913,-1.76037784239929,33.8305837392638));
#72902=CARTESIAN_POINT('',(32.1127162260913,-1.76037784239929,16.));
#72903=CARTESIAN_POINT('',(32.2049422706078,-1.6433896626446,33.8305837392638));
#72904=CARTESIAN_POINT('',(32.2049422706077,-1.64338966264459,16.));
#72905=CARTESIAN_POINT('Origin',(30.,-1.32966554433622E-14,33.8305837392638));
#72906=CARTESIAN_POINT('Origin',(30.,-1.32966554433622E-14,16.));
#72907=CARTESIAN_POINT('',(32.2443210807037,-1.5891893803789,33.8305837392638));
#72908=CARTESIAN_POINT('',(32.2443210807037,-1.5891893803789,16.));
#72909=CARTESIAN_POINT('',(32.3270840363093,-1.46532586408425,33.8305837392638));
#72910=CARTESIAN_POINT('',(32.3270840363093,-1.46532586408424,16.));
#72911=CARTESIAN_POINT('Origin',(30.,-1.32966554433622E-14,33.8305837392638));
#72912=CARTESIAN_POINT('Origin',(30.,-1.32966554433622E-14,16.));
#72913=CARTESIAN_POINT('',(32.362088949541,-1.40820303736938,33.8305837392638));
#72914=CARTESIAN_POINT('',(32.362088949541,-1.40820303736938,16.));
#72915=CARTESIAN_POINT('',(32.4348785550931,-1.27822784430152,33.8305837392638));
#72916=CARTESIAN_POINT('',(32.4348785550931,-1.27822784430152,16.));
#72917=CARTESIAN_POINT('Origin',(30.,-1.32966554433622E-14,33.8305837392638));
#72918=CARTESIAN_POINT('Origin',(30.,-1.32966554433622E-14,16.));
#72919=CARTESIAN_POINT('',(32.4652937545301,-1.21853465435946,33.8305837392638));
#72920=CARTESIAN_POINT('',(32.4652937545301,-1.21853465435946,16.));
#72921=CARTESIAN_POINT('',(32.5276612379054,-1.08324912480479,33.8305837392638));
#72922=CARTESIAN_POINT('',(32.5276612379054,-1.08324912480479,16.));
#72923=CARTESIAN_POINT('Origin',(30.,-1.32966554433622E-14,33.8305837392638));
#72924=CARTESIAN_POINT('Origin',(30.,-1.32966554433622E-14,16.));
#72925=CARTESIAN_POINT('',(32.5532992037291,-1.02135360000151,33.8305837392638));
#72926=CARTESIAN_POINT('',(32.5532992037291,-1.02135360000151,16.));
#72927=CARTESIAN_POINT('',(32.6048600486534,-0.88159181423675,33.8305837392638));
#72928=CARTESIAN_POINT('',(32.6048600486534,-0.881591814236746,16.));
#72929=CARTESIAN_POINT('Origin',(30.,-1.32966554433622E-14,33.8305837392638));
#72930=CARTESIAN_POINT('Origin',(30.,-1.32966554433622E-14,16.));
#72931=CARTESIAN_POINT('',(32.6255627142791,-0.817875561065022,33.8305837392638));
#72932=CARTESIAN_POINT('',(32.6255627142791,-0.817875561065022,16.));
#72933=CARTESIAN_POINT('',(32.6659990309976,-0.674499196974912,33.8305837392638));
#72934=CARTESIAN_POINT('',(32.6659990309976,-0.674499196974908,16.));
#72935=CARTESIAN_POINT('Origin',(30.,-1.32966554433622E-14,33.8305837392638));
#72936=CARTESIAN_POINT('Origin',(30.,-1.32966554433622E-14,16.));
#72937=CARTESIAN_POINT('',(32.6816387576073,-0.609355047323342,33.8305837392638));
#72938=CARTESIAN_POINT('',(32.6816387576073,-0.609355047323343,16.));
#72939=CARTESIAN_POINT('',(32.710701242781,-0.463248067869981,33.8305837392638));
#72940=CARTESIAN_POINT('',(32.710701242781,-0.463248067869977,16.));
#72941=CARTESIAN_POINT('Origin',(30.,-1.32966554433622E-14,33.8305837392638));
#72942=CARTESIAN_POINT('Origin',(30.,-1.32966554433622E-14,16.));
#72943=CARTESIAN_POINT('',(32.7211816062594,-0.3970776570838,33.8305837392638));
#72944=CARTESIAN_POINT('',(32.7211816062594,-0.397077657083801,16.));
#72945=CARTESIAN_POINT('',(32.7386910800031,-0.249140860381016,33.8305837392638));
#72946=CARTESIAN_POINT('',(32.7386910800031,-0.249140860381013,16.));
#72947=CARTESIAN_POINT('Origin',(30.,-1.32966554433622E-14,33.8305837392638));
#72948=CARTESIAN_POINT('Origin',(30.,-1.32966554433622E-14,16.));
#72949=CARTESIAN_POINT('',(32.7439474654243,-0.182352151046616,33.8305837392638));
#72950=CARTESIAN_POINT('',(32.7439474654243,-0.182352151046618,16.));
#72951=CARTESIAN_POINT('',(32.7497959760097,-0.03349761664006,33.8305837392638));
#72952=CARTESIAN_POINT('',(32.7497959760097,-0.0334976166400576,16.));
#72953=CARTESIAN_POINT('Origin',(30.,-1.32966554433622E-14,33.8305837392638));
#72954=CARTESIAN_POINT('Origin',(30.,-1.32966554433622E-14,16.));
#72955=CARTESIAN_POINT('',(32.7497959760097,0.0334976166400146,33.8305837392638));
#72956=CARTESIAN_POINT('',(32.7497959760097,0.0334976166400122,16.));
#72957=CARTESIAN_POINT('',(32.7439474654243,0.18235215104657,33.8305837392638));
#72958=CARTESIAN_POINT('',(32.7439474654243,0.182352151046572,16.));
#72959=CARTESIAN_POINT('Origin',(30.,-1.32966554433622E-14,33.8305837392638));
#72960=CARTESIAN_POINT('Origin',(30.,-1.32966554433622E-14,16.));
#72961=CARTESIAN_POINT('',(32.7386910800031,0.249140860380971,33.8305837392638));
#72962=CARTESIAN_POINT('',(32.7386910800031,0.249140860380968,16.));
#72963=CARTESIAN_POINT('',(32.7211816062594,0.397077657083754,33.8305837392638));
#72964=CARTESIAN_POINT('',(32.7211816062594,0.397077657083756,16.));
#72965=CARTESIAN_POINT('Origin',(30.,-1.32966554433622E-14,33.8305837392638));
#72966=CARTESIAN_POINT('Origin',(30.,-1.32966554433622E-14,16.));
#72967=CARTESIAN_POINT('',(32.710701242781,0.463248067869934,33.8305837392638));
#72968=CARTESIAN_POINT('',(32.710701242781,0.463248067869931,16.));
#72969=CARTESIAN_POINT('',(32.6816387576073,0.609355047323297,33.8305837392638));
#72970=CARTESIAN_POINT('',(32.6816387576073,0.609355047323298,16.));
#72971=CARTESIAN_POINT('Origin',(30.,-1.32966554433622E-14,33.8305837392638));
#72972=CARTESIAN_POINT('Origin',(30.,-1.32966554433622E-14,16.));
#72973=CARTESIAN_POINT('',(32.6659990309976,0.674499196974867,33.8305837392638));
#72974=CARTESIAN_POINT('',(32.6659990309976,0.674499196974863,16.));
#72975=CARTESIAN_POINT('',(32.6255627142791,0.817875561064977,33.8305837392638));
#72976=CARTESIAN_POINT('',(32.6255627142791,0.817875561064977,16.));
#72977=CARTESIAN_POINT('Origin',(30.,-1.32966554433622E-14,33.8305837392638));
#72978=CARTESIAN_POINT('Origin',(30.,-1.32966554433622E-14,16.));
#72979=CARTESIAN_POINT('',(32.6048600486534,0.881591814236705,33.8305837392638));
#72980=CARTESIAN_POINT('',(32.6048600486534,0.881591814236701,16.));
#72981=CARTESIAN_POINT('',(32.5532992037292,1.02135360000147,33.8305837392638));
#72982=CARTESIAN_POINT('',(32.5532992037291,1.02135360000147,16.));
#72983=CARTESIAN_POINT('Origin',(30.,-1.32966554433622E-14,33.8305837392638));
#72984=CARTESIAN_POINT('Origin',(30.,-1.32966554433622E-14,16.));
#72985=CARTESIAN_POINT('',(32.5276612379054,1.08324912480475,33.8305837392638));
#72986=CARTESIAN_POINT('',(32.5276612379054,1.08324912480474,16.));
#72987=CARTESIAN_POINT('',(32.4652937545301,1.21853465435941,33.8305837392638));
#72988=CARTESIAN_POINT('',(32.4652937545301,1.21853465435941,16.));
#72989=CARTESIAN_POINT('Origin',(30.,-1.32966554433622E-14,33.8305837392638));
#72990=CARTESIAN_POINT('Origin',(30.,-1.32966554433622E-14,16.));
#72991=CARTESIAN_POINT('',(32.4348785550931,1.27822784430148,33.8305837392638));
#72992=CARTESIAN_POINT('',(32.4348785550931,1.27822784430148,16.));
#72993=CARTESIAN_POINT('',(32.362088949541,1.40820303736934,33.8305837392638));
#72994=CARTESIAN_POINT('',(32.362088949541,1.40820303736934,16.));
#72995=CARTESIAN_POINT('Origin',(30.,-1.32966554433622E-14,33.8305837392638));
#72996=CARTESIAN_POINT('Origin',(30.,-1.32966554433622E-14,16.));
#72997=CARTESIAN_POINT('',(32.3270840363093,1.4653258640842,33.8305837392638));
#72998=CARTESIAN_POINT('',(32.3270840363093,1.4653258640842,16.));
#72999=CARTESIAN_POINT('',(32.2443210807037,1.58918938037886,33.8305837392638));
#73000=CARTESIAN_POINT('',(32.2443210807037,1.58918938037886,16.));
#73001=CARTESIAN_POINT('Origin',(30.,-1.32966554433622E-14,33.8305837392638));
#73002=CARTESIAN_POINT('Origin',(30.,-1.32966554433622E-14,16.));
#73003=CARTESIAN_POINT('',(32.2049422706078,1.64338966264455,33.8305837392638));
#73004=CARTESIAN_POINT('',(32.2049422706078,1.64338966264455,16.));
#73005=CARTESIAN_POINT('',(32.1127162260914,1.76037784239925,33.8305837392638));
#73006=CARTESIAN_POINT('',(32.1127162260913,1.76037784239925,16.));
#73007=CARTESIAN_POINT('Origin',(30.,-1.32966554433622E-14,33.8305837392638));
#73008=CARTESIAN_POINT('Origin',(30.,-1.32966554433622E-14,16.));
#73009=CARTESIAN_POINT('',(32.0692063025902,1.81132141745218,33.8305837392638));
#73010=CARTESIAN_POINT('',(32.0692063025902,1.81132141745218,16.));
#73011=CARTESIAN_POINT('',(31.9680857733957,1.92071298963621,33.8305837392638));
#73012=CARTESIAN_POINT('',(31.9680857733957,1.92071298963621,16.));
#73013=CARTESIAN_POINT('Origin',(30.,-1.32966554433622E-14,33.8305837392638));
#73014=CARTESIAN_POINT('Origin',(30.,-1.32966554433622E-14,16.));
#73015=CARTESIAN_POINT('',(31.9207129896362,1.96808577339572,33.8305837392638));
#73016=CARTESIAN_POINT('',(31.9207129896362,1.96808577339572,16.));
#73017=CARTESIAN_POINT('',(31.8113214174522,2.06920630259018,33.8305837392638));
#73018=CARTESIAN_POINT('',(31.8113214174522,2.06920630259018,16.));
#73019=CARTESIAN_POINT('Origin',(30.,-1.32966554433622E-14,33.8305837392638));
#73020=CARTESIAN_POINT('Origin',(30.,-1.32966554433622E-14,16.));
#73021=CARTESIAN_POINT('',(31.7603778423992,2.11271622609135,33.8305837392638));
#73022=CARTESIAN_POINT('',(31.7603778423992,2.11271622609134,16.));
#73023=CARTESIAN_POINT('',(31.6433896626446,2.20494227060777,33.8305837392638));
#73024=CARTESIAN_POINT('',(31.6433896626445,2.20494227060776,16.));
#73025=CARTESIAN_POINT('Origin',(30.,-1.32966554433622E-14,33.8305837392638));
#73026=CARTESIAN_POINT('Origin',(30.,-1.32966554433622E-14,16.));
#73027=CARTESIAN_POINT('',(31.5891893803789,2.24432108070369,33.8305837392638));
#73028=CARTESIAN_POINT('',(31.5891893803789,2.24432108070368,16.));
#73029=CARTESIAN_POINT('',(31.4653258640842,2.32708403630934,33.8305837392638));
#73030=CARTESIAN_POINT('',(31.4653258640842,2.32708403630934,16.));
#73031=CARTESIAN_POINT('Origin',(30.,-1.32966554433622E-14,33.8305837392638));
#73032=CARTESIAN_POINT('Origin',(30.,-1.32966554433622E-14,16.));
#73033=CARTESIAN_POINT('',(31.4082030373693,2.36208894954099,33.8305837392638));
#73034=CARTESIAN_POINT('',(31.4082030373693,2.36208894954099,16.));
#73035=CARTESIAN_POINT('',(31.2782278443015,2.43487855509311,33.8305837392638));
#73036=CARTESIAN_POINT('',(31.2782278443015,2.4348785550931,16.));
#73037=CARTESIAN_POINT('Origin',(30.,-1.32966554433622E-14,33.8305837392638));
#73038=CARTESIAN_POINT('Origin',(30.,-1.32966554433622E-14,16.));
#73039=CARTESIAN_POINT('',(31.2185346543594,2.4652937545301,33.8305837392638));
#73040=CARTESIAN_POINT('',(31.2185346543594,2.46529375453009,16.));
#73041=CARTESIAN_POINT('',(31.0832491248047,2.52766123790544,33.8305837392638));
#73042=CARTESIAN_POINT('',(31.0832491248047,2.52766123790544,16.));
#73043=CARTESIAN_POINT('Origin',(30.,-1.32966554433622E-14,33.8305837392638));
#73044=CARTESIAN_POINT('Origin',(30.,-1.32966554433622E-14,16.));
#73045=CARTESIAN_POINT('',(31.0213536000015,2.55329920372916,33.8305837392638));
#73046=CARTESIAN_POINT('',(31.0213536000015,2.55329920372915,16.));
#73047=CARTESIAN_POINT('',(30.8815918142367,2.60486004865343,33.8305837392638));
#73048=CARTESIAN_POINT('',(30.8815918142367,2.60486004865343,16.));
#73049=CARTESIAN_POINT('Origin',(30.,-1.32966554433622E-14,33.8305837392638));
#73050=CARTESIAN_POINT('Origin',(30.,-1.32966554433622E-14,16.));
#73051=CARTESIAN_POINT('',(30.817875561065,2.62556271427909,33.8305837392638));
#73052=CARTESIAN_POINT('',(30.817875561065,2.62556271427908,16.));
#73053=CARTESIAN_POINT('',(30.6744991969749,2.66599903099761,33.8305837392638));
#73054=CARTESIAN_POINT('',(30.6744991969749,2.6659990309976,16.));
#73055=CARTESIAN_POINT('Origin',(30.,-1.32966554433622E-14,33.8305837392638));
#73056=CARTESIAN_POINT('Origin',(30.,-1.32966554433622E-14,16.));
#73057=CARTESIAN_POINT('',(30.6093550473233,2.68163875760729,33.8305837392638));
#73058=CARTESIAN_POINT('',(30.6093550473233,2.68163875760728,16.));
#73059=CARTESIAN_POINT('',(30.4632480678699,2.71070124278105,33.8305837392638));
#73060=CARTESIAN_POINT('',(30.4632480678699,2.71070124278104,16.));
#73061=CARTESIAN_POINT('Origin',(30.,-1.32966554433622E-14,33.8305837392638));
#73062=CARTESIAN_POINT('Origin',(30.,-1.32966554433622E-14,16.));
#73063=CARTESIAN_POINT('',(27.5651214449069,1.27822784430151,33.8305837392638));
#73064=CARTESIAN_POINT('',(27.5651214449069,1.27822784430151,16.));
#73065=CARTESIAN_POINT('',(27.637911050459,1.40820303736937,33.8305837392638));
#73066=CARTESIAN_POINT('Origin',(30.,-1.32966554433622E-14,33.8305837392638));
#73067=CARTESIAN_POINT('',(27.637911050459,1.40820303736937,16.));
#73068=CARTESIAN_POINT('Origin',(30.,-1.32966554433622E-14,16.));
#73069=CARTESIAN_POINT('',(27.6729159636906,1.46532586408424,33.8305837392638));
#73070=CARTESIAN_POINT('',(27.6729159636906,1.46532586408423,16.));
#73071=CARTESIAN_POINT('',(27.7556789192963,1.58918938037889,33.8305837392638));
#73072=CARTESIAN_POINT('Origin',(30.,-1.32966554433622E-14,33.8305837392638));
#73073=CARTESIAN_POINT('',(27.7556789192963,1.58918938037889,16.));
#73074=CARTESIAN_POINT('Origin',(30.,-1.32966554433622E-14,16.));
#73075=CARTESIAN_POINT('',(27.7950577293922,1.64338966264458,33.8305837392638));
#73076=CARTESIAN_POINT('',(27.7950577293922,1.64338966264458,16.));
#73077=CARTESIAN_POINT('',(27.8872837739086,1.76037784239928,33.8305837392638));
#73078=CARTESIAN_POINT('Origin',(30.,-1.32966554433622E-14,33.8305837392638));
#73079=CARTESIAN_POINT('',(27.8872837739086,1.76037784239928,16.));
#73080=CARTESIAN_POINT('Origin',(30.,-1.32966554433622E-14,16.));
#73081=CARTESIAN_POINT('',(27.9307936974098,1.81132141745221,33.8305837392638));
#73082=CARTESIAN_POINT('',(27.9307936974098,1.81132141745221,16.));
#73083=CARTESIAN_POINT('',(28.0319142266043,1.92071298963624,33.8305837392638));
#73084=CARTESIAN_POINT('Origin',(30.,-1.32966554433622E-14,33.8305837392638));
#73085=CARTESIAN_POINT('',(28.0319142266043,1.92071298963623,16.));
#73086=CARTESIAN_POINT('Origin',(30.,-1.32966554433622E-14,16.));
#73087=CARTESIAN_POINT('',(28.0792870103638,1.96808577339575,33.8305837392638));
#73088=CARTESIAN_POINT('',(28.0792870103638,1.96808577339574,16.));
#73089=CARTESIAN_POINT('',(28.1886785825478,2.06920630259021,33.8305837392638));
#73090=CARTESIAN_POINT('Origin',(30.,-1.32966554433622E-14,33.8305837392638));
#73091=CARTESIAN_POINT('',(28.1886785825478,2.0692063025902,16.));
#73092=CARTESIAN_POINT('Origin',(30.,-1.32966554433622E-14,16.));
#73093=CARTESIAN_POINT('',(28.2396221576007,2.11271622609138,33.8305837392638));
#73094=CARTESIAN_POINT('',(28.2396221576007,2.11271622609137,16.));
#73095=CARTESIAN_POINT('',(28.3566103373554,2.20494227060779,33.8305837392638));
#73096=CARTESIAN_POINT('Origin',(30.,-1.32966554433622E-14,33.8305837392638));
#73097=CARTESIAN_POINT('',(28.3566103373554,2.20494227060779,16.));
#73098=CARTESIAN_POINT('Origin',(30.,-1.32966554433622E-14,16.));
#73099=CARTESIAN_POINT('',(28.4108106196211,2.24432108070371,33.8305837392638));
#73100=CARTESIAN_POINT('',(28.4108106196211,2.2443210807037,16.));
#73101=CARTESIAN_POINT('',(28.5346741359158,2.32708403630936,33.8305837392638));
#73102=CARTESIAN_POINT('Origin',(30.,-1.32966554433622E-14,33.8305837392638));
#73103=CARTESIAN_POINT('',(28.5346741359158,2.32708403630936,16.));
#73104=CARTESIAN_POINT('Origin',(30.,-1.32966554433622E-14,16.));
#73105=CARTESIAN_POINT('',(28.5917969626306,2.36208894954101,33.8305837392638));
#73106=CARTESIAN_POINT('',(28.5917969626306,2.36208894954101,16.));
#73107=CARTESIAN_POINT('',(28.7217721556985,2.43487855509313,33.8305837392638));
#73108=CARTESIAN_POINT('Origin',(30.,-1.32966554433622E-14,33.8305837392638));
#73109=CARTESIAN_POINT('',(28.7217721556985,2.43487855509312,16.));
#73110=CARTESIAN_POINT('Origin',(30.,-1.32966554433622E-14,16.));
#73111=CARTESIAN_POINT('',(28.7814653456406,2.46529375453011,33.8305837392638));
#73112=CARTESIAN_POINT('',(28.7814653456406,2.46529375453011,16.));
#73113=CARTESIAN_POINT('',(28.9167508751952,2.52766123790546,33.8305837392638));
#73114=CARTESIAN_POINT('Origin',(30.,-1.32966554433622E-14,33.8305837392638));
#73115=CARTESIAN_POINT('',(28.9167508751953,2.52766123790545,16.));
#73116=CARTESIAN_POINT('Origin',(30.,-1.32966554433622E-14,16.));
#73117=CARTESIAN_POINT('',(28.9786463999985,2.55329920372917,33.8305837392638));
#73118=CARTESIAN_POINT('',(28.9786463999985,2.55329920372917,16.));
#73119=CARTESIAN_POINT('',(29.1184081857633,2.60486004865344,33.8305837392638));
#73120=CARTESIAN_POINT('Origin',(30.,-1.32966554433622E-14,33.8305837392638));
#73121=CARTESIAN_POINT('',(29.1184081857633,2.60486004865344,16.));
#73122=CARTESIAN_POINT('Origin',(30.,-1.32966554433622E-14,16.));
#73123=CARTESIAN_POINT('',(29.182124438935,2.6255627142791,33.8305837392638));
#73124=CARTESIAN_POINT('',(29.182124438935,2.62556271427909,16.));
#73125=CARTESIAN_POINT('',(29.3255008030251,2.66599903099762,33.8305837392638));
#73126=CARTESIAN_POINT('Origin',(30.,-1.32966554433622E-14,33.8305837392638));
#73127=CARTESIAN_POINT('',(29.3255008030251,2.66599903099761,16.));
#73128=CARTESIAN_POINT('Origin',(30.,-1.32966554433622E-14,16.));
#73129=CARTESIAN_POINT('',(29.3906449526767,2.6816387576073,33.8305837392638));
#73130=CARTESIAN_POINT('',(29.3906449526767,2.68163875760729,16.));
#73131=CARTESIAN_POINT('',(29.5367519321301,2.71070124278105,33.8305837392638));
#73132=CARTESIAN_POINT('Origin',(30.,-1.32966554433622E-14,33.8305837392638));
#73133=CARTESIAN_POINT('',(29.5367519321301,2.71070124278105,16.));
#73134=CARTESIAN_POINT('Origin',(30.,-1.32966554433622E-14,16.));
#73135=CARTESIAN_POINT('',(29.6029223429162,2.72118160625947,33.8305837392638));
#73136=CARTESIAN_POINT('',(29.6029223429162,2.72118160625946,16.));
#73137=CARTESIAN_POINT('',(29.750859139619,2.73869108000311,33.8305837392638));
#73138=CARTESIAN_POINT('Origin',(30.,-1.32966554433622E-14,33.8305837392638));
#73139=CARTESIAN_POINT('',(29.750859139619,2.7386910800031,16.));
#73140=CARTESIAN_POINT('Origin',(30.,-1.32966554433622E-14,16.));
#73141=CARTESIAN_POINT('',(29.8176478489534,2.74394746542434,33.8305837392638));
#73142=CARTESIAN_POINT('',(29.8176478489534,2.74394746542433,16.));
#73143=CARTESIAN_POINT('',(29.9665023833599,2.74979597600975,33.8305837392638));
#73144=CARTESIAN_POINT('Origin',(30.,-1.32966554433622E-14,33.8305837392638));
#73145=CARTESIAN_POINT('',(29.9665023833599,2.74979597600974,16.));
#73146=CARTESIAN_POINT('Origin',(30.,-1.32966554433622E-14,16.));
#73147=CARTESIAN_POINT('',(30.3970776570838,2.72118160625946,33.8305837392638));
#73148=CARTESIAN_POINT('',(30.3970776570838,2.72118160625945,16.));
#73149=CARTESIAN_POINT('',(30.249140860381,2.73869108000311,33.8305837392638));
#73150=CARTESIAN_POINT('',(30.249140860381,2.7386910800031,16.));
#73151=CARTESIAN_POINT('Origin',(30.,-1.32966554433622E-14,33.8305837392638));
#73152=CARTESIAN_POINT('Origin',(30.,-1.32966554433622E-14,33.8305837392638));
#73153=CARTESIAN_POINT('Origin',(27.5075580599235,1.0459901541636,33.8304779343707));
#73154=CARTESIAN_POINT('Origin',(27.5859153117241,1.21595293501799,33.830456743813));
#73155=CARTESIAN_POINT('Origin',(30.,-1.32966554433622E-14,33.8305837392638));
#73156=CARTESIAN_POINT('Origin',(27.4979545614264,1.02279765627048,33.8304567438139));
#73157=CARTESIAN_POINT('Origin',(27.4331739849704,0.847210974834779,33.830477934375));
#73158=CARTESIAN_POINT('Origin',(30.,-1.32966554433622E-14,33.8305837392638));
#73159=CARTESIAN_POINT('Origin',(27.4254197532764,0.823336489857381,33.8304567438132));
#73160=CARTESIAN_POINT('Origin',(27.3746152459633,0.643208458112014,33.8304779343751));
#73161=CARTESIAN_POINT('Origin',(30.,-1.32966554433622E-14,33.8305837392638));
#73162=CARTESIAN_POINT('Origin',(27.368758088479,0.618799180196873,33.8304567438137));
#73163=CARTESIAN_POINT('Origin',(27.3322428769935,0.435240347356666,33.8304779343754));
#73164=CARTESIAN_POINT('Origin',(30.,-1.32966554433622E-14,33.8305837392638));
#73165=CARTESIAN_POINT('Origin',(27.3283189050469,0.410446767819665,33.8304567438127));
#73166=CARTESIAN_POINT('Origin',(27.3063181178076,0.224588835126915,33.8304779343751));
#73167=CARTESIAN_POINT('Origin',(30.,-1.32966554433622E-14,33.8305837392638));
#73168=CARTESIAN_POINT('Origin',(27.3043515239852,0.199563814630461,33.8304567438133));
#73169=CARTESIAN_POINT('Origin',(27.2970008031678,0.0125526580442922,33.8304779343738));
#73170=CARTESIAN_POINT('Origin',(30.,-1.32966554433622E-14,33.8305837392638));
#73171=CARTESIAN_POINT('Origin',(27.2970037121732,-0.012549515837469,33.8304567438135));
#73172=CARTESIAN_POINT('Origin',(27.3043483774083,-0.199560910346332,33.8304779343754));
#73173=CARTESIAN_POINT('Origin',(30.,-1.32966554433622E-14,33.8305837392638));
#73174=CARTESIAN_POINT('Origin',(27.3063207713147,-0.224585474366301,33.8304567438129));
#73175=CARTESIAN_POINT('Origin',(27.3283155403039,-0.410444119366497,33.8304779343742));
#73176=CARTESIAN_POINT('Origin',(30.,-1.32966554433622E-14,33.8305837392638));
#73177=CARTESIAN_POINT('Origin',(27.3322452586388,-0.435236788764194,33.8304567438132));
#73178=CARTESIAN_POINT('Origin',(27.3687545263134,-0.618796803902706,33.8304779343752));
#73179=CARTESIAN_POINT('Origin',(30.,-1.32966554433622E-14,33.8305837392638));
#73180=CARTESIAN_POINT('Origin',(27.3746173410614,-0.643204723628853,33.8304567438136));
#73181=CARTESIAN_POINT('Origin',(27.4254160156486,-0.823334400372707,33.8304779343751));
#73182=CARTESIAN_POINT('Origin',(30.,-1.32966554433622E-14,33.8305837392638));
#73183=CARTESIAN_POINT('Origin',(27.433175780606,-0.847207087484101,33.8304567438133));
#73184=CARTESIAN_POINT('Origin',(27.4979506713824,-1.02279586647791,33.8304779343754));
#73185=CARTESIAN_POINT('Origin',(30.,-1.32966554433622E-14,33.8305837392638));
#73186=CARTESIAN_POINT('Origin',(27.5075595450189,-1.04598613791989,33.830456743813));
#73187=CARTESIAN_POINT('Origin',(27.5859112932449,-1.21595145595217,33.830477934375));
#73188=CARTESIAN_POINT('Origin',(30.,-1.32966554433622E-14,33.8305837392638));
#73189=CARTESIAN_POINT('Origin',(27.5973100336554,-1.23831633599182,33.8304567438138));
#73190=CARTESIAN_POINT('Origin',(27.6887555747498,-1.40161030035549,33.8304779343749));
#73191=CARTESIAN_POINT('Origin',(30.,-1.32966554433622E-14,33.8305837392638));
#73192=CARTESIAN_POINT('Origin',(27.7018739049122,-1.42301190206769,33.8304567438132));
#73193=CARTESIAN_POINT('Origin',(27.8058494467036,-1.57862775117429,33.8304779343746));
#73194=CARTESIAN_POINT('Origin',(30.,-1.32966554433622E-14,33.8305837392638));
#73195=CARTESIAN_POINT('Origin',(27.8206064877493,-1.59893412656796,33.8304567438128));
#73196=CARTESIAN_POINT('Origin',(27.9364709864456,-1.74591243696051,33.830477934375));
#73197=CARTESIAN_POINT('Origin',(30.,-1.32966554433622E-14,33.8305837392638));
#73198=CARTESIAN_POINT('Origin',(27.9527757563098,-1.76499839048126,33.8304567438135));
#73199=CARTESIAN_POINT('Origin',(28.0798148687495,-1.90243299199812,33.8304779343753));
#73200=CARTESIAN_POINT('Origin',(30.,-1.32966554433622E-14,33.8305837392638));
#73201=CARTESIAN_POINT('Origin',(28.0975668431045,-1.92018085239454,33.8304567438138));
#73202=CARTESIAN_POINT('Origin',(28.234997330915,-2.04722441501659,33.8304779343752));
#73203=CARTESIAN_POINT('Origin',(30.,-1.32966554433622E-14,33.8305837392638));
#73204=CARTESIAN_POINT('Origin',(28.2540870629355,-2.06352476082575,33.8304567438132));
#73205=CARTESIAN_POINT('Origin',(28.4010616214883,-2.1793940187284,33.8304779343619));
#73206=CARTESIAN_POINT('Origin',(30.,-1.32966554433622E-14,33.8305837392638));
#73207=CARTESIAN_POINT('Origin',(28.4213714165976,-2.19414635291788,33.8304567438138));
#73208=CARTESIAN_POINT('Origin',(28.5769838988107,-2.29812693362319,33.8304779343729));
#73209=CARTESIAN_POINT('Origin',(30.,-1.32966554433622E-14,33.8305837392638));
#73210=CARTESIAN_POINT('Origin',(28.5983885404242,-2.31124030311337,33.8304567438133));
#73211=CARTESIAN_POINT('Origin',(28.7616795436178,-2.40269113175742,33.8304779343754));
#73212=CARTESIAN_POINT('Origin',(30.,-1.32966554433622E-14,33.8305837392638));
#73213=CARTESIAN_POINT('Origin',(28.7840470649819,-2.41408468827727,33.8304567438135));
#73214=CARTESIAN_POINT('Origin',(28.9540098458287,-2.49244194008352,33.8304779343747));
#73215=CARTESIAN_POINT('Origin',(30.,-1.32966554433622E-14,33.8305837392638));
#73216=CARTESIAN_POINT('Origin',(28.9772023437295,-2.50204543857419,33.8304567438141));
#73217=CARTESIAN_POINT('Origin',(29.1527890251654,-2.5668260150294,33.8304779343748));
#73218=CARTESIAN_POINT('Origin',(30.,-1.32966554433622E-14,33.8305837392638));
#73219=CARTESIAN_POINT('Origin',(29.1766635101425,-2.57458024672298,33.8304567438129));
#73220=CARTESIAN_POINT('Origin',(29.3567915418921,-2.62538475403142,33.8304779343725));
#73221=CARTESIAN_POINT('Origin',(30.,-1.32966554433622E-14,33.8305837392638));
#73222=CARTESIAN_POINT('Origin',(29.3812008198029,-2.63124191151983,33.8304567438133));
#73223=CARTESIAN_POINT('Origin',(29.5647596526443,-2.66775712300496,33.8304779343746));
#73224=CARTESIAN_POINT('Origin',(30.,-1.32966554433622E-14,33.8305837392638));
#73225=CARTESIAN_POINT('Origin',(29.589553232181,-2.67168109495555,33.8304567438136));
#73226=CARTESIAN_POINT('Origin',(29.7754111648755,-2.69368188218804,33.8304779343731));
#73227=CARTESIAN_POINT('Origin',(30.,-1.32966554433622E-14,33.8305837392638));
#73228=CARTESIAN_POINT('Origin',(29.8004361853699,-2.69564847601571,33.8304567438137));
#73229=CARTESIAN_POINT('Origin',(29.9874473419542,-2.70299919683539,33.8304779343752));
#73230=CARTESIAN_POINT('Origin',(30.,-1.32966554433622E-14,33.8305837392638));
#73231=CARTESIAN_POINT('Origin',(30.0125495158367,-2.70299628782517,33.8304567438128));
#73232=CARTESIAN_POINT('Origin',(30.199560910346,-2.6956516225925,33.8304779343757));
#73233=CARTESIAN_POINT('Origin',(30.,-1.32966554433622E-14,33.8305837392638));
#73234=CARTESIAN_POINT('Origin',(30.2245854743665,-2.69367922868563,33.8304567438131));
#73235=CARTESIAN_POINT('Origin',(30.4104441193657,-2.67168445969903,33.8304779343754));
#73236=CARTESIAN_POINT('Origin',(30.,-1.32966554433622E-14,33.8305837392638));
#73237=CARTESIAN_POINT('Origin',(30.4352367887642,-2.66775474136125,33.8304567438132));
#73238=CARTESIAN_POINT('Origin',(30.6187968039027,-2.63124547368644,33.8304779343751));
#73239=CARTESIAN_POINT('Origin',(30.,-1.32966554433622E-14,33.8305837392638));
#73240=CARTESIAN_POINT('Origin',(30.6432047236274,-2.6253826589367,33.8304567438126));
#73241=CARTESIAN_POINT('Origin',(30.8233344003726,-2.57458398435223,33.8304779343755));
#73242=CARTESIAN_POINT('Origin',(30.,-1.32966554433622E-14,33.8305837392638));
#73243=CARTESIAN_POINT('Origin',(30.8472070874839,-2.5668242193938,33.8304567438132));
#73244=CARTESIAN_POINT('Origin',(31.0227958664778,-2.50204932861793,33.8304779343756));
#73245=CARTESIAN_POINT('Origin',(30.,-1.32966554433622E-14,33.8305837392638));
#73246=CARTESIAN_POINT('Origin',(31.0459861379201,-2.49244045498134,33.8304567438131));
#73247=CARTESIAN_POINT('Origin',(31.2159514559521,-2.41408870675381,33.8304779343746));
#73248=CARTESIAN_POINT('Origin',(30.,-1.32966554433622E-14,33.8305837392638));
#73249=CARTESIAN_POINT('Origin',(31.2383163359911,-2.402689966344,33.8304567438135));
#73250=CARTESIAN_POINT('Origin',(31.4016103003557,-2.3112444252517,33.8304779343755));
#73251=CARTESIAN_POINT('Origin',(30.,-1.32966554433622E-14,33.8305837392638));
#73252=CARTESIAN_POINT('Origin',(31.4230119020685,-2.29812609508837,33.8304567438136));
#73253=CARTESIAN_POINT('Origin',(31.5786277511746,-2.19415055329817,33.8304779343753));
#73254=CARTESIAN_POINT('Origin',(30.,-1.32966554433622E-14,33.8305837392638));
#73255=CARTESIAN_POINT('Origin',(31.5989341265715,-2.17939351225268,33.8304567438143));
#73256=CARTESIAN_POINT('Origin',(31.7459124369605,-2.06352901355452,33.8304779343751));
#73257=CARTESIAN_POINT('Origin',(30.,-1.32966554433622E-14,33.8305837392638));
#73258=CARTESIAN_POINT('Origin',(31.764998390482,-2.04722424369058,33.8304567438139));
#73259=CARTESIAN_POINT('Origin',(31.9024329919978,-1.92018513124985,33.8304779343751));
#73260=CARTESIAN_POINT('Origin',(30.,-1.32966554433622E-14,33.8305837392638));
#73261=CARTESIAN_POINT('Origin',(31.9201808523926,-1.90243315689474,33.8304567438131));
#73262=CARTESIAN_POINT('Origin',(32.0472244150163,-1.76500266908446,33.830477934375));
#73263=CARTESIAN_POINT('Origin',(30.,-1.32966554433622E-14,33.8305837392638));
#73264=CARTESIAN_POINT('Origin',(32.0635247608254,-1.74591293706441,33.8304567438131));
#73265=CARTESIAN_POINT('Origin',(32.1793940187282,-1.59893837851134,33.8304779343617));
#73266=CARTESIAN_POINT('Origin',(30.,-1.32966554433622E-14,33.8305837392638));
#73267=CARTESIAN_POINT('Origin',(32.1941463529172,-1.57862858340229,33.8304567438136));
#73268=CARTESIAN_POINT('Origin',(32.2981269336233,-1.42301610118952,33.830477934373));
#73269=CARTESIAN_POINT('Origin',(30.,-1.32966554433622E-14,33.8305837392638));
#73270=CARTESIAN_POINT('Origin',(32.311240303114,-1.40161145957583,33.8304567438134));
#73271=CARTESIAN_POINT('Origin',(32.4026911317571,-1.23832045638176,33.8304779343753));
#73272=CARTESIAN_POINT('Origin',(30.,-1.32966554433622E-14,33.8305837392638));
#73273=CARTESIAN_POINT('Origin',(32.4140846882749,-1.21595293501797,33.8304567438127));
#73274=CARTESIAN_POINT('Origin',(32.4924419400838,-1.04599015417152,33.8304779343749));
#73275=CARTESIAN_POINT('Origin',(30.,-1.32966554433622E-14,33.8305837392638));
#73276=CARTESIAN_POINT('Origin',(32.5020454385714,-1.02279765627054,33.8304567438132));
#73277=CARTESIAN_POINT('Origin',(32.56682601503,-0.847210974835106,33.8304779343751));
#73278=CARTESIAN_POINT('Origin',(30.,-1.32966554433622E-14,33.8305837392638));
#73279=CARTESIAN_POINT('Origin',(32.5745802467237,-0.823336489857386,33.8304567438133));
#73280=CARTESIAN_POINT('Origin',(32.6253847540299,-0.643208458106727,33.8304779343718));
#73281=CARTESIAN_POINT('Origin',(30.,-1.32966554433622E-14,33.8305837392638));
#73282=CARTESIAN_POINT('Origin',(32.6312419115182,-0.618799180197391,33.8304567438127));
#73283=CARTESIAN_POINT('Origin',(32.6677571230055,-0.435240347356057,33.830477934375));
#73284=CARTESIAN_POINT('Origin',(30.,-1.32966554433622E-14,33.8305837392638));
#73285=CARTESIAN_POINT('Origin',(32.6716810949544,-0.410446767819313,33.8304567438133));
#73286=CARTESIAN_POINT('Origin',(32.6936818821919,-0.224588835126652,33.8304779343749));
#73287=CARTESIAN_POINT('Origin',(30.,-1.32966554433622E-14,33.8305837392638));
#73288=CARTESIAN_POINT('Origin',(32.6956484760151,-0.199563814630355,33.8304567438134));
#73289=CARTESIAN_POINT('Origin',(32.7029991968333,-0.0125526580448477,33.8304779343743));
#73290=CARTESIAN_POINT('Origin',(30.,-1.32966554433622E-14,33.8305837392638));
#73291=CARTESIAN_POINT('Origin',(32.7029962878262,0.0125495158371826,33.8304567438133));
#73292=CARTESIAN_POINT('Origin',(32.6956516225903,0.19956091034681,33.8304779343749));
#73293=CARTESIAN_POINT('Origin',(30.,-1.32966554433622E-14,33.8305837392638));
#73294=CARTESIAN_POINT('Origin',(32.6936792286859,0.22458547436666,33.8304567438133));
#73295=CARTESIAN_POINT('Origin',(32.6716844596177,0.410444119388619,33.8304779343428));
#73296=CARTESIAN_POINT('Origin',(30.,-1.32966554433622E-14,33.8305837392638));
#73297=CARTESIAN_POINT('Origin',(32.6677547413622,0.435236788764869,33.8304567438136));
#73298=CARTESIAN_POINT('Origin',(32.6312454736863,0.618796803902747,33.8304779343751));
#73299=CARTESIAN_POINT('Origin',(30.,-1.32966554433622E-14,33.8305837392638));
#73300=CARTESIAN_POINT('Origin',(32.625382658939,0.643204723629168,33.8304567438138));
#73301=CARTESIAN_POINT('Origin',(32.5745839843506,0.823334400372804,33.8304779343749));
#73302=CARTESIAN_POINT('Origin',(30.,-1.32966554433622E-14,33.8305837392638));
#73303=CARTESIAN_POINT('Origin',(32.5668242193939,0.847207087484111,33.8304567438133));
#73304=CARTESIAN_POINT('Origin',(32.5020493286164,1.02279586647793,33.830477934375));
#73305=CARTESIAN_POINT('Origin',(30.,-1.32966554433622E-14,33.8305837392638));
#73306=CARTESIAN_POINT('Origin',(32.4924404549818,1.04598613792066,33.8304567438134));
#73307=CARTESIAN_POINT('Origin',(32.4140887067556,1.21595145595219,33.8304779343752));
#73308=CARTESIAN_POINT('Origin',(30.,-1.32966554433622E-14,33.8305837392638));
#73309=CARTESIAN_POINT('Origin',(32.4026899663445,1.2383163359917,33.8304567438137));
#73310=CARTESIAN_POINT('Origin',(32.3112444252326,1.40161030035344,33.830477934368));
#73311=CARTESIAN_POINT('Origin',(30.,-1.32966554433622E-14,33.8305837392638));
#73312=CARTESIAN_POINT('Origin',(32.2981260950878,1.42301190206775,33.8304567438133));
#73313=CARTESIAN_POINT('Origin',(32.1941505532983,1.57862775117468,33.8304779343753));
#73314=CARTESIAN_POINT('Origin',(30.,-1.32966554433622E-14,33.8305837392638));
#73315=CARTESIAN_POINT('Origin',(32.1793935122518,1.59893412656992,33.8304567438136));
#73316=CARTESIAN_POINT('Origin',(32.0635290135536,1.74591243696026,33.8304779343747));
#73317=CARTESIAN_POINT('Origin',(30.,-1.32966554433622E-14,33.8305837392638));
#73318=CARTESIAN_POINT('Origin',(32.04722424369,1.76499839048088,33.8304567438134));
#73319=CARTESIAN_POINT('Origin',(31.9201851312459,1.90243299199643,33.8304779343734));
#73320=CARTESIAN_POINT('Origin',(30.,-1.32966554433622E-14,33.8305837392638));
#73321=CARTESIAN_POINT('Origin',(31.9024331568948,1.92018085239292,33.8304567438132));
#73322=CARTESIAN_POINT('Origin',(31.7650026690842,2.0472244150162,33.8304779343749));
#73323=CARTESIAN_POINT('Origin',(30.,-1.32966554433622E-14,33.8305837392638));
#73324=CARTESIAN_POINT('Origin',(31.7459129370645,2.06352476082576,33.8304567438132));
#73325=CARTESIAN_POINT('Origin',(31.5989383785419,2.17939401874533,33.8304779343753));
#73326=CARTESIAN_POINT('Origin',(30.,-1.32966554433622E-14,33.8305837392638));
#73327=CARTESIAN_POINT('Origin',(31.5786285834019,2.1941463529156,33.830456743813));
#73328=CARTESIAN_POINT('Origin',(31.4230161011941,2.29812693362645,33.8304779343752));
#73329=CARTESIAN_POINT('Origin',(30.,-1.32966554433622E-14,33.8305837392638));
#73330=CARTESIAN_POINT('Origin',(31.4016114595758,2.31124030311394,33.8304567438134));
#73331=CARTESIAN_POINT('Origin',(31.2383204563814,2.40269113175683,33.8304779343751));
#73332=CARTESIAN_POINT('Origin',(30.,-1.32966554433622E-14,33.8305837392638));
#73333=CARTESIAN_POINT('Origin',(31.215952935018,2.41408468827632,33.8304567438131));
#73334=CARTESIAN_POINT('Origin',(31.0459901541714,2.49244194008366,33.8304779343748));
#73335=CARTESIAN_POINT('Origin',(30.,-1.32966554433622E-14,33.8305837392638));
#73336=CARTESIAN_POINT('Origin',(31.0227976562705,2.50204543857161,33.8304567438132));
#73337=CARTESIAN_POINT('Origin',(30.8472109748356,2.56682601503055,33.8304779343754));
#73338=CARTESIAN_POINT('Origin',(30.,-1.32966554433622E-14,33.8305837392638));
#73339=CARTESIAN_POINT('Origin',(30.8233364898573,2.574580246724,33.8304567438134));
#73340=CARTESIAN_POINT('Origin',(30.6432084580721,2.62538475398616,33.8304779343503));
#73341=CARTESIAN_POINT('Origin',(30.,-1.32966554433622E-14,33.8305837392638));
#73342=CARTESIAN_POINT('Origin',(30.6187991801972,2.63124191151918,33.8304567438131));
#73343=CARTESIAN_POINT('Origin',(30.4352403473569,2.66775712300684,33.8304779343755));
#73344=CARTESIAN_POINT('Origin',(30.,-1.32966554433622E-14,33.8305837392638));
#73345=CARTESIAN_POINT('Origin',(27.5973088682432,1.23832045638137,33.8304779343751));
#73346=CARTESIAN_POINT('Origin',(27.6887596968862,1.40161145957579,33.8304567438134));
#73347=CARTESIAN_POINT('Origin',(30.,-1.32966554433622E-14,33.8305837392638));
#73348=CARTESIAN_POINT('Origin',(27.7018730663741,1.4230161011934,33.8304779343749));
#73349=CARTESIAN_POINT('Origin',(27.8058536470835,1.57862858340213,33.8304567438133));
#73350=CARTESIAN_POINT('Origin',(30.,-1.32966554433622E-14,33.8305837392638));
#73351=CARTESIAN_POINT('Origin',(27.8206059812548,1.59893837854177,33.8304779343751));
#73352=CARTESIAN_POINT('Origin',(27.9364752391745,1.7459129370644,33.8304567438132));
#73353=CARTESIAN_POINT('Origin',(30.,-1.32966554433622E-14,33.8305837392638));
#73354=CARTESIAN_POINT('Origin',(27.952775584984,1.76500266908388,33.8304779343747));
#73355=CARTESIAN_POINT('Origin',(28.0798191476065,1.90243315689505,33.8304567438134));
#73356=CARTESIAN_POINT('Origin',(30.,-1.32966554433622E-14,33.8305837392638));
#73357=CARTESIAN_POINT('Origin',(28.0975670080041,1.92018513124447,33.8304779343728));
#73358=CARTESIAN_POINT('Origin',(28.23500160952,2.04722424368963,33.830456743813));
#73359=CARTESIAN_POINT('Origin',(30.,-1.32966554433622E-14,33.8305837392638));
#73360=CARTESIAN_POINT('Origin',(28.2540875630398,2.06352901355343,33.8304779343746));
#73361=CARTESIAN_POINT('Origin',(28.4010658734306,2.17939351225149,33.8304567438134));
#73362=CARTESIAN_POINT('Origin',(30.,-1.32966554433622E-14,33.8305837392638));
#73363=CARTESIAN_POINT('Origin',(28.4213722488255,2.19415055329726,33.8304779343749));
#73364=CARTESIAN_POINT('Origin',(28.5769880979325,2.29812609508769,33.8304567438131));
#73365=CARTESIAN_POINT('Origin',(30.,-1.32966554433622E-14,33.8305837392638));
#73366=CARTESIAN_POINT('Origin',(28.5983896996467,2.31124442523142,33.8304779343677));
#73367=CARTESIAN_POINT('Origin',(28.7616836640084,2.40268996634441,33.8304567438137));
#73368=CARTESIAN_POINT('Origin',(30.,-1.32966554433622E-14,33.8305837392638));
#73369=CARTESIAN_POINT('Origin',(28.7840485440478,2.41408870675589,33.8304779343753));
#73370=CARTESIAN_POINT('Origin',(28.9540138620795,2.49244045498167,33.8304567438133));
#73371=CARTESIAN_POINT('Origin',(30.,-1.32966554433622E-14,33.8305837392638));
#73372=CARTESIAN_POINT('Origin',(28.9772041335221,2.50204932861683,33.8304779343752));
#73373=CARTESIAN_POINT('Origin',(29.1527929125161,2.56682421939371,33.8304567438132));
#73374=CARTESIAN_POINT('Origin',(30.,-1.32966554433622E-14,33.8305837392638));
#73375=CARTESIAN_POINT('Origin',(29.1766655996273,2.57458398435145,33.8304779343752));
#73376=CARTESIAN_POINT('Origin',(29.3567952763716,2.62538265893797,33.8304567438133));
#73377=CARTESIAN_POINT('Origin',(30.,-1.32966554433622E-14,33.8305837392638));
#73378=CARTESIAN_POINT('Origin',(29.3812031960975,2.63124547368767,33.8304779343756));
#73379=CARTESIAN_POINT('Origin',(29.5647632112354,2.66775474136179,33.8304567438135));
#73380=CARTESIAN_POINT('Origin',(30.,-1.32966554433622E-14,33.8305837392638));
#73381=CARTESIAN_POINT('Origin',(29.5895558806117,2.67168445961877,33.8304779343432));
#73382=CARTESIAN_POINT('Origin',(29.775414525633,2.69367922868643,33.8304567438135));
#73383=CARTESIAN_POINT('Origin',(30.,-1.32966554433622E-14,33.8305837392638));
#73384=CARTESIAN_POINT('Origin',(29.8004390896529,2.69565162258947,33.8304779343745));
#73385=CARTESIAN_POINT('Origin',(29.9874504841622,2.70299628782743,33.8304567438137));
#73386=CARTESIAN_POINT('Origin',(30.,-1.32966554433622E-14,33.8305837392638));
#73387=CARTESIAN_POINT('Origin',(30.4104467678198,2.67168109495229,33.8304567438124));
#73388=CARTESIAN_POINT('Origin',(30.2245888351268,2.69368188219228,33.830477934375));
#73389=CARTESIAN_POINT('Origin',(30.,1.17524047358083,16.));
#73390=CARTESIAN_POINT('Origin',(30.,2.60624999999999,31.));
#73391=CARTESIAN_POINT('Origin',(30.,-1.32966554433622E-14,31.6569162607362));
#73392=CARTESIAN_POINT('',(30.1823521510466,2.74394746542433,31.6569162607362));
#73393=CARTESIAN_POINT('Origin',(30.1995609103462,2.69565162259179,31.6570220656244));
#73394=CARTESIAN_POINT('',(30.03349761664,2.74979597600974,31.6569162607362));
#73395=CARTESIAN_POINT('Origin',(30.0125495158372,2.70299628782596,31.6570432561867));
#73396=CARTESIAN_POINT('Origin',(30.,-1.32966554433622E-14,31.6569162607362));
#73397=CARTESIAN_POINT('Origin',(30.,-1.32966554433622E-14,16.));
#73398=CARTESIAN_POINT('',(30.1823521510466,2.74394746542434,33.8305837392638));
#73399=CARTESIAN_POINT('',(30.1823521510466,2.74394746542433,16.));
#73400=CARTESIAN_POINT('',(30.03349761664,2.74979597600975,33.8305837392638));
#73401=CARTESIAN_POINT('',(30.03349761664,2.74979597600974,16.));
#73402=CARTESIAN_POINT('Origin',(30.,-1.32966554433622E-14,33.8305837392638));
#73403=CARTESIAN_POINT('Origin',(30.,-1.32966554433622E-14,33.8305837392638));
#73404=CARTESIAN_POINT('Origin',(30.1995638146302,2.69564847601544,33.8304567438135));
#73405=CARTESIAN_POINT('Origin',(30.0125526580447,2.70299919683307,33.8304779343742));
#73406=CARTESIAN_POINT('Origin',(30.,-1.32966554433622E-14,34.));
#73407=CARTESIAN_POINT('Origin',(30.,-1.32966554433622E-14,32.5));
#73408=CARTESIAN_POINT('',(30.,-1.44337567297407,32.5));
#73409=CARTESIAN_POINT('',(31.25,-0.72168783648704,32.5));
#73410=CARTESIAN_POINT('',(30.,-1.44337567297407,32.5));
#73411=CARTESIAN_POINT('',(31.25,0.721687836487017,32.5));
#73412=CARTESIAN_POINT('',(31.25,-0.72168783648704,32.5));
#73413=CARTESIAN_POINT('',(30.,1.44337567297405,32.5));
#73414=CARTESIAN_POINT('',(31.25,0.721687836487017,32.5));
#73415=CARTESIAN_POINT('',(28.75,0.721687836487017,32.5));
#73416=CARTESIAN_POINT('',(30.,1.44337567297405,32.5));
#73417=CARTESIAN_POINT('',(28.75,-0.721687836487044,32.5));
#73418=CARTESIAN_POINT('',(28.75,0.721687836487017,32.5));
#73419=CARTESIAN_POINT('',(28.75,-0.721687836487044,32.5));
#73420=CARTESIAN_POINT('Origin',(31.25,-0.72168783648704,32.5));
#73421=CARTESIAN_POINT('',(31.25,-0.72168783648704,32.5));
#73422=CARTESIAN_POINT('',(31.25,0.721687836487017,32.5));
#73423=CARTESIAN_POINT('Origin',(31.25,0.721687836487017,32.5));
#73424=CARTESIAN_POINT('',(30.,1.44337567297405,32.5));
#73425=CARTESIAN_POINT('Origin',(30.,1.44337567297405,32.5));
#73426=CARTESIAN_POINT('',(28.75,0.721687836487017,32.5));
#73427=CARTESIAN_POINT('Origin',(28.75,0.721687836487017,32.5));
#73428=CARTESIAN_POINT('',(28.75,-0.721687836487044,32.5));
#73429=CARTESIAN_POINT('Origin',(28.75,-0.721687836487044,32.5));
#73430=CARTESIAN_POINT('',(30.,-1.44337567297407,32.5));
#73431=CARTESIAN_POINT('Origin',(30.,-1.44337567297407,32.5));
#73432=CARTESIAN_POINT('Ctrl Pts',(30.,1.17523237272422,15.7500046770317));
#73433=CARTESIAN_POINT('Ctrl Pts',(29.3214792732473,1.17523237272422,15.7916713436984));
#73434=CARTESIAN_POINT('Ctrl Pts',(28.9822189098709,0.587616186362105,15.8333380103651));
#73435=CARTESIAN_POINT('Ctrl Pts',(28.6429585464946,-1.32141491426617E-14,
15.8750046770317));
#73436=CARTESIAN_POINT('Ctrl Pts',(28.9822189098709,-0.587616186362132,
15.9166713436984));
#73437=CARTESIAN_POINT('Ctrl Pts',(29.3214792732473,-1.17523237272425,15.9583380103651));
#73438=CARTESIAN_POINT('Ctrl Pts',(30.,-1.17523237272425,16.0000046770317));
#73439=CARTESIAN_POINT('Ctrl Pts',(30.6785207267527,-1.17523237272425,16.0416713436984));
#73440=CARTESIAN_POINT('Ctrl Pts',(31.017781090129,-0.587616186362132,16.0833380103651));
#73441=CARTESIAN_POINT('Ctrl Pts',(31.3570414535054,-1.35453513912972E-14,
16.1250046770317));
#73442=CARTESIAN_POINT('Ctrl Pts',(31.017781090129,0.587616186362104,16.1666713436984));
#73443=CARTESIAN_POINT('Ctrl Pts',(30.6785207267527,1.17523237272422,16.2083380103651));
#73444=CARTESIAN_POINT('Ctrl Pts',(30.,1.17523237272422,16.2500046770317));
#73445=CARTESIAN_POINT('Ctrl Pts',(29.3214792732473,1.17523237272422,16.2916713436984));
#73446=CARTESIAN_POINT('Ctrl Pts',(28.9822189098709,0.587616186362105,16.3333380103651));
#73447=CARTESIAN_POINT('Ctrl Pts',(28.6429585464946,-1.32141491426617E-14,
16.3750046770317));
#73448=CARTESIAN_POINT('Ctrl Pts',(28.9822189098709,-0.587616186362132,
16.4166713436984));
#73449=CARTESIAN_POINT('Ctrl Pts',(29.3214792732473,-1.17523237272425,16.4583380103651));
#73450=CARTESIAN_POINT('Ctrl Pts',(30.,-1.17523237272425,16.5000046770317));
#73451=CARTESIAN_POINT('Ctrl Pts',(30.6785207267527,-1.17523237272425,16.5416713436984));
#73452=CARTESIAN_POINT('Ctrl Pts',(31.017781090129,-0.587616186362132,16.5833380103651));
#73453=CARTESIAN_POINT('Ctrl Pts',(31.3570414535054,-1.35453513912972E-14,
16.6250046770317));
#73454=CARTESIAN_POINT('Ctrl Pts',(31.017781090129,0.587616186362104,16.6666713436984));
#73455=CARTESIAN_POINT('Ctrl Pts',(30.6785207267527,1.17523237272422,16.7083380103651));
#73456=CARTESIAN_POINT('Ctrl Pts',(30.,1.17523237272422,16.7500046770317));
#73457=CARTESIAN_POINT('Ctrl Pts',(29.3214792732473,1.17523237272422,16.7916713436984));
#73458=CARTESIAN_POINT('Ctrl Pts',(28.9822189098709,0.587616186362105,16.8333380103651));
#73459=CARTESIAN_POINT('Ctrl Pts',(28.6429585464946,-1.32141491426617E-14,
16.8750046770317));
#73460=CARTESIAN_POINT('Ctrl Pts',(28.9822189098709,-0.587616186362132,
16.9166713436984));
#73461=CARTESIAN_POINT('Ctrl Pts',(29.3214792732473,-1.17523237272425,16.9583380103651));
#73462=CARTESIAN_POINT('Ctrl Pts',(30.,-1.17523237272425,17.0000046770317));
#73463=CARTESIAN_POINT('Ctrl Pts',(30.6785207267527,-1.17523237272425,17.0416713436984));
#73464=CARTESIAN_POINT('Ctrl Pts',(31.017781090129,-0.587616186362132,17.0833380103651));
#73465=CARTESIAN_POINT('Ctrl Pts',(31.3570414535054,-1.35453513912972E-14,
17.1250046770317));
#73466=CARTESIAN_POINT('Ctrl Pts',(31.017781090129,0.587616186362104,17.1666713436984));
#73467=CARTESIAN_POINT('Ctrl Pts',(30.6785207267527,1.17523237272422,17.2083380103651));
#73468=CARTESIAN_POINT('Ctrl Pts',(30.,1.17523237272422,17.2500046770317));
#73469=CARTESIAN_POINT('Ctrl Pts',(29.3214792732473,1.17523237272422,17.2916713436984));
#73470=CARTESIAN_POINT('Ctrl Pts',(28.9822189098709,0.587616186362105,17.3333380103651));
#73471=CARTESIAN_POINT('Ctrl Pts',(28.6429585464946,-1.32141491426617E-14,
17.3750046770317));
#73472=CARTESIAN_POINT('Ctrl Pts',(28.9822189098709,-0.587616186362132,
17.4166713436984));
#73473=CARTESIAN_POINT('Ctrl Pts',(29.3214792732473,-1.17523237272425,17.4583380103651));
#73474=CARTESIAN_POINT('Ctrl Pts',(30.,-1.17523237272425,17.5000046770317));
#73475=CARTESIAN_POINT('Ctrl Pts',(30.6785207267527,-1.17523237272425,17.5416713436984));
#73476=CARTESIAN_POINT('Ctrl Pts',(31.017781090129,-0.587616186362132,17.5833380103651));
#73477=CARTESIAN_POINT('Ctrl Pts',(31.3570414535054,-1.35453513912972E-14,
17.6250046770317));
#73478=CARTESIAN_POINT('Ctrl Pts',(31.017781090129,0.587616186362104,17.6666713436984));
#73479=CARTESIAN_POINT('Ctrl Pts',(30.6785207267527,1.17523237272422,17.7083380103651));
#73480=CARTESIAN_POINT('Ctrl Pts',(30.,1.17523237272422,17.7500046770317));
#73481=CARTESIAN_POINT('Ctrl Pts',(29.3214792732473,1.17523237272422,17.7916713436984));
#73482=CARTESIAN_POINT('Ctrl Pts',(28.9822189098709,0.587616186362105,17.8333380103651));
#73483=CARTESIAN_POINT('Ctrl Pts',(28.6429585464946,-1.32141491426617E-14,
17.8750046770317));
#73484=CARTESIAN_POINT('Ctrl Pts',(28.9822189098709,-0.587616186362132,
17.9166713436984));
#73485=CARTESIAN_POINT('Ctrl Pts',(29.3214792732473,-1.17523237272425,17.9583380103651));
#73486=CARTESIAN_POINT('Ctrl Pts',(30.,-1.17523237272425,18.0000046770317));
#73487=CARTESIAN_POINT('Ctrl Pts',(30.6785207267527,-1.17523237272425,18.0416713436984));
#73488=CARTESIAN_POINT('Ctrl Pts',(31.017781090129,-0.587616186362132,18.0833380103651));
#73489=CARTESIAN_POINT('Ctrl Pts',(31.3570414535054,-1.35453513912972E-14,
18.1250046770317));
#73490=CARTESIAN_POINT('Ctrl Pts',(31.017781090129,0.587616186362104,18.1666713436984));
#73491=CARTESIAN_POINT('Ctrl Pts',(30.6785207267527,1.17523237272422,18.2083380103651));
#73492=CARTESIAN_POINT('Ctrl Pts',(30.,1.17523237272422,18.2500046770317));
#73493=CARTESIAN_POINT('Ctrl Pts',(29.3214792732473,1.17523237272422,18.2916713436984));
#73494=CARTESIAN_POINT('Ctrl Pts',(28.9822189098709,0.587616186362105,18.3333380103651));
#73495=CARTESIAN_POINT('Ctrl Pts',(28.6429585464946,-1.32141491426617E-14,
18.3750046770317));
#73496=CARTESIAN_POINT('Ctrl Pts',(28.9822189098709,-0.587616186362132,
18.4166713436984));
#73497=CARTESIAN_POINT('Ctrl Pts',(29.3214792732473,-1.17523237272425,18.4583380103651));
#73498=CARTESIAN_POINT('Ctrl Pts',(30.,-1.17523237272425,18.5000046770317));
#73499=CARTESIAN_POINT('Ctrl Pts',(30.6785207267527,-1.17523237272425,18.5416713436984));
#73500=CARTESIAN_POINT('Ctrl Pts',(31.017781090129,-0.587616186362132,18.5833380103651));
#73501=CARTESIAN_POINT('Ctrl Pts',(31.3570414535054,-1.35453513912972E-14,
18.6250046770317));
#73502=CARTESIAN_POINT('Ctrl Pts',(31.017781090129,0.587616186362104,18.6666713436984));
#73503=CARTESIAN_POINT('Ctrl Pts',(30.6785207267527,1.17523237272422,18.7083380103651));
#73504=CARTESIAN_POINT('Ctrl Pts',(30.,1.17523237272422,18.7500046770317));
#73505=CARTESIAN_POINT('Ctrl Pts',(29.3214792732473,1.17523237272422,18.7916713436984));
#73506=CARTESIAN_POINT('Ctrl Pts',(28.9822189098709,0.587616186362105,18.8333380103651));
#73507=CARTESIAN_POINT('Ctrl Pts',(28.6429585464946,-1.32141491426617E-14,
18.8750046770317));
#73508=CARTESIAN_POINT('Ctrl Pts',(28.9822189098709,-0.587616186362132,
18.9166713436984));
#73509=CARTESIAN_POINT('Ctrl Pts',(29.3214792732473,-1.17523237272425,18.9583380103651));
#73510=CARTESIAN_POINT('Ctrl Pts',(30.,-1.17523237272425,19.0000046770317));
#73511=CARTESIAN_POINT('Ctrl Pts',(30.6785207267527,-1.17523237272425,19.0416713436984));
#73512=CARTESIAN_POINT('Ctrl Pts',(31.017781090129,-0.587616186362132,19.0833380103651));
#73513=CARTESIAN_POINT('Ctrl Pts',(31.3570414535054,-1.35453513912972E-14,
19.1250046770317));
#73514=CARTESIAN_POINT('Ctrl Pts',(31.017781090129,0.587616186362104,19.1666713436984));
#73515=CARTESIAN_POINT('Ctrl Pts',(30.6785207267527,1.17523237272422,19.2083380103651));
#73516=CARTESIAN_POINT('Ctrl Pts',(30.,1.17523237272422,19.2500046770317));
#73517=CARTESIAN_POINT('Ctrl Pts',(29.3214792732473,1.17523237272422,19.2916713436984));
#73518=CARTESIAN_POINT('Ctrl Pts',(28.9822189098709,0.587616186362105,19.3333380103651));
#73519=CARTESIAN_POINT('Ctrl Pts',(28.6429585464946,-1.32141491426617E-14,
19.3750046770317));
#73520=CARTESIAN_POINT('Ctrl Pts',(28.9822189098709,-0.587616186362132,
19.4166713436984));
#73521=CARTESIAN_POINT('Ctrl Pts',(29.3214792732473,-1.17523237272425,19.4583380103651));
#73522=CARTESIAN_POINT('Ctrl Pts',(30.,-1.17523237272425,19.5000046770317));
#73523=CARTESIAN_POINT('Ctrl Pts',(30.6785207267527,-1.17523237272425,19.5416713436984));
#73524=CARTESIAN_POINT('Ctrl Pts',(31.017781090129,-0.587616186362132,19.5833380103651));
#73525=CARTESIAN_POINT('Ctrl Pts',(31.3570414535054,-1.35453513912972E-14,
19.6250046770317));
#73526=CARTESIAN_POINT('Ctrl Pts',(31.017781090129,0.587616186362104,19.6666713436984));
#73527=CARTESIAN_POINT('Ctrl Pts',(30.6785207267527,1.17523237272422,19.7083380103651));
#73528=CARTESIAN_POINT('Ctrl Pts',(30.,1.17523237272422,19.7500046770317));
#73529=CARTESIAN_POINT('Ctrl Pts',(29.3214792732473,1.17523237272422,19.7916713436984));
#73530=CARTESIAN_POINT('Ctrl Pts',(28.9822189098709,0.587616186362105,19.8333380103651));
#73531=CARTESIAN_POINT('Ctrl Pts',(28.6429585464946,-1.32141491426617E-14,
19.8750046770317));
#73532=CARTESIAN_POINT('Ctrl Pts',(28.9822189098709,-0.587616186362132,
19.9166713436984));
#73533=CARTESIAN_POINT('Ctrl Pts',(29.3214792732473,-1.17523237272425,19.9583380103651));
#73534=CARTESIAN_POINT('Ctrl Pts',(30.,-1.17523237272425,20.0000046770317));
#73535=CARTESIAN_POINT('Ctrl Pts',(30.6785207267527,-1.17523237272425,20.0416713436984));
#73536=CARTESIAN_POINT('Ctrl Pts',(31.017781090129,-0.587616186362132,20.0833380103651));
#73537=CARTESIAN_POINT('Ctrl Pts',(31.3570414535054,-1.35453513912972E-14,
20.1250046770317));
#73538=CARTESIAN_POINT('Ctrl Pts',(31.017781090129,0.587616186362104,20.1666713436984));
#73539=CARTESIAN_POINT('Ctrl Pts',(30.6785207267527,1.17523237272422,20.2083380103651));
#73540=CARTESIAN_POINT('Ctrl Pts',(30.,1.17523237272422,20.2500046770317));
#73541=CARTESIAN_POINT('Ctrl Pts',(29.3214792732473,1.17523237272422,20.2916713436984));
#73542=CARTESIAN_POINT('Ctrl Pts',(28.9822189098709,0.587616186362105,20.3333380103651));
#73543=CARTESIAN_POINT('Ctrl Pts',(28.6429585464946,-1.32141491426617E-14,
20.3750046770317));
#73544=CARTESIAN_POINT('Ctrl Pts',(28.9822189098709,-0.587616186362132,
20.4166713436984));
#73545=CARTESIAN_POINT('Ctrl Pts',(29.3214792732473,-1.17523237272425,20.4583380103651));
#73546=CARTESIAN_POINT('Ctrl Pts',(30.,-1.17523237272425,20.5000046770317));
#73547=CARTESIAN_POINT('Ctrl Pts',(30.6785207267527,-1.17523237272425,20.5416713436984));
#73548=CARTESIAN_POINT('Ctrl Pts',(31.017781090129,-0.587616186362132,20.5833380103651));
#73549=CARTESIAN_POINT('Ctrl Pts',(31.3570414535054,-1.35453513912972E-14,
20.6250046770317));
#73550=CARTESIAN_POINT('Ctrl Pts',(31.017781090129,0.587616186362104,20.6666713436984));
#73551=CARTESIAN_POINT('Ctrl Pts',(30.6785207267527,1.17523237272422,20.7083380103651));
#73552=CARTESIAN_POINT('Ctrl Pts',(30.,1.17523237272422,20.7500046770317));
#73553=CARTESIAN_POINT('Ctrl Pts',(29.3214792732473,1.17523237272422,20.7916713436984));
#73554=CARTESIAN_POINT('Ctrl Pts',(28.9822189098709,0.587616186362105,20.8333380103651));
#73555=CARTESIAN_POINT('Ctrl Pts',(28.6429585464946,-1.32141491426617E-14,
20.8750046770317));
#73556=CARTESIAN_POINT('Ctrl Pts',(28.9822189098709,-0.587616186362132,
20.9166713436984));
#73557=CARTESIAN_POINT('Ctrl Pts',(29.3214792732473,-1.17523237272425,20.9583380103651));
#73558=CARTESIAN_POINT('Ctrl Pts',(30.,-1.17523237272425,21.0000046770317));
#73559=CARTESIAN_POINT('Ctrl Pts',(30.6785207267527,-1.17523237272425,21.0416713436984));
#73560=CARTESIAN_POINT('Ctrl Pts',(31.017781090129,-0.587616186362132,21.0833380103651));
#73561=CARTESIAN_POINT('Ctrl Pts',(31.3570414535054,-1.35453513912972E-14,
21.1250046770317));
#73562=CARTESIAN_POINT('Ctrl Pts',(31.017781090129,0.587616186362104,21.1666713436984));
#73563=CARTESIAN_POINT('Ctrl Pts',(30.6785207267527,1.17523237272422,21.2083380103651));
#73564=CARTESIAN_POINT('Ctrl Pts',(30.,1.17523237272422,21.2500046770317));
#73565=CARTESIAN_POINT('Ctrl Pts',(29.3214792732473,1.17523237272422,21.2916713436984));
#73566=CARTESIAN_POINT('Ctrl Pts',(28.9822189098709,0.587616186362105,21.3333380103651));
#73567=CARTESIAN_POINT('Ctrl Pts',(28.6429585464946,-1.32141491426617E-14,
21.3750046770317));
#73568=CARTESIAN_POINT('Ctrl Pts',(28.9822189098709,-0.587616186362132,
21.4166713436984));
#73569=CARTESIAN_POINT('Ctrl Pts',(29.3214792732473,-1.17523237272425,21.4583380103651));
#73570=CARTESIAN_POINT('Ctrl Pts',(30.,-1.17523237272425,21.5000046770317));
#73571=CARTESIAN_POINT('Ctrl Pts',(30.6785207267527,-1.17523237272425,21.5416713436984));
#73572=CARTESIAN_POINT('Ctrl Pts',(31.017781090129,-0.587616186362132,21.5833380103651));
#73573=CARTESIAN_POINT('Ctrl Pts',(31.3570414535054,-1.35453513912972E-14,
21.6250046770317));
#73574=CARTESIAN_POINT('Ctrl Pts',(31.017781090129,0.587616186362104,21.6666713436984));
#73575=CARTESIAN_POINT('Ctrl Pts',(30.6785207267527,1.17523237272422,21.7083380103651));
#73576=CARTESIAN_POINT('Ctrl Pts',(30.,1.17523237272422,21.7500046770317));
#73577=CARTESIAN_POINT('Ctrl Pts',(29.3214792732473,1.17523237272422,21.7916713436984));
#73578=CARTESIAN_POINT('Ctrl Pts',(28.9822189098709,0.587616186362105,21.8333380103651));
#73579=CARTESIAN_POINT('Ctrl Pts',(28.6429585464946,-1.32141491426617E-14,
21.8750046770317));
#73580=CARTESIAN_POINT('Ctrl Pts',(28.9822189098709,-0.587616186362132,
21.9166713436984));
#73581=CARTESIAN_POINT('Ctrl Pts',(29.3214792732473,-1.17523237272425,21.9583380103651));
#73582=CARTESIAN_POINT('Ctrl Pts',(30.,-1.17523237272425,22.0000046770317));
#73583=CARTESIAN_POINT('Ctrl Pts',(30.6785207267527,-1.17523237272425,22.0416713436984));
#73584=CARTESIAN_POINT('Ctrl Pts',(31.017781090129,-0.587616186362132,22.0833380103651));
#73585=CARTESIAN_POINT('Ctrl Pts',(31.3570414535054,-1.35453513912972E-14,
22.1250046770317));
#73586=CARTESIAN_POINT('Ctrl Pts',(31.017781090129,0.587616186362104,22.1666713436984));
#73587=CARTESIAN_POINT('Ctrl Pts',(30.6785207267527,1.17523237272422,22.2083380103651));
#73588=CARTESIAN_POINT('Ctrl Pts',(30.,1.17523237272422,22.2500046770317));
#73589=CARTESIAN_POINT('Ctrl Pts',(29.3214792732473,1.17523237272422,22.2916713436984));
#73590=CARTESIAN_POINT('Ctrl Pts',(28.9822189098709,0.587616186362105,22.3333380103651));
#73591=CARTESIAN_POINT('Ctrl Pts',(28.6429585464946,-1.32141491426617E-14,
22.3750046770317));
#73592=CARTESIAN_POINT('Ctrl Pts',(28.9822189098709,-0.587616186362132,
22.4166713436984));
#73593=CARTESIAN_POINT('Ctrl Pts',(29.3214792732473,-1.17523237272425,22.4583380103651));
#73594=CARTESIAN_POINT('Ctrl Pts',(30.,-1.17523237272425,22.5000046770317));
#73595=CARTESIAN_POINT('Ctrl Pts',(30.6785207267527,-1.17523237272425,22.5416713436984));
#73596=CARTESIAN_POINT('Ctrl Pts',(31.017781090129,-0.587616186362132,22.5833380103651));
#73597=CARTESIAN_POINT('Ctrl Pts',(31.3570414535054,-1.35453513912972E-14,
22.6250046770317));
#73598=CARTESIAN_POINT('Ctrl Pts',(31.017781090129,0.587616186362104,22.6666713436984));
#73599=CARTESIAN_POINT('Ctrl Pts',(30.6785207267527,1.17523237272422,22.7083380103651));
#73600=CARTESIAN_POINT('Ctrl Pts',(30.,1.17523237272422,22.7500046770317));
#73601=CARTESIAN_POINT('Ctrl Pts',(29.3214792732473,1.17523237272422,22.7916713436984));
#73602=CARTESIAN_POINT('Ctrl Pts',(28.9822189098709,0.587616186362105,22.8333380103651));
#73603=CARTESIAN_POINT('Ctrl Pts',(28.6429585464946,-1.32141491426617E-14,
22.8750046770317));
#73604=CARTESIAN_POINT('Ctrl Pts',(28.9822189098709,-0.587616186362132,
22.9166713436984));
#73605=CARTESIAN_POINT('Ctrl Pts',(29.3214792732473,-1.17523237272425,22.9583380103651));
#73606=CARTESIAN_POINT('Ctrl Pts',(30.,-1.17523237272425,23.0000046770317));
#73607=CARTESIAN_POINT('Ctrl Pts',(30.6785207267527,-1.17523237272425,23.0416713436984));
#73608=CARTESIAN_POINT('Ctrl Pts',(31.017781090129,-0.587616186362132,23.0833380103651));
#73609=CARTESIAN_POINT('Ctrl Pts',(31.3570414535054,-1.35453513912972E-14,
23.1250046770317));
#73610=CARTESIAN_POINT('Ctrl Pts',(31.017781090129,0.587616186362104,23.1666713436984));
#73611=CARTESIAN_POINT('Ctrl Pts',(30.6785207267527,1.17523237272422,23.2083380103651));
#73612=CARTESIAN_POINT('Ctrl Pts',(30.,1.17523237272422,23.2500046770317));
#73613=CARTESIAN_POINT('Ctrl Pts',(29.3214792732473,1.17523237272422,23.2916713436984));
#73614=CARTESIAN_POINT('Ctrl Pts',(28.9822189098709,0.587616186362105,23.3333380103651));
#73615=CARTESIAN_POINT('Ctrl Pts',(28.6429585464946,-1.32141491426617E-14,
23.3750046770317));
#73616=CARTESIAN_POINT('Ctrl Pts',(28.9822189098709,-0.587616186362132,
23.4166713436984));
#73617=CARTESIAN_POINT('Ctrl Pts',(29.3214792732473,-1.17523237272425,23.4583380103651));
#73618=CARTESIAN_POINT('Ctrl Pts',(30.,-1.17523237272425,23.5000046770317));
#73619=CARTESIAN_POINT('Ctrl Pts',(30.6785207267527,-1.17523237272425,23.5416713436984));
#73620=CARTESIAN_POINT('Ctrl Pts',(31.017781090129,-0.587616186362132,23.5833380103651));
#73621=CARTESIAN_POINT('Ctrl Pts',(31.3570414535054,-1.35453513912972E-14,
23.6250046770317));
#73622=CARTESIAN_POINT('Ctrl Pts',(31.017781090129,0.587616186362104,23.6666713436984));
#73623=CARTESIAN_POINT('Ctrl Pts',(30.6785207267527,1.17523237272422,23.7083380103651));
#73624=CARTESIAN_POINT('Ctrl Pts',(30.,1.17523237272422,23.7500046770317));
#73625=CARTESIAN_POINT('Ctrl Pts',(29.3214792732473,1.17523237272422,23.7916713436984));
#73626=CARTESIAN_POINT('Ctrl Pts',(28.9822189098709,0.587616186362105,23.8333380103651));
#73627=CARTESIAN_POINT('Ctrl Pts',(28.6429585464946,-1.32141491426617E-14,
23.8750046770317));
#73628=CARTESIAN_POINT('Ctrl Pts',(28.9822189098709,-0.587616186362132,
23.9166713436984));
#73629=CARTESIAN_POINT('Ctrl Pts',(29.3214792732473,-1.17523237272425,23.9583380103651));
#73630=CARTESIAN_POINT('Ctrl Pts',(30.,-1.17523237272425,24.0000046770317));
#73631=CARTESIAN_POINT('Ctrl Pts',(30.6785207267527,-1.17523237272425,24.0416713436984));
#73632=CARTESIAN_POINT('Ctrl Pts',(31.017781090129,-0.587616186362132,24.0833380103651));
#73633=CARTESIAN_POINT('Ctrl Pts',(31.3570414535054,-1.35453513912972E-14,
24.1250046770317));
#73634=CARTESIAN_POINT('Ctrl Pts',(31.017781090129,0.587616186362104,24.1666713436984));
#73635=CARTESIAN_POINT('Ctrl Pts',(30.6785207267527,1.17523237272422,24.2083380103651));
#73636=CARTESIAN_POINT('Ctrl Pts',(30.,1.17523237272422,24.2500046770317));
#73637=CARTESIAN_POINT('Ctrl Pts',(29.3214792732473,1.17523237272422,24.2916713436984));
#73638=CARTESIAN_POINT('Ctrl Pts',(28.9822189098709,0.587616186362105,24.3333380103651));
#73639=CARTESIAN_POINT('Ctrl Pts',(28.6429585464946,-1.32141491426617E-14,
24.3750046770317));
#73640=CARTESIAN_POINT('Ctrl Pts',(28.9822189098709,-0.587616186362132,
24.4166713436984));
#73641=CARTESIAN_POINT('Ctrl Pts',(29.3214792732473,-1.17523237272425,24.4583380103651));
#73642=CARTESIAN_POINT('Ctrl Pts',(30.,-1.17523237272425,24.5000046770317));
#73643=CARTESIAN_POINT('Ctrl Pts',(30.6785207267527,-1.17523237272425,24.5416713436984));
#73644=CARTESIAN_POINT('Ctrl Pts',(31.017781090129,-0.587616186362132,24.5833380103651));
#73645=CARTESIAN_POINT('Ctrl Pts',(31.3570414535054,-1.35453513912972E-14,
24.6250046770317));
#73646=CARTESIAN_POINT('Ctrl Pts',(31.017781090129,0.587616186362104,24.6666713436984));
#73647=CARTESIAN_POINT('Ctrl Pts',(30.6785207267527,1.17523237272422,24.7083380103651));
#73648=CARTESIAN_POINT('Ctrl Pts',(30.,1.17523237272422,24.7500046770317));
#73649=CARTESIAN_POINT('Ctrl Pts',(29.3214792732473,1.17523237272422,24.7916713436984));
#73650=CARTESIAN_POINT('Ctrl Pts',(28.9822189098709,0.587616186362105,24.8333380103651));
#73651=CARTESIAN_POINT('Ctrl Pts',(28.6429585464946,-1.32141491426617E-14,
24.8750046770317));
#73652=CARTESIAN_POINT('Ctrl Pts',(28.9822189098709,-0.587616186362132,
24.9166713436984));
#73653=CARTESIAN_POINT('Ctrl Pts',(29.3214792732473,-1.17523237272425,24.9583380103651));
#73654=CARTESIAN_POINT('Ctrl Pts',(30.,-1.17523237272425,25.0000046770317));
#73655=CARTESIAN_POINT('Ctrl Pts',(30.6785207267527,-1.17523237272425,25.0416713436984));
#73656=CARTESIAN_POINT('Ctrl Pts',(31.017781090129,-0.587616186362132,25.0833380103651));
#73657=CARTESIAN_POINT('Ctrl Pts',(31.3570414535054,-1.35453513912972E-14,
25.1250046770317));
#73658=CARTESIAN_POINT('Ctrl Pts',(31.017781090129,0.587616186362104,25.1666713436984));
#73659=CARTESIAN_POINT('Ctrl Pts',(30.6785207267527,1.17523237272422,25.2083380103651));
#73660=CARTESIAN_POINT('Ctrl Pts',(30.,1.17523237272422,25.2500046770317));
#73661=CARTESIAN_POINT('Ctrl Pts',(29.3214792732473,1.17523237272422,25.2916713436984));
#73662=CARTESIAN_POINT('Ctrl Pts',(28.9822189098709,0.587616186362105,25.3333380103651));
#73663=CARTESIAN_POINT('Ctrl Pts',(28.6429585464946,-1.32141491426617E-14,
25.3750046770317));
#73664=CARTESIAN_POINT('Ctrl Pts',(28.9822189098709,-0.587616186362132,
25.4166713436984));
#73665=CARTESIAN_POINT('Ctrl Pts',(29.3214792732473,-1.17523237272425,25.4583380103651));
#73666=CARTESIAN_POINT('Ctrl Pts',(30.,-1.17523237272425,25.5000046770317));
#73667=CARTESIAN_POINT('Ctrl Pts',(30.6785207267527,-1.17523237272425,25.5416713436984));
#73668=CARTESIAN_POINT('Ctrl Pts',(31.017781090129,-0.587616186362132,25.5833380103651));
#73669=CARTESIAN_POINT('Ctrl Pts',(31.3570414535054,-1.35453513912972E-14,
25.6250046770317));
#73670=CARTESIAN_POINT('Ctrl Pts',(31.017781090129,0.587616186362104,25.6666713436984));
#73671=CARTESIAN_POINT('Ctrl Pts',(30.6785207267527,1.17523237272422,25.7083380103651));
#73672=CARTESIAN_POINT('Ctrl Pts',(30.,1.17523237272422,25.7500046770317));
#73673=CARTESIAN_POINT('Ctrl Pts',(29.3214792732473,1.17523237272422,25.7916713436984));
#73674=CARTESIAN_POINT('Ctrl Pts',(28.9822189098709,0.587616186362105,25.8333380103651));
#73675=CARTESIAN_POINT('Ctrl Pts',(28.6429585464946,-1.32141491426617E-14,
25.8750046770317));
#73676=CARTESIAN_POINT('Ctrl Pts',(28.9822189098709,-0.587616186362132,
25.9166713436984));
#73677=CARTESIAN_POINT('Ctrl Pts',(29.3214792732473,-1.17523237272425,25.9583380103651));
#73678=CARTESIAN_POINT('Ctrl Pts',(30.,-1.17523237272425,26.0000046770317));
#73679=CARTESIAN_POINT('Ctrl Pts',(30.6785207267527,-1.17523237272425,26.0416713436984));
#73680=CARTESIAN_POINT('Ctrl Pts',(31.017781090129,-0.587616186362132,26.0833380103651));
#73681=CARTESIAN_POINT('Ctrl Pts',(31.3570414535054,-1.35453513912972E-14,
26.1250046770317));
#73682=CARTESIAN_POINT('Ctrl Pts',(31.017781090129,0.587616186362104,26.1666713436984));
#73683=CARTESIAN_POINT('Ctrl Pts',(30.6785207267527,1.17523237272422,26.2083380103651));
#73684=CARTESIAN_POINT('Ctrl Pts',(30.,1.17523237272422,26.2500046770317));
#73685=CARTESIAN_POINT('Ctrl Pts',(29.3214792732473,1.17523237272422,26.2916713436984));
#73686=CARTESIAN_POINT('Ctrl Pts',(28.9822189098709,0.587616186362105,26.3333380103651));
#73687=CARTESIAN_POINT('Ctrl Pts',(28.6429585464946,-1.32141491426617E-14,
26.3750046770317));
#73688=CARTESIAN_POINT('Ctrl Pts',(28.9822189098709,-0.587616186362132,
26.4166713436984));
#73689=CARTESIAN_POINT('Ctrl Pts',(29.3214792732473,-1.17523237272425,26.4583380103651));
#73690=CARTESIAN_POINT('Ctrl Pts',(30.,-1.17523237272425,26.5000046770317));
#73691=CARTESIAN_POINT('Ctrl Pts',(30.6785207267527,-1.17523237272425,26.5416713436984));
#73692=CARTESIAN_POINT('Ctrl Pts',(31.017781090129,-0.587616186362132,26.5833380103651));
#73693=CARTESIAN_POINT('Ctrl Pts',(31.3570414535054,-1.35453513912972E-14,
26.6250046770317));
#73694=CARTESIAN_POINT('Ctrl Pts',(31.017781090129,0.587616186362104,26.6666713436984));
#73695=CARTESIAN_POINT('Ctrl Pts',(30.6785207267527,1.17523237272422,26.7083380103651));
#73696=CARTESIAN_POINT('Ctrl Pts',(30.,1.17523237272422,26.7500046770317));
#73697=CARTESIAN_POINT('Ctrl Pts',(29.3214792732473,1.17523237272422,26.7916713436984));
#73698=CARTESIAN_POINT('Ctrl Pts',(28.9822189098709,0.587616186362105,26.8333380103651));
#73699=CARTESIAN_POINT('Ctrl Pts',(28.6429585464946,-1.32141491426617E-14,
26.8750046770317));
#73700=CARTESIAN_POINT('Ctrl Pts',(28.9822189098709,-0.587616186362132,
26.9166713436984));
#73701=CARTESIAN_POINT('Ctrl Pts',(29.3214792732473,-1.17523237272425,26.9583380103651));
#73702=CARTESIAN_POINT('Ctrl Pts',(30.,-1.17523237272425,27.0000046770317));
#73703=CARTESIAN_POINT('Ctrl Pts',(30.6785207267527,-1.17523237272425,27.0416713436984));
#73704=CARTESIAN_POINT('Ctrl Pts',(31.017781090129,-0.587616186362132,27.0833380103651));
#73705=CARTESIAN_POINT('Ctrl Pts',(31.3570414535054,-1.35453513912972E-14,
27.1250046770317));
#73706=CARTESIAN_POINT('Ctrl Pts',(31.017781090129,0.587616186362104,27.1666713436984));
#73707=CARTESIAN_POINT('Ctrl Pts',(30.6785207267527,1.17523237272422,27.2083380103651));
#73708=CARTESIAN_POINT('Ctrl Pts',(30.,1.17523237272422,27.2500046770317));
#73709=CARTESIAN_POINT('Ctrl Pts',(29.3214792732473,1.17523237272422,27.2916713436984));
#73710=CARTESIAN_POINT('Ctrl Pts',(28.9822189098709,0.587616186362105,27.3333380103651));
#73711=CARTESIAN_POINT('Ctrl Pts',(28.6429585464946,-1.32141491426617E-14,
27.3750046770317));
#73712=CARTESIAN_POINT('Ctrl Pts',(28.9822189098709,-0.587616186362132,
27.4166713436984));
#73713=CARTESIAN_POINT('Ctrl Pts',(29.3214792732473,-1.17523237272425,27.4583380103651));
#73714=CARTESIAN_POINT('Ctrl Pts',(30.,-1.17523237272425,27.5000046770317));
#73715=CARTESIAN_POINT('Ctrl Pts',(30.6785207267527,-1.17523237272425,27.5416713436984));
#73716=CARTESIAN_POINT('Ctrl Pts',(31.017781090129,-0.587616186362132,27.5833380103651));
#73717=CARTESIAN_POINT('Ctrl Pts',(31.3570414535054,-1.35453513912972E-14,
27.6250046770317));
#73718=CARTESIAN_POINT('Ctrl Pts',(31.017781090129,0.587616186362104,27.6666713436984));
#73719=CARTESIAN_POINT('Ctrl Pts',(30.6785207267527,1.17523237272422,27.7083380103651));
#73720=CARTESIAN_POINT('Ctrl Pts',(30.,1.17523237272422,27.7500046770317));
#73721=CARTESIAN_POINT('Ctrl Pts',(29.3214792732473,1.17523237272422,27.7916713436984));
#73722=CARTESIAN_POINT('Ctrl Pts',(28.9822189098709,0.587616186362105,27.8333380103651));
#73723=CARTESIAN_POINT('Ctrl Pts',(28.6429585464946,-1.32141491426617E-14,
27.8750046770317));
#73724=CARTESIAN_POINT('Ctrl Pts',(28.9822189098709,-0.587616186362132,
27.9166713436984));
#73725=CARTESIAN_POINT('Ctrl Pts',(29.3214792732473,-1.17523237272425,27.9583380103651));
#73726=CARTESIAN_POINT('Ctrl Pts',(30.,-1.17523237272425,28.0000046770317));
#73727=CARTESIAN_POINT('Ctrl Pts',(30.6785207267527,-1.17523237272425,28.0416713436984));
#73728=CARTESIAN_POINT('Ctrl Pts',(31.017781090129,-0.587616186362132,28.0833380103651));
#73729=CARTESIAN_POINT('Ctrl Pts',(31.3570414535054,-1.35453513912972E-14,
28.1250046770317));
#73730=CARTESIAN_POINT('Ctrl Pts',(31.017781090129,0.587616186362104,28.1666713436984));
#73731=CARTESIAN_POINT('Ctrl Pts',(30.6785207267527,1.17523237272422,28.2083380103651));
#73732=CARTESIAN_POINT('Ctrl Pts',(30.,1.17523237272422,28.2500046770317));
#73733=CARTESIAN_POINT('Ctrl Pts',(29.3214792732473,1.17523237272422,28.2916713436984));
#73734=CARTESIAN_POINT('Ctrl Pts',(28.9822189098709,0.587616186362105,28.3333380103651));
#73735=CARTESIAN_POINT('Ctrl Pts',(28.6429585464946,-1.32141491426617E-14,
28.3750046770317));
#73736=CARTESIAN_POINT('Ctrl Pts',(28.9822189098709,-0.587616186362132,
28.4166713436984));
#73737=CARTESIAN_POINT('Ctrl Pts',(29.3214792732473,-1.17523237272425,28.4583380103651));
#73738=CARTESIAN_POINT('Ctrl Pts',(30.,-1.17523237272425,28.5000046770317));
#73739=CARTESIAN_POINT('Ctrl Pts',(30.6785207267527,-1.17523237272425,28.5416713436984));
#73740=CARTESIAN_POINT('Ctrl Pts',(31.017781090129,-0.587616186362132,28.5833380103651));
#73741=CARTESIAN_POINT('Ctrl Pts',(31.3570414535054,-1.35453513912972E-14,
28.6250046770317));
#73742=CARTESIAN_POINT('Ctrl Pts',(31.017781090129,0.587616186362104,28.6666713436984));
#73743=CARTESIAN_POINT('Ctrl Pts',(30.6785207267527,1.17523237272422,28.7083380103651));
#73744=CARTESIAN_POINT('Ctrl Pts',(30.,1.17523237272422,28.7500046770317));
#73745=CARTESIAN_POINT('Ctrl Pts',(29.3214792732473,1.17523237272422,28.7916713436984));
#73746=CARTESIAN_POINT('Ctrl Pts',(28.9822189098709,0.587616186362105,28.8333380103651));
#73747=CARTESIAN_POINT('Ctrl Pts',(28.6429585464946,-1.32141491426617E-14,
28.8750046770317));
#73748=CARTESIAN_POINT('Ctrl Pts',(28.9822189098709,-0.587616186362132,
28.9166713436984));
#73749=CARTESIAN_POINT('Ctrl Pts',(29.3214792732473,-1.17523237272425,28.9583380103651));
#73750=CARTESIAN_POINT('Ctrl Pts',(30.,-1.17523237272425,29.0000046770317));
#73751=CARTESIAN_POINT('Ctrl Pts',(30.6785207267527,-1.17523237272425,29.0416713436984));
#73752=CARTESIAN_POINT('Ctrl Pts',(31.017781090129,-0.587616186362132,29.0833380103651));
#73753=CARTESIAN_POINT('Ctrl Pts',(31.3570414535054,-1.35453513912972E-14,
29.1250046770317));
#73754=CARTESIAN_POINT('Ctrl Pts',(31.017781090129,0.587616186362104,29.1666713436984));
#73755=CARTESIAN_POINT('Ctrl Pts',(30.6785207267527,1.17523237272422,29.2083380103651));
#73756=CARTESIAN_POINT('Ctrl Pts',(30.,1.17523237272422,29.2500046770317));
#73757=CARTESIAN_POINT('Ctrl Pts',(29.3214792732473,1.17523237272422,29.2916713436984));
#73758=CARTESIAN_POINT('Ctrl Pts',(28.9822189098709,0.587616186362105,29.3333380103651));
#73759=CARTESIAN_POINT('Ctrl Pts',(28.6429585464946,-1.32141491426617E-14,
29.3750046770317));
#73760=CARTESIAN_POINT('Ctrl Pts',(28.9822189098709,-0.587616186362132,
29.4166713436984));
#73761=CARTESIAN_POINT('Ctrl Pts',(29.3214792732473,-1.17523237272425,29.4583380103651));
#73762=CARTESIAN_POINT('Ctrl Pts',(30.,-1.17523237272425,29.5000046770317));
#73763=CARTESIAN_POINT('Ctrl Pts',(30.6785207267527,-1.17523237272425,29.5416713436984));
#73764=CARTESIAN_POINT('Ctrl Pts',(31.017781090129,-0.587616186362132,29.5833380103651));
#73765=CARTESIAN_POINT('Ctrl Pts',(31.3570414535054,-1.35453513912972E-14,
29.6250046770317));
#73766=CARTESIAN_POINT('Ctrl Pts',(31.017781090129,0.587616186362104,29.6666713436984));
#73767=CARTESIAN_POINT('Ctrl Pts',(30.6785207267527,1.17523237272422,29.7083380103651));
#73768=CARTESIAN_POINT('Ctrl Pts',(30.,1.17523237272422,29.7500046770317));
#73769=CARTESIAN_POINT('Ctrl Pts',(29.3214792732473,1.17523237272422,29.7916713436984));
#73770=CARTESIAN_POINT('Ctrl Pts',(28.9822189098709,0.587616186362105,29.8333380103651));
#73771=CARTESIAN_POINT('Ctrl Pts',(28.6429585464946,-1.32141491426617E-14,
29.8750046770317));
#73772=CARTESIAN_POINT('Ctrl Pts',(28.9822189098709,-0.587616186362132,
29.9166713436984));
#73773=CARTESIAN_POINT('Ctrl Pts',(29.3214792732473,-1.17523237272425,29.9583380103651));
#73774=CARTESIAN_POINT('Ctrl Pts',(30.,-1.17523237272425,30.0000046770317));
#73775=CARTESIAN_POINT('Ctrl Pts',(30.6785207267527,-1.17523237272425,30.0416713436984));
#73776=CARTESIAN_POINT('Ctrl Pts',(31.017781090129,-0.587616186362132,30.0833380103651));
#73777=CARTESIAN_POINT('Ctrl Pts',(31.3570414535054,-1.35453513912972E-14,
30.1250046770317));
#73778=CARTESIAN_POINT('Ctrl Pts',(31.017781090129,0.587616186362104,30.1666713436984));
#73779=CARTESIAN_POINT('Ctrl Pts',(30.6785207267527,1.17523237272422,30.2083380103651));
#73780=CARTESIAN_POINT('Ctrl Pts',(30.,1.17523237272422,30.2500046770317));
#73781=CARTESIAN_POINT('Ctrl Pts',(29.3214792732473,1.17523237272422,30.2916713436984));
#73782=CARTESIAN_POINT('Ctrl Pts',(28.9822189098709,0.587616186362105,30.3333380103651));
#73783=CARTESIAN_POINT('Ctrl Pts',(28.6429585464946,-1.32141491426617E-14,
30.3750046770317));
#73784=CARTESIAN_POINT('Ctrl Pts',(28.9822189098709,-0.587616186362132,
30.4166713436984));
#73785=CARTESIAN_POINT('Ctrl Pts',(29.3214792732473,-1.17523237272425,30.4583380103651));
#73786=CARTESIAN_POINT('Ctrl Pts',(30.,-1.17523237272425,30.5000046770317));
#73787=CARTESIAN_POINT('Ctrl Pts',(30.6785207267527,-1.17523237272425,30.5416713436984));
#73788=CARTESIAN_POINT('Ctrl Pts',(31.017781090129,-0.587616186362132,30.5833380103651));
#73789=CARTESIAN_POINT('Ctrl Pts',(31.3570414535054,-1.35453513912972E-14,
30.6250046770317));
#73790=CARTESIAN_POINT('Ctrl Pts',(31.017781090129,0.587616186362104,30.6666713436984));
#73791=CARTESIAN_POINT('Ctrl Pts',(30.6785207267527,1.17523237272422,30.7083380103651));
#73792=CARTESIAN_POINT('Ctrl Pts',(30.,1.17523237272422,30.7500046770317));
#73793=CARTESIAN_POINT('Ctrl Pts',(29.3214792732473,1.17523237272422,30.7916713436984));
#73794=CARTESIAN_POINT('Ctrl Pts',(28.9822189098709,0.587616186362105,30.8333380103651));
#73795=CARTESIAN_POINT('Ctrl Pts',(28.6429585464946,-1.32141491426617E-14,
30.8750046770317));
#73796=CARTESIAN_POINT('Ctrl Pts',(28.9822189098709,-0.587616186362132,
30.9166713436984));
#73797=CARTESIAN_POINT('Ctrl Pts',(29.3214792732473,-1.17523237272425,30.9583380103651));
#73798=CARTESIAN_POINT('Ctrl Pts',(30.,-1.17523237272425,31.0000046770317));
#73799=CARTESIAN_POINT('Ctrl Pts',(30.6785207267527,-1.17523237272425,31.0416713436984));
#73800=CARTESIAN_POINT('Ctrl Pts',(31.017781090129,-0.587616186362132,31.0833380103651));
#73801=CARTESIAN_POINT('Ctrl Pts',(31.3570414535054,-1.35453513912972E-14,
31.1250046770317));
#73802=CARTESIAN_POINT('Ctrl Pts',(31.017781090129,0.587616186362104,31.1666713436984));
#73803=CARTESIAN_POINT('Ctrl Pts',(30.6785207267527,1.17523237272422,31.2083380103651));
#73804=CARTESIAN_POINT('Ctrl Pts',(30.,1.17523237272422,31.2500046770317));
#73805=CARTESIAN_POINT('Ctrl Pts',(30.,1.52706329386825,15.546875));
#73806=CARTESIAN_POINT('Ctrl Pts',(29.1183495962155,1.52706329386825,15.5885416666667));
#73807=CARTESIAN_POINT('Ctrl Pts',(28.6775243943233,0.76353164693412,15.6302083333334));
#73808=CARTESIAN_POINT('Ctrl Pts',(28.2366991924311,-1.31894491186926E-14,
15.671875));
#73809=CARTESIAN_POINT('Ctrl Pts',(28.6775243943233,-0.763531646934146,
15.7135416666667));
#73810=CARTESIAN_POINT('Ctrl Pts',(29.1183495962155,-1.52706329386828,15.7552083333334));
#73811=CARTESIAN_POINT('Ctrl Pts',(30.,-1.52706329386828,15.796875));
#73812=CARTESIAN_POINT('Ctrl Pts',(30.8816504037844,-1.52706329386828,15.8385416666667));
#73813=CARTESIAN_POINT('Ctrl Pts',(31.3224756056766,-0.763531646934147,
15.8802083333334));
#73814=CARTESIAN_POINT('Ctrl Pts',(31.7633008075689,-1.36198038370242E-14,
15.921875));
#73815=CARTESIAN_POINT('Ctrl Pts',(31.3224756056766,0.763531646934118,15.9635416666667));
#73816=CARTESIAN_POINT('Ctrl Pts',(30.8816504037844,1.52706329386825,16.0052083333334));
#73817=CARTESIAN_POINT('Ctrl Pts',(30.,1.52706329386825,16.046875));
#73818=CARTESIAN_POINT('Ctrl Pts',(29.1183495962155,1.52706329386825,16.0885416666667));
#73819=CARTESIAN_POINT('Ctrl Pts',(28.6775243943233,0.76353164693412,16.1302083333334));
#73820=CARTESIAN_POINT('Ctrl Pts',(28.2366991924311,-1.31894491186926E-14,
16.171875));
#73821=CARTESIAN_POINT('Ctrl Pts',(28.6775243943233,-0.763531646934146,
16.2135416666667));
#73822=CARTESIAN_POINT('Ctrl Pts',(29.1183495962155,-1.52706329386828,16.2552083333334));
#73823=CARTESIAN_POINT('Ctrl Pts',(30.,-1.52706329386828,16.296875));
#73824=CARTESIAN_POINT('Ctrl Pts',(30.8816504037844,-1.52706329386828,16.3385416666667));
#73825=CARTESIAN_POINT('Ctrl Pts',(31.3224756056766,-0.763531646934147,
16.3802083333334));
#73826=CARTESIAN_POINT('Ctrl Pts',(31.7633008075689,-1.36198038370242E-14,
16.421875));
#73827=CARTESIAN_POINT('Ctrl Pts',(31.3224756056766,0.763531646934118,16.4635416666667));
#73828=CARTESIAN_POINT('Ctrl Pts',(30.8816504037844,1.52706329386825,16.5052083333334));
#73829=CARTESIAN_POINT('Ctrl Pts',(30.,1.52706329386825,16.546875));
#73830=CARTESIAN_POINT('Ctrl Pts',(29.1183495962155,1.52706329386825,16.5885416666667));
#73831=CARTESIAN_POINT('Ctrl Pts',(28.6775243943233,0.76353164693412,16.6302083333334));
#73832=CARTESIAN_POINT('Ctrl Pts',(28.2366991924311,-1.31894491186926E-14,
16.671875));
#73833=CARTESIAN_POINT('Ctrl Pts',(28.6775243943233,-0.763531646934146,
16.7135416666667));
#73834=CARTESIAN_POINT('Ctrl Pts',(29.1183495962155,-1.52706329386828,16.7552083333334));
#73835=CARTESIAN_POINT('Ctrl Pts',(30.,-1.52706329386828,16.796875));
#73836=CARTESIAN_POINT('Ctrl Pts',(30.8816504037844,-1.52706329386828,16.8385416666667));
#73837=CARTESIAN_POINT('Ctrl Pts',(31.3224756056766,-0.763531646934147,
16.8802083333334));
#73838=CARTESIAN_POINT('Ctrl Pts',(31.7633008075689,-1.36198038370242E-14,
16.921875));
#73839=CARTESIAN_POINT('Ctrl Pts',(31.3224756056766,0.763531646934118,16.9635416666667));
#73840=CARTESIAN_POINT('Ctrl Pts',(30.8816504037844,1.52706329386825,17.0052083333334));
#73841=CARTESIAN_POINT('Ctrl Pts',(30.,1.52706329386825,17.046875));
#73842=CARTESIAN_POINT('Ctrl Pts',(29.1183495962155,1.52706329386825,17.0885416666667));
#73843=CARTESIAN_POINT('Ctrl Pts',(28.6775243943233,0.76353164693412,17.1302083333334));
#73844=CARTESIAN_POINT('Ctrl Pts',(28.2366991924311,-1.31894491186926E-14,
17.171875));
#73845=CARTESIAN_POINT('Ctrl Pts',(28.6775243943233,-0.763531646934146,
17.2135416666667));
#73846=CARTESIAN_POINT('Ctrl Pts',(29.1183495962155,-1.52706329386828,17.2552083333334));
#73847=CARTESIAN_POINT('Ctrl Pts',(30.,-1.52706329386828,17.296875));
#73848=CARTESIAN_POINT('Ctrl Pts',(30.8816504037844,-1.52706329386828,17.3385416666667));
#73849=CARTESIAN_POINT('Ctrl Pts',(31.3224756056766,-0.763531646934147,
17.3802083333334));
#73850=CARTESIAN_POINT('Ctrl Pts',(31.7633008075689,-1.36198038370242E-14,
17.421875));
#73851=CARTESIAN_POINT('Ctrl Pts',(31.3224756056766,0.763531646934118,17.4635416666667));
#73852=CARTESIAN_POINT('Ctrl Pts',(30.8816504037844,1.52706329386825,17.5052083333334));
#73853=CARTESIAN_POINT('Ctrl Pts',(30.,1.52706329386825,17.546875));
#73854=CARTESIAN_POINT('Ctrl Pts',(29.1183495962155,1.52706329386825,17.5885416666667));
#73855=CARTESIAN_POINT('Ctrl Pts',(28.6775243943233,0.76353164693412,17.6302083333334));
#73856=CARTESIAN_POINT('Ctrl Pts',(28.2366991924311,-1.31894491186926E-14,
17.671875));
#73857=CARTESIAN_POINT('Ctrl Pts',(28.6775243943233,-0.763531646934146,
17.7135416666667));
#73858=CARTESIAN_POINT('Ctrl Pts',(29.1183495962155,-1.52706329386828,17.7552083333334));
#73859=CARTESIAN_POINT('Ctrl Pts',(30.,-1.52706329386828,17.796875));
#73860=CARTESIAN_POINT('Ctrl Pts',(30.8816504037844,-1.52706329386828,17.8385416666667));
#73861=CARTESIAN_POINT('Ctrl Pts',(31.3224756056766,-0.763531646934147,
17.8802083333334));
#73862=CARTESIAN_POINT('Ctrl Pts',(31.7633008075689,-1.36198038370242E-14,
17.921875));
#73863=CARTESIAN_POINT('Ctrl Pts',(31.3224756056766,0.763531646934118,17.9635416666667));
#73864=CARTESIAN_POINT('Ctrl Pts',(30.8816504037844,1.52706329386825,18.0052083333334));
#73865=CARTESIAN_POINT('Ctrl Pts',(30.,1.52706329386825,18.046875));
#73866=CARTESIAN_POINT('Ctrl Pts',(29.1183495962155,1.52706329386825,18.0885416666667));
#73867=CARTESIAN_POINT('Ctrl Pts',(28.6775243943233,0.76353164693412,18.1302083333334));
#73868=CARTESIAN_POINT('Ctrl Pts',(28.2366991924311,-1.31894491186926E-14,
18.171875));
#73869=CARTESIAN_POINT('Ctrl Pts',(28.6775243943233,-0.763531646934146,
18.2135416666667));
#73870=CARTESIAN_POINT('Ctrl Pts',(29.1183495962155,-1.52706329386828,18.2552083333334));
#73871=CARTESIAN_POINT('Ctrl Pts',(30.,-1.52706329386828,18.296875));
#73872=CARTESIAN_POINT('Ctrl Pts',(30.8816504037844,-1.52706329386828,18.3385416666667));
#73873=CARTESIAN_POINT('Ctrl Pts',(31.3224756056766,-0.763531646934147,
18.3802083333334));
#73874=CARTESIAN_POINT('Ctrl Pts',(31.7633008075689,-1.36198038370242E-14,
18.421875));
#73875=CARTESIAN_POINT('Ctrl Pts',(31.3224756056766,0.763531646934118,18.4635416666667));
#73876=CARTESIAN_POINT('Ctrl Pts',(30.8816504037844,1.52706329386825,18.5052083333334));
#73877=CARTESIAN_POINT('Ctrl Pts',(30.,1.52706329386825,18.546875));
#73878=CARTESIAN_POINT('Ctrl Pts',(29.1183495962155,1.52706329386825,18.5885416666667));
#73879=CARTESIAN_POINT('Ctrl Pts',(28.6775243943233,0.76353164693412,18.6302083333334));
#73880=CARTESIAN_POINT('Ctrl Pts',(28.2366991924311,-1.31894491186926E-14,
18.671875));
#73881=CARTESIAN_POINT('Ctrl Pts',(28.6775243943233,-0.763531646934146,
18.7135416666667));
#73882=CARTESIAN_POINT('Ctrl Pts',(29.1183495962155,-1.52706329386828,18.7552083333334));
#73883=CARTESIAN_POINT('Ctrl Pts',(30.,-1.52706329386828,18.796875));
#73884=CARTESIAN_POINT('Ctrl Pts',(30.8816504037844,-1.52706329386828,18.8385416666667));
#73885=CARTESIAN_POINT('Ctrl Pts',(31.3224756056766,-0.763531646934147,
18.8802083333334));
#73886=CARTESIAN_POINT('Ctrl Pts',(31.7633008075689,-1.36198038370242E-14,
18.921875));
#73887=CARTESIAN_POINT('Ctrl Pts',(31.3224756056766,0.763531646934118,18.9635416666667));
#73888=CARTESIAN_POINT('Ctrl Pts',(30.8816504037844,1.52706329386825,19.0052083333334));
#73889=CARTESIAN_POINT('Ctrl Pts',(30.,1.52706329386825,19.046875));
#73890=CARTESIAN_POINT('Ctrl Pts',(29.1183495962155,1.52706329386825,19.0885416666667));
#73891=CARTESIAN_POINT('Ctrl Pts',(28.6775243943233,0.76353164693412,19.1302083333334));
#73892=CARTESIAN_POINT('Ctrl Pts',(28.2366991924311,-1.31894491186926E-14,
19.171875));
#73893=CARTESIAN_POINT('Ctrl Pts',(28.6775243943233,-0.763531646934146,
19.2135416666667));
#73894=CARTESIAN_POINT('Ctrl Pts',(29.1183495962155,-1.52706329386828,19.2552083333334));
#73895=CARTESIAN_POINT('Ctrl Pts',(30.,-1.52706329386828,19.296875));
#73896=CARTESIAN_POINT('Ctrl Pts',(30.8816504037844,-1.52706329386828,19.3385416666667));
#73897=CARTESIAN_POINT('Ctrl Pts',(31.3224756056766,-0.763531646934147,
19.3802083333334));
#73898=CARTESIAN_POINT('Ctrl Pts',(31.7633008075689,-1.36198038370242E-14,
19.421875));
#73899=CARTESIAN_POINT('Ctrl Pts',(31.3224756056766,0.763531646934118,19.4635416666667));
#73900=CARTESIAN_POINT('Ctrl Pts',(30.8816504037844,1.52706329386825,19.5052083333334));
#73901=CARTESIAN_POINT('Ctrl Pts',(30.,1.52706329386825,19.546875));
#73902=CARTESIAN_POINT('Ctrl Pts',(29.1183495962155,1.52706329386825,19.5885416666667));
#73903=CARTESIAN_POINT('Ctrl Pts',(28.6775243943233,0.76353164693412,19.6302083333334));
#73904=CARTESIAN_POINT('Ctrl Pts',(28.2366991924311,-1.31894491186926E-14,
19.671875));
#73905=CARTESIAN_POINT('Ctrl Pts',(28.6775243943233,-0.763531646934146,
19.7135416666667));
#73906=CARTESIAN_POINT('Ctrl Pts',(29.1183495962155,-1.52706329386828,19.7552083333334));
#73907=CARTESIAN_POINT('Ctrl Pts',(30.,-1.52706329386828,19.796875));
#73908=CARTESIAN_POINT('Ctrl Pts',(30.8816504037844,-1.52706329386828,19.8385416666667));
#73909=CARTESIAN_POINT('Ctrl Pts',(31.3224756056766,-0.763531646934147,
19.8802083333334));
#73910=CARTESIAN_POINT('Ctrl Pts',(31.7633008075689,-1.36198038370242E-14,
19.921875));
#73911=CARTESIAN_POINT('Ctrl Pts',(31.3224756056766,0.763531646934118,19.9635416666667));
#73912=CARTESIAN_POINT('Ctrl Pts',(30.8816504037844,1.52706329386825,20.0052083333334));
#73913=CARTESIAN_POINT('Ctrl Pts',(30.,1.52706329386825,20.046875));
#73914=CARTESIAN_POINT('Ctrl Pts',(29.1183495962155,1.52706329386825,20.0885416666667));
#73915=CARTESIAN_POINT('Ctrl Pts',(28.6775243943233,0.76353164693412,20.1302083333334));
#73916=CARTESIAN_POINT('Ctrl Pts',(28.2366991924311,-1.31894491186926E-14,
20.171875));
#73917=CARTESIAN_POINT('Ctrl Pts',(28.6775243943233,-0.763531646934146,
20.2135416666667));
#73918=CARTESIAN_POINT('Ctrl Pts',(29.1183495962155,-1.52706329386828,20.2552083333334));
#73919=CARTESIAN_POINT('Ctrl Pts',(30.,-1.52706329386828,20.296875));
#73920=CARTESIAN_POINT('Ctrl Pts',(30.8816504037844,-1.52706329386828,20.3385416666667));
#73921=CARTESIAN_POINT('Ctrl Pts',(31.3224756056766,-0.763531646934147,
20.3802083333334));
#73922=CARTESIAN_POINT('Ctrl Pts',(31.7633008075689,-1.36198038370242E-14,
20.421875));
#73923=CARTESIAN_POINT('Ctrl Pts',(31.3224756056766,0.763531646934118,20.4635416666667));
#73924=CARTESIAN_POINT('Ctrl Pts',(30.8816504037844,1.52706329386825,20.5052083333334));
#73925=CARTESIAN_POINT('Ctrl Pts',(30.,1.52706329386825,20.546875));
#73926=CARTESIAN_POINT('Ctrl Pts',(29.1183495962155,1.52706329386825,20.5885416666667));
#73927=CARTESIAN_POINT('Ctrl Pts',(28.6775243943233,0.76353164693412,20.6302083333334));
#73928=CARTESIAN_POINT('Ctrl Pts',(28.2366991924311,-1.31894491186926E-14,
20.671875));
#73929=CARTESIAN_POINT('Ctrl Pts',(28.6775243943233,-0.763531646934146,
20.7135416666667));
#73930=CARTESIAN_POINT('Ctrl Pts',(29.1183495962155,-1.52706329386828,20.7552083333334));
#73931=CARTESIAN_POINT('Ctrl Pts',(30.,-1.52706329386828,20.796875));
#73932=CARTESIAN_POINT('Ctrl Pts',(30.8816504037844,-1.52706329386828,20.8385416666667));
#73933=CARTESIAN_POINT('Ctrl Pts',(31.3224756056766,-0.763531646934147,
20.8802083333334));
#73934=CARTESIAN_POINT('Ctrl Pts',(31.7633008075689,-1.36198038370242E-14,
20.921875));
#73935=CARTESIAN_POINT('Ctrl Pts',(31.3224756056766,0.763531646934118,20.9635416666667));
#73936=CARTESIAN_POINT('Ctrl Pts',(30.8816504037844,1.52706329386825,21.0052083333334));
#73937=CARTESIAN_POINT('Ctrl Pts',(30.,1.52706329386825,21.046875));
#73938=CARTESIAN_POINT('Ctrl Pts',(29.1183495962155,1.52706329386825,21.0885416666667));
#73939=CARTESIAN_POINT('Ctrl Pts',(28.6775243943233,0.76353164693412,21.1302083333334));
#73940=CARTESIAN_POINT('Ctrl Pts',(28.2366991924311,-1.31894491186926E-14,
21.171875));
#73941=CARTESIAN_POINT('Ctrl Pts',(28.6775243943233,-0.763531646934146,
21.2135416666667));
#73942=CARTESIAN_POINT('Ctrl Pts',(29.1183495962155,-1.52706329386828,21.2552083333334));
#73943=CARTESIAN_POINT('Ctrl Pts',(30.,-1.52706329386828,21.296875));
#73944=CARTESIAN_POINT('Ctrl Pts',(30.8816504037844,-1.52706329386828,21.3385416666667));
#73945=CARTESIAN_POINT('Ctrl Pts',(31.3224756056766,-0.763531646934147,
21.3802083333334));
#73946=CARTESIAN_POINT('Ctrl Pts',(31.7633008075689,-1.36198038370242E-14,
21.421875));
#73947=CARTESIAN_POINT('Ctrl Pts',(31.3224756056766,0.763531646934118,21.4635416666667));
#73948=CARTESIAN_POINT('Ctrl Pts',(30.8816504037844,1.52706329386825,21.5052083333334));
#73949=CARTESIAN_POINT('Ctrl Pts',(30.,1.52706329386825,21.546875));
#73950=CARTESIAN_POINT('Ctrl Pts',(29.1183495962155,1.52706329386825,21.5885416666667));
#73951=CARTESIAN_POINT('Ctrl Pts',(28.6775243943233,0.76353164693412,21.6302083333334));
#73952=CARTESIAN_POINT('Ctrl Pts',(28.2366991924311,-1.31894491186926E-14,
21.671875));
#73953=CARTESIAN_POINT('Ctrl Pts',(28.6775243943233,-0.763531646934146,
21.7135416666667));
#73954=CARTESIAN_POINT('Ctrl Pts',(29.1183495962155,-1.52706329386828,21.7552083333334));
#73955=CARTESIAN_POINT('Ctrl Pts',(30.,-1.52706329386828,21.796875));
#73956=CARTESIAN_POINT('Ctrl Pts',(30.8816504037844,-1.52706329386828,21.8385416666667));
#73957=CARTESIAN_POINT('Ctrl Pts',(31.3224756056766,-0.763531646934147,
21.8802083333334));
#73958=CARTESIAN_POINT('Ctrl Pts',(31.7633008075689,-1.36198038370242E-14,
21.921875));
#73959=CARTESIAN_POINT('Ctrl Pts',(31.3224756056766,0.763531646934118,21.9635416666667));
#73960=CARTESIAN_POINT('Ctrl Pts',(30.8816504037844,1.52706329386825,22.0052083333334));
#73961=CARTESIAN_POINT('Ctrl Pts',(30.,1.52706329386825,22.046875));
#73962=CARTESIAN_POINT('Ctrl Pts',(29.1183495962155,1.52706329386825,22.0885416666667));
#73963=CARTESIAN_POINT('Ctrl Pts',(28.6775243943233,0.76353164693412,22.1302083333334));
#73964=CARTESIAN_POINT('Ctrl Pts',(28.2366991924311,-1.31894491186926E-14,
22.171875));
#73965=CARTESIAN_POINT('Ctrl Pts',(28.6775243943233,-0.763531646934146,
22.2135416666667));
#73966=CARTESIAN_POINT('Ctrl Pts',(29.1183495962155,-1.52706329386828,22.2552083333334));
#73967=CARTESIAN_POINT('Ctrl Pts',(30.,-1.52706329386828,22.296875));
#73968=CARTESIAN_POINT('Ctrl Pts',(30.8816504037844,-1.52706329386828,22.3385416666667));
#73969=CARTESIAN_POINT('Ctrl Pts',(31.3224756056766,-0.763531646934147,
22.3802083333334));
#73970=CARTESIAN_POINT('Ctrl Pts',(31.7633008075689,-1.36198038370242E-14,
22.421875));
#73971=CARTESIAN_POINT('Ctrl Pts',(31.3224756056766,0.763531646934118,22.4635416666667));
#73972=CARTESIAN_POINT('Ctrl Pts',(30.8816504037844,1.52706329386825,22.5052083333334));
#73973=CARTESIAN_POINT('Ctrl Pts',(30.,1.52706329386825,22.546875));
#73974=CARTESIAN_POINT('Ctrl Pts',(29.1183495962155,1.52706329386825,22.5885416666667));
#73975=CARTESIAN_POINT('Ctrl Pts',(28.6775243943233,0.76353164693412,22.6302083333334));
#73976=CARTESIAN_POINT('Ctrl Pts',(28.2366991924311,-1.31894491186926E-14,
22.671875));
#73977=CARTESIAN_POINT('Ctrl Pts',(28.6775243943233,-0.763531646934146,
22.7135416666667));
#73978=CARTESIAN_POINT('Ctrl Pts',(29.1183495962155,-1.52706329386828,22.7552083333334));
#73979=CARTESIAN_POINT('Ctrl Pts',(30.,-1.52706329386828,22.796875));
#73980=CARTESIAN_POINT('Ctrl Pts',(30.8816504037844,-1.52706329386828,22.8385416666667));
#73981=CARTESIAN_POINT('Ctrl Pts',(31.3224756056766,-0.763531646934147,
22.8802083333334));
#73982=CARTESIAN_POINT('Ctrl Pts',(31.7633008075689,-1.36198038370242E-14,
22.921875));
#73983=CARTESIAN_POINT('Ctrl Pts',(31.3224756056766,0.763531646934118,22.9635416666667));
#73984=CARTESIAN_POINT('Ctrl Pts',(30.8816504037844,1.52706329386825,23.0052083333334));
#73985=CARTESIAN_POINT('Ctrl Pts',(30.,1.52706329386825,23.046875));
#73986=CARTESIAN_POINT('Ctrl Pts',(29.1183495962155,1.52706329386825,23.0885416666667));
#73987=CARTESIAN_POINT('Ctrl Pts',(28.6775243943233,0.76353164693412,23.1302083333334));
#73988=CARTESIAN_POINT('Ctrl Pts',(28.2366991924311,-1.31894491186926E-14,
23.171875));
#73989=CARTESIAN_POINT('Ctrl Pts',(28.6775243943233,-0.763531646934146,
23.2135416666667));
#73990=CARTESIAN_POINT('Ctrl Pts',(29.1183495962155,-1.52706329386828,23.2552083333334));
#73991=CARTESIAN_POINT('Ctrl Pts',(30.,-1.52706329386828,23.296875));
#73992=CARTESIAN_POINT('Ctrl Pts',(30.8816504037844,-1.52706329386828,23.3385416666667));
#73993=CARTESIAN_POINT('Ctrl Pts',(31.3224756056766,-0.763531646934147,
23.3802083333334));
#73994=CARTESIAN_POINT('Ctrl Pts',(31.7633008075689,-1.36198038370242E-14,
23.421875));
#73995=CARTESIAN_POINT('Ctrl Pts',(31.3224756056766,0.763531646934118,23.4635416666667));
#73996=CARTESIAN_POINT('Ctrl Pts',(30.8816504037844,1.52706329386825,23.5052083333334));
#73997=CARTESIAN_POINT('Ctrl Pts',(30.,1.52706329386825,23.546875));
#73998=CARTESIAN_POINT('Ctrl Pts',(29.1183495962155,1.52706329386825,23.5885416666667));
#73999=CARTESIAN_POINT('Ctrl Pts',(28.6775243943233,0.76353164693412,23.6302083333334));
#74000=CARTESIAN_POINT('Ctrl Pts',(28.2366991924311,-1.31894491186926E-14,
23.671875));
#74001=CARTESIAN_POINT('Ctrl Pts',(28.6775243943233,-0.763531646934146,
23.7135416666667));
#74002=CARTESIAN_POINT('Ctrl Pts',(29.1183495962155,-1.52706329386828,23.7552083333334));
#74003=CARTESIAN_POINT('Ctrl Pts',(30.,-1.52706329386828,23.796875));
#74004=CARTESIAN_POINT('Ctrl Pts',(30.8816504037844,-1.52706329386828,23.8385416666667));
#74005=CARTESIAN_POINT('Ctrl Pts',(31.3224756056766,-0.763531646934147,
23.8802083333334));
#74006=CARTESIAN_POINT('Ctrl Pts',(31.7633008075689,-1.36198038370242E-14,
23.921875));
#74007=CARTESIAN_POINT('Ctrl Pts',(31.3224756056766,0.763531646934118,23.9635416666667));
#74008=CARTESIAN_POINT('Ctrl Pts',(30.8816504037844,1.52706329386825,24.0052083333334));
#74009=CARTESIAN_POINT('Ctrl Pts',(30.,1.52706329386825,24.046875));
#74010=CARTESIAN_POINT('Ctrl Pts',(29.1183495962155,1.52706329386825,24.0885416666667));
#74011=CARTESIAN_POINT('Ctrl Pts',(28.6775243943233,0.76353164693412,24.1302083333334));
#74012=CARTESIAN_POINT('Ctrl Pts',(28.2366991924311,-1.31894491186926E-14,
24.171875));
#74013=CARTESIAN_POINT('Ctrl Pts',(28.6775243943233,-0.763531646934146,
24.2135416666667));
#74014=CARTESIAN_POINT('Ctrl Pts',(29.1183495962155,-1.52706329386828,24.2552083333334));
#74015=CARTESIAN_POINT('Ctrl Pts',(30.,-1.52706329386828,24.296875));
#74016=CARTESIAN_POINT('Ctrl Pts',(30.8816504037844,-1.52706329386828,24.3385416666667));
#74017=CARTESIAN_POINT('Ctrl Pts',(31.3224756056766,-0.763531646934147,
24.3802083333334));
#74018=CARTESIAN_POINT('Ctrl Pts',(31.7633008075689,-1.36198038370242E-14,
24.421875));
#74019=CARTESIAN_POINT('Ctrl Pts',(31.3224756056766,0.763531646934118,24.4635416666667));
#74020=CARTESIAN_POINT('Ctrl Pts',(30.8816504037844,1.52706329386825,24.5052083333334));
#74021=CARTESIAN_POINT('Ctrl Pts',(30.,1.52706329386825,24.546875));
#74022=CARTESIAN_POINT('Ctrl Pts',(29.1183495962155,1.52706329386825,24.5885416666667));
#74023=CARTESIAN_POINT('Ctrl Pts',(28.6775243943233,0.76353164693412,24.6302083333334));
#74024=CARTESIAN_POINT('Ctrl Pts',(28.2366991924311,-1.31894491186926E-14,
24.671875));
#74025=CARTESIAN_POINT('Ctrl Pts',(28.6775243943233,-0.763531646934146,
24.7135416666667));
#74026=CARTESIAN_POINT('Ctrl Pts',(29.1183495962155,-1.52706329386828,24.7552083333334));
#74027=CARTESIAN_POINT('Ctrl Pts',(30.,-1.52706329386828,24.796875));
#74028=CARTESIAN_POINT('Ctrl Pts',(30.8816504037844,-1.52706329386828,24.8385416666667));
#74029=CARTESIAN_POINT('Ctrl Pts',(31.3224756056766,-0.763531646934147,
24.8802083333334));
#74030=CARTESIAN_POINT('Ctrl Pts',(31.7633008075689,-1.36198038370242E-14,
24.921875));
#74031=CARTESIAN_POINT('Ctrl Pts',(31.3224756056766,0.763531646934118,24.9635416666667));
#74032=CARTESIAN_POINT('Ctrl Pts',(30.8816504037844,1.52706329386825,25.0052083333334));
#74033=CARTESIAN_POINT('Ctrl Pts',(30.,1.52706329386825,25.046875));
#74034=CARTESIAN_POINT('Ctrl Pts',(29.1183495962155,1.52706329386825,25.0885416666667));
#74035=CARTESIAN_POINT('Ctrl Pts',(28.6775243943233,0.76353164693412,25.1302083333334));
#74036=CARTESIAN_POINT('Ctrl Pts',(28.2366991924311,-1.31894491186926E-14,
25.171875));
#74037=CARTESIAN_POINT('Ctrl Pts',(28.6775243943233,-0.763531646934146,
25.2135416666667));
#74038=CARTESIAN_POINT('Ctrl Pts',(29.1183495962155,-1.52706329386828,25.2552083333334));
#74039=CARTESIAN_POINT('Ctrl Pts',(30.,-1.52706329386828,25.296875));
#74040=CARTESIAN_POINT('Ctrl Pts',(30.8816504037844,-1.52706329386828,25.3385416666667));
#74041=CARTESIAN_POINT('Ctrl Pts',(31.3224756056766,-0.763531646934147,
25.3802083333334));
#74042=CARTESIAN_POINT('Ctrl Pts',(31.7633008075689,-1.36198038370242E-14,
25.421875));
#74043=CARTESIAN_POINT('Ctrl Pts',(31.3224756056766,0.763531646934118,25.4635416666667));
#74044=CARTESIAN_POINT('Ctrl Pts',(30.8816504037844,1.52706329386825,25.5052083333334));
#74045=CARTESIAN_POINT('Ctrl Pts',(30.,1.52706329386825,25.546875));
#74046=CARTESIAN_POINT('Ctrl Pts',(29.1183495962155,1.52706329386825,25.5885416666667));
#74047=CARTESIAN_POINT('Ctrl Pts',(28.6775243943233,0.76353164693412,25.6302083333334));
#74048=CARTESIAN_POINT('Ctrl Pts',(28.2366991924311,-1.31894491186926E-14,
25.671875));
#74049=CARTESIAN_POINT('Ctrl Pts',(28.6775243943233,-0.763531646934146,
25.7135416666667));
#74050=CARTESIAN_POINT('Ctrl Pts',(29.1183495962155,-1.52706329386828,25.7552083333334));
#74051=CARTESIAN_POINT('Ctrl Pts',(30.,-1.52706329386828,25.796875));
#74052=CARTESIAN_POINT('Ctrl Pts',(30.8816504037844,-1.52706329386828,25.8385416666667));
#74053=CARTESIAN_POINT('Ctrl Pts',(31.3224756056766,-0.763531646934147,
25.8802083333334));
#74054=CARTESIAN_POINT('Ctrl Pts',(31.7633008075689,-1.36198038370242E-14,
25.921875));
#74055=CARTESIAN_POINT('Ctrl Pts',(31.3224756056766,0.763531646934118,25.9635416666667));
#74056=CARTESIAN_POINT('Ctrl Pts',(30.8816504037844,1.52706329386825,26.0052083333334));
#74057=CARTESIAN_POINT('Ctrl Pts',(30.,1.52706329386825,26.046875));
#74058=CARTESIAN_POINT('Ctrl Pts',(29.1183495962155,1.52706329386825,26.0885416666667));
#74059=CARTESIAN_POINT('Ctrl Pts',(28.6775243943233,0.76353164693412,26.1302083333334));
#74060=CARTESIAN_POINT('Ctrl Pts',(28.2366991924311,-1.31894491186926E-14,
26.171875));
#74061=CARTESIAN_POINT('Ctrl Pts',(28.6775243943233,-0.763531646934146,
26.2135416666667));
#74062=CARTESIAN_POINT('Ctrl Pts',(29.1183495962155,-1.52706329386828,26.2552083333334));
#74063=CARTESIAN_POINT('Ctrl Pts',(30.,-1.52706329386828,26.296875));
#74064=CARTESIAN_POINT('Ctrl Pts',(30.8816504037844,-1.52706329386828,26.3385416666667));
#74065=CARTESIAN_POINT('Ctrl Pts',(31.3224756056766,-0.763531646934147,
26.3802083333334));
#74066=CARTESIAN_POINT('Ctrl Pts',(31.7633008075689,-1.36198038370242E-14,
26.421875));
#74067=CARTESIAN_POINT('Ctrl Pts',(31.3224756056766,0.763531646934118,26.4635416666667));
#74068=CARTESIAN_POINT('Ctrl Pts',(30.8816504037844,1.52706329386825,26.5052083333334));
#74069=CARTESIAN_POINT('Ctrl Pts',(30.,1.52706329386825,26.546875));
#74070=CARTESIAN_POINT('Ctrl Pts',(29.1183495962155,1.52706329386825,26.5885416666667));
#74071=CARTESIAN_POINT('Ctrl Pts',(28.6775243943233,0.76353164693412,26.6302083333334));
#74072=CARTESIAN_POINT('Ctrl Pts',(28.2366991924311,-1.31894491186926E-14,
26.671875));
#74073=CARTESIAN_POINT('Ctrl Pts',(28.6775243943233,-0.763531646934146,
26.7135416666667));
#74074=CARTESIAN_POINT('Ctrl Pts',(29.1183495962155,-1.52706329386828,26.7552083333334));
#74075=CARTESIAN_POINT('Ctrl Pts',(30.,-1.52706329386828,26.796875));
#74076=CARTESIAN_POINT('Ctrl Pts',(30.8816504037844,-1.52706329386828,26.8385416666667));
#74077=CARTESIAN_POINT('Ctrl Pts',(31.3224756056766,-0.763531646934147,
26.8802083333334));
#74078=CARTESIAN_POINT('Ctrl Pts',(31.7633008075689,-1.36198038370242E-14,
26.921875));
#74079=CARTESIAN_POINT('Ctrl Pts',(31.3224756056766,0.763531646934118,26.9635416666667));
#74080=CARTESIAN_POINT('Ctrl Pts',(30.8816504037844,1.52706329386825,27.0052083333334));
#74081=CARTESIAN_POINT('Ctrl Pts',(30.,1.52706329386825,27.046875));
#74082=CARTESIAN_POINT('Ctrl Pts',(29.1183495962155,1.52706329386825,27.0885416666667));
#74083=CARTESIAN_POINT('Ctrl Pts',(28.6775243943233,0.76353164693412,27.1302083333334));
#74084=CARTESIAN_POINT('Ctrl Pts',(28.2366991924311,-1.31894491186926E-14,
27.171875));
#74085=CARTESIAN_POINT('Ctrl Pts',(28.6775243943233,-0.763531646934146,
27.2135416666667));
#74086=CARTESIAN_POINT('Ctrl Pts',(29.1183495962155,-1.52706329386828,27.2552083333334));
#74087=CARTESIAN_POINT('Ctrl Pts',(30.,-1.52706329386828,27.296875));
#74088=CARTESIAN_POINT('Ctrl Pts',(30.8816504037844,-1.52706329386828,27.3385416666667));
#74089=CARTESIAN_POINT('Ctrl Pts',(31.3224756056766,-0.763531646934147,
27.3802083333334));
#74090=CARTESIAN_POINT('Ctrl Pts',(31.7633008075689,-1.36198038370242E-14,
27.421875));
#74091=CARTESIAN_POINT('Ctrl Pts',(31.3224756056766,0.763531646934118,27.4635416666667));
#74092=CARTESIAN_POINT('Ctrl Pts',(30.8816504037844,1.52706329386825,27.5052083333334));
#74093=CARTESIAN_POINT('Ctrl Pts',(30.,1.52706329386825,27.546875));
#74094=CARTESIAN_POINT('Ctrl Pts',(29.1183495962155,1.52706329386825,27.5885416666667));
#74095=CARTESIAN_POINT('Ctrl Pts',(28.6775243943233,0.76353164693412,27.6302083333334));
#74096=CARTESIAN_POINT('Ctrl Pts',(28.2366991924311,-1.31894491186926E-14,
27.671875));
#74097=CARTESIAN_POINT('Ctrl Pts',(28.6775243943233,-0.763531646934146,
27.7135416666667));
#74098=CARTESIAN_POINT('Ctrl Pts',(29.1183495962155,-1.52706329386828,27.7552083333334));
#74099=CARTESIAN_POINT('Ctrl Pts',(30.,-1.52706329386828,27.796875));
#74100=CARTESIAN_POINT('Ctrl Pts',(30.8816504037844,-1.52706329386828,27.8385416666667));
#74101=CARTESIAN_POINT('Ctrl Pts',(31.3224756056766,-0.763531646934147,
27.8802083333334));
#74102=CARTESIAN_POINT('Ctrl Pts',(31.7633008075689,-1.36198038370242E-14,
27.921875));
#74103=CARTESIAN_POINT('Ctrl Pts',(31.3224756056766,0.763531646934118,27.9635416666667));
#74104=CARTESIAN_POINT('Ctrl Pts',(30.8816504037844,1.52706329386825,28.0052083333334));
#74105=CARTESIAN_POINT('Ctrl Pts',(30.,1.52706329386825,28.046875));
#74106=CARTESIAN_POINT('Ctrl Pts',(29.1183495962155,1.52706329386825,28.0885416666667));
#74107=CARTESIAN_POINT('Ctrl Pts',(28.6775243943233,0.76353164693412,28.1302083333334));
#74108=CARTESIAN_POINT('Ctrl Pts',(28.2366991924311,-1.31894491186926E-14,
28.171875));
#74109=CARTESIAN_POINT('Ctrl Pts',(28.6775243943233,-0.763531646934146,
28.2135416666667));
#74110=CARTESIAN_POINT('Ctrl Pts',(29.1183495962155,-1.52706329386828,28.2552083333334));
#74111=CARTESIAN_POINT('Ctrl Pts',(30.,-1.52706329386828,28.296875));
#74112=CARTESIAN_POINT('Ctrl Pts',(30.8816504037844,-1.52706329386828,28.3385416666667));
#74113=CARTESIAN_POINT('Ctrl Pts',(31.3224756056766,-0.763531646934147,
28.3802083333334));
#74114=CARTESIAN_POINT('Ctrl Pts',(31.7633008075689,-1.36198038370242E-14,
28.421875));
#74115=CARTESIAN_POINT('Ctrl Pts',(31.3224756056766,0.763531646934118,28.4635416666667));
#74116=CARTESIAN_POINT('Ctrl Pts',(30.8816504037844,1.52706329386825,28.5052083333334));
#74117=CARTESIAN_POINT('Ctrl Pts',(30.,1.52706329386825,28.546875));
#74118=CARTESIAN_POINT('Ctrl Pts',(29.1183495962155,1.52706329386825,28.5885416666667));
#74119=CARTESIAN_POINT('Ctrl Pts',(28.6775243943233,0.76353164693412,28.6302083333334));
#74120=CARTESIAN_POINT('Ctrl Pts',(28.2366991924311,-1.31894491186926E-14,
28.671875));
#74121=CARTESIAN_POINT('Ctrl Pts',(28.6775243943233,-0.763531646934146,
28.7135416666667));
#74122=CARTESIAN_POINT('Ctrl Pts',(29.1183495962155,-1.52706329386828,28.7552083333334));
#74123=CARTESIAN_POINT('Ctrl Pts',(30.,-1.52706329386828,28.796875));
#74124=CARTESIAN_POINT('Ctrl Pts',(30.8816504037844,-1.52706329386828,28.8385416666667));
#74125=CARTESIAN_POINT('Ctrl Pts',(31.3224756056766,-0.763531646934147,
28.8802083333334));
#74126=CARTESIAN_POINT('Ctrl Pts',(31.7633008075689,-1.36198038370242E-14,
28.921875));
#74127=CARTESIAN_POINT('Ctrl Pts',(31.3224756056766,0.763531646934118,28.9635416666667));
#74128=CARTESIAN_POINT('Ctrl Pts',(30.8816504037844,1.52706329386825,29.0052083333334));
#74129=CARTESIAN_POINT('Ctrl Pts',(30.,1.52706329386825,29.046875));
#74130=CARTESIAN_POINT('Ctrl Pts',(29.1183495962155,1.52706329386825,29.0885416666667));
#74131=CARTESIAN_POINT('Ctrl Pts',(28.6775243943233,0.76353164693412,29.1302083333334));
#74132=CARTESIAN_POINT('Ctrl Pts',(28.2366991924311,-1.31894491186926E-14,
29.171875));
#74133=CARTESIAN_POINT('Ctrl Pts',(28.6775243943233,-0.763531646934146,
29.2135416666667));
#74134=CARTESIAN_POINT('Ctrl Pts',(29.1183495962155,-1.52706329386828,29.2552083333334));
#74135=CARTESIAN_POINT('Ctrl Pts',(30.,-1.52706329386828,29.296875));
#74136=CARTESIAN_POINT('Ctrl Pts',(30.8816504037844,-1.52706329386828,29.3385416666667));
#74137=CARTESIAN_POINT('Ctrl Pts',(31.3224756056766,-0.763531646934147,
29.3802083333334));
#74138=CARTESIAN_POINT('Ctrl Pts',(31.7633008075689,-1.36198038370242E-14,
29.421875));
#74139=CARTESIAN_POINT('Ctrl Pts',(31.3224756056766,0.763531646934118,29.4635416666667));
#74140=CARTESIAN_POINT('Ctrl Pts',(30.8816504037844,1.52706329386825,29.5052083333334));
#74141=CARTESIAN_POINT('Ctrl Pts',(30.,1.52706329386825,29.546875));
#74142=CARTESIAN_POINT('Ctrl Pts',(29.1183495962155,1.52706329386825,29.5885416666667));
#74143=CARTESIAN_POINT('Ctrl Pts',(28.6775243943233,0.76353164693412,29.6302083333334));
#74144=CARTESIAN_POINT('Ctrl Pts',(28.2366991924311,-1.31894491186926E-14,
29.671875));
#74145=CARTESIAN_POINT('Ctrl Pts',(28.6775243943233,-0.763531646934146,
29.7135416666667));
#74146=CARTESIAN_POINT('Ctrl Pts',(29.1183495962155,-1.52706329386828,29.7552083333334));
#74147=CARTESIAN_POINT('Ctrl Pts',(30.,-1.52706329386828,29.796875));
#74148=CARTESIAN_POINT('Ctrl Pts',(30.8816504037844,-1.52706329386828,29.8385416666667));
#74149=CARTESIAN_POINT('Ctrl Pts',(31.3224756056766,-0.763531646934147,
29.8802083333334));
#74150=CARTESIAN_POINT('Ctrl Pts',(31.7633008075689,-1.36198038370242E-14,
29.921875));
#74151=CARTESIAN_POINT('Ctrl Pts',(31.3224756056766,0.763531646934118,29.9635416666667));
#74152=CARTESIAN_POINT('Ctrl Pts',(30.8816504037844,1.52706329386825,30.0052083333334));
#74153=CARTESIAN_POINT('Ctrl Pts',(30.,1.52706329386825,30.046875));
#74154=CARTESIAN_POINT('Ctrl Pts',(29.1183495962155,1.52706329386825,30.0885416666667));
#74155=CARTESIAN_POINT('Ctrl Pts',(28.6775243943233,0.76353164693412,30.1302083333334));
#74156=CARTESIAN_POINT('Ctrl Pts',(28.2366991924311,-1.31894491186926E-14,
30.171875));
#74157=CARTESIAN_POINT('Ctrl Pts',(28.6775243943233,-0.763531646934146,
30.2135416666667));
#74158=CARTESIAN_POINT('Ctrl Pts',(29.1183495962155,-1.52706329386828,30.2552083333334));
#74159=CARTESIAN_POINT('Ctrl Pts',(30.,-1.52706329386828,30.296875));
#74160=CARTESIAN_POINT('Ctrl Pts',(30.8816504037844,-1.52706329386828,30.3385416666667));
#74161=CARTESIAN_POINT('Ctrl Pts',(31.3224756056766,-0.763531646934147,
30.3802083333334));
#74162=CARTESIAN_POINT('Ctrl Pts',(31.7633008075689,-1.36198038370242E-14,
30.421875));
#74163=CARTESIAN_POINT('Ctrl Pts',(31.3224756056766,0.763531646934118,30.4635416666667));
#74164=CARTESIAN_POINT('Ctrl Pts',(30.8816504037844,1.52706329386825,30.5052083333334));
#74165=CARTESIAN_POINT('Ctrl Pts',(30.,1.52706329386825,30.546875));
#74166=CARTESIAN_POINT('Ctrl Pts',(29.1183495962155,1.52706329386825,30.5885416666667));
#74167=CARTESIAN_POINT('Ctrl Pts',(28.6775243943233,0.76353164693412,30.6302083333334));
#74168=CARTESIAN_POINT('Ctrl Pts',(28.2366991924311,-1.31894491186926E-14,
30.671875));
#74169=CARTESIAN_POINT('Ctrl Pts',(28.6775243943233,-0.763531646934146,
30.7135416666667));
#74170=CARTESIAN_POINT('Ctrl Pts',(29.1183495962155,-1.52706329386828,30.7552083333334));
#74171=CARTESIAN_POINT('Ctrl Pts',(30.,-1.52706329386828,30.796875));
#74172=CARTESIAN_POINT('Ctrl Pts',(30.8816504037844,-1.52706329386828,30.8385416666667));
#74173=CARTESIAN_POINT('Ctrl Pts',(31.3224756056766,-0.763531646934147,
30.8802083333334));
#74174=CARTESIAN_POINT('Ctrl Pts',(31.7633008075689,-1.36198038370242E-14,
30.921875));
#74175=CARTESIAN_POINT('Ctrl Pts',(31.3224756056766,0.763531646934118,30.9635416666667));
#74176=CARTESIAN_POINT('Ctrl Pts',(30.8816504037844,1.52706329386825,31.0052083333334));
#74177=CARTESIAN_POINT('Ctrl Pts',(30.,1.52706329386825,31.046875));
#74178=CARTESIAN_POINT('Ctrl Pts',(30.8234003400376,-0.838570603170131,
30.5624996575278));
#74179=CARTESIAN_POINT('Ctrl Pts',(30.9252409219315,-0.749808119816165,
30.5671289662449));
#74180=CARTESIAN_POINT('Ctrl Pts',(31.0094069192668,-0.645130506686946,
30.571193014068));
#74181=CARTESIAN_POINT('Ctrl Pts',(31.1396529784097,-0.412074319923831,
30.5795221820465));
#74182=CARTESIAN_POINT('Ctrl Pts',(31.1849584507844,-0.287685440765051,
30.5838904393726));
#74183=CARTESIAN_POINT('Ctrl Pts',(31.2386945750578,-0.00655181811616603,
30.5935664195233));
#74184=CARTESIAN_POINT('Ctrl Pts',(31.2387490550162,0.149503133824081,30.5988162542928));
#74185=CARTESIAN_POINT('Ctrl Pts',(31.1719223736106,0.500568259068406,30.610386374166));
#74186=CARTESIAN_POINT('Ctrl Pts',(31.0923154827319,0.652496494934345,30.6150433766711));
#74187=CARTESIAN_POINT('Ctrl Pts',(30.9283336729762,0.900293879400657,30.6239504439807));
#74188=CARTESIAN_POINT('Ctrl Pts',(30.8055598520391,1.02369588322745,30.6294622341334));
#74189=CARTESIAN_POINT('Ctrl Pts',(30.5288337282237,1.20882504193349,30.6401101417162));
#74190=CARTESIAN_POINT('Ctrl Pts',(30.3799906896905,1.27260041719159,30.6451552807199));
#74191=CARTESIAN_POINT('Ctrl Pts',(30.0014927028803,1.35728019461807,30.6565651904367));
#74192=CARTESIAN_POINT('Ctrl Pts',(29.8132785668206,1.33887636851719,30.6613880776071));
#74193=CARTESIAN_POINT('Ctrl Pts',(29.5198061598154,1.28660005614596,30.6701589170659));
#74194=CARTESIAN_POINT('Ctrl Pts',(29.3521505621284,1.22147978200258,30.6756096035631));
#74195=CARTESIAN_POINT('Ctrl Pts',(29.0485837866741,1.02916361274227,30.6863949411503));
#74196=CARTESIAN_POINT('Ctrl Pts',(28.9162494293832,0.902843317652004,30.6916208752244));
#74197=CARTESIAN_POINT('Ctrl Pts',(28.7272437086822,0.633185410868888,30.7002552651022));
#74198=CARTESIAN_POINT('Ctrl Pts',(28.6461891944724,0.476094037694283,30.7048351996635));
#74199=CARTESIAN_POINT('Ctrl Pts',(28.551105022901,0.105569064666544,30.715730913862));
#74200=CARTESIAN_POINT('Ctrl Pts',(28.5402826505383,-0.0831493783931786,
30.7211721595761));
#74201=CARTESIAN_POINT('Ctrl Pts',(28.5859138822382,-0.415083694084825,
30.7305650693331));
#74202=CARTESIAN_POINT('Ctrl Pts',(28.6283908398168,-0.557537406078615,
30.7345346397522));
#74203=CARTESIAN_POINT('Ctrl Pts',(28.7447696187018,-0.802908073480822,
30.7412906353098));
#74204=CARTESIAN_POINT('Ctrl Pts',(28.8264704242263,-0.938163811130005,
30.7451577422722));
#74205=CARTESIAN_POINT('Ctrl Pts',(28.9490560961683,-1.07028823734174,30.7500000000014));
#74206=CARTESIAN_POINT('Ctrl Pts',(30.,1.52706329386825,16.015625));
#74207=CARTESIAN_POINT('Ctrl Pts',(29.1183495962155,1.52706329386825,16.0572916666666));
#74208=CARTESIAN_POINT('Ctrl Pts',(28.6775243943233,0.76353164693412,16.0989583333333));
#74209=CARTESIAN_POINT('Ctrl Pts',(28.2366991924311,-1.31894491186926E-14,
16.140625));
#74210=CARTESIAN_POINT('Ctrl Pts',(28.6775243943233,-0.763531646934146,
16.1822916666666));
#74211=CARTESIAN_POINT('Ctrl Pts',(29.1183495962155,-1.52706329386828,16.2239583333333));
#74212=CARTESIAN_POINT('Ctrl Pts',(30.,-1.52706329386828,16.265625));
#74213=CARTESIAN_POINT('Ctrl Pts',(30.8816504037844,-1.52706329386828,16.3072916666666));
#74214=CARTESIAN_POINT('Ctrl Pts',(31.3224756056766,-0.763531646934147,
16.3489583333333));
#74215=CARTESIAN_POINT('Ctrl Pts',(31.7633008075689,-1.36198038370242E-14,
16.390625));
#74216=CARTESIAN_POINT('Ctrl Pts',(31.3224756056766,0.763531646934118,16.4322916666666));
#74217=CARTESIAN_POINT('Ctrl Pts',(30.8816504037844,1.52706329386825,16.4739583333333));
#74218=CARTESIAN_POINT('Ctrl Pts',(30.,1.52706329386825,16.515625));
#74219=CARTESIAN_POINT('Ctrl Pts',(29.1183495962155,1.52706329386825,16.5572916666666));
#74220=CARTESIAN_POINT('Ctrl Pts',(28.6775243943233,0.76353164693412,16.5989583333333));
#74221=CARTESIAN_POINT('Ctrl Pts',(28.2366991924311,-1.31894491186926E-14,
16.640625));
#74222=CARTESIAN_POINT('Ctrl Pts',(28.6775243943233,-0.763531646934146,
16.6822916666666));
#74223=CARTESIAN_POINT('Ctrl Pts',(29.1183495962155,-1.52706329386828,16.7239583333333));
#74224=CARTESIAN_POINT('Ctrl Pts',(30.,-1.52706329386828,16.765625));
#74225=CARTESIAN_POINT('Ctrl Pts',(30.8816504037844,-1.52706329386828,16.8072916666666));
#74226=CARTESIAN_POINT('Ctrl Pts',(31.3224756056766,-0.763531646934147,
16.8489583333333));
#74227=CARTESIAN_POINT('Ctrl Pts',(31.7633008075689,-1.36198038370242E-14,
16.890625));
#74228=CARTESIAN_POINT('Ctrl Pts',(31.3224756056766,0.763531646934118,16.9322916666666));
#74229=CARTESIAN_POINT('Ctrl Pts',(30.8816504037844,1.52706329386825,16.9739583333333));
#74230=CARTESIAN_POINT('Ctrl Pts',(30.,1.52706329386825,17.015625));
#74231=CARTESIAN_POINT('Ctrl Pts',(29.1183495962155,1.52706329386825,17.0572916666666));
#74232=CARTESIAN_POINT('Ctrl Pts',(28.6775243943233,0.76353164693412,17.0989583333333));
#74233=CARTESIAN_POINT('Ctrl Pts',(28.2366991924311,-1.31894491186926E-14,
17.140625));
#74234=CARTESIAN_POINT('Ctrl Pts',(28.6775243943233,-0.763531646934146,
17.1822916666666));
#74235=CARTESIAN_POINT('Ctrl Pts',(29.1183495962155,-1.52706329386828,17.2239583333333));
#74236=CARTESIAN_POINT('Ctrl Pts',(30.,-1.52706329386828,17.265625));
#74237=CARTESIAN_POINT('Ctrl Pts',(30.8816504037844,-1.52706329386828,17.3072916666666));
#74238=CARTESIAN_POINT('Ctrl Pts',(31.3224756056766,-0.763531646934147,
17.3489583333333));
#74239=CARTESIAN_POINT('Ctrl Pts',(31.7633008075689,-1.36198038370242E-14,
17.390625));
#74240=CARTESIAN_POINT('Ctrl Pts',(31.3224756056766,0.763531646934118,17.4322916666666));
#74241=CARTESIAN_POINT('Ctrl Pts',(30.8816504037844,1.52706329386825,17.4739583333333));
#74242=CARTESIAN_POINT('Ctrl Pts',(30.,1.52706329386825,17.515625));
#74243=CARTESIAN_POINT('Ctrl Pts',(29.1183495962155,1.52706329386825,17.5572916666666));
#74244=CARTESIAN_POINT('Ctrl Pts',(28.6775243943233,0.76353164693412,17.5989583333333));
#74245=CARTESIAN_POINT('Ctrl Pts',(28.2366991924311,-1.31894491186926E-14,
17.640625));
#74246=CARTESIAN_POINT('Ctrl Pts',(28.6775243943233,-0.763531646934146,
17.6822916666666));
#74247=CARTESIAN_POINT('Ctrl Pts',(29.1183495962155,-1.52706329386828,17.7239583333333));
#74248=CARTESIAN_POINT('Ctrl Pts',(30.,-1.52706329386828,17.765625));
#74249=CARTESIAN_POINT('Ctrl Pts',(30.8816504037844,-1.52706329386828,17.8072916666666));
#74250=CARTESIAN_POINT('Ctrl Pts',(31.3224756056766,-0.763531646934147,
17.8489583333333));
#74251=CARTESIAN_POINT('Ctrl Pts',(31.7633008075689,-1.36198038370242E-14,
17.890625));
#74252=CARTESIAN_POINT('Ctrl Pts',(31.3224756056766,0.763531646934118,17.9322916666666));
#74253=CARTESIAN_POINT('Ctrl Pts',(30.8816504037844,1.52706329386825,17.9739583333333));
#74254=CARTESIAN_POINT('Ctrl Pts',(30.,1.52706329386825,18.015625));
#74255=CARTESIAN_POINT('Ctrl Pts',(29.1183495962155,1.52706329386825,18.0572916666666));
#74256=CARTESIAN_POINT('Ctrl Pts',(28.6775243943233,0.76353164693412,18.0989583333333));
#74257=CARTESIAN_POINT('Ctrl Pts',(28.2366991924311,-1.31894491186926E-14,
18.140625));
#74258=CARTESIAN_POINT('Ctrl Pts',(28.6775243943233,-0.763531646934146,
18.1822916666666));
#74259=CARTESIAN_POINT('Ctrl Pts',(29.1183495962155,-1.52706329386828,18.2239583333333));
#74260=CARTESIAN_POINT('Ctrl Pts',(30.,-1.52706329386828,18.265625));
#74261=CARTESIAN_POINT('Ctrl Pts',(30.8816504037844,-1.52706329386828,18.3072916666666));
#74262=CARTESIAN_POINT('Ctrl Pts',(31.3224756056766,-0.763531646934147,
18.3489583333333));
#74263=CARTESIAN_POINT('Ctrl Pts',(31.7633008075689,-1.36198038370242E-14,
18.390625));
#74264=CARTESIAN_POINT('Ctrl Pts',(31.3224756056766,0.763531646934118,18.4322916666666));
#74265=CARTESIAN_POINT('Ctrl Pts',(30.8816504037844,1.52706329386825,18.4739583333333));
#74266=CARTESIAN_POINT('Ctrl Pts',(30.,1.52706329386825,18.515625));
#74267=CARTESIAN_POINT('Ctrl Pts',(29.1183495962155,1.52706329386825,18.5572916666666));
#74268=CARTESIAN_POINT('Ctrl Pts',(28.6775243943233,0.76353164693412,18.5989583333333));
#74269=CARTESIAN_POINT('Ctrl Pts',(28.2366991924311,-1.31894491186926E-14,
18.640625));
#74270=CARTESIAN_POINT('Ctrl Pts',(28.6775243943233,-0.763531646934146,
18.6822916666666));
#74271=CARTESIAN_POINT('Ctrl Pts',(29.1183495962155,-1.52706329386828,18.7239583333333));
#74272=CARTESIAN_POINT('Ctrl Pts',(30.,-1.52706329386828,18.765625));
#74273=CARTESIAN_POINT('Ctrl Pts',(30.8816504037844,-1.52706329386828,18.8072916666666));
#74274=CARTESIAN_POINT('Ctrl Pts',(31.3224756056766,-0.763531646934147,
18.8489583333333));
#74275=CARTESIAN_POINT('Ctrl Pts',(31.7633008075689,-1.36198038370242E-14,
18.890625));
#74276=CARTESIAN_POINT('Ctrl Pts',(31.3224756056766,0.763531646934118,18.9322916666666));
#74277=CARTESIAN_POINT('Ctrl Pts',(30.8816504037844,1.52706329386825,18.9739583333333));
#74278=CARTESIAN_POINT('Ctrl Pts',(30.,1.52706329386825,19.015625));
#74279=CARTESIAN_POINT('Ctrl Pts',(29.1183495962155,1.52706329386825,19.0572916666666));
#74280=CARTESIAN_POINT('Ctrl Pts',(28.6775243943233,0.76353164693412,19.0989583333333));
#74281=CARTESIAN_POINT('Ctrl Pts',(28.2366991924311,-1.31894491186926E-14,
19.140625));
#74282=CARTESIAN_POINT('Ctrl Pts',(28.6775243943233,-0.763531646934146,
19.1822916666666));
#74283=CARTESIAN_POINT('Ctrl Pts',(29.1183495962155,-1.52706329386828,19.2239583333333));
#74284=CARTESIAN_POINT('Ctrl Pts',(30.,-1.52706329386828,19.265625));
#74285=CARTESIAN_POINT('Ctrl Pts',(30.8816504037844,-1.52706329386828,19.3072916666666));
#74286=CARTESIAN_POINT('Ctrl Pts',(31.3224756056766,-0.763531646934147,
19.3489583333333));
#74287=CARTESIAN_POINT('Ctrl Pts',(31.7633008075689,-1.36198038370242E-14,
19.390625));
#74288=CARTESIAN_POINT('Ctrl Pts',(31.3224756056766,0.763531646934118,19.4322916666666));
#74289=CARTESIAN_POINT('Ctrl Pts',(30.8816504037844,1.52706329386825,19.4739583333333));
#74290=CARTESIAN_POINT('Ctrl Pts',(30.,1.52706329386825,19.515625));
#74291=CARTESIAN_POINT('Ctrl Pts',(29.1183495962155,1.52706329386825,19.5572916666666));
#74292=CARTESIAN_POINT('Ctrl Pts',(28.6775243943233,0.76353164693412,19.5989583333333));
#74293=CARTESIAN_POINT('Ctrl Pts',(28.2366991924311,-1.31894491186926E-14,
19.640625));
#74294=CARTESIAN_POINT('Ctrl Pts',(28.6775243943233,-0.763531646934146,
19.6822916666666));
#74295=CARTESIAN_POINT('Ctrl Pts',(29.1183495962155,-1.52706329386828,19.7239583333333));
#74296=CARTESIAN_POINT('Ctrl Pts',(30.,-1.52706329386828,19.765625));
#74297=CARTESIAN_POINT('Ctrl Pts',(30.8816504037844,-1.52706329386828,19.8072916666666));
#74298=CARTESIAN_POINT('Ctrl Pts',(31.3224756056766,-0.763531646934147,
19.8489583333333));
#74299=CARTESIAN_POINT('Ctrl Pts',(31.7633008075689,-1.36198038370242E-14,
19.890625));
#74300=CARTESIAN_POINT('Ctrl Pts',(31.3224756056766,0.763531646934118,19.9322916666666));
#74301=CARTESIAN_POINT('Ctrl Pts',(30.8816504037844,1.52706329386825,19.9739583333333));
#74302=CARTESIAN_POINT('Ctrl Pts',(30.,1.52706329386825,20.015625));
#74303=CARTESIAN_POINT('Ctrl Pts',(29.1183495962155,1.52706329386825,20.0572916666666));
#74304=CARTESIAN_POINT('Ctrl Pts',(28.6775243943233,0.76353164693412,20.0989583333333));
#74305=CARTESIAN_POINT('Ctrl Pts',(28.2366991924311,-1.31894491186926E-14,
20.140625));
#74306=CARTESIAN_POINT('Ctrl Pts',(28.6775243943233,-0.763531646934146,
20.1822916666666));
#74307=CARTESIAN_POINT('Ctrl Pts',(29.1183495962155,-1.52706329386828,20.2239583333333));
#74308=CARTESIAN_POINT('Ctrl Pts',(30.,-1.52706329386828,20.265625));
#74309=CARTESIAN_POINT('Ctrl Pts',(30.8816504037844,-1.52706329386828,20.3072916666666));
#74310=CARTESIAN_POINT('Ctrl Pts',(31.3224756056766,-0.763531646934147,
20.3489583333333));
#74311=CARTESIAN_POINT('Ctrl Pts',(31.7633008075689,-1.36198038370242E-14,
20.390625));
#74312=CARTESIAN_POINT('Ctrl Pts',(31.3224756056766,0.763531646934118,20.4322916666666));
#74313=CARTESIAN_POINT('Ctrl Pts',(30.8816504037844,1.52706329386825,20.4739583333333));
#74314=CARTESIAN_POINT('Ctrl Pts',(30.,1.52706329386825,20.515625));
#74315=CARTESIAN_POINT('Ctrl Pts',(29.1183495962155,1.52706329386825,20.5572916666666));
#74316=CARTESIAN_POINT('Ctrl Pts',(28.6775243943233,0.76353164693412,20.5989583333333));
#74317=CARTESIAN_POINT('Ctrl Pts',(28.2366991924311,-1.31894491186926E-14,
20.640625));
#74318=CARTESIAN_POINT('Ctrl Pts',(28.6775243943233,-0.763531646934146,
20.6822916666666));
#74319=CARTESIAN_POINT('Ctrl Pts',(29.1183495962155,-1.52706329386828,20.7239583333333));
#74320=CARTESIAN_POINT('Ctrl Pts',(30.,-1.52706329386828,20.765625));
#74321=CARTESIAN_POINT('Ctrl Pts',(30.8816504037844,-1.52706329386828,20.8072916666666));
#74322=CARTESIAN_POINT('Ctrl Pts',(31.3224756056766,-0.763531646934147,
20.8489583333333));
#74323=CARTESIAN_POINT('Ctrl Pts',(31.7633008075689,-1.36198038370242E-14,
20.890625));
#74324=CARTESIAN_POINT('Ctrl Pts',(31.3224756056766,0.763531646934118,20.9322916666666));
#74325=CARTESIAN_POINT('Ctrl Pts',(30.8816504037844,1.52706329386825,20.9739583333333));
#74326=CARTESIAN_POINT('Ctrl Pts',(30.,1.52706329386825,21.015625));
#74327=CARTESIAN_POINT('Ctrl Pts',(29.1183495962155,1.52706329386825,21.0572916666666));
#74328=CARTESIAN_POINT('Ctrl Pts',(28.6775243943233,0.76353164693412,21.0989583333333));
#74329=CARTESIAN_POINT('Ctrl Pts',(28.2366991924311,-1.31894491186926E-14,
21.140625));
#74330=CARTESIAN_POINT('Ctrl Pts',(28.6775243943233,-0.763531646934146,
21.1822916666666));
#74331=CARTESIAN_POINT('Ctrl Pts',(29.1183495962155,-1.52706329386828,21.2239583333333));
#74332=CARTESIAN_POINT('Ctrl Pts',(30.,-1.52706329386828,21.265625));
#74333=CARTESIAN_POINT('Ctrl Pts',(30.8816504037844,-1.52706329386828,21.3072916666666));
#74334=CARTESIAN_POINT('Ctrl Pts',(31.3224756056766,-0.763531646934147,
21.3489583333333));
#74335=CARTESIAN_POINT('Ctrl Pts',(31.7633008075689,-1.36198038370242E-14,
21.390625));
#74336=CARTESIAN_POINT('Ctrl Pts',(31.3224756056766,0.763531646934118,21.4322916666666));
#74337=CARTESIAN_POINT('Ctrl Pts',(30.8816504037844,1.52706329386825,21.4739583333333));
#74338=CARTESIAN_POINT('Ctrl Pts',(30.,1.52706329386825,21.515625));
#74339=CARTESIAN_POINT('Ctrl Pts',(29.1183495962155,1.52706329386825,21.5572916666666));
#74340=CARTESIAN_POINT('Ctrl Pts',(28.6775243943233,0.76353164693412,21.5989583333333));
#74341=CARTESIAN_POINT('Ctrl Pts',(28.2366991924311,-1.31894491186926E-14,
21.640625));
#74342=CARTESIAN_POINT('Ctrl Pts',(28.6775243943233,-0.763531646934146,
21.6822916666666));
#74343=CARTESIAN_POINT('Ctrl Pts',(29.1183495962155,-1.52706329386828,21.7239583333333));
#74344=CARTESIAN_POINT('Ctrl Pts',(30.,-1.52706329386828,21.765625));
#74345=CARTESIAN_POINT('Ctrl Pts',(30.8816504037844,-1.52706329386828,21.8072916666666));
#74346=CARTESIAN_POINT('Ctrl Pts',(31.3224756056766,-0.763531646934147,
21.8489583333333));
#74347=CARTESIAN_POINT('Ctrl Pts',(31.7633008075689,-1.36198038370242E-14,
21.890625));
#74348=CARTESIAN_POINT('Ctrl Pts',(31.3224756056766,0.763531646934118,21.9322916666666));
#74349=CARTESIAN_POINT('Ctrl Pts',(30.8816504037844,1.52706329386825,21.9739583333333));
#74350=CARTESIAN_POINT('Ctrl Pts',(30.,1.52706329386825,22.015625));
#74351=CARTESIAN_POINT('Ctrl Pts',(29.1183495962155,1.52706329386825,22.0572916666666));
#74352=CARTESIAN_POINT('Ctrl Pts',(28.6775243943233,0.76353164693412,22.0989583333333));
#74353=CARTESIAN_POINT('Ctrl Pts',(28.2366991924311,-1.31894491186926E-14,
22.140625));
#74354=CARTESIAN_POINT('Ctrl Pts',(28.6775243943233,-0.763531646934146,
22.1822916666666));
#74355=CARTESIAN_POINT('Ctrl Pts',(29.1183495962155,-1.52706329386828,22.2239583333333));
#74356=CARTESIAN_POINT('Ctrl Pts',(30.,-1.52706329386828,22.265625));
#74357=CARTESIAN_POINT('Ctrl Pts',(30.8816504037844,-1.52706329386828,22.3072916666666));
#74358=CARTESIAN_POINT('Ctrl Pts',(31.3224756056766,-0.763531646934147,
22.3489583333333));
#74359=CARTESIAN_POINT('Ctrl Pts',(31.7633008075689,-1.36198038370242E-14,
22.390625));
#74360=CARTESIAN_POINT('Ctrl Pts',(31.3224756056766,0.763531646934118,22.4322916666666));
#74361=CARTESIAN_POINT('Ctrl Pts',(30.8816504037844,1.52706329386825,22.4739583333333));
#74362=CARTESIAN_POINT('Ctrl Pts',(30.,1.52706329386825,22.515625));
#74363=CARTESIAN_POINT('Ctrl Pts',(29.1183495962155,1.52706329386825,22.5572916666666));
#74364=CARTESIAN_POINT('Ctrl Pts',(28.6775243943233,0.76353164693412,22.5989583333333));
#74365=CARTESIAN_POINT('Ctrl Pts',(28.2366991924311,-1.31894491186926E-14,
22.640625));
#74366=CARTESIAN_POINT('Ctrl Pts',(28.6775243943233,-0.763531646934146,
22.6822916666666));
#74367=CARTESIAN_POINT('Ctrl Pts',(29.1183495962155,-1.52706329386828,22.7239583333333));
#74368=CARTESIAN_POINT('Ctrl Pts',(30.,-1.52706329386828,22.765625));
#74369=CARTESIAN_POINT('Ctrl Pts',(30.8816504037844,-1.52706329386828,22.8072916666666));
#74370=CARTESIAN_POINT('Ctrl Pts',(31.3224756056766,-0.763531646934147,
22.8489583333333));
#74371=CARTESIAN_POINT('Ctrl Pts',(31.7633008075689,-1.36198038370242E-14,
22.890625));
#74372=CARTESIAN_POINT('Ctrl Pts',(31.3224756056766,0.763531646934118,22.9322916666666));
#74373=CARTESIAN_POINT('Ctrl Pts',(30.8816504037844,1.52706329386825,22.9739583333333));
#74374=CARTESIAN_POINT('Ctrl Pts',(30.,1.52706329386825,23.015625));
#74375=CARTESIAN_POINT('Ctrl Pts',(29.1183495962155,1.52706329386825,23.0572916666666));
#74376=CARTESIAN_POINT('Ctrl Pts',(28.6775243943233,0.76353164693412,23.0989583333333));
#74377=CARTESIAN_POINT('Ctrl Pts',(28.2366991924311,-1.31894491186926E-14,
23.140625));
#74378=CARTESIAN_POINT('Ctrl Pts',(28.6775243943233,-0.763531646934146,
23.1822916666666));
#74379=CARTESIAN_POINT('Ctrl Pts',(29.1183495962155,-1.52706329386828,23.2239583333333));
#74380=CARTESIAN_POINT('Ctrl Pts',(30.,-1.52706329386828,23.265625));
#74381=CARTESIAN_POINT('Ctrl Pts',(30.8816504037844,-1.52706329386828,23.3072916666666));
#74382=CARTESIAN_POINT('Ctrl Pts',(31.3224756056766,-0.763531646934147,
23.3489583333333));
#74383=CARTESIAN_POINT('Ctrl Pts',(31.7633008075689,-1.36198038370242E-14,
23.390625));
#74384=CARTESIAN_POINT('Ctrl Pts',(31.3224756056766,0.763531646934118,23.4322916666666));
#74385=CARTESIAN_POINT('Ctrl Pts',(30.8816504037844,1.52706329386825,23.4739583333333));
#74386=CARTESIAN_POINT('Ctrl Pts',(30.,1.52706329386825,23.515625));
#74387=CARTESIAN_POINT('Ctrl Pts',(29.1183495962155,1.52706329386825,23.5572916666666));
#74388=CARTESIAN_POINT('Ctrl Pts',(28.6775243943233,0.76353164693412,23.5989583333333));
#74389=CARTESIAN_POINT('Ctrl Pts',(28.2366991924311,-1.31894491186926E-14,
23.640625));
#74390=CARTESIAN_POINT('Ctrl Pts',(28.6775243943233,-0.763531646934146,
23.6822916666666));
#74391=CARTESIAN_POINT('Ctrl Pts',(29.1183495962155,-1.52706329386828,23.7239583333333));
#74392=CARTESIAN_POINT('Ctrl Pts',(30.,-1.52706329386828,23.765625));
#74393=CARTESIAN_POINT('Ctrl Pts',(30.8816504037844,-1.52706329386828,23.8072916666666));
#74394=CARTESIAN_POINT('Ctrl Pts',(31.3224756056766,-0.763531646934147,
23.8489583333333));
#74395=CARTESIAN_POINT('Ctrl Pts',(31.7633008075689,-1.36198038370242E-14,
23.890625));
#74396=CARTESIAN_POINT('Ctrl Pts',(31.3224756056766,0.763531646934118,23.9322916666666));
#74397=CARTESIAN_POINT('Ctrl Pts',(30.8816504037844,1.52706329386825,23.9739583333333));
#74398=CARTESIAN_POINT('Ctrl Pts',(30.,1.52706329386825,24.015625));
#74399=CARTESIAN_POINT('Ctrl Pts',(29.1183495962155,1.52706329386825,24.0572916666666));
#74400=CARTESIAN_POINT('Ctrl Pts',(28.6775243943233,0.76353164693412,24.0989583333333));
#74401=CARTESIAN_POINT('Ctrl Pts',(28.2366991924311,-1.31894491186926E-14,
24.140625));
#74402=CARTESIAN_POINT('Ctrl Pts',(28.6775243943233,-0.763531646934146,
24.1822916666666));
#74403=CARTESIAN_POINT('Ctrl Pts',(29.1183495962155,-1.52706329386828,24.2239583333333));
#74404=CARTESIAN_POINT('Ctrl Pts',(30.,-1.52706329386828,24.265625));
#74405=CARTESIAN_POINT('Ctrl Pts',(30.8816504037844,-1.52706329386828,24.3072916666666));
#74406=CARTESIAN_POINT('Ctrl Pts',(31.3224756056766,-0.763531646934147,
24.3489583333333));
#74407=CARTESIAN_POINT('Ctrl Pts',(31.7633008075689,-1.36198038370242E-14,
24.390625));
#74408=CARTESIAN_POINT('Ctrl Pts',(31.3224756056766,0.763531646934118,24.4322916666666));
#74409=CARTESIAN_POINT('Ctrl Pts',(30.8816504037844,1.52706329386825,24.4739583333333));
#74410=CARTESIAN_POINT('Ctrl Pts',(30.,1.52706329386825,24.515625));
#74411=CARTESIAN_POINT('Ctrl Pts',(29.1183495962155,1.52706329386825,24.5572916666666));
#74412=CARTESIAN_POINT('Ctrl Pts',(28.6775243943233,0.76353164693412,24.5989583333333));
#74413=CARTESIAN_POINT('Ctrl Pts',(28.2366991924311,-1.31894491186926E-14,
24.640625));
#74414=CARTESIAN_POINT('Ctrl Pts',(28.6775243943233,-0.763531646934146,
24.6822916666666));
#74415=CARTESIAN_POINT('Ctrl Pts',(29.1183495962155,-1.52706329386828,24.7239583333333));
#74416=CARTESIAN_POINT('Ctrl Pts',(30.,-1.52706329386828,24.765625));
#74417=CARTESIAN_POINT('Ctrl Pts',(30.8816504037844,-1.52706329386828,24.8072916666666));
#74418=CARTESIAN_POINT('Ctrl Pts',(31.3224756056766,-0.763531646934147,
24.8489583333333));
#74419=CARTESIAN_POINT('Ctrl Pts',(31.7633008075689,-1.36198038370242E-14,
24.890625));
#74420=CARTESIAN_POINT('Ctrl Pts',(31.3224756056766,0.763531646934118,24.9322916666666));
#74421=CARTESIAN_POINT('Ctrl Pts',(30.8816504037844,1.52706329386825,24.9739583333333));
#74422=CARTESIAN_POINT('Ctrl Pts',(30.,1.52706329386825,25.015625));
#74423=CARTESIAN_POINT('Ctrl Pts',(29.1183495962155,1.52706329386825,25.0572916666666));
#74424=CARTESIAN_POINT('Ctrl Pts',(28.6775243943233,0.76353164693412,25.0989583333333));
#74425=CARTESIAN_POINT('Ctrl Pts',(28.2366991924311,-1.31894491186926E-14,
25.140625));
#74426=CARTESIAN_POINT('Ctrl Pts',(28.6775243943233,-0.763531646934146,
25.1822916666666));
#74427=CARTESIAN_POINT('Ctrl Pts',(29.1183495962155,-1.52706329386828,25.2239583333333));
#74428=CARTESIAN_POINT('Ctrl Pts',(30.,-1.52706329386828,25.265625));
#74429=CARTESIAN_POINT('Ctrl Pts',(30.8816504037844,-1.52706329386828,25.3072916666666));
#74430=CARTESIAN_POINT('Ctrl Pts',(31.3224756056766,-0.763531646934147,
25.3489583333333));
#74431=CARTESIAN_POINT('Ctrl Pts',(31.7633008075689,-1.36198038370242E-14,
25.390625));
#74432=CARTESIAN_POINT('Ctrl Pts',(31.3224756056766,0.763531646934118,25.4322916666666));
#74433=CARTESIAN_POINT('Ctrl Pts',(30.8816504037844,1.52706329386825,25.4739583333333));
#74434=CARTESIAN_POINT('Ctrl Pts',(30.,1.52706329386825,25.515625));
#74435=CARTESIAN_POINT('Ctrl Pts',(29.1183495962155,1.52706329386825,25.5572916666666));
#74436=CARTESIAN_POINT('Ctrl Pts',(28.6775243943233,0.76353164693412,25.5989583333333));
#74437=CARTESIAN_POINT('Ctrl Pts',(28.2366991924311,-1.31894491186926E-14,
25.640625));
#74438=CARTESIAN_POINT('Ctrl Pts',(28.6775243943233,-0.763531646934146,
25.6822916666666));
#74439=CARTESIAN_POINT('Ctrl Pts',(29.1183495962155,-1.52706329386828,25.7239583333333));
#74440=CARTESIAN_POINT('Ctrl Pts',(30.,-1.52706329386828,25.765625));
#74441=CARTESIAN_POINT('Ctrl Pts',(30.8816504037844,-1.52706329386828,25.8072916666666));
#74442=CARTESIAN_POINT('Ctrl Pts',(31.3224756056766,-0.763531646934147,
25.8489583333333));
#74443=CARTESIAN_POINT('Ctrl Pts',(31.7633008075689,-1.36198038370242E-14,
25.890625));
#74444=CARTESIAN_POINT('Ctrl Pts',(31.3224756056766,0.763531646934118,25.9322916666666));
#74445=CARTESIAN_POINT('Ctrl Pts',(30.8816504037844,1.52706329386825,25.9739583333333));
#74446=CARTESIAN_POINT('Ctrl Pts',(30.,1.52706329386825,26.015625));
#74447=CARTESIAN_POINT('Ctrl Pts',(29.1183495962155,1.52706329386825,26.0572916666666));
#74448=CARTESIAN_POINT('Ctrl Pts',(28.6775243943233,0.76353164693412,26.0989583333333));
#74449=CARTESIAN_POINT('Ctrl Pts',(28.2366991924311,-1.31894491186926E-14,
26.140625));
#74450=CARTESIAN_POINT('Ctrl Pts',(28.6775243943233,-0.763531646934146,
26.1822916666666));
#74451=CARTESIAN_POINT('Ctrl Pts',(29.1183495962155,-1.52706329386828,26.2239583333333));
#74452=CARTESIAN_POINT('Ctrl Pts',(30.,-1.52706329386828,26.265625));
#74453=CARTESIAN_POINT('Ctrl Pts',(30.8816504037844,-1.52706329386828,26.3072916666666));
#74454=CARTESIAN_POINT('Ctrl Pts',(31.3224756056766,-0.763531646934147,
26.3489583333333));
#74455=CARTESIAN_POINT('Ctrl Pts',(31.7633008075689,-1.36198038370242E-14,
26.390625));
#74456=CARTESIAN_POINT('Ctrl Pts',(31.3224756056766,0.763531646934118,26.4322916666666));
#74457=CARTESIAN_POINT('Ctrl Pts',(30.8816504037844,1.52706329386825,26.4739583333333));
#74458=CARTESIAN_POINT('Ctrl Pts',(30.,1.52706329386825,26.515625));
#74459=CARTESIAN_POINT('Ctrl Pts',(29.1183495962155,1.52706329386825,26.5572916666666));
#74460=CARTESIAN_POINT('Ctrl Pts',(28.6775243943233,0.76353164693412,26.5989583333333));
#74461=CARTESIAN_POINT('Ctrl Pts',(28.2366991924311,-1.31894491186926E-14,
26.640625));
#74462=CARTESIAN_POINT('Ctrl Pts',(28.6775243943233,-0.763531646934146,
26.6822916666666));
#74463=CARTESIAN_POINT('Ctrl Pts',(29.1183495962155,-1.52706329386828,26.7239583333333));
#74464=CARTESIAN_POINT('Ctrl Pts',(30.,-1.52706329386828,26.765625));
#74465=CARTESIAN_POINT('Ctrl Pts',(30.8816504037844,-1.52706329386828,26.8072916666666));
#74466=CARTESIAN_POINT('Ctrl Pts',(31.3224756056766,-0.763531646934147,
26.8489583333333));
#74467=CARTESIAN_POINT('Ctrl Pts',(31.7633008075689,-1.36198038370242E-14,
26.890625));
#74468=CARTESIAN_POINT('Ctrl Pts',(31.3224756056766,0.763531646934118,26.9322916666666));
#74469=CARTESIAN_POINT('Ctrl Pts',(30.8816504037844,1.52706329386825,26.9739583333333));
#74470=CARTESIAN_POINT('Ctrl Pts',(30.,1.52706329386825,27.015625));
#74471=CARTESIAN_POINT('Ctrl Pts',(29.1183495962155,1.52706329386825,27.0572916666666));
#74472=CARTESIAN_POINT('Ctrl Pts',(28.6775243943233,0.76353164693412,27.0989583333333));
#74473=CARTESIAN_POINT('Ctrl Pts',(28.2366991924311,-1.31894491186926E-14,
27.140625));
#74474=CARTESIAN_POINT('Ctrl Pts',(28.6775243943233,-0.763531646934146,
27.1822916666666));
#74475=CARTESIAN_POINT('Ctrl Pts',(29.1183495962155,-1.52706329386828,27.2239583333333));
#74476=CARTESIAN_POINT('Ctrl Pts',(30.,-1.52706329386828,27.265625));
#74477=CARTESIAN_POINT('Ctrl Pts',(30.8816504037844,-1.52706329386828,27.3072916666666));
#74478=CARTESIAN_POINT('Ctrl Pts',(31.3224756056766,-0.763531646934147,
27.3489583333333));
#74479=CARTESIAN_POINT('Ctrl Pts',(31.7633008075689,-1.36198038370242E-14,
27.390625));
#74480=CARTESIAN_POINT('Ctrl Pts',(31.3224756056766,0.763531646934118,27.4322916666666));
#74481=CARTESIAN_POINT('Ctrl Pts',(30.8816504037844,1.52706329386825,27.4739583333333));
#74482=CARTESIAN_POINT('Ctrl Pts',(30.,1.52706329386825,27.515625));
#74483=CARTESIAN_POINT('Ctrl Pts',(29.1183495962155,1.52706329386825,27.5572916666666));
#74484=CARTESIAN_POINT('Ctrl Pts',(28.6775243943233,0.76353164693412,27.5989583333333));
#74485=CARTESIAN_POINT('Ctrl Pts',(28.2366991924311,-1.31894491186926E-14,
27.640625));
#74486=CARTESIAN_POINT('Ctrl Pts',(28.6775243943233,-0.763531646934146,
27.6822916666666));
#74487=CARTESIAN_POINT('Ctrl Pts',(29.1183495962155,-1.52706329386828,27.7239583333333));
#74488=CARTESIAN_POINT('Ctrl Pts',(30.,-1.52706329386828,27.765625));
#74489=CARTESIAN_POINT('Ctrl Pts',(30.8816504037844,-1.52706329386828,27.8072916666666));
#74490=CARTESIAN_POINT('Ctrl Pts',(31.3224756056766,-0.763531646934147,
27.8489583333333));
#74491=CARTESIAN_POINT('Ctrl Pts',(31.7633008075689,-1.36198038370242E-14,
27.890625));
#74492=CARTESIAN_POINT('Ctrl Pts',(31.3224756056766,0.763531646934118,27.9322916666666));
#74493=CARTESIAN_POINT('Ctrl Pts',(30.8816504037844,1.52706329386825,27.9739583333333));
#74494=CARTESIAN_POINT('Ctrl Pts',(30.,1.52706329386825,28.015625));
#74495=CARTESIAN_POINT('Ctrl Pts',(29.1183495962155,1.52706329386825,28.0572916666666));
#74496=CARTESIAN_POINT('Ctrl Pts',(28.6775243943233,0.76353164693412,28.0989583333333));
#74497=CARTESIAN_POINT('Ctrl Pts',(28.2366991924311,-1.31894491186926E-14,
28.140625));
#74498=CARTESIAN_POINT('Ctrl Pts',(28.6775243943233,-0.763531646934146,
28.1822916666666));
#74499=CARTESIAN_POINT('Ctrl Pts',(29.1183495962155,-1.52706329386828,28.2239583333333));
#74500=CARTESIAN_POINT('Ctrl Pts',(30.,-1.52706329386828,28.265625));
#74501=CARTESIAN_POINT('Ctrl Pts',(30.8816504037844,-1.52706329386828,28.3072916666666));
#74502=CARTESIAN_POINT('Ctrl Pts',(31.3224756056766,-0.763531646934147,
28.3489583333333));
#74503=CARTESIAN_POINT('Ctrl Pts',(31.7633008075689,-1.36198038370242E-14,
28.390625));
#74504=CARTESIAN_POINT('Ctrl Pts',(31.3224756056766,0.763531646934118,28.4322916666666));
#74505=CARTESIAN_POINT('Ctrl Pts',(30.8816504037844,1.52706329386825,28.4739583333333));
#74506=CARTESIAN_POINT('Ctrl Pts',(30.,1.52706329386825,28.515625));
#74507=CARTESIAN_POINT('Ctrl Pts',(29.1183495962155,1.52706329386825,28.5572916666666));
#74508=CARTESIAN_POINT('Ctrl Pts',(28.6775243943233,0.76353164693412,28.5989583333333));
#74509=CARTESIAN_POINT('Ctrl Pts',(28.2366991924311,-1.31894491186926E-14,
28.640625));
#74510=CARTESIAN_POINT('Ctrl Pts',(28.6775243943233,-0.763531646934146,
28.6822916666666));
#74511=CARTESIAN_POINT('Ctrl Pts',(29.1183495962155,-1.52706329386828,28.7239583333333));
#74512=CARTESIAN_POINT('Ctrl Pts',(30.,-1.52706329386828,28.765625));
#74513=CARTESIAN_POINT('Ctrl Pts',(30.8816504037844,-1.52706329386828,28.8072916666666));
#74514=CARTESIAN_POINT('Ctrl Pts',(31.3224756056766,-0.763531646934147,
28.8489583333333));
#74515=CARTESIAN_POINT('Ctrl Pts',(31.7633008075689,-1.36198038370242E-14,
28.890625));
#74516=CARTESIAN_POINT('Ctrl Pts',(31.3224756056766,0.763531646934118,28.9322916666666));
#74517=CARTESIAN_POINT('Ctrl Pts',(30.8816504037844,1.52706329386825,28.9739583333333));
#74518=CARTESIAN_POINT('Ctrl Pts',(30.,1.52706329386825,29.015625));
#74519=CARTESIAN_POINT('Ctrl Pts',(29.1183495962155,1.52706329386825,29.0572916666666));
#74520=CARTESIAN_POINT('Ctrl Pts',(28.6775243943233,0.76353164693412,29.0989583333333));
#74521=CARTESIAN_POINT('Ctrl Pts',(28.2366991924311,-1.31894491186926E-14,
29.140625));
#74522=CARTESIAN_POINT('Ctrl Pts',(28.6775243943233,-0.763531646934146,
29.1822916666666));
#74523=CARTESIAN_POINT('Ctrl Pts',(29.1183495962155,-1.52706329386828,29.2239583333333));
#74524=CARTESIAN_POINT('Ctrl Pts',(30.,-1.52706329386828,29.265625));
#74525=CARTESIAN_POINT('Ctrl Pts',(30.8816504037844,-1.52706329386828,29.3072916666666));
#74526=CARTESIAN_POINT('Ctrl Pts',(31.3224756056766,-0.763531646934147,
29.3489583333333));
#74527=CARTESIAN_POINT('Ctrl Pts',(31.7633008075689,-1.36198038370242E-14,
29.390625));
#74528=CARTESIAN_POINT('Ctrl Pts',(31.3224756056766,0.763531646934118,29.4322916666666));
#74529=CARTESIAN_POINT('Ctrl Pts',(30.8816504037844,1.52706329386825,29.4739583333333));
#74530=CARTESIAN_POINT('Ctrl Pts',(30.,1.52706329386825,29.515625));
#74531=CARTESIAN_POINT('Ctrl Pts',(29.1183495962155,1.52706329386825,29.5572916666666));
#74532=CARTESIAN_POINT('Ctrl Pts',(28.6775243943233,0.76353164693412,29.5989583333333));
#74533=CARTESIAN_POINT('Ctrl Pts',(28.2366991924311,-1.31894491186926E-14,
29.640625));
#74534=CARTESIAN_POINT('Ctrl Pts',(28.6775243943233,-0.763531646934146,
29.6822916666666));
#74535=CARTESIAN_POINT('Ctrl Pts',(29.1183495962155,-1.52706329386828,29.7239583333333));
#74536=CARTESIAN_POINT('Ctrl Pts',(30.,-1.52706329386828,29.765625));
#74537=CARTESIAN_POINT('Ctrl Pts',(30.8816504037844,-1.52706329386828,29.8072916666666));
#74538=CARTESIAN_POINT('Ctrl Pts',(31.3224756056766,-0.763531646934147,
29.8489583333333));
#74539=CARTESIAN_POINT('Ctrl Pts',(31.7633008075689,-1.36198038370242E-14,
29.890625));
#74540=CARTESIAN_POINT('Ctrl Pts',(31.3224756056766,0.763531646934118,29.9322916666666));
#74541=CARTESIAN_POINT('Ctrl Pts',(30.8816504037844,1.52706329386825,29.9739583333333));
#74542=CARTESIAN_POINT('Ctrl Pts',(30.,1.52706329386825,30.015625));
#74543=CARTESIAN_POINT('Ctrl Pts',(29.1183495962155,1.52706329386825,30.0572916666666));
#74544=CARTESIAN_POINT('Ctrl Pts',(28.6775243943233,0.76353164693412,30.0989583333333));
#74545=CARTESIAN_POINT('Ctrl Pts',(28.2366991924311,-1.31894491186926E-14,
30.140625));
#74546=CARTESIAN_POINT('Ctrl Pts',(28.6775243943233,-0.763531646934146,
30.1822916666666));
#74547=CARTESIAN_POINT('Ctrl Pts',(29.1183495962155,-1.52706329386828,30.2239583333333));
#74548=CARTESIAN_POINT('Ctrl Pts',(30.,-1.52706329386828,30.265625));
#74549=CARTESIAN_POINT('Ctrl Pts',(30.8816504037844,-1.52706329386828,30.3072916666666));
#74550=CARTESIAN_POINT('Ctrl Pts',(31.3224756056766,-0.763531646934147,
30.3489583333333));
#74551=CARTESIAN_POINT('Ctrl Pts',(31.7633008075689,-1.36198038370242E-14,
30.390625));
#74552=CARTESIAN_POINT('Ctrl Pts',(31.3224756056766,0.763531646934118,30.4322916666666));
#74553=CARTESIAN_POINT('Ctrl Pts',(30.8816504037844,1.52706329386825,30.4739583333333));
#74554=CARTESIAN_POINT('Ctrl Pts',(30.,1.52706329386825,30.515625));
#74555=CARTESIAN_POINT('Ctrl Pts',(29.1183495962155,1.52706329386825,30.5572916666666));
#74556=CARTESIAN_POINT('Ctrl Pts',(28.6775243943233,0.76353164693412,30.5989583333333));
#74557=CARTESIAN_POINT('Ctrl Pts',(28.2366991924311,-1.31894491186926E-14,
30.640625));
#74558=CARTESIAN_POINT('Ctrl Pts',(28.6775243943233,-0.763531646934146,
30.6822916666666));
#74559=CARTESIAN_POINT('Ctrl Pts',(29.1183495962155,-1.52706329386828,30.7239583333333));
#74560=CARTESIAN_POINT('Ctrl Pts',(30.,-1.52706329386828,30.765625));
#74561=CARTESIAN_POINT('Ctrl Pts',(30.8816504037844,-1.52706329386828,30.8072916666666));
#74562=CARTESIAN_POINT('Ctrl Pts',(31.3224756056766,-0.763531646934147,
30.8489583333333));
#74563=CARTESIAN_POINT('Ctrl Pts',(31.7633008075689,-1.36198038370242E-14,
30.890625));
#74564=CARTESIAN_POINT('Ctrl Pts',(31.3224756056766,0.763531646934118,30.9322916666666));
#74565=CARTESIAN_POINT('Ctrl Pts',(30.8816504037844,1.52706329386825,30.9739583333333));
#74566=CARTESIAN_POINT('Ctrl Pts',(30.,1.52706329386825,31.015625));
#74567=CARTESIAN_POINT('Ctrl Pts',(29.1183495962155,1.52706329386825,31.0572916666666));
#74568=CARTESIAN_POINT('Ctrl Pts',(28.6775243943233,0.76353164693412,31.0989583333333));
#74569=CARTESIAN_POINT('Ctrl Pts',(28.2366991924311,-1.31894491186926E-14,
31.140625));
#74570=CARTESIAN_POINT('Ctrl Pts',(28.6775243943233,-0.763531646934146,
31.1822916666666));
#74571=CARTESIAN_POINT('Ctrl Pts',(29.1183495962155,-1.52706329386828,31.2239583333333));
#74572=CARTESIAN_POINT('Ctrl Pts',(30.,-1.52706329386828,31.265625));
#74573=CARTESIAN_POINT('Ctrl Pts',(30.8816504037844,-1.52706329386828,31.3072916666666));
#74574=CARTESIAN_POINT('Ctrl Pts',(31.3224756056766,-0.763531646934147,
31.3489583333333));
#74575=CARTESIAN_POINT('Ctrl Pts',(31.7633008075689,-1.36198038370242E-14,
31.390625));
#74576=CARTESIAN_POINT('Ctrl Pts',(31.3224756056766,0.763531646934118,31.4322916666666));
#74577=CARTESIAN_POINT('Ctrl Pts',(30.8816504037844,1.52706329386825,31.4739583333333));
#74578=CARTESIAN_POINT('Ctrl Pts',(30.,1.52706329386825,31.515625));
#74579=CARTESIAN_POINT('Ctrl Pts',(30.,1.17523507120987,15.8124968809397));
#74580=CARTESIAN_POINT('Ctrl Pts',(29.3214777152758,1.17523507120987,15.8541635476064));
#74581=CARTESIAN_POINT('Ctrl Pts',(28.9822165729138,0.587617535604928,15.895830214273));
#74582=CARTESIAN_POINT('Ctrl Pts',(28.6429554305518,-1.32141489532166E-14,
15.9374968809397));
#74583=CARTESIAN_POINT('Ctrl Pts',(28.9822165729138,-0.587617535604954,
15.9791635476064));
#74584=CARTESIAN_POINT('Ctrl Pts',(29.3214777152758,-1.17523507120989,16.020830214273));
#74585=CARTESIAN_POINT('Ctrl Pts',(30.,-1.17523507120989,16.0624968809397));
#74586=CARTESIAN_POINT('Ctrl Pts',(30.6785222847241,-1.17523507120989,16.1041635476064));
#74587=CARTESIAN_POINT('Ctrl Pts',(31.0177834270861,-0.587617535604955,
16.145830214273));
#74588=CARTESIAN_POINT('Ctrl Pts',(31.3570445694482,-1.35453519623354E-14,
16.1874968809397));
#74589=CARTESIAN_POINT('Ctrl Pts',(31.0177834270861,0.587617535604927,16.2291635476064));
#74590=CARTESIAN_POINT('Ctrl Pts',(30.6785222847241,1.17523507120987,16.270830214273));
#74591=CARTESIAN_POINT('Ctrl Pts',(30.,1.17523507120987,16.3124968809397));
#74592=CARTESIAN_POINT('Ctrl Pts',(29.3214777152758,1.17523507120987,16.3541635476064));
#74593=CARTESIAN_POINT('Ctrl Pts',(28.9822165729138,0.587617535604928,16.395830214273));
#74594=CARTESIAN_POINT('Ctrl Pts',(28.6429554305518,-1.32141489532166E-14,
16.4374968809397));
#74595=CARTESIAN_POINT('Ctrl Pts',(28.9822165729138,-0.587617535604954,
16.4791635476064));
#74596=CARTESIAN_POINT('Ctrl Pts',(29.3214777152758,-1.17523507120989,16.520830214273));
#74597=CARTESIAN_POINT('Ctrl Pts',(30.,-1.17523507120989,16.5624968809397));
#74598=CARTESIAN_POINT('Ctrl Pts',(30.6785222847241,-1.17523507120989,16.6041635476064));
#74599=CARTESIAN_POINT('Ctrl Pts',(31.0177834270861,-0.587617535604955,
16.645830214273));
#74600=CARTESIAN_POINT('Ctrl Pts',(31.3570445694482,-1.35453519623354E-14,
16.6874968809397));
#74601=CARTESIAN_POINT('Ctrl Pts',(31.0177834270861,0.587617535604927,16.7291635476064));
#74602=CARTESIAN_POINT('Ctrl Pts',(30.6785222847241,1.17523507120987,16.770830214273));
#74603=CARTESIAN_POINT('Ctrl Pts',(30.,1.17523507120987,16.8124968809397));
#74604=CARTESIAN_POINT('Ctrl Pts',(29.3214777152758,1.17523507120987,16.8541635476064));
#74605=CARTESIAN_POINT('Ctrl Pts',(28.9822165729138,0.587617535604928,16.895830214273));
#74606=CARTESIAN_POINT('Ctrl Pts',(28.6429554305518,-1.32141489532166E-14,
16.9374968809397));
#74607=CARTESIAN_POINT('Ctrl Pts',(28.9822165729138,-0.587617535604954,
16.9791635476064));
#74608=CARTESIAN_POINT('Ctrl Pts',(29.3214777152758,-1.17523507120989,17.020830214273));
#74609=CARTESIAN_POINT('Ctrl Pts',(30.,-1.17523507120989,17.0624968809397));
#74610=CARTESIAN_POINT('Ctrl Pts',(30.6785222847241,-1.17523507120989,17.1041635476064));
#74611=CARTESIAN_POINT('Ctrl Pts',(31.0177834270861,-0.587617535604955,
17.145830214273));
#74612=CARTESIAN_POINT('Ctrl Pts',(31.3570445694482,-1.35453519623354E-14,
17.1874968809397));
#74613=CARTESIAN_POINT('Ctrl Pts',(31.0177834270861,0.587617535604927,17.2291635476064));
#74614=CARTESIAN_POINT('Ctrl Pts',(30.6785222847241,1.17523507120987,17.270830214273));
#74615=CARTESIAN_POINT('Ctrl Pts',(30.,1.17523507120987,17.3124968809397));
#74616=CARTESIAN_POINT('Ctrl Pts',(29.3214777152758,1.17523507120987,17.3541635476064));
#74617=CARTESIAN_POINT('Ctrl Pts',(28.9822165729138,0.587617535604928,17.395830214273));
#74618=CARTESIAN_POINT('Ctrl Pts',(28.6429554305518,-1.32141489532166E-14,
17.4374968809397));
#74619=CARTESIAN_POINT('Ctrl Pts',(28.9822165729138,-0.587617535604954,
17.4791635476064));
#74620=CARTESIAN_POINT('Ctrl Pts',(29.3214777152758,-1.17523507120989,17.520830214273));
#74621=CARTESIAN_POINT('Ctrl Pts',(30.,-1.17523507120989,17.5624968809397));
#74622=CARTESIAN_POINT('Ctrl Pts',(30.6785222847241,-1.17523507120989,17.6041635476064));
#74623=CARTESIAN_POINT('Ctrl Pts',(31.0177834270861,-0.587617535604955,
17.645830214273));
#74624=CARTESIAN_POINT('Ctrl Pts',(31.3570445694482,-1.35453519623354E-14,
17.6874968809397));
#74625=CARTESIAN_POINT('Ctrl Pts',(31.0177834270861,0.587617535604927,17.7291635476064));
#74626=CARTESIAN_POINT('Ctrl Pts',(30.6785222847241,1.17523507120987,17.770830214273));
#74627=CARTESIAN_POINT('Ctrl Pts',(30.,1.17523507120987,17.8124968809397));
#74628=CARTESIAN_POINT('Ctrl Pts',(29.3214777152758,1.17523507120987,17.8541635476064));
#74629=CARTESIAN_POINT('Ctrl Pts',(28.9822165729138,0.587617535604928,17.895830214273));
#74630=CARTESIAN_POINT('Ctrl Pts',(28.6429554305518,-1.32141489532166E-14,
17.9374968809397));
#74631=CARTESIAN_POINT('Ctrl Pts',(28.9822165729138,-0.587617535604954,
17.9791635476064));
#74632=CARTESIAN_POINT('Ctrl Pts',(29.3214777152758,-1.17523507120989,18.020830214273));
#74633=CARTESIAN_POINT('Ctrl Pts',(30.,-1.17523507120989,18.0624968809397));
#74634=CARTESIAN_POINT('Ctrl Pts',(30.6785222847241,-1.17523507120989,18.1041635476064));
#74635=CARTESIAN_POINT('Ctrl Pts',(31.0177834270861,-0.587617535604955,
18.145830214273));
#74636=CARTESIAN_POINT('Ctrl Pts',(31.3570445694482,-1.35453519623354E-14,
18.1874968809397));
#74637=CARTESIAN_POINT('Ctrl Pts',(31.0177834270861,0.587617535604927,18.2291635476064));
#74638=CARTESIAN_POINT('Ctrl Pts',(30.6785222847241,1.17523507120987,18.270830214273));
#74639=CARTESIAN_POINT('Ctrl Pts',(30.,1.17523507120987,18.3124968809397));
#74640=CARTESIAN_POINT('Ctrl Pts',(29.3214777152758,1.17523507120987,18.3541635476064));
#74641=CARTESIAN_POINT('Ctrl Pts',(28.9822165729138,0.587617535604928,18.395830214273));
#74642=CARTESIAN_POINT('Ctrl Pts',(28.6429554305518,-1.32141489532166E-14,
18.4374968809397));
#74643=CARTESIAN_POINT('Ctrl Pts',(28.9822165729138,-0.587617535604954,
18.4791635476064));
#74644=CARTESIAN_POINT('Ctrl Pts',(29.3214777152758,-1.17523507120989,18.520830214273));
#74645=CARTESIAN_POINT('Ctrl Pts',(30.,-1.17523507120989,18.5624968809397));
#74646=CARTESIAN_POINT('Ctrl Pts',(30.6785222847241,-1.17523507120989,18.6041635476064));
#74647=CARTESIAN_POINT('Ctrl Pts',(31.0177834270861,-0.587617535604955,
18.645830214273));
#74648=CARTESIAN_POINT('Ctrl Pts',(31.3570445694482,-1.35453519623354E-14,
18.6874968809397));
#74649=CARTESIAN_POINT('Ctrl Pts',(31.0177834270861,0.587617535604927,18.7291635476064));
#74650=CARTESIAN_POINT('Ctrl Pts',(30.6785222847241,1.17523507120987,18.770830214273));
#74651=CARTESIAN_POINT('Ctrl Pts',(30.,1.17523507120987,18.8124968809397));
#74652=CARTESIAN_POINT('Ctrl Pts',(29.3214777152758,1.17523507120987,18.8541635476064));
#74653=CARTESIAN_POINT('Ctrl Pts',(28.9822165729138,0.587617535604928,18.895830214273));
#74654=CARTESIAN_POINT('Ctrl Pts',(28.6429554305518,-1.32141489532166E-14,
18.9374968809397));
#74655=CARTESIAN_POINT('Ctrl Pts',(28.9822165729138,-0.587617535604954,
18.9791635476064));
#74656=CARTESIAN_POINT('Ctrl Pts',(29.3214777152758,-1.17523507120989,19.020830214273));
#74657=CARTESIAN_POINT('Ctrl Pts',(30.,-1.17523507120989,19.0624968809397));
#74658=CARTESIAN_POINT('Ctrl Pts',(30.6785222847241,-1.17523507120989,19.1041635476064));
#74659=CARTESIAN_POINT('Ctrl Pts',(31.0177834270861,-0.587617535604955,
19.145830214273));
#74660=CARTESIAN_POINT('Ctrl Pts',(31.3570445694482,-1.35453519623354E-14,
19.1874968809397));
#74661=CARTESIAN_POINT('Ctrl Pts',(31.0177834270861,0.587617535604927,19.2291635476064));
#74662=CARTESIAN_POINT('Ctrl Pts',(30.6785222847241,1.17523507120987,19.270830214273));
#74663=CARTESIAN_POINT('Ctrl Pts',(30.,1.17523507120987,19.3124968809397));
#74664=CARTESIAN_POINT('Ctrl Pts',(29.3214777152758,1.17523507120987,19.3541635476064));
#74665=CARTESIAN_POINT('Ctrl Pts',(28.9822165729138,0.587617535604928,19.395830214273));
#74666=CARTESIAN_POINT('Ctrl Pts',(28.6429554305518,-1.32141489532166E-14,
19.4374968809397));
#74667=CARTESIAN_POINT('Ctrl Pts',(28.9822165729138,-0.587617535604954,
19.4791635476064));
#74668=CARTESIAN_POINT('Ctrl Pts',(29.3214777152758,-1.17523507120989,19.520830214273));
#74669=CARTESIAN_POINT('Ctrl Pts',(30.,-1.17523507120989,19.5624968809397));
#74670=CARTESIAN_POINT('Ctrl Pts',(30.6785222847241,-1.17523507120989,19.6041635476064));
#74671=CARTESIAN_POINT('Ctrl Pts',(31.0177834270861,-0.587617535604955,
19.645830214273));
#74672=CARTESIAN_POINT('Ctrl Pts',(31.3570445694482,-1.35453519623354E-14,
19.6874968809397));
#74673=CARTESIAN_POINT('Ctrl Pts',(31.0177834270861,0.587617535604927,19.7291635476064));
#74674=CARTESIAN_POINT('Ctrl Pts',(30.6785222847241,1.17523507120987,19.770830214273));
#74675=CARTESIAN_POINT('Ctrl Pts',(30.,1.17523507120987,19.8124968809397));
#74676=CARTESIAN_POINT('Ctrl Pts',(29.3214777152758,1.17523507120987,19.8541635476064));
#74677=CARTESIAN_POINT('Ctrl Pts',(28.9822165729138,0.587617535604928,19.895830214273));
#74678=CARTESIAN_POINT('Ctrl Pts',(28.6429554305518,-1.32141489532166E-14,
19.9374968809397));
#74679=CARTESIAN_POINT('Ctrl Pts',(28.9822165729138,-0.587617535604954,
19.9791635476064));
#74680=CARTESIAN_POINT('Ctrl Pts',(29.3214777152758,-1.17523507120989,20.020830214273));
#74681=CARTESIAN_POINT('Ctrl Pts',(30.,-1.17523507120989,20.0624968809397));
#74682=CARTESIAN_POINT('Ctrl Pts',(30.6785222847241,-1.17523507120989,20.1041635476064));
#74683=CARTESIAN_POINT('Ctrl Pts',(31.0177834270861,-0.587617535604955,
20.145830214273));
#74684=CARTESIAN_POINT('Ctrl Pts',(31.3570445694482,-1.35453519623354E-14,
20.1874968809397));
#74685=CARTESIAN_POINT('Ctrl Pts',(31.0177834270861,0.587617535604927,20.2291635476064));
#74686=CARTESIAN_POINT('Ctrl Pts',(30.6785222847241,1.17523507120987,20.270830214273));
#74687=CARTESIAN_POINT('Ctrl Pts',(30.,1.17523507120987,20.3124968809397));
#74688=CARTESIAN_POINT('Ctrl Pts',(29.3214777152758,1.17523507120987,20.3541635476064));
#74689=CARTESIAN_POINT('Ctrl Pts',(28.9822165729138,0.587617535604928,20.395830214273));
#74690=CARTESIAN_POINT('Ctrl Pts',(28.6429554305518,-1.32141489532166E-14,
20.4374968809397));
#74691=CARTESIAN_POINT('Ctrl Pts',(28.9822165729138,-0.587617535604954,
20.4791635476064));
#74692=CARTESIAN_POINT('Ctrl Pts',(29.3214777152758,-1.17523507120989,20.520830214273));
#74693=CARTESIAN_POINT('Ctrl Pts',(30.,-1.17523507120989,20.5624968809397));
#74694=CARTESIAN_POINT('Ctrl Pts',(30.6785222847241,-1.17523507120989,20.6041635476064));
#74695=CARTESIAN_POINT('Ctrl Pts',(31.0177834270861,-0.587617535604955,
20.645830214273));
#74696=CARTESIAN_POINT('Ctrl Pts',(31.3570445694482,-1.35453519623354E-14,
20.6874968809397));
#74697=CARTESIAN_POINT('Ctrl Pts',(31.0177834270861,0.587617535604927,20.7291635476064));
#74698=CARTESIAN_POINT('Ctrl Pts',(30.6785222847241,1.17523507120987,20.770830214273));
#74699=CARTESIAN_POINT('Ctrl Pts',(30.,1.17523507120987,20.8124968809397));
#74700=CARTESIAN_POINT('Ctrl Pts',(29.3214777152758,1.17523507120987,20.8541635476064));
#74701=CARTESIAN_POINT('Ctrl Pts',(28.9822165729138,0.587617535604928,20.895830214273));
#74702=CARTESIAN_POINT('Ctrl Pts',(28.6429554305518,-1.32141489532166E-14,
20.9374968809397));
#74703=CARTESIAN_POINT('Ctrl Pts',(28.9822165729138,-0.587617535604954,
20.9791635476064));
#74704=CARTESIAN_POINT('Ctrl Pts',(29.3214777152758,-1.17523507120989,21.020830214273));
#74705=CARTESIAN_POINT('Ctrl Pts',(30.,-1.17523507120989,21.0624968809397));
#74706=CARTESIAN_POINT('Ctrl Pts',(30.6785222847241,-1.17523507120989,21.1041635476064));
#74707=CARTESIAN_POINT('Ctrl Pts',(31.0177834270861,-0.587617535604955,
21.145830214273));
#74708=CARTESIAN_POINT('Ctrl Pts',(31.3570445694482,-1.35453519623354E-14,
21.1874968809397));
#74709=CARTESIAN_POINT('Ctrl Pts',(31.0177834270861,0.587617535604927,21.2291635476064));
#74710=CARTESIAN_POINT('Ctrl Pts',(30.6785222847241,1.17523507120987,21.270830214273));
#74711=CARTESIAN_POINT('Ctrl Pts',(30.,1.17523507120987,21.3124968809397));
#74712=CARTESIAN_POINT('Ctrl Pts',(29.3214777152758,1.17523507120987,21.3541635476064));
#74713=CARTESIAN_POINT('Ctrl Pts',(28.9822165729138,0.587617535604928,21.395830214273));
#74714=CARTESIAN_POINT('Ctrl Pts',(28.6429554305518,-1.32141489532166E-14,
21.4374968809397));
#74715=CARTESIAN_POINT('Ctrl Pts',(28.9822165729138,-0.587617535604954,
21.4791635476064));
#74716=CARTESIAN_POINT('Ctrl Pts',(29.3214777152758,-1.17523507120989,21.520830214273));
#74717=CARTESIAN_POINT('Ctrl Pts',(30.,-1.17523507120989,21.5624968809397));
#74718=CARTESIAN_POINT('Ctrl Pts',(30.6785222847241,-1.17523507120989,21.6041635476064));
#74719=CARTESIAN_POINT('Ctrl Pts',(31.0177834270861,-0.587617535604955,
21.645830214273));
#74720=CARTESIAN_POINT('Ctrl Pts',(31.3570445694482,-1.35453519623354E-14,
21.6874968809397));
#74721=CARTESIAN_POINT('Ctrl Pts',(31.0177834270861,0.587617535604927,21.7291635476064));
#74722=CARTESIAN_POINT('Ctrl Pts',(30.6785222847241,1.17523507120987,21.770830214273));
#74723=CARTESIAN_POINT('Ctrl Pts',(30.,1.17523507120987,21.8124968809397));
#74724=CARTESIAN_POINT('Ctrl Pts',(29.3214777152758,1.17523507120987,21.8541635476064));
#74725=CARTESIAN_POINT('Ctrl Pts',(28.9822165729138,0.587617535604928,21.895830214273));
#74726=CARTESIAN_POINT('Ctrl Pts',(28.6429554305518,-1.32141489532166E-14,
21.9374968809397));
#74727=CARTESIAN_POINT('Ctrl Pts',(28.9822165729138,-0.587617535604954,
21.9791635476064));
#74728=CARTESIAN_POINT('Ctrl Pts',(29.3214777152758,-1.17523507120989,22.020830214273));
#74729=CARTESIAN_POINT('Ctrl Pts',(30.,-1.17523507120989,22.0624968809397));
#74730=CARTESIAN_POINT('Ctrl Pts',(30.6785222847241,-1.17523507120989,22.1041635476064));
#74731=CARTESIAN_POINT('Ctrl Pts',(31.0177834270861,-0.587617535604955,
22.145830214273));
#74732=CARTESIAN_POINT('Ctrl Pts',(31.3570445694482,-1.35453519623354E-14,
22.1874968809397));
#74733=CARTESIAN_POINT('Ctrl Pts',(31.0177834270861,0.587617535604927,22.2291635476064));
#74734=CARTESIAN_POINT('Ctrl Pts',(30.6785222847241,1.17523507120987,22.270830214273));
#74735=CARTESIAN_POINT('Ctrl Pts',(30.,1.17523507120987,22.3124968809397));
#74736=CARTESIAN_POINT('Ctrl Pts',(29.3214777152758,1.17523507120987,22.3541635476064));
#74737=CARTESIAN_POINT('Ctrl Pts',(28.9822165729138,0.587617535604928,22.395830214273));
#74738=CARTESIAN_POINT('Ctrl Pts',(28.6429554305518,-1.32141489532166E-14,
22.4374968809397));
#74739=CARTESIAN_POINT('Ctrl Pts',(28.9822165729138,-0.587617535604954,
22.4791635476064));
#74740=CARTESIAN_POINT('Ctrl Pts',(29.3214777152758,-1.17523507120989,22.520830214273));
#74741=CARTESIAN_POINT('Ctrl Pts',(30.,-1.17523507120989,22.5624968809397));
#74742=CARTESIAN_POINT('Ctrl Pts',(30.6785222847241,-1.17523507120989,22.6041635476064));
#74743=CARTESIAN_POINT('Ctrl Pts',(31.0177834270861,-0.587617535604955,
22.645830214273));
#74744=CARTESIAN_POINT('Ctrl Pts',(31.3570445694482,-1.35453519623354E-14,
22.6874968809397));
#74745=CARTESIAN_POINT('Ctrl Pts',(31.0177834270861,0.587617535604927,22.7291635476064));
#74746=CARTESIAN_POINT('Ctrl Pts',(30.6785222847241,1.17523507120987,22.770830214273));
#74747=CARTESIAN_POINT('Ctrl Pts',(30.,1.17523507120987,22.8124968809397));
#74748=CARTESIAN_POINT('Ctrl Pts',(29.3214777152758,1.17523507120987,22.8541635476064));
#74749=CARTESIAN_POINT('Ctrl Pts',(28.9822165729138,0.587617535604928,22.895830214273));
#74750=CARTESIAN_POINT('Ctrl Pts',(28.6429554305518,-1.32141489532166E-14,
22.9374968809397));
#74751=CARTESIAN_POINT('Ctrl Pts',(28.9822165729138,-0.587617535604954,
22.9791635476064));
#74752=CARTESIAN_POINT('Ctrl Pts',(29.3214777152758,-1.17523507120989,23.020830214273));
#74753=CARTESIAN_POINT('Ctrl Pts',(30.,-1.17523507120989,23.0624968809397));
#74754=CARTESIAN_POINT('Ctrl Pts',(30.6785222847241,-1.17523507120989,23.1041635476064));
#74755=CARTESIAN_POINT('Ctrl Pts',(31.0177834270861,-0.587617535604955,
23.145830214273));
#74756=CARTESIAN_POINT('Ctrl Pts',(31.3570445694482,-1.35453519623354E-14,
23.1874968809397));
#74757=CARTESIAN_POINT('Ctrl Pts',(31.0177834270861,0.587617535604927,23.2291635476064));
#74758=CARTESIAN_POINT('Ctrl Pts',(30.6785222847241,1.17523507120987,23.270830214273));
#74759=CARTESIAN_POINT('Ctrl Pts',(30.,1.17523507120987,23.3124968809397));
#74760=CARTESIAN_POINT('Ctrl Pts',(29.3214777152758,1.17523507120987,23.3541635476064));
#74761=CARTESIAN_POINT('Ctrl Pts',(28.9822165729138,0.587617535604928,23.395830214273));
#74762=CARTESIAN_POINT('Ctrl Pts',(28.6429554305518,-1.32141489532166E-14,
23.4374968809397));
#74763=CARTESIAN_POINT('Ctrl Pts',(28.9822165729138,-0.587617535604954,
23.4791635476064));
#74764=CARTESIAN_POINT('Ctrl Pts',(29.3214777152758,-1.17523507120989,23.520830214273));
#74765=CARTESIAN_POINT('Ctrl Pts',(30.,-1.17523507120989,23.5624968809397));
#74766=CARTESIAN_POINT('Ctrl Pts',(30.6785222847241,-1.17523507120989,23.6041635476064));
#74767=CARTESIAN_POINT('Ctrl Pts',(31.0177834270861,-0.587617535604955,
23.645830214273));
#74768=CARTESIAN_POINT('Ctrl Pts',(31.3570445694482,-1.35453519623354E-14,
23.6874968809397));
#74769=CARTESIAN_POINT('Ctrl Pts',(31.0177834270861,0.587617535604927,23.7291635476064));
#74770=CARTESIAN_POINT('Ctrl Pts',(30.6785222847241,1.17523507120987,23.770830214273));
#74771=CARTESIAN_POINT('Ctrl Pts',(30.,1.17523507120987,23.8124968809397));
#74772=CARTESIAN_POINT('Ctrl Pts',(29.3214777152758,1.17523507120987,23.8541635476064));
#74773=CARTESIAN_POINT('Ctrl Pts',(28.9822165729138,0.587617535604928,23.895830214273));
#74774=CARTESIAN_POINT('Ctrl Pts',(28.6429554305518,-1.32141489532166E-14,
23.9374968809397));
#74775=CARTESIAN_POINT('Ctrl Pts',(28.9822165729138,-0.587617535604954,
23.9791635476064));
#74776=CARTESIAN_POINT('Ctrl Pts',(29.3214777152758,-1.17523507120989,24.020830214273));
#74777=CARTESIAN_POINT('Ctrl Pts',(30.,-1.17523507120989,24.0624968809397));
#74778=CARTESIAN_POINT('Ctrl Pts',(30.6785222847241,-1.17523507120989,24.1041635476064));
#74779=CARTESIAN_POINT('Ctrl Pts',(31.0177834270861,-0.587617535604955,
24.145830214273));
#74780=CARTESIAN_POINT('Ctrl Pts',(31.3570445694482,-1.35453519623354E-14,
24.1874968809397));
#74781=CARTESIAN_POINT('Ctrl Pts',(31.0177834270861,0.587617535604927,24.2291635476064));
#74782=CARTESIAN_POINT('Ctrl Pts',(30.6785222847241,1.17523507120987,24.270830214273));
#74783=CARTESIAN_POINT('Ctrl Pts',(30.,1.17523507120987,24.3124968809397));
#74784=CARTESIAN_POINT('Ctrl Pts',(29.3214777152758,1.17523507120987,24.3541635476064));
#74785=CARTESIAN_POINT('Ctrl Pts',(28.9822165729138,0.587617535604928,24.395830214273));
#74786=CARTESIAN_POINT('Ctrl Pts',(28.6429554305518,-1.32141489532166E-14,
24.4374968809397));
#74787=CARTESIAN_POINT('Ctrl Pts',(28.9822165729138,-0.587617535604954,
24.4791635476064));
#74788=CARTESIAN_POINT('Ctrl Pts',(29.3214777152758,-1.17523507120989,24.520830214273));
#74789=CARTESIAN_POINT('Ctrl Pts',(30.,-1.17523507120989,24.5624968809397));
#74790=CARTESIAN_POINT('Ctrl Pts',(30.6785222847241,-1.17523507120989,24.6041635476064));
#74791=CARTESIAN_POINT('Ctrl Pts',(31.0177834270861,-0.587617535604955,
24.645830214273));
#74792=CARTESIAN_POINT('Ctrl Pts',(31.3570445694482,-1.35453519623354E-14,
24.6874968809397));
#74793=CARTESIAN_POINT('Ctrl Pts',(31.0177834270861,0.587617535604927,24.7291635476064));
#74794=CARTESIAN_POINT('Ctrl Pts',(30.6785222847241,1.17523507120987,24.770830214273));
#74795=CARTESIAN_POINT('Ctrl Pts',(30.,1.17523507120987,24.8124968809397));
#74796=CARTESIAN_POINT('Ctrl Pts',(29.3214777152758,1.17523507120987,24.8541635476064));
#74797=CARTESIAN_POINT('Ctrl Pts',(28.9822165729138,0.587617535604928,24.895830214273));
#74798=CARTESIAN_POINT('Ctrl Pts',(28.6429554305518,-1.32141489532166E-14,
24.9374968809397));
#74799=CARTESIAN_POINT('Ctrl Pts',(28.9822165729138,-0.587617535604954,
24.9791635476064));
#74800=CARTESIAN_POINT('Ctrl Pts',(29.3214777152758,-1.17523507120989,25.020830214273));
#74801=CARTESIAN_POINT('Ctrl Pts',(30.,-1.17523507120989,25.0624968809397));
#74802=CARTESIAN_POINT('Ctrl Pts',(30.6785222847241,-1.17523507120989,25.1041635476064));
#74803=CARTESIAN_POINT('Ctrl Pts',(31.0177834270861,-0.587617535604955,
25.145830214273));
#74804=CARTESIAN_POINT('Ctrl Pts',(31.3570445694482,-1.35453519623354E-14,
25.1874968809397));
#74805=CARTESIAN_POINT('Ctrl Pts',(31.0177834270861,0.587617535604927,25.2291635476064));
#74806=CARTESIAN_POINT('Ctrl Pts',(30.6785222847241,1.17523507120987,25.270830214273));
#74807=CARTESIAN_POINT('Ctrl Pts',(30.,1.17523507120987,25.3124968809397));
#74808=CARTESIAN_POINT('Ctrl Pts',(29.3214777152758,1.17523507120987,25.3541635476064));
#74809=CARTESIAN_POINT('Ctrl Pts',(28.9822165729138,0.587617535604928,25.395830214273));
#74810=CARTESIAN_POINT('Ctrl Pts',(28.6429554305518,-1.32141489532166E-14,
25.4374968809397));
#74811=CARTESIAN_POINT('Ctrl Pts',(28.9822165729138,-0.587617535604954,
25.4791635476064));
#74812=CARTESIAN_POINT('Ctrl Pts',(29.3214777152758,-1.17523507120989,25.520830214273));
#74813=CARTESIAN_POINT('Ctrl Pts',(30.,-1.17523507120989,25.5624968809397));
#74814=CARTESIAN_POINT('Ctrl Pts',(30.6785222847241,-1.17523507120989,25.6041635476064));
#74815=CARTESIAN_POINT('Ctrl Pts',(31.0177834270861,-0.587617535604955,
25.645830214273));
#74816=CARTESIAN_POINT('Ctrl Pts',(31.3570445694482,-1.35453519623354E-14,
25.6874968809397));
#74817=CARTESIAN_POINT('Ctrl Pts',(31.0177834270861,0.587617535604927,25.7291635476064));
#74818=CARTESIAN_POINT('Ctrl Pts',(30.6785222847241,1.17523507120987,25.770830214273));
#74819=CARTESIAN_POINT('Ctrl Pts',(30.,1.17523507120987,25.8124968809397));
#74820=CARTESIAN_POINT('Ctrl Pts',(29.3214777152758,1.17523507120987,25.8541635476064));
#74821=CARTESIAN_POINT('Ctrl Pts',(28.9822165729138,0.587617535604928,25.895830214273));
#74822=CARTESIAN_POINT('Ctrl Pts',(28.6429554305518,-1.32141489532166E-14,
25.9374968809397));
#74823=CARTESIAN_POINT('Ctrl Pts',(28.9822165729138,-0.587617535604954,
25.9791635476064));
#74824=CARTESIAN_POINT('Ctrl Pts',(29.3214777152758,-1.17523507120989,26.020830214273));
#74825=CARTESIAN_POINT('Ctrl Pts',(30.,-1.17523507120989,26.0624968809397));
#74826=CARTESIAN_POINT('Ctrl Pts',(30.6785222847241,-1.17523507120989,26.1041635476064));
#74827=CARTESIAN_POINT('Ctrl Pts',(31.0177834270861,-0.587617535604955,
26.145830214273));
#74828=CARTESIAN_POINT('Ctrl Pts',(31.3570445694482,-1.35453519623354E-14,
26.1874968809397));
#74829=CARTESIAN_POINT('Ctrl Pts',(31.0177834270861,0.587617535604927,26.2291635476064));
#74830=CARTESIAN_POINT('Ctrl Pts',(30.6785222847241,1.17523507120987,26.270830214273));
#74831=CARTESIAN_POINT('Ctrl Pts',(30.,1.17523507120987,26.3124968809397));
#74832=CARTESIAN_POINT('Ctrl Pts',(29.3214777152758,1.17523507120987,26.3541635476064));
#74833=CARTESIAN_POINT('Ctrl Pts',(28.9822165729138,0.587617535604928,26.395830214273));
#74834=CARTESIAN_POINT('Ctrl Pts',(28.6429554305518,-1.32141489532166E-14,
26.4374968809397));
#74835=CARTESIAN_POINT('Ctrl Pts',(28.9822165729138,-0.587617535604954,
26.4791635476064));
#74836=CARTESIAN_POINT('Ctrl Pts',(29.3214777152758,-1.17523507120989,26.520830214273));
#74837=CARTESIAN_POINT('Ctrl Pts',(30.,-1.17523507120989,26.5624968809397));
#74838=CARTESIAN_POINT('Ctrl Pts',(30.6785222847241,-1.17523507120989,26.6041635476064));
#74839=CARTESIAN_POINT('Ctrl Pts',(31.0177834270861,-0.587617535604955,
26.645830214273));
#74840=CARTESIAN_POINT('Ctrl Pts',(31.3570445694482,-1.35453519623354E-14,
26.6874968809397));
#74841=CARTESIAN_POINT('Ctrl Pts',(31.0177834270861,0.587617535604927,26.7291635476064));
#74842=CARTESIAN_POINT('Ctrl Pts',(30.6785222847241,1.17523507120987,26.770830214273));
#74843=CARTESIAN_POINT('Ctrl Pts',(30.,1.17523507120987,26.8124968809397));
#74844=CARTESIAN_POINT('Ctrl Pts',(29.3214777152758,1.17523507120987,26.8541635476064));
#74845=CARTESIAN_POINT('Ctrl Pts',(28.9822165729138,0.587617535604928,26.895830214273));
#74846=CARTESIAN_POINT('Ctrl Pts',(28.6429554305518,-1.32141489532166E-14,
26.9374968809397));
#74847=CARTESIAN_POINT('Ctrl Pts',(28.9822165729138,-0.587617535604954,
26.9791635476064));
#74848=CARTESIAN_POINT('Ctrl Pts',(29.3214777152758,-1.17523507120989,27.020830214273));
#74849=CARTESIAN_POINT('Ctrl Pts',(30.,-1.17523507120989,27.0624968809397));
#74850=CARTESIAN_POINT('Ctrl Pts',(30.6785222847241,-1.17523507120989,27.1041635476064));
#74851=CARTESIAN_POINT('Ctrl Pts',(31.0177834270861,-0.587617535604955,
27.145830214273));
#74852=CARTESIAN_POINT('Ctrl Pts',(31.3570445694482,-1.35453519623354E-14,
27.1874968809397));
#74853=CARTESIAN_POINT('Ctrl Pts',(31.0177834270861,0.587617535604927,27.2291635476064));
#74854=CARTESIAN_POINT('Ctrl Pts',(30.6785222847241,1.17523507120987,27.270830214273));
#74855=CARTESIAN_POINT('Ctrl Pts',(30.,1.17523507120987,27.3124968809397));
#74856=CARTESIAN_POINT('Ctrl Pts',(29.3214777152758,1.17523507120987,27.3541635476064));
#74857=CARTESIAN_POINT('Ctrl Pts',(28.9822165729138,0.587617535604928,27.395830214273));
#74858=CARTESIAN_POINT('Ctrl Pts',(28.6429554305518,-1.32141489532166E-14,
27.4374968809397));
#74859=CARTESIAN_POINT('Ctrl Pts',(28.9822165729138,-0.587617535604954,
27.4791635476064));
#74860=CARTESIAN_POINT('Ctrl Pts',(29.3214777152758,-1.17523507120989,27.520830214273));
#74861=CARTESIAN_POINT('Ctrl Pts',(30.,-1.17523507120989,27.5624968809397));
#74862=CARTESIAN_POINT('Ctrl Pts',(30.6785222847241,-1.17523507120989,27.6041635476064));
#74863=CARTESIAN_POINT('Ctrl Pts',(31.0177834270861,-0.587617535604955,
27.645830214273));
#74864=CARTESIAN_POINT('Ctrl Pts',(31.3570445694482,-1.35453519623354E-14,
27.6874968809397));
#74865=CARTESIAN_POINT('Ctrl Pts',(31.0177834270861,0.587617535604927,27.7291635476064));
#74866=CARTESIAN_POINT('Ctrl Pts',(30.6785222847241,1.17523507120987,27.770830214273));
#74867=CARTESIAN_POINT('Ctrl Pts',(30.,1.17523507120987,27.8124968809397));
#74868=CARTESIAN_POINT('Ctrl Pts',(29.3214777152758,1.17523507120987,27.8541635476064));
#74869=CARTESIAN_POINT('Ctrl Pts',(28.9822165729138,0.587617535604928,27.895830214273));
#74870=CARTESIAN_POINT('Ctrl Pts',(28.6429554305518,-1.32141489532166E-14,
27.9374968809397));
#74871=CARTESIAN_POINT('Ctrl Pts',(28.9822165729138,-0.587617535604954,
27.9791635476064));
#74872=CARTESIAN_POINT('Ctrl Pts',(29.3214777152758,-1.17523507120989,28.020830214273));
#74873=CARTESIAN_POINT('Ctrl Pts',(30.,-1.17523507120989,28.0624968809397));
#74874=CARTESIAN_POINT('Ctrl Pts',(30.6785222847241,-1.17523507120989,28.1041635476064));
#74875=CARTESIAN_POINT('Ctrl Pts',(31.0177834270861,-0.587617535604955,
28.145830214273));
#74876=CARTESIAN_POINT('Ctrl Pts',(31.3570445694482,-1.35453519623354E-14,
28.1874968809397));
#74877=CARTESIAN_POINT('Ctrl Pts',(31.0177834270861,0.587617535604927,28.2291635476064));
#74878=CARTESIAN_POINT('Ctrl Pts',(30.6785222847241,1.17523507120987,28.270830214273));
#74879=CARTESIAN_POINT('Ctrl Pts',(30.,1.17523507120987,28.3124968809397));
#74880=CARTESIAN_POINT('Ctrl Pts',(29.3214777152758,1.17523507120987,28.3541635476064));
#74881=CARTESIAN_POINT('Ctrl Pts',(28.9822165729138,0.587617535604928,28.395830214273));
#74882=CARTESIAN_POINT('Ctrl Pts',(28.6429554305518,-1.32141489532166E-14,
28.4374968809397));
#74883=CARTESIAN_POINT('Ctrl Pts',(28.9822165729138,-0.587617535604954,
28.4791635476064));
#74884=CARTESIAN_POINT('Ctrl Pts',(29.3214777152758,-1.17523507120989,28.520830214273));
#74885=CARTESIAN_POINT('Ctrl Pts',(30.,-1.17523507120989,28.5624968809397));
#74886=CARTESIAN_POINT('Ctrl Pts',(30.6785222847241,-1.17523507120989,28.6041635476064));
#74887=CARTESIAN_POINT('Ctrl Pts',(31.0177834270861,-0.587617535604955,
28.645830214273));
#74888=CARTESIAN_POINT('Ctrl Pts',(31.3570445694482,-1.35453519623354E-14,
28.6874968809397));
#74889=CARTESIAN_POINT('Ctrl Pts',(31.0177834270861,0.587617535604927,28.7291635476064));
#74890=CARTESIAN_POINT('Ctrl Pts',(30.6785222847241,1.17523507120987,28.770830214273));
#74891=CARTESIAN_POINT('Ctrl Pts',(30.,1.17523507120987,28.8124968809397));
#74892=CARTESIAN_POINT('Ctrl Pts',(29.3214777152758,1.17523507120987,28.8541635476064));
#74893=CARTESIAN_POINT('Ctrl Pts',(28.9822165729138,0.587617535604928,28.895830214273));
#74894=CARTESIAN_POINT('Ctrl Pts',(28.6429554305518,-1.32141489532166E-14,
28.9374968809397));
#74895=CARTESIAN_POINT('Ctrl Pts',(28.9822165729138,-0.587617535604954,
28.9791635476064));
#74896=CARTESIAN_POINT('Ctrl Pts',(29.3214777152758,-1.17523507120989,29.020830214273));
#74897=CARTESIAN_POINT('Ctrl Pts',(30.,-1.17523507120989,29.0624968809397));
#74898=CARTESIAN_POINT('Ctrl Pts',(30.6785222847241,-1.17523507120989,29.1041635476064));
#74899=CARTESIAN_POINT('Ctrl Pts',(31.0177834270861,-0.587617535604955,
29.145830214273));
#74900=CARTESIAN_POINT('Ctrl Pts',(31.3570445694482,-1.35453519623354E-14,
29.1874968809397));
#74901=CARTESIAN_POINT('Ctrl Pts',(31.0177834270861,0.587617535604927,29.2291635476064));
#74902=CARTESIAN_POINT('Ctrl Pts',(30.6785222847241,1.17523507120987,29.270830214273));
#74903=CARTESIAN_POINT('Ctrl Pts',(30.,1.17523507120987,29.3124968809397));
#74904=CARTESIAN_POINT('Ctrl Pts',(29.3214777152758,1.17523507120987,29.3541635476064));
#74905=CARTESIAN_POINT('Ctrl Pts',(28.9822165729138,0.587617535604928,29.395830214273));
#74906=CARTESIAN_POINT('Ctrl Pts',(28.6429554305518,-1.32141489532166E-14,
29.4374968809397));
#74907=CARTESIAN_POINT('Ctrl Pts',(28.9822165729138,-0.587617535604954,
29.4791635476064));
#74908=CARTESIAN_POINT('Ctrl Pts',(29.3214777152758,-1.17523507120989,29.520830214273));
#74909=CARTESIAN_POINT('Ctrl Pts',(30.,-1.17523507120989,29.5624968809397));
#74910=CARTESIAN_POINT('Ctrl Pts',(30.6785222847241,-1.17523507120989,29.6041635476064));
#74911=CARTESIAN_POINT('Ctrl Pts',(31.0177834270861,-0.587617535604955,
29.645830214273));
#74912=CARTESIAN_POINT('Ctrl Pts',(31.3570445694482,-1.35453519623354E-14,
29.6874968809397));
#74913=CARTESIAN_POINT('Ctrl Pts',(31.0177834270861,0.587617535604927,29.7291635476064));
#74914=CARTESIAN_POINT('Ctrl Pts',(30.6785222847241,1.17523507120987,29.770830214273));
#74915=CARTESIAN_POINT('Ctrl Pts',(30.,1.17523507120987,29.8124968809397));
#74916=CARTESIAN_POINT('Ctrl Pts',(29.3214777152758,1.17523507120987,29.8541635476064));
#74917=CARTESIAN_POINT('Ctrl Pts',(28.9822165729138,0.587617535604928,29.895830214273));
#74918=CARTESIAN_POINT('Ctrl Pts',(28.6429554305518,-1.32141489532166E-14,
29.9374968809397));
#74919=CARTESIAN_POINT('Ctrl Pts',(28.9822165729138,-0.587617535604954,
29.9791635476064));
#74920=CARTESIAN_POINT('Ctrl Pts',(29.3214777152758,-1.17523507120989,30.020830214273));
#74921=CARTESIAN_POINT('Ctrl Pts',(30.,-1.17523507120989,30.0624968809397));
#74922=CARTESIAN_POINT('Ctrl Pts',(30.6785222847241,-1.17523507120989,30.1041635476064));
#74923=CARTESIAN_POINT('Ctrl Pts',(31.0177834270861,-0.587617535604955,
30.145830214273));
#74924=CARTESIAN_POINT('Ctrl Pts',(31.3570445694482,-1.35453519623354E-14,
30.1874968809397));
#74925=CARTESIAN_POINT('Ctrl Pts',(31.0177834270861,0.587617535604927,30.2291635476064));
#74926=CARTESIAN_POINT('Ctrl Pts',(30.6785222847241,1.17523507120987,30.270830214273));
#74927=CARTESIAN_POINT('Ctrl Pts',(30.,1.17523507120987,30.3124968809397));
#74928=CARTESIAN_POINT('Ctrl Pts',(29.3214777152758,1.17523507120987,30.3541635476064));
#74929=CARTESIAN_POINT('Ctrl Pts',(28.9822165729138,0.587617535604928,30.395830214273));
#74930=CARTESIAN_POINT('Ctrl Pts',(28.6429554305518,-1.32141489532166E-14,
30.4374968809397));
#74931=CARTESIAN_POINT('Ctrl Pts',(28.9822165729138,-0.587617535604954,
30.4791635476064));
#74932=CARTESIAN_POINT('Ctrl Pts',(29.3214777152758,-1.17523507120989,30.520830214273));
#74933=CARTESIAN_POINT('Ctrl Pts',(30.,-1.17523507120989,30.5624968809397));
#74934=CARTESIAN_POINT('Ctrl Pts',(30.6785222847241,-1.17523507120989,30.6041635476064));
#74935=CARTESIAN_POINT('Ctrl Pts',(31.0177834270861,-0.587617535604955,
30.645830214273));
#74936=CARTESIAN_POINT('Ctrl Pts',(31.3570445694482,-1.35453519623354E-14,
30.6874968809397));
#74937=CARTESIAN_POINT('Ctrl Pts',(31.0177834270861,0.587617535604927,30.7291635476064));
#74938=CARTESIAN_POINT('Ctrl Pts',(30.6785222847241,1.17523507120987,30.770830214273));
#74939=CARTESIAN_POINT('Ctrl Pts',(30.,1.17523507120987,30.8124968809397));
#74940=CARTESIAN_POINT('Ctrl Pts',(29.3214777152758,1.17523507120987,30.8541635476064));
#74941=CARTESIAN_POINT('Ctrl Pts',(28.9822165729138,0.587617535604928,30.895830214273));
#74942=CARTESIAN_POINT('Ctrl Pts',(28.6429554305518,-1.32141489532166E-14,
30.9374968809397));
#74943=CARTESIAN_POINT('Ctrl Pts',(28.9822165729138,-0.587617535604954,
30.9791635476064));
#74944=CARTESIAN_POINT('Ctrl Pts',(29.3214777152758,-1.17523507120989,31.020830214273));
#74945=CARTESIAN_POINT('Ctrl Pts',(30.,-1.17523507120989,31.0624968809397));
#74946=CARTESIAN_POINT('Ctrl Pts',(30.6785222847241,-1.17523507120989,31.1041635476064));
#74947=CARTESIAN_POINT('Ctrl Pts',(31.0177834270861,-0.587617535604955,
31.145830214273));
#74948=CARTESIAN_POINT('Ctrl Pts',(31.3570445694482,-1.35453519623354E-14,
31.1874968809397));
#74949=CARTESIAN_POINT('Ctrl Pts',(31.0177834270861,0.587617535604927,31.2291635476064));
#74950=CARTESIAN_POINT('Ctrl Pts',(30.6785222847241,1.17523507120987,31.270830214273));
#74951=CARTESIAN_POINT('Ctrl Pts',(30.,1.17523507120987,31.3124968809397));
#74952=CARTESIAN_POINT('',(30.,-1.50000000000002,30.75));
#74953=CARTESIAN_POINT('Origin',(30.,-1.24258096838242E-13,1029.88397459622));
#74954=CARTESIAN_POINT('Origin',(30.06875,2.82851012598683,15.7235432561772));
#74955=CARTESIAN_POINT('',(30.012548982272,2.70302030326666,15.7235432561772));
#74956=CARTESIAN_POINT('Origin',(30.,2.70864040503946,15.7235432561772));
#74957=CARTESIAN_POINT('',(29.987451017728,2.70302030326666,15.7235432561772));
#74958=CARTESIAN_POINT('Origin',(29.987451017728,2.70302030326666,15.7235432561772));
#74959=CARTESIAN_POINT('Origin',(30.2904604134361,2.81439671040465,15.7235432561772));
#74960=CARTESIAN_POINT('',(30.224586826676,2.69370321195774,15.7235432561772));
#74961=CARTESIAN_POINT('Origin',(30.2125174768313,2.70029057063376,15.7235432561772));
#74962=CARTESIAN_POINT('',(30.1995662307806,2.69567237556048,15.7235432561772));
#74963=CARTESIAN_POINT('Origin',(30.1995662307806,2.69567237556048,15.7235432561772));
#74964=CARTESIAN_POINT('Origin',(29.8466157199522,2.82518483606723,15.7235432561772));
#74965=CARTESIAN_POINT('',(29.8004337692194,2.69567237556048,15.7235432561772));
#74966=CARTESIAN_POINT('Origin',(29.7874825231687,2.70029057063376,15.7235432561772));
#74967=CARTESIAN_POINT('',(29.775413173324,2.69370321195775,15.7235432561772));
#74968=CARTESIAN_POINT('Origin',(29.775413173324,2.69370321195775,15.7235432561772));
#74969=CARTESIAN_POINT('Origin',(29.6254271049963,2.804441342164,15.7235432561772));
#74970=CARTESIAN_POINT('',(29.589548948342,2.67170473125694,15.7235432561772));
#74971=CARTESIAN_POINT('Origin',(29.5762752872513,2.67529254692237,15.7235432561772));
#74972=CARTESIAN_POINT('',(29.5647599813892,2.6677785445999,15.7235432561772));
#74973=CARTESIAN_POINT('Origin',(29.5647599813892,2.6677785445999,15.7235432561772));
#74974=CARTESIAN_POINT('Origin',(29.4065478564962,2.76640753481494,15.7235432561772));
#74975=CARTESIAN_POINT('',(29.3811946946869,2.63126513885323,15.7235432561772));
#74976=CARTESIAN_POINT('Origin',(29.3676804550908,2.63380045503416,15.7235432561772));
#74977=CARTESIAN_POINT('',(29.3567901889011,2.6254061353882,15.7235432561772));
#74978=CARTESIAN_POINT('Origin',(29.3567901889011,2.6254061353882,15.7235432561772));
#74979=CARTESIAN_POINT('Origin',(29.1913274378037,2.71131790508989,15.7235432561772));
#74980=CARTESIAN_POINT('',(29.1766555815128,2.57460292188403,15.7235432561772));
#74981=CARTESIAN_POINT('Origin',(29.1629840831922,2.57607010751313,15.7235432561772));
#74982=CARTESIAN_POINT('',(29.1527859987874,2.56684722431571,15.7235432561772));
#74983=CARTESIAN_POINT('Origin',(29.1527859987874,2.56684722431571,15.7235432561772));
#74984=CARTESIAN_POINT('Origin',(28.9810927543681,2.63951209887526,15.7235432561772));
#74985=CARTESIAN_POINT('',(28.9771926604684,2.50206742175908,15.7235432561772));
#74986=CARTESIAN_POINT('Origin',(28.9634481927567,2.50245743114905,15.7235432561772));
#74987=CARTESIAN_POINT('',(28.9540051647184,2.49246284654199,15.7235432561772));
#74988=CARTESIAN_POINT('Origin',(28.9540051647184,2.49246284654199,15.7235432561772));
#74989=CARTESIAN_POINT('Origin',(28.7771399729228,2.55143282284423,15.7235432561772));
#74990=CARTESIAN_POINT('Origin',(28.7616732366375,2.40271160649133,15.7235432561772));
#74991=CARTESIAN_POINT('Origin',(28.5807265301867,2.44762311502286,15.7235432561772));
#74992=CARTESIAN_POINT('Origin',(28.5769760048382,2.29814685040398,15.7235432561772));
#74993=CARTESIAN_POINT('Origin',(28.3930633803483,2.32872299678009,15.7235432561772));
#74994=CARTESIAN_POINT('Origin',(28.4010521891726,2.1794132547725,15.7235432561772));
#74995=CARTESIAN_POINT('Origin',(28.2153075291307,2.1954655268832,15.7235432561772));
#74996=CARTESIAN_POINT('Origin',(28.2349864184648,2.0472428516969,15.7235432561772));
#74997=CARTESIAN_POINT('Origin',(28.0485549004665,2.0486722819467,15.7235432561772));
#74998=CARTESIAN_POINT('Origin',(28.0798025434137,1.90245051566326,15.7235432561772));
#74999=CARTESIAN_POINT('Origin',(27.8938335797622,1.88924829113933,15.7235432561772));
#75000=CARTESIAN_POINT('Origin',(27.9364573242129,1.74592893957157,15.7235432561772));
#75001=CARTESIAN_POINT('Origin',(27.7520974754101,1.71817645637828,15.7235432561772));
#75002=CARTESIAN_POINT('Origin',(27.805834531806,1.57864313098712,15.7235432561772));
#75003=CARTESIAN_POINT('Origin',(27.6242204376256,1.53651149241201,15.7235432561772));
#75004=CARTESIAN_POINT('Origin',(27.6887394991445,1.40162446254803,15.7235432561772));
#75005=CARTESIAN_POINT('Origin',(27.5109908708699,1.3453734241531,15.7235432561772));
#75006=CARTESIAN_POINT('Origin',(27.5858941560429,1.2159643132099,15.7235432561772));
#75007=CARTESIAN_POINT('Origin',(30.5103800418355,2.78293160322096,15.7235432561772));
#75008=CARTESIAN_POINT('',(30.4352400186108,2.66777854459989,15.7235432561772));
#75009=CARTESIAN_POINT('Origin',(30.4237247127487,2.67529254692237,15.7235432561772));
#75010=CARTESIAN_POINT('',(30.410451051658,2.67170473125694,15.7235432561772));
#75011=CARTESIAN_POINT('Origin',(30.410451051658,2.67170473125694,15.7235432561772));
#75012=CARTESIAN_POINT('Origin',(30.7271530075584,2.73430879728474,15.7235432561772));
#75013=CARTESIAN_POINT('',(30.6432098110989,2.62540613538819,15.7235432561772));
#75014=CARTESIAN_POINT('Origin',(30.6323195449092,2.63380045503415,15.7235432561772));
#75015=CARTESIAN_POINT('',(30.6188053053131,2.63126513885322,15.7235432561772));
#75016=CARTESIAN_POINT('Origin',(30.6188053053131,2.63126513885322,15.7235432561772));
#75017=CARTESIAN_POINT('Origin',(30.9394428331868,2.66882806836332,15.7235432561772));
#75018=CARTESIAN_POINT('',(30.8472140012126,2.5668472243157,15.7235432561772));
#75019=CARTESIAN_POINT('Origin',(30.8370159168078,2.57607010751312,15.7235432561772));
#75020=CARTESIAN_POINT('',(30.8233444184872,2.57460292188402,15.7235432561772));
#75021=CARTESIAN_POINT('Origin',(30.8233444184872,2.57460292188402,15.7235432561772));
#75022=CARTESIAN_POINT('Origin',(31.1459406813522,2.58689312692505,15.7235432561772));
#75023=CARTESIAN_POINT('',(31.0459948352816,2.49246284654197,15.7235432561772));
#75024=CARTESIAN_POINT('Origin',(31.0365518072432,2.50245743114904,15.7235432561772));
#75025=CARTESIAN_POINT('',(31.0228073395316,2.50206742175906,15.7235432561772));
#75026=CARTESIAN_POINT('Origin',(31.0228073395316,2.50206742175906,15.7235432561772));
#75027=CARTESIAN_POINT('Origin',(31.3453734241531,2.48900912913003,15.7235432561772));
#75028=CARTESIAN_POINT('',(31.2383267633625,2.40271160649132,15.7235432561772));
#75029=CARTESIAN_POINT('Origin',(31.2296970110986,2.41341627257038,15.7235432561772));
#75030=CARTESIAN_POINT('',(31.2159643132099,2.41410584395711,15.7235432561772));
#75031=CARTESIAN_POINT('Origin',(31.2159643132099,2.41410584395711,15.7235432561772));
#75032=CARTESIAN_POINT('Origin',(31.536511492412,2.3757795623744,15.7235432561772));
#75033=CARTESIAN_POINT('',(31.4230239951618,2.29814685040396,15.7235432561772));
#75034=CARTESIAN_POINT('Origin',(31.4152607239647,2.30949560012898,15.7235432561772));
#75035=CARTESIAN_POINT('',(31.401624462548,2.3112605008555,15.7235432561772));
#75036=CARTESIAN_POINT('Origin',(31.401624462548,2.3112605008555,15.7235432561772));
#75037=CARTESIAN_POINT('Origin',(31.7181764563782,2.24790252458986,15.7235432561772));
#75038=CARTESIAN_POINT('',(31.5989478108274,2.17941325477248,15.7235432561772));
#75039=CARTESIAN_POINT('Origin',(31.5920988838457,2.19133611932756,15.7235432561772));
#75040=CARTESIAN_POINT('',(31.5786431309871,2.19416546819402,15.7235432561772));
#75041=CARTESIAN_POINT('Origin',(31.5786431309871,2.19416546819402,15.7235432561772));
#75042=CARTESIAN_POINT('Origin',(31.8892482911393,2.10616642023777,15.7235432561772));
#75043=CARTESIAN_POINT('',(31.7650135815352,2.04724285169688,15.7235432561772));
#75044=CARTESIAN_POINT('Origin',(31.7591212246811,2.05966632265728,15.7235432561772));
#75045=CARTESIAN_POINT('',(31.7459289395715,2.06354267578706,15.7235432561772));
#75046=CARTESIAN_POINT('Origin',(31.7459289395715,2.06354267578706,15.7235432561772));
#75047=CARTESIAN_POINT('Origin',(32.0486722819467,1.95144509953352,15.7235432561772));
#75048=CARTESIAN_POINT('',(31.9201974565863,1.90245051566323,15.7235432561772));
#75049=CARTESIAN_POINT('Origin',(31.9152979981993,1.91529799819927,15.7235432561772));
#75050=CARTESIAN_POINT('',(31.9024505156632,1.9201974565863,15.7235432561772));
#75051=CARTESIAN_POINT('Origin',(31.9024505156632,1.9201974565863,15.7235432561772));
#75052=CARTESIAN_POINT('Origin',(32.1954655268832,1.7846924708693,15.7235432561772));
#75053=CARTESIAN_POINT('',(32.0635426757871,1.74592893957153,15.7235432561772));
#75054=CARTESIAN_POINT('Origin',(32.0596663226573,1.75912122468115,15.7235432561772));
#75055=CARTESIAN_POINT('',(32.0472428516969,1.76501358153524,15.7235432561772));
#75056=CARTESIAN_POINT('Origin',(32.0472428516969,1.76501358153524,15.7235432561772));
#75057=CARTESIAN_POINT('Origin',(32.3287229967801,1.6069366196517,15.7235432561772));
#75058=CARTESIAN_POINT('',(32.194165468194,1.57864313098709,15.7235432561772));
#75059=CARTESIAN_POINT('Origin',(32.1913361193276,1.59209888384569,15.7235432561772));
#75060=CARTESIAN_POINT('',(32.1794132547725,1.59894781082743,15.7235432561772));
#75061=CARTESIAN_POINT('Origin',(32.1794132547725,1.59894781082743,15.7235432561772));
#75062=CARTESIAN_POINT('Origin',(32.4476231150228,1.41927346981329,15.7235432561772));
#75063=CARTESIAN_POINT('',(32.3112605008555,1.401624462548,15.7235432561772));
#75064=CARTESIAN_POINT('Origin',(32.309495600129,1.41526072396473,15.7235432561772));
#75065=CARTESIAN_POINT('',(32.298146850404,1.42302399516178,15.7235432561772));
#75066=CARTESIAN_POINT('Origin',(32.298146850404,1.42302399516178,15.7235432561772));
#75067=CARTESIAN_POINT('Origin',(32.5514328228442,1.22286002707717,15.7235432561772));
#75068=CARTESIAN_POINT('',(32.4141058439571,1.21596431320987,15.7235432561772));
#75069=CARTESIAN_POINT('Origin',(32.4134162725704,1.22969701109858,15.7235432561772));
#75070=CARTESIAN_POINT('',(32.4027116064913,1.23832676336245,15.7235432561772));
#75071=CARTESIAN_POINT('Origin',(32.4027116064913,1.23832676336245,15.7235432561772));
#75072=CARTESIAN_POINT('Origin',(32.6395120988752,1.01890724563189,15.7235432561772));
#75073=CARTESIAN_POINT('',(32.5020674217591,1.02280733953163,15.7235432561772));
#75074=CARTESIAN_POINT('Origin',(32.502457431149,1.03655180724325,15.7235432561772));
#75075=CARTESIAN_POINT('',(32.492462846542,1.04599483528156,15.7235432561772));
#75076=CARTESIAN_POINT('Origin',(32.492462846542,1.04599483528156,15.7235432561772));
#75077=CARTESIAN_POINT('Origin',(32.7113179050899,0.808672562196245,15.7235432561772));
#75078=CARTESIAN_POINT('',(32.574602921884,0.823344418487232,15.7235432561772));
#75079=CARTESIAN_POINT('Origin',(32.5760701075131,0.837015916807817,15.7235432561772));
#75080=CARTESIAN_POINT('',(32.5668472243157,0.84721400121258,15.7235432561772));
#75081=CARTESIAN_POINT('Origin',(32.5668472243157,0.84721400121258,15.7235432561772));
#75082=CARTESIAN_POINT('Origin',(32.7664075348149,0.593452143503749,15.7235432561772));
#75083=CARTESIAN_POINT('',(32.6312651388532,0.618805305313054,15.7235432561772));
#75084=CARTESIAN_POINT('Origin',(32.6338004550341,0.632319544909225,15.7235432561772));
#75085=CARTESIAN_POINT('',(32.6254061353882,0.64320981109888,15.7235432561772));
#75086=CARTESIAN_POINT('Origin',(32.6254061353882,0.64320981109888,15.7235432561772));
#75087=CARTESIAN_POINT('Origin',(32.804441342164,0.37457289500369,15.7235432561772));
#75088=CARTESIAN_POINT('',(32.6717047312569,0.410451051657977,15.7235432561772));
#75089=CARTESIAN_POINT('Origin',(32.6752925469224,0.423724712748682,15.7235432561772));
#75090=CARTESIAN_POINT('',(32.6677785445999,0.435240018610789,15.7235432561772));
#75091=CARTESIAN_POINT('Origin',(32.6677785445999,0.435240018610789,15.7235432561772));
#75092=CARTESIAN_POINT('Origin',(32.8251848360672,0.153384280047806,15.7235432561772));
#75093=CARTESIAN_POINT('',(32.6956723755605,0.199566230780603,15.7235432561772));
#75094=CARTESIAN_POINT('Origin',(32.7002905706337,0.212517476831278,15.7235432561772));
#75095=CARTESIAN_POINT('',(32.6937032119577,0.224586826675969,15.7235432561772));
#75096=CARTESIAN_POINT('Origin',(32.6937032119577,0.224586826675969,15.7235432561772));
#75097=CARTESIAN_POINT('Origin',(32.8285101259868,-0.0687500000000229,15.7235432561772));
#75098=CARTESIAN_POINT('',(32.7030203032667,-0.0125489822720396,15.7235432561772));
#75099=CARTESIAN_POINT('Origin',(32.7086404050395,-2.31188656783185E-14,
15.7235432561772));
#75100=CARTESIAN_POINT('',(32.7030203032667,0.0125489822719939,15.7235432561772));
#75101=CARTESIAN_POINT('Origin',(32.7030203032667,0.0125489822719939,15.7235432561772));
#75102=CARTESIAN_POINT('Origin',(32.8143967104046,-0.290460413436156,15.7235432561772));
#75103=CARTESIAN_POINT('',(32.6937032119577,-0.224586826676015,15.7235432561772));
#75104=CARTESIAN_POINT('Origin',(32.7002905706337,-0.212517476831324,15.7235432561772));
#75105=CARTESIAN_POINT('',(32.6956723755605,-0.199566230780649,15.7235432561772));
#75106=CARTESIAN_POINT('Origin',(32.6956723755605,-0.199566230780649,15.7235432561772));
#75107=CARTESIAN_POINT('Origin',(32.7829316032209,-0.510380041835567,15.7235432561772));
#75108=CARTESIAN_POINT('',(32.6677785445999,-0.435240018610835,15.7235432561772));
#75109=CARTESIAN_POINT('Origin',(32.6752925469224,-0.423724712748728,15.7235432561772));
#75110=CARTESIAN_POINT('',(32.6717047312569,-0.410451051658023,15.7235432561772));
#75111=CARTESIAN_POINT('Origin',(32.6717047312569,-0.410451051658023,15.7235432561772));
#75112=CARTESIAN_POINT('Origin',(32.7343087972847,-0.727153007558476,15.7235432561772));
#75113=CARTESIAN_POINT('',(32.6254061353882,-0.643209811098926,15.7235432561772));
#75114=CARTESIAN_POINT('Origin',(32.6338004550341,-0.632319544909271,15.7235432561772));
#75115=CARTESIAN_POINT('',(32.6312651388532,-0.6188053053131,15.7235432561772));
#75116=CARTESIAN_POINT('Origin',(32.6312651388532,-0.6188053053131,15.7235432561772));
#75117=CARTESIAN_POINT('Origin',(32.6688280683633,-0.939442833186874,15.7235432561772));
#75118=CARTESIAN_POINT('',(32.5668472243157,-0.847214001212625,15.7235432561772));
#75119=CARTESIAN_POINT('Origin',(32.5760701075131,-0.837015916807863,15.7235432561772));
#75120=CARTESIAN_POINT('',(32.574602921884,-0.823344418487278,15.7235432561772));
#75121=CARTESIAN_POINT('Origin',(32.574602921884,-0.823344418487278,15.7235432561772));
#75122=CARTESIAN_POINT('Origin',(32.586893126925,-1.14594068135223,15.7235432561772));
#75123=CARTESIAN_POINT('',(32.492462846542,-1.0459948352816,15.7235432561772));
#75124=CARTESIAN_POINT('Origin',(32.502457431149,-1.0365518072433,15.7235432561772));
#75125=CARTESIAN_POINT('',(32.5020674217591,-1.02280733953168,15.7235432561772));
#75126=CARTESIAN_POINT('Origin',(32.5020674217591,-1.02280733953168,15.7235432561772));
#75127=CARTESIAN_POINT('Origin',(32.48900912913,-1.34537342415311,15.7235432561772));
#75128=CARTESIAN_POINT('',(32.4027116064913,-1.2383267633625,15.7235432561772));
#75129=CARTESIAN_POINT('Origin',(32.4134162725704,-1.22969701109862,15.7235432561772));
#75130=CARTESIAN_POINT('',(32.4141058439571,-1.21596431320991,15.7235432561772));
#75131=CARTESIAN_POINT('Origin',(32.4141058439571,-1.21596431320991,15.7235432561772));
#75132=CARTESIAN_POINT('Origin',(32.3757795623744,-1.53651149241202,15.7235432561772));
#75133=CARTESIAN_POINT('',(32.2981468504039,-1.42302399516182,15.7235432561772));
#75134=CARTESIAN_POINT('Origin',(32.309495600129,-1.41526072396478,15.7235432561772));
#75135=CARTESIAN_POINT('',(32.3112605008555,-1.40162446254804,15.7235432561772));
#75136=CARTESIAN_POINT('Origin',(32.3112605008555,-1.40162446254804,15.7235432561772));
#75137=CARTESIAN_POINT('Origin',(32.2479025245898,-1.71817645637829,15.7235432561772));
#75138=CARTESIAN_POINT('',(32.1794132547725,-1.59894781082747,15.7235432561772));
#75139=CARTESIAN_POINT('Origin',(32.1913361193275,-1.59209888384574,15.7235432561772));
#75140=CARTESIAN_POINT('',(32.194165468194,-1.57864313098713,15.7235432561772));
#75141=CARTESIAN_POINT('Origin',(32.194165468194,-1.57864313098713,15.7235432561772));
#75142=CARTESIAN_POINT('Origin',(32.1061664202378,-1.88924829113934,15.7235432561772));
#75143=CARTESIAN_POINT('',(32.0472428516969,-1.76501358153528,15.7235432561772));
#75144=CARTESIAN_POINT('Origin',(32.0596663226573,-1.75912122468119,15.7235432561772));
#75145=CARTESIAN_POINT('',(32.063542675787,-1.74592893957158,15.7235432561772));
#75146=CARTESIAN_POINT('Origin',(32.063542675787,-1.74592893957158,15.7235432561772));
#75147=CARTESIAN_POINT('Origin',(31.9514450995335,-2.04867228194671,15.7235432561772));
#75148=CARTESIAN_POINT('',(31.9024505156632,-1.92019745658634,15.7235432561772));
#75149=CARTESIAN_POINT('Origin',(31.9152979981993,-1.91529799819931,15.7235432561772));
#75150=CARTESIAN_POINT('',(31.9201974565863,-1.90245051566327,15.7235432561772));
#75151=CARTESIAN_POINT('Origin',(31.9201974565863,-1.90245051566327,15.7235432561772));
#75152=CARTESIAN_POINT('Origin',(31.7846924708693,-2.19546552688321,15.7235432561772));
#75153=CARTESIAN_POINT('',(31.7459289395715,-2.0635426757871,15.7235432561772));
#75154=CARTESIAN_POINT('Origin',(31.7591212246811,-2.05966632265732,15.7235432561772));
#75155=CARTESIAN_POINT('',(31.7650135815352,-2.04724285169692,15.7235432561772));
#75156=CARTESIAN_POINT('Origin',(31.7650135815352,-2.04724285169692,15.7235432561772));
#75157=CARTESIAN_POINT('Origin',(31.6069366196517,-2.32872299678011,15.7235432561772));
#75158=CARTESIAN_POINT('',(31.5786431309871,-2.19416546819406,15.7235432561772));
#75159=CARTESIAN_POINT('Origin',(31.5920988838457,-2.1913361193276,15.7235432561772));
#75160=CARTESIAN_POINT('',(31.5989478108274,-2.17941325477251,15.7235432561772));
#75161=CARTESIAN_POINT('Origin',(31.5989478108274,-2.17941325477251,15.7235432561772));
#75162=CARTESIAN_POINT('Origin',(31.4192734698133,-2.44762311502288,15.7235432561772));
#75163=CARTESIAN_POINT('',(31.401624462548,-2.31126050085554,15.7235432561772));
#75164=CARTESIAN_POINT('Origin',(31.4152607239647,-2.30949560012901,15.7235432561772));
#75165=CARTESIAN_POINT('',(31.4230239951618,-2.29814685040399,15.7235432561772));
#75166=CARTESIAN_POINT('Origin',(31.4230239951618,-2.29814685040399,15.7235432561772));
#75167=CARTESIAN_POINT('Origin',(31.2228600270771,-2.55143282284425,15.7235432561772));
#75168=CARTESIAN_POINT('',(31.2159643132098,-2.41410584395714,15.7235432561772));
#75169=CARTESIAN_POINT('Origin',(31.2296970110986,-2.41341627257041,15.7235432561772));
#75170=CARTESIAN_POINT('',(31.2383267633624,-2.40271160649135,15.7235432561772));
#75171=CARTESIAN_POINT('Origin',(31.2383267633624,-2.40271160649135,15.7235432561772));
#75172=CARTESIAN_POINT('Origin',(31.0189072456319,-2.63951209887528,15.7235432561772));
#75173=CARTESIAN_POINT('',(31.0228073395316,-2.5020674217591,15.7235432561772));
#75174=CARTESIAN_POINT('Origin',(31.0365518072432,-2.50245743114907,15.7235432561772));
#75175=CARTESIAN_POINT('',(31.0459948352815,-2.49246284654201,15.7235432561772));
#75176=CARTESIAN_POINT('Origin',(31.0459948352815,-2.49246284654201,15.7235432561772));
#75177=CARTESIAN_POINT('Origin',(30.8086725621962,-2.71131790508991,15.7235432561772));
#75178=CARTESIAN_POINT('',(30.8233444184872,-2.57460292188405,15.7235432561772));
#75179=CARTESIAN_POINT('Origin',(30.8370159168078,-2.57607010751315,15.7235432561772));
#75180=CARTESIAN_POINT('',(30.8472140012126,-2.56684722431573,15.7235432561772));
#75181=CARTESIAN_POINT('Origin',(30.8472140012126,-2.56684722431573,15.7235432561772));
#75182=CARTESIAN_POINT('Origin',(30.5934521435037,-2.76640753481496,15.7235432561772));
#75183=CARTESIAN_POINT('',(30.618805305313,-2.63126513885325,15.7235432561772));
#75184=CARTESIAN_POINT('Origin',(30.6323195449092,-2.63380045503418,15.7235432561772));
#75185=CARTESIAN_POINT('',(30.6432098110989,-2.62540613538822,15.7235432561772));
#75186=CARTESIAN_POINT('Origin',(30.6432098110989,-2.62540613538822,15.7235432561772));
#75187=CARTESIAN_POINT('Origin',(30.3745728950037,-2.80444134216402,15.7235432561772));
#75188=CARTESIAN_POINT('',(30.410451051658,-2.67170473125697,15.7235432561772));
#75189=CARTESIAN_POINT('Origin',(30.4237247127487,-2.67529254692239,15.7235432561772));
#75190=CARTESIAN_POINT('',(30.4352400186108,-2.66777854459992,15.7235432561772));
#75191=CARTESIAN_POINT('Origin',(30.4352400186108,-2.66777854459992,15.7235432561772));
#75192=CARTESIAN_POINT('Origin',(30.1533842800478,-2.82518483606726,15.7235432561772));
#75193=CARTESIAN_POINT('',(30.1995662307806,-2.69567237556051,15.7235432561772));
#75194=CARTESIAN_POINT('Origin',(30.2125174768313,-2.70029057063379,15.7235432561772));
#75195=CARTESIAN_POINT('',(30.224586826676,-2.69370321195777,15.7235432561772));
#75196=CARTESIAN_POINT('Origin',(30.224586826676,-2.69370321195777,15.7235432561772));
#75197=CARTESIAN_POINT('Origin',(29.93125,-2.82851012598686,15.7235432561772));
#75198=CARTESIAN_POINT('',(29.987451017728,-2.70302030326669,15.7235432561772));
#75199=CARTESIAN_POINT('Origin',(30.,-2.70864040503949,15.7235432561772));
#75200=CARTESIAN_POINT('',(30.012548982272,-2.70302030326669,15.7235432561772));
#75201=CARTESIAN_POINT('Origin',(30.012548982272,-2.70302030326669,15.7235432561772));
#75202=CARTESIAN_POINT('Origin',(29.7095395865638,-2.81439671040468,15.7235432561772));
#75203=CARTESIAN_POINT('',(29.775413173324,-2.69370321195777,15.7235432561772));
#75204=CARTESIAN_POINT('Origin',(29.7874825231687,-2.70029057063378,15.7235432561772));
#75205=CARTESIAN_POINT('',(29.8004337692193,-2.6956723755605,15.7235432561772));
#75206=CARTESIAN_POINT('Origin',(29.8004337692193,-2.6956723755605,15.7235432561772));
#75207=CARTESIAN_POINT('Origin',(29.4896199581644,-2.78293160322098,15.7235432561772));
#75208=CARTESIAN_POINT('',(29.5647599813891,-2.66777854459992,15.7235432561772));
#75209=CARTESIAN_POINT('Origin',(29.5762752872513,-2.67529254692239,15.7235432561772));
#75210=CARTESIAN_POINT('',(29.589548948342,-2.67170473125696,15.7235432561772));
#75211=CARTESIAN_POINT('Origin',(29.589548948342,-2.67170473125696,15.7235432561772));
#75212=CARTESIAN_POINT('Origin',(29.2728469924415,-2.73430879728476,15.7235432561772));
#75213=CARTESIAN_POINT('',(29.3567901889011,-2.62540613538822,15.7235432561772));
#75214=CARTESIAN_POINT('Origin',(29.3676804550907,-2.63380045503417,15.7235432561772));
#75215=CARTESIAN_POINT('',(29.3811946946869,-2.63126513885324,15.7235432561772));
#75216=CARTESIAN_POINT('Origin',(29.3811946946869,-2.63126513885324,15.7235432561772));
#75217=CARTESIAN_POINT('Origin',(29.0605571668131,-2.66882806836334,15.7235432561772));
#75218=CARTESIAN_POINT('',(29.1527859987874,-2.56684722431572,15.7235432561772));
#75219=CARTESIAN_POINT('Origin',(29.1629840831921,-2.57607010751314,15.7235432561772));
#75220=CARTESIAN_POINT('',(29.1766555815127,-2.57460292188404,15.7235432561772));
#75221=CARTESIAN_POINT('Origin',(29.1766555815127,-2.57460292188404,15.7235432561772));
#75222=CARTESIAN_POINT('Origin',(28.8540593186477,-2.58689312692507,15.7235432561772));
#75223=CARTESIAN_POINT('',(28.9540051647184,-2.49246284654199,15.7235432561772));
#75224=CARTESIAN_POINT('Origin',(28.9634481927567,-2.50245743114906,15.7235432561772));
#75225=CARTESIAN_POINT('',(28.9771926604683,-2.50206742175908,15.7235432561772));
#75226=CARTESIAN_POINT('Origin',(28.9771926604683,-2.50206742175908,15.7235432561772));
#75227=CARTESIAN_POINT('Origin',(28.6546265758469,-2.48900912913005,15.7235432561772));
#75228=CARTESIAN_POINT('',(28.7616732366375,-2.40271160649133,15.7235432561772));
#75229=CARTESIAN_POINT('Origin',(28.7703029889014,-2.4134162725704,15.7235432561772));
#75230=CARTESIAN_POINT('',(28.7840356867901,-2.41410584395713,15.7235432561772));
#75231=CARTESIAN_POINT('Origin',(28.7840356867901,-2.41410584395713,15.7235432561772));
#75232=CARTESIAN_POINT('Origin',(28.463488507588,-2.37577956237441,15.7235432561772));
#75233=CARTESIAN_POINT('',(28.5769760048382,-2.29814685040397,15.7235432561772));
#75234=CARTESIAN_POINT('Origin',(28.5847392760352,-2.30949560012899,15.7235432561772));
#75235=CARTESIAN_POINT('',(28.5983755374519,-2.31126050085552,15.7235432561772));
#75236=CARTESIAN_POINT('Origin',(28.5983755374519,-2.31126050085552,15.7235432561772));
#75237=CARTESIAN_POINT('Origin',(28.2818235436217,-2.24790252458987,15.7235432561772));
#75238=CARTESIAN_POINT('',(28.4010521891725,-2.17941325477249,15.7235432561772));
#75239=CARTESIAN_POINT('Origin',(28.4079011161542,-2.19133611932757,15.7235432561772));
#75240=CARTESIAN_POINT('',(28.4213568690129,-2.19416546819403,15.7235432561772));
#75241=CARTESIAN_POINT('Origin',(28.4213568690129,-2.19416546819403,15.7235432561772));
#75242=CARTESIAN_POINT('Origin',(28.1107517088606,-2.10616642023779,15.7235432561772));
#75243=CARTESIAN_POINT('',(28.2349864184647,-2.04724285169689,15.7235432561772));
#75244=CARTESIAN_POINT('Origin',(28.2408787753188,-2.0596663226573,15.7235432561772));
#75245=CARTESIAN_POINT('',(28.2540710604284,-2.06354267578707,15.7235432561772));
#75246=CARTESIAN_POINT('Origin',(28.2540710604284,-2.06354267578707,15.7235432561772));
#75247=CARTESIAN_POINT('Origin',(27.9513277180533,-1.95144509953353,15.7235432561772));
#75248=CARTESIAN_POINT('',(28.0798025434136,-1.90245051566325,15.7235432561772));
#75249=CARTESIAN_POINT('Origin',(28.0847020018007,-1.91529799819928,15.7235432561772));
#75250=CARTESIAN_POINT('',(28.0975494843367,-1.92019745658631,15.7235432561772));
#75251=CARTESIAN_POINT('Origin',(28.0975494843367,-1.92019745658631,15.7235432561772));
#75252=CARTESIAN_POINT('Origin',(27.8045344731168,-1.78469247086931,15.7235432561772));
#75253=CARTESIAN_POINT('',(27.9364573242129,-1.74592893957155,15.7235432561772));
#75254=CARTESIAN_POINT('Origin',(27.9403336773427,-1.75912122468116,15.7235432561772));
#75255=CARTESIAN_POINT('',(27.9527571483031,-1.76501358153525,15.7235432561772));
#75256=CARTESIAN_POINT('Origin',(27.9527571483031,-1.76501358153525,15.7235432561772));
#75257=CARTESIAN_POINT('Origin',(27.6712770032199,-1.6069366196517,15.7235432561772));
#75258=CARTESIAN_POINT('',(27.8058345318059,-1.5786431309871,15.7235432561772));
#75259=CARTESIAN_POINT('Origin',(27.8086638806724,-1.59209888384571,15.7235432561772));
#75260=CARTESIAN_POINT('',(27.8205867452275,-1.59894781082744,15.7235432561772));
#75261=CARTESIAN_POINT('Origin',(27.8205867452275,-1.59894781082744,15.7235432561772));
#75262=CARTESIAN_POINT('Origin',(27.5523768849771,-1.4192734698133,15.7235432561772));
#75263=CARTESIAN_POINT('',(27.6887394991444,-1.40162446254801,15.7235432561772));
#75264=CARTESIAN_POINT('Origin',(27.690504399871,-1.41526072396474,15.7235432561772));
#75265=CARTESIAN_POINT('',(27.701853149596,-1.42302399516179,15.7235432561772));
#75266=CARTESIAN_POINT('Origin',(27.701853149596,-1.42302399516179,15.7235432561772));
#75267=CARTESIAN_POINT('Origin',(27.4485671771557,-1.22286002707717,15.7235432561772));
#75268=CARTESIAN_POINT('',(27.5858941560428,-1.21596431320988,15.7235432561772));
#75269=CARTESIAN_POINT('Origin',(27.5865837274296,-1.22969701109859,15.7235432561772));
#75270=CARTESIAN_POINT('',(27.5972883935086,-1.23832676336246,15.7235432561772));
#75271=CARTESIAN_POINT('Origin',(27.5972883935086,-1.23832676336246,15.7235432561772));
#75272=CARTESIAN_POINT('Origin',(27.3604879011247,-1.01890724563189,15.7235432561772));
#75273=CARTESIAN_POINT('',(27.4979325782409,-1.02280733953164,15.7235432561772));
#75274=CARTESIAN_POINT('Origin',(27.4975425688509,-1.03655180724326,15.7235432561772));
#75275=CARTESIAN_POINT('',(27.507537153458,-1.04599483528157,15.7235432561772));
#75276=CARTESIAN_POINT('Origin',(27.507537153458,-1.04599483528157,15.7235432561772));
#75277=CARTESIAN_POINT('Origin',(27.2886820949101,-0.808672562196254,15.7235432561772));
#75278=CARTESIAN_POINT('',(27.4253970781159,-0.823344418487241,15.7235432561772));
#75279=CARTESIAN_POINT('Origin',(27.4239298924868,-0.837015916807826,15.7235432561772));
#75280=CARTESIAN_POINT('',(27.4331527756843,-0.847214001212589,15.7235432561772));
#75281=CARTESIAN_POINT('Origin',(27.4331527756843,-0.847214001212589,15.7235432561772));
#75282=CARTESIAN_POINT('Origin',(27.233592465185,-0.593452143503757,15.7235432561772));
#75283=CARTESIAN_POINT('',(27.3687348611467,-0.618805305313063,15.7235432561772));
#75284=CARTESIAN_POINT('Origin',(27.3661995449658,-0.632319544909233,15.7235432561772));
#75285=CARTESIAN_POINT('',(27.3745938646118,-0.643209811098888,15.7235432561772));
#75286=CARTESIAN_POINT('Origin',(27.3745938646118,-0.643209811098888,15.7235432561772));
#75287=CARTESIAN_POINT('Origin',(27.195558657836,-0.374572895003696,15.7235432561772));
#75288=CARTESIAN_POINT('',(27.328295268743,-0.410451051657984,15.7235432561772));
#75289=CARTESIAN_POINT('Origin',(27.3247074530776,-0.423724712748689,15.7235432561772));
#75290=CARTESIAN_POINT('',(27.3322214554001,-0.435240018610796,15.7235432561772));
#75291=CARTESIAN_POINT('Origin',(27.3322214554001,-0.435240018610796,15.7235432561772));
#75292=CARTESIAN_POINT('Origin',(27.1748151639327,-0.153384280047813,15.7235432561772));
#75293=CARTESIAN_POINT('',(27.3043276244395,-0.199566230780611,15.7235432561772));
#75294=CARTESIAN_POINT('Origin',(27.2997094293662,-0.212517476831286,15.7235432561772));
#75295=CARTESIAN_POINT('',(27.3062967880422,-0.224586826675978,15.7235432561772));
#75296=CARTESIAN_POINT('Origin',(27.3062967880422,-0.224586826675978,15.7235432561772));
#75297=CARTESIAN_POINT('Origin',(27.1714898740131,0.068750000000016,15.7235432561772));
#75298=CARTESIAN_POINT('Origin',(27.2969796967333,-0.0125489822720016,15.7235432561772));
#75299=CARTESIAN_POINT('Origin',(27.1856032895953,0.29046041343615,15.7235432561772));
#75300=CARTESIAN_POINT('Origin',(27.3043276244395,0.199566230780642,15.7235432561772));
#75301=CARTESIAN_POINT('Origin',(27.217068396779,0.510380041835561,15.7235432561772));
#75302=CARTESIAN_POINT('Origin',(27.328295268743,0.410451051658016,15.7235432561772));
#75303=CARTESIAN_POINT('Origin',(27.2656912027152,0.727153007558468,15.7235432561772));
#75304=CARTESIAN_POINT('Origin',(27.3687348611468,0.618805305313091,15.7235432561772));
#75305=CARTESIAN_POINT('Origin',(27.3311719316367,0.939442833186866,15.7235432561772));
#75306=CARTESIAN_POINT('Origin',(27.4253970781159,0.823344418487269,15.7235432561772));
#75307=CARTESIAN_POINT('Origin',(27.4131068730749,1.14594068135223,15.7235432561772));
#75308=CARTESIAN_POINT('Origin',(27.4979325782409,1.02280733953167,15.7235432561772));
#75325=UNCERTAINTY_MEASURE_WITH_UNIT(LENGTH_MEASURE(0.01),#75337,
'DISTANCE_ACCURACY_VALUE',
'Maximum model space distance between geometric entities at asserted c
onnectivities');
#75326=UNCERTAINTY_MEASURE_WITH_UNIT(LENGTH_MEASURE(0.01),#75337,
'DISTANCE_ACCURACY_VALUE',
'Maximum model space distance between geometric entities at asserted c
onnectivities');
#75335=(
GEOMETRIC_REPRESENTATION_CONTEXT(3)
GLOBAL_UNCERTAINTY_ASSIGNED_CONTEXT((#75325))
GLOBAL_UNIT_ASSIGNED_CONTEXT((#75337,#75339,#75340))
REPRESENTATION_CONTEXT('','3D')
);
#75336=(
GEOMETRIC_REPRESENTATION_CONTEXT(3)
GLOBAL_UNCERTAINTY_ASSIGNED_CONTEXT((#75326))
GLOBAL_UNIT_ASSIGNED_CONTEXT((#75337,#75339,#75340))
REPRESENTATION_CONTEXT('','3D')
);
#75337=(
LENGTH_UNIT()
NAMED_UNIT(*)
SI_UNIT(.MILLI.,.METRE.)
);
#75339=(
NAMED_UNIT(*)
PLANE_ANGLE_UNIT()
SI_UNIT($,.RADIAN.)
);
#75340=(
NAMED_UNIT(*)
SI_UNIT($,.STERADIAN.)
SOLID_ANGLE_UNIT()
);
#75349=SHAPE_DEFINITION_REPRESENTATION(#75358,#75375);
#75358=PRODUCT_DEFINITION_SHAPE('',$,#75385);
#75375=SHAPE_REPRESENTATION('',(#34957),#75335);
#75376=PRODUCT_DEFINITION_CONTEXT('part definition',#75405,'design');
#75385=PRODUCT_DEFINITION('Screw_03','Screw_03',#75394,#75376);
#75394=PRODUCT_DEFINITION_FORMATION('',$,#75415);
#75405=APPLICATION_CONTEXT(
'Core Data for Automotive Mechanical Design Process');
#75406=PRODUCT_CONTEXT('part definition',#75405,'mechanical');
#75415=PRODUCT('Screw_03','Screw_03',$,(#75406));
#75419=PRESENTATION_STYLE_ASSIGNMENT((#75423));
#75423=SURFACE_STYLE_USAGE(.BOTH.,#75427);
#75427=SURFACE_SIDE_STYLE('',(#75431));
#75431=SURFACE_STYLE_FILL_AREA(#75435);
#75435=FILL_AREA_STYLE('Opaque(86,86,86)',(#75439));
#75439=FILL_AREA_STYLE_COLOUR('Opaque(86,86,86)',#75443);
#75443=COLOUR_RGB('Opaque(86,86,86)', 0.08235294, 0.09019608, 0.10196078);
ENDSEC;
END-ISO-10303-21;
